ISO-10303-21;
HEADER;
FILE_DESCRIPTION (('STEP AP214'),
    '1' );
FILE_NAME ('Injection Molded Chain Links 2.step',
    '2026-10-08T22:59:04',
    ( '' ),
    ( '' ),
    'SwSTEP 2.0',
    'SolidWorks 2020',
    '' );
FILE_SCHEMA (( 'AUTOMOTIVE_DESIGN' ));
ENDSEC;

DATA;
#8=ORIENTED_EDGE ( 'NONE', *, *, #143500, .T. ) ;
#12=CARTESIAN_POINT ( 'NONE',  ( 20.94999999999999929, 11.65000000001115943, -67.00000000000000000 ) ) ;
#16=CARTESIAN_POINT ( 'NONE',  ( -22.47071067811865319, 0.09909245471376178227, -25.77992525550193648 ) ) ;
#48=CARTESIAN_POINT ( 'NONE',  ( 21.05000000000000071, 5.850000000011156942, -56.86750277572208034 ) ) ;
#63=LINE ( 'NONE', #3928, #147005 ) ;
#122=TOROIDAL_SURFACE ( 'NONE', #25285, 11.65000000000000036, 0.1000000000000000056 ) ;
#145=VECTOR ( 'NONE', #17658, 1000.000000000000000 ) ;
#150=DIRECTION ( 'NONE',  ( 0.000000000000000000, 0.8660254037844309360, -0.5000000000000134337 ) ) ;
#159=DIRECTION ( 'NONE',  ( -1.000000000000000000, 0.000000000000000000, 0.000000000000000000 ) ) ;
#245=DIRECTION ( 'NONE',  ( -1.000000000000000000, 0.000000000000000000, 0.000000000000000000 ) ) ;
#253=CYLINDRICAL_SURFACE ( 'NONE', #33673, 0.1000000000000000472 ) ;
#329=ORIENTED_EDGE ( 'NONE', *, *, #220458, .F. ) ;
#406=DIRECTION ( 'NONE',  ( 0.000000000000000000, 0.000000000000000000, -1.000000000000000000 ) ) ;
#422=ORIENTED_EDGE ( 'NONE', *, *, #103927, .F. ) ;
#455=AXIS2_PLACEMENT_3D ( 'NONE', #75670, #54785, #56055 ) ;
#490=ORIENTED_EDGE ( 'NONE', *, *, #191260, .T. ) ;
#494=DIRECTION ( 'NONE',  ( 0.000000000000000000, -1.000000000000000000, -2.891205793294679805E-16 ) ) ;
#511=CARTESIAN_POINT ( 'NONE',  ( -23.25000000000000000, 2.000000000011154189, -53.77537807723790309 ) ) ;
#513=CIRCLE ( 'NONE', #221269, 0.09999999999999939493 ) ;
#520=ADVANCED_FACE ( 'NONE', ( #209471 ), #170403, .T. ) ;
#521=EDGE_CURVE ( 'NONE', #72122, #174796, #227746, .T. ) ;
#627=CARTESIAN_POINT ( 'NONE',  ( 18.49999999999999645, 1.637172712981537659, -45.08215336547201701 ) ) ;
#635=ORIENTED_EDGE ( 'NONE', *, *, #34729, .F. ) ;
#637=CARTESIAN_POINT ( 'NONE',  ( 21.12400222705963060, 8.778511907088196509, -45.75000000000000000 ) ) ;
#703=CARTESIAN_POINT ( 'NONE',  ( -20.54999999999999716, 1.115625160336667635E-11, -69.00000000000000000 ) ) ;
#707=ORIENTED_EDGE ( 'NONE', *, *, #23388, .F. ) ;
#721=LINE ( 'NONE', #159848, #119717 ) ;
#722=EDGE_LOOP ( 'NONE', ( #109350, #213225, #212878, #122895 ) ) ;
#737=AXIS2_PLACEMENT_3D ( 'NONE', #87488, #126631, #168379 ) ;
#746=CARTESIAN_POINT ( 'NONE',  ( 20.94999999999999574, -11.64999999998883595, -36.60000000000000853 ) ) ;
#750=CARTESIAN_POINT ( 'NONE',  ( 18.41356215285961895, -9.499999999988869348, -40.53206939669960462 ) ) ;
#790=CARTESIAN_POINT ( 'NONE',  ( 20.85000000106584750, 11.75000000001115907, -60.15550465647353207 ) ) ;
#794=CARTESIAN_POINT ( 'NONE',  ( -18.59999999999999787, 9.350000000011156942, -45.65000000000000568 ) ) ;
#817=ORIENTED_EDGE ( 'NONE', *, *, #80729, .T. ) ;
#828=FACE_OUTER_BOUND ( 'NONE', #254581, .T. ) ;
#862=AXIS2_PLACEMENT_3D ( 'NONE', #221308, #2266, #162654 ) ;
#940=CARTESIAN_POINT ( 'NONE',  ( 21.05000000000000071, -8.999999999988842703, -57.10603087734755690 ) ) ;
#947=DIRECTION ( 'NONE',  ( -1.000000000000000000, 6.938893903907270030E-14, 0.000000000000000000 ) ) ;
#971=VERTEX_POINT ( 'NONE', #210151 ) ;
#986=CARTESIAN_POINT ( 'NONE',  ( 21.05000000000000071, 0.09779029131994770863, -27.24218538952387547 ) ) ;
#1049=ORIENTED_EDGE ( 'NONE', *, *, #19953, .F. ) ;
#1073=CARTESIAN_POINT ( 'NONE',  ( -23.15000000000000213, 1.115600667400684642E-11, -65.00000000000000000 ) ) ;
#1091=VERTEX_POINT ( 'NONE', #138280 ) ;
#1093=CIRCLE ( 'NONE', #167741, 0.1000000000000028644 ) ;
#1096=EDGE_CURVE ( 'NONE', #181952, #210604, #195739, .T. ) ;
#1106=CARTESIAN_POINT ( 'NONE',  ( 20.94999999999999929, -9.399999999988844834, -57.10603087734755690 ) ) ;
#1139=VERTEX_POINT ( 'NONE', #3933 ) ;
#1144=LINE ( 'NONE', #173765, #92456 ) ;
#1152=EDGE_LOOP ( 'NONE', ( #213535, #112196, #56971, #205951 ) ) ;
#1300=ADVANCED_FACE ( 'NONE', ( #170762 ), #69060, .F. ) ;
#1318=DIRECTION ( 'NONE',  ( 1.000000000000000000, 0.000000000000000000, 0.000000000000000000 ) ) ;
#1347=AXIS2_PLACEMENT_3D ( 'NONE', #224806, #43623, #241811 ) ;
#1348=VERTEX_POINT ( 'NONE', #209839 ) ;
#1353=ORIENTED_EDGE ( 'NONE', *, *, #85308, .T. ) ;
#1388=CARTESIAN_POINT ( 'NONE',  ( -18.59999999999999787, 5.341242990002807112, -23.69334979351197745 ) ) ;
#1409=VERTEX_POINT ( 'NONE', #197953 ) ;
#1413=ORIENTED_EDGE ( 'NONE', *, *, #158241, .F. ) ;
#1418=AXIS2_PLACEMENT_3D ( 'NONE', #15989, #95484, #255802 ) ;
#1454=FACE_OUTER_BOUND ( 'NONE', #199672, .T. ) ;
#1455=AXIS2_PLACEMENT_3D ( 'NONE', #14863, #232629, #76091 ) ;
#1458=TOROIDAL_SURFACE ( 'NONE', #201375, 0.2000000000000000111, 0.1000000000000000056 ) ;
#1492=CYLINDRICAL_SURFACE ( 'NONE', #191762, 0.09999999999999892308 ) ;
#1494=LINE ( 'NONE', #24948, #45413 ) ;
#1502=TOROIDAL_SURFACE ( 'NONE', #14190, 0.2000000000000000111, 0.1000000000000000056 ) ;
#1507=CARTESIAN_POINT ( 'NONE',  ( -23.25000000000000000, 1.115600667400684642E-11, -33.50000000000000000 ) ) ;
#1518=CARTESIAN_POINT ( 'NONE',  ( 20.94999999999999929, -8.999999999988844479, -43.39396912265245021 ) ) ;
#1530=CARTESIAN_POINT ( 'NONE',  ( -21.05000000000000071, 1.115600667400684642E-11, -67.00000000000000000 ) ) ;
#1541=AXIS2_PLACEMENT_3D ( 'NONE', #159374, #156826, #236325 ) ;
#1604=EDGE_LOOP ( 'NONE', ( #60654, #74965, #96659, #87879 ) ) ;
#1607=EDGE_CURVE ( 'NONE', #216121, #231120, #9420, .T. ) ;
#1618=AXIS2_PLACEMENT_3D ( 'NONE', #201862, #105290, #104016 ) ;
#1621=CIRCLE ( 'NONE', #101554, 0.1000000000000000472 ) ;
#1629=DIRECTION ( 'NONE',  ( 0.000000000000000000, -0.9908441862701596881, 0.1350103645451904977 ) ) ;
#1716=ORIENTED_EDGE ( 'NONE', *, *, #59055, .F. ) ;
#1739=CARTESIAN_POINT ( 'NONE',  ( -21.14999999999999858, 1.115600667400684642E-11, -33.50000000000000000 ) ) ;
#1750=CARTESIAN_POINT ( 'NONE',  ( -23.15000000000000213, -8.999999999988844479, -57.10603087734755690 ) ) ;
#1771=ORIENTED_EDGE ( 'NONE', *, *, #204835, .F. ) ;
#1794=AXIS2_PLACEMENT_3D ( 'NONE', #171098, #206329, #165938 ) ;
#1826=FILL_AREA_STYLE ('',( #224731 ) ) ;
#1833=CARTESIAN_POINT ( 'NONE',  ( 18.49999999999999645, -1.164121893230052995, -74.91484808557160591 ) ) ;
#1834=CARTESIAN_POINT ( 'NONE',  ( -22.50000000000088463, 0.04536165659890484952, -21.84949116579043604 ) ) ;
#1836=ORIENTED_EDGE ( 'NONE', *, *, #22910, .F. ) ;
#1871=CIRCLE ( 'NONE', #14577, 4.049999999999998046 ) ;
#1879=CARTESIAN_POINT ( 'NONE',  ( -23.15000000000000213, 11.75000000001115552, -63.89999999999999858 ) ) ;
#1912=ADVANCED_FACE ( 'NONE', ( #228786 ), #185790, .F. ) ;
#1916=DIRECTION ( 'NONE',  ( 0.000000000000000000, 0.000000000000000000, -1.000000000000000000 ) ) ;
#1920=FACE_OUTER_BOUND ( 'NONE', #225522, .T. ) ;
#1937=DIRECTION ( 'NONE',  ( 0.000000000000000000, -0.5000000000000275335, -0.8660254037844228314 ) ) ;
#1939=FACE_BOUND ( 'NONE', #159620, .T. ) ;
#1989=CARTESIAN_POINT ( 'NONE',  ( -20.54999999999999716, 1.115600667400684642E-11, -67.00000000000000000 ) ) ;
#2016=CARTESIAN_POINT ( 'NONE',  ( -20.93975676684922504, 10.31104185824063180, -72.52045169831058047 ) ) ;
#2044=CARTESIAN_POINT ( 'NONE',  ( 20.94999999999999929, 14.05000000001115623, -61.48630492923908974 ) ) ;
#2057=DIRECTION ( 'NONE',  ( 0.000000000000000000, 0.000000000000000000, 1.000000000000000000 ) ) ;
#2084=CARTESIAN_POINT ( 'NONE',  ( -21.64999999999999858, 7.350000000011155166, -54.65000000000000568 ) ) ;
#2087=DIRECTION ( 'NONE',  ( 1.000000000000000000, 2.952720810173289112E-16, -0.000000000000000000 ) ) ;
#2092=CARTESIAN_POINT ( 'NONE',  ( 20.99749315643149217, 11.75000000001115907, -59.98519423124097472 ) ) ;
#2095=FACE_OUTER_BOUND ( 'NONE', #88596, .T. ) ;
#2099=ORIENTED_EDGE ( 'NONE', *, *, #22221, .T. ) ;
#2102=ADVANCED_FACE ( 'NONE', ( #74872 ), #243018, .F. ) ;
#2128=( BOUNDED_CURVE ( )  B_SPLINE_CURVE ( 3, ( #228953, #211966, #188532, #33357 ),
 .UNSPECIFIED., .F., .F. ) 
 B_SPLINE_CURVE_WITH_KNOTS ( ( 4, 4 ),
 ( 0.000000000000000000, 1.570796326794908992 ),
 .UNSPECIFIED. ) 
 CURVE ( )  GEOMETRIC_REPRESENTATION_ITEM ( )  RATIONAL_B_SPLINE_CURVE ( ( 1.000000000000000000, 0.8047378541243619399, 0.8047378541243619399, 1.000000000000000000 ) ) 
 REPRESENTATION_ITEM ( '' )  );
#2131=CYLINDRICAL_SURFACE ( 'NONE', #62295, 0.1000000000000028644 ) ;
#2148=DIRECTION ( 'NONE',  ( 0.000000000000000000, 0.000000000000000000, 1.000000000000000000 ) ) ;
#2159=TOROIDAL_SURFACE ( 'NONE', #222737, 0.4000000000000003553, 0.1000000000000000056 ) ;
#2182=ORIENTED_EDGE ( 'NONE', *, *, #222072, .F. ) ;
#2240=VERTEX_POINT ( 'NONE', #179108 ) ;
#2245=EDGE_CURVE ( 'NONE', #48124, #203548, #241611, .T. ) ;
#2250=DIRECTION ( 'NONE',  ( -0.000000000000000000, -0.000000000000000000, 1.000000000000000000 ) ) ;
#2262=ADVANCED_FACE ( 'NONE', ( #4266 ), #59079, .F. ) ;
#2266=DIRECTION ( 'NONE',  ( 0.000000000000000000, -0.000000000000000000, -1.000000000000000000 ) ) ;
#2294=EDGE_CURVE ( 'NONE', #210604, #245137, #5670, .T. ) ;
#2313=VERTEX_POINT ( 'NONE', #8145 ) ;
#2321=B_SPLINE_CURVE_WITH_KNOTS ( 'NONE', 3,
 ( #18012, #135383, #35060, #114557, #256573, #194114, #115837, #15475, #255290, #157576 ),
 .UNSPECIFIED., .F., .F.,
 ( 4, 3, 3, 4 ),
 ( 0.000000000000000000, 0.0002000000000008585893, 0.001000000000082977483, 0.001967863649483336721 ),
 .UNSPECIFIED. ) ;
#2334=ORIENTED_EDGE ( 'NONE', *, *, #214841, .T. ) ;
#2348=ORIENTED_EDGE ( 'NONE', *, *, #74702, .T. ) ;
#2365=CARTESIAN_POINT ( 'NONE',  ( -22.39999999999999858, 0.1000000000111554016, -25.70922040162659883 ) ) ;
#2368=VERTEX_POINT ( 'NONE', #147646 ) ;
#2416=CARTESIAN_POINT ( 'NONE',  ( -20.05000000000000426, 9.250000000011157297, -54.65000000000000568 ) ) ;
#2425=AXIS2_PLACEMENT_3D ( 'NONE', #153513, #135160, #16531 ) ;
#2443=VERTEX_POINT ( 'NONE', #185492 ) ;
#2465=DIRECTION ( 'NONE',  ( -1.000000000000000000, 0.000000000000000000, 0.000000000000000000 ) ) ;
#2508=VERTEX_POINT ( 'NONE', #182504 ) ;
#2520=CARTESIAN_POINT ( 'NONE',  ( 18.49999999999999289, 11.65000000001115943, -21.75000000000000355 ) ) ;
#2525=DIRECTION ( 'NONE',  ( 1.000000000000000000, 0.000000000000000000, 0.000000000000000000 ) ) ;
#2527=CARTESIAN_POINT ( 'NONE',  ( -23.25000000000000000, 1.115600667400684642E-11, -67.00000000000000000 ) ) ;
#2534=AXIS2_PLACEMENT_3D ( 'NONE', #101667, #222921, #181265 ) ;
#2540=CARTESIAN_POINT ( 'NONE',  ( 21.05000000000000071, -8.999999999988842703, -57.50603087734755547 ) ) ;
#2550=AXIS2_PLACEMENT_3D ( 'NONE', #27538, #164451, #167043 ) ;
#2596=CIRCLE ( 'NONE', #148357, 0.09999999999999939493 ) ;
#2605=EDGE_CURVE ( 'NONE', #26511, #77835, #89078, .T. ) ;
#2607=LINE ( 'NONE', #161720, #199608 ) ;
#2621=CARTESIAN_POINT ( 'NONE',  ( -21.05000000000000071, 11.65000000001115588, -59.98519422934605672 ) ) ;
#2644=CIRCLE ( 'NONE', #144266, 7.900000000000003908 ) ;
#2648=FACE_OUTER_BOUND ( 'NONE', #40487, .T. ) ;
#2706=EDGE_CURVE ( 'NONE', #12615, #103845, #230754, .T. ) ;
#2722=ORIENTED_EDGE ( 'NONE', *, *, #35767, .T. ) ;
#2779=ORIENTED_EDGE ( 'NONE', *, *, #64412, .F. ) ;
#2782=ORIENTED_EDGE ( 'NONE', *, *, #180395, .F. ) ;
#2823=CYLINDRICAL_SURFACE ( 'NONE', #111142, 0.09999999999999939493 ) ;
#2836=CARTESIAN_POINT ( 'NONE',  ( 23.14999999999999858, 3.900000000011155432, -67.00000000000000000 ) ) ;
#2883=CARTESIAN_POINT ( 'NONE',  ( 20.94999999999999929, 1.115600667400684642E-11, -33.50000000000000000 ) ) ;
#2915=CYLINDRICAL_SURFACE ( 'NONE', #193148, 11.74999999999999645 ) ;
#2922=ORIENTED_EDGE ( 'NONE', *, *, #127069, .F. ) ;
#2925=DIRECTION ( 'NONE',  ( 0.000000000000000000, 1.000000000000000000, 0.000000000000000000 ) ) ;
#2961=AXIS2_PLACEMENT_3D ( 'NONE', #160224, #221422, #201889 ) ;
#2962=DIRECTION ( 'NONE',  ( 0.000000000000000000, -0.000000000000000000, 1.000000000000000000 ) ) ;
#2982=AXIS2_PLACEMENT_3D ( 'NONE', #19948, #124184, #142441 ) ;
#3001=CARTESIAN_POINT ( 'NONE',  ( 20.94999999999999929, -1.362429037182151470, -74.88888124792120493 ) ) ;
#3004=ORIENTED_EDGE ( 'NONE', *, *, #222378, .T. ) ;
#3046=CYLINDRICAL_SURFACE ( 'NONE', #158314, 0.09999999999999892308 ) ;
#3120=CARTESIAN_POINT ( 'NONE',  ( -22.50000000000094147, 0.1000000000110504439, -21.85042919245518434 ) ) ;
#3130=CARTESIAN_POINT ( 'NONE',  ( -20.00857864376270001, 9.150000000011157653, -54.65000000000000568 ) ) ;
#3135=CARTESIAN_POINT ( 'NONE',  ( -21.07928932188134041, 6.328516656409859387, -33.40110485434536969 ) ) ;
#3169=DIRECTION ( 'NONE',  ( 0.000000000000000000, 0.000000000000000000, -1.000000000000000000 ) ) ;
#3179=VERTEX_POINT ( 'NONE', #174054 ) ;
#3216=EDGE_CURVE ( 'NONE', #27454, #61108, #172890, .T. ) ;
#3238=CARTESIAN_POINT ( 'NONE',  ( -21.44999999999999929, 7.250000000011155521, -54.75000000000000000 ) ) ;
#3253=ORIENTED_EDGE ( 'NONE', *, *, #83176, .F. ) ;
#3284=VERTEX_POINT ( 'NONE', #236539 ) ;
#3293=AXIS2_PLACEMENT_3D ( 'NONE', #186793, #146346, #126800 ) ;
#3297=CARTESIAN_POINT ( 'NONE',  ( -20.89878130938411616, 10.32747123227773045, -72.57740328502492844 ) ) ;
#3299=DIRECTION ( 'NONE',  ( 0.000000000000000000, 0.000000000000000000, -1.000000000000000000 ) ) ;
#3306=ORIENTED_EDGE ( 'NONE', *, *, #174471, .F. ) ;
#3347=FACE_OUTER_BOUND ( 'NONE', #161235, .T. ) ;
#3370=AXIS2_PLACEMENT_3D ( 'NONE', #161532, #144492, #238481 ) ;
#3414=ORIENTED_EDGE ( 'NONE', *, *, #74007, .F. ) ;
#3451=EDGE_CURVE ( 'NONE', #97145, #11718, #114587, .T. ) ;
#3463=ORIENTED_EDGE ( 'NONE', *, *, #183596, .F. ) ;
#3526=EDGE_LOOP ( 'NONE', ( #230708, #143177, #157804, #12102, #33859 ) ) ;
#3539=DIRECTION ( 'NONE',  ( -1.000000000000000000, 0.000000000000000000, 0.000000000000000000 ) ) ;
#3560=EDGE_CURVE ( 'NONE', #188358, #1091, #227182, .T. ) ;
#3570=CARTESIAN_POINT ( 'NONE',  ( 21.05000000000000071, 0.09779029132038109806, -27.24218538951847535 ) ) ;
#3581=ADVANCED_FACE ( 'NONE', ( #95454 ), #132014, .F. ) ;
#3656=VERTEX_POINT ( 'NONE', #242346 ) ;
#3674=VERTEX_POINT ( 'NONE', #234980 ) ;
#3690=VERTEX_POINT ( 'NONE', #175050 ) ;
#3770=VECTOR ( 'NONE', #210131, 1000.000000000000000 ) ;
#3772=ADVANCED_FACE ( 'NONE', ( #188791 ), #88385, .F. ) ;
#3774=CYLINDRICAL_SURFACE ( 'NONE', #90563, 0.09999999999999939493 ) ;
#3805=EDGE_CURVE ( 'NONE', #147427, #17741, #181237, .T. ) ;
#3807=ORIENTED_EDGE ( 'NONE', *, *, #193638, .F. ) ;
#3809=EDGE_CURVE ( 'NONE', #256921, #971, #244914, .T. ) ;
#3818=CARTESIAN_POINT ( 'NONE',  ( -18.59999999999999787, 7.250000000011155521, -54.85000000000000142 ) ) ;
#3826=AXIS2_PLACEMENT_3D ( 'NONE', #135317, #170669, #229316 ) ;
#3827=EDGE_CURVE ( 'NONE', #61003, #159998, #167986, .T. ) ;
#3852=AXIS2_PLACEMENT_3D ( 'NONE', #94641, #230302, #169093 ) ;
#3863=DIRECTION ( 'NONE',  ( 0.000000000000000000, 0.2605042016806672911, -0.9654727137038716656 ) ) ;
#3896=CARTESIAN_POINT ( 'NONE',  ( -21.64999999999999858, 7.350000000011155166, -54.75000000000000000 ) ) ;
#3899=DIRECTION ( 'NONE',  ( -0.000000000000000000, -0.000000000000000000, -1.000000000000000000 ) ) ;
#3900=EDGE_CURVE ( 'NONE', #95339, #150427, #193876, .T. ) ;
#3922=CARTESIAN_POINT ( 'NONE',  ( -1.820710678118657944, -9.929289321870186313, -58.25000000000000000 ) ) ;
#3928=CARTESIAN_POINT ( 'NONE',  ( 18.57071067811864040, 10.17928932189250091, -54.75000000000000000 ) ) ;
#3933=CARTESIAN_POINT ( 'NONE',  ( -21.05000000000000071, 11.75000000001115552, -59.98519422934605672 ) ) ;
#3943=ORIENTED_EDGE ( 'NONE', *, *, #98583, .T. ) ;
#3981=EDGE_CURVE ( 'NONE', #165098, #91127, #72733, .T. ) ;
#3987=ORIENTED_EDGE ( 'NONE', *, *, #66005, .T. ) ;
#3988=ORIENTED_EDGE ( 'NONE', *, *, #147676, .T. ) ;
#4002=ORIENTED_EDGE ( 'NONE', *, *, #27353, .T. ) ;
#4011=TOROIDAL_SURFACE ( 'NONE', #33279, 0.2000000000000000111, 0.1000000000000000056 ) ;
#4022=DIRECTION ( 'NONE',  ( 0.000000000000000000, 0.8700118002898321601, -0.4930308989875230585 ) ) ;
#4067=DIRECTION ( 'NONE',  ( -1.000000000000000000, 0.000000000000000000, 0.000000000000000000 ) ) ;
#4089=CIRCLE ( 'NONE', #8204, 0.09999999999999939493 ) ;
#4104=CIRCLE ( 'NONE', #91590, 0.1000000000000028644 ) ;
#4116=ORIENTED_EDGE ( 'NONE', *, *, #251473, .T. ) ;
#4177=DIRECTION ( 'NONE',  ( -1.000000000000000000, 0.000000000000000000, 0.000000000000000000 ) ) ;
#4181=DIRECTION ( 'NONE',  ( 0.000000000000000000, -0.000000000000000000, -1.000000000000000000 ) ) ;
#4182=ORIENTED_EDGE ( 'NONE', *, *, #94931, .F. ) ;
#4183=EDGE_CURVE ( 'NONE', #226447, #156407, #227604, .T. ) ;
#4204=DIRECTION ( 'NONE',  ( 0.000000000000000000, 0.008583690987127922528, 0.9999631594459055250 ) ) ;
#4236=LINE ( 'NONE', #83747, #80498 ) ;
#4248=AXIS2_PLACEMENT_3D ( 'NONE', #172280, #73165, #212655 ) ;
#4265=DIRECTION ( 'NONE',  ( 1.000000000000000000, 0.000000000000000000, 0.000000000000000000 ) ) ;
#4266=FACE_OUTER_BOUND ( 'NONE', #120318, .T. ) ;
#4284=ORIENTED_EDGE ( 'NONE', *, *, #157000, .T. ) ;
#4455=CIRCLE ( 'NONE', #87652, 0.1000000000000028644 ) ;
#4470=CARTESIAN_POINT ( 'NONE',  ( 23.14999999999999858, 5.000000000011153745, -45.90526601891310321 ) ) ;
#4490=( BOUNDED_CURVE ( )  B_SPLINE_CURVE ( 3, ( #197429, #177892, #78756, #21397 ),
 .UNSPECIFIED., .F., .F. ) 
 B_SPLINE_CURVE_WITH_KNOTS ( ( 4, 4 ),
 ( 3.141592653589793116, 4.712388980384689674 ),
 .UNSPECIFIED. ) 
 CURVE ( )  GEOMETRIC_REPRESENTATION_ITEM ( )  RATIONAL_B_SPLINE_CURVE ( ( 1.000000000000000000, 0.8047378541243649375, 0.8047378541243649375, 1.000000000000000000 ) ) 
 REPRESENTATION_ITEM ( '' )  );
#4491=CARTESIAN_POINT ( 'NONE',  ( 21.05000000000000071, 6.450000000011156587, -43.51702717044002355 ) ) ;
#4555=DIRECTION ( 'NONE',  ( 2.952720810173289112E-16, -1.000000000000000000, 0.000000000000000000 ) ) ;
#4582=EDGE_CURVE ( 'NONE', #215029, #71326, #205056, .T. ) ;
#4601=AXIS2_PLACEMENT_3D ( 'NONE', #205285, #111017, #151447 ) ;
#4640=ORIENTED_EDGE ( 'NONE', *, *, #248109, .T. ) ;
#4644=DIRECTION ( 'NONE',  ( 3.265361837132813093E-16, -1.000000000000000000, -0.000000000000000000 ) ) ;
#4647=AXIS2_PLACEMENT_3D ( 'NONE', #67449, #124868, #126129 ) ;
#4650=DIRECTION ( 'NONE',  ( -1.000000000000000000, 0.000000000000000000, 0.000000000000000000 ) ) ;
#4665=DIRECTION ( 'NONE',  ( 0.000000000000000000, 0.000000000000000000, -1.000000000000000000 ) ) ;
#4685=DIRECTION ( 'NONE',  ( 1.000000000000000000, 0.000000000000000000, 0.000000000000000000 ) ) ;
#4693=ORIENTED_EDGE ( 'NONE', *, *, #226947, .F. ) ;
#4740=VERTEX_POINT ( 'NONE', #36845 ) ;
#4752=CARTESIAN_POINT ( 'NONE',  ( -18.59999999999999787, 1.750000000011155743, -45.16951155790164307 ) ) ;
#4756=CARTESIAN_POINT ( 'NONE',  ( 20.94999999999999929, 5.500000000011153745, -45.90526601891310321 ) ) ;
#4768=DIRECTION ( 'NONE',  ( 3.469446951953728416E-14, -0.8660254037844309360, 0.5000000000000134337 ) ) ;
#4800=EDGE_CURVE ( 'NONE', #45011, #152028, #223139, .T. ) ;
#4802=CARTESIAN_POINT ( 'NONE',  ( 22.45463910399149299, 1.026727559903828595E-11, -21.85042918981591953 ) ) ;
#4804=DIRECTION ( 'NONE',  ( -1.000000000000000000, -0.000000000000000000, -0.000000000000000000 ) ) ;
#4805=EDGE_CURVE ( 'NONE', #202789, #17741, #202306, .T. ) ;
#4823=CARTESIAN_POINT ( 'NONE',  ( -20.85000000000000142, 11.75000000001115552, -67.00000000000000000 ) ) ;
#4846=EDGE_LOOP ( 'NONE', ( #125717, #11484, #187456 ) ) ;
#4886=ADVANCED_FACE ( 'NONE', ( #191765 ), #209166, .T. ) ;
#4909=DIRECTION ( 'NONE',  ( 0.000000000000000000, 0.000000000000000000, 1.000000000000000000 ) ) ;
#4926=AXIS2_PLACEMENT_3D ( 'NONE', #165212, #88211, #11279 ) ;
#4936=ORIENTED_EDGE ( 'NONE', *, *, #228633, .F. ) ;
#4956=CARTESIAN_POINT ( 'NONE',  ( 21.05000000000000071, 10.72371710471867701, -45.65000000000000568 ) ) ;
#4969=LINE ( 'NONE', #44136, #34956 ) ;
#4975=CARTESIAN_POINT ( 'NONE',  ( -21.05000000000000071, 5.900000000011162093, -56.78090023534362984 ) ) ;
#4998=CARTESIAN_POINT ( 'NONE',  ( -22.59999999999999787, 1.115600667400684642E-11, -33.50000000000000000 ) ) ;
#5006=ADVANCED_FACE ( 'NONE', ( #54773 ), #95197, .F. ) ;
#5017=DIRECTION ( 'NONE',  ( 0.000000000000000000, -0.4930308989875248349, -0.8700118002898312719 ) ) ;
#5027=EDGE_CURVE ( 'NONE', #201418, #101718, #142707, .T. ) ;
#5032=ORIENTED_EDGE ( 'NONE', *, *, #250398, .T. ) ;
#5033=EDGE_CURVE ( 'NONE', #41243, #104053, #19525, .T. ) ;
#5050=ORIENTED_EDGE ( 'NONE', *, *, #87797, .T. ) ;
#5052=CARTESIAN_POINT ( 'NONE',  ( -20.15000000000000568, 9.291421356248463326, -45.75000000000000000 ) ) ;
#5060=DIRECTION ( 'NONE',  ( 0.000000000000000000, -1.000000000000000000, -0.000000000000000000 ) ) ;
#5079=CARTESIAN_POINT ( 'NONE',  ( -20.64999999999999858, -8.663551401858004652, -43.02410111806730697 ) ) ;
#5088=FACE_OUTER_BOUND ( 'NONE', #168490, .T. ) ;
#5104=ORIENTED_EDGE ( 'NONE', *, *, #80572, .T. ) ;
#5122=ORIENTED_EDGE ( 'NONE', *, *, #64906, .F. ) ;
#5140=ORIENTED_EDGE ( 'NONE', *, *, #83826, .F. ) ;
#5181=ADVANCED_FACE ( 'NONE', ( #177337 ), #58618, .F. ) ;
#5213=ORIENTED_EDGE ( 'NONE', *, *, #110331, .F. ) ;
#5218=EDGE_LOOP ( 'NONE', ( #192245, #102500, #98596 ) ) ;
#5225=CIRCLE ( 'NONE', #184307, 0.8750000000000007772 ) ;
#5237=CARTESIAN_POINT ( 'NONE',  ( -21.05000000000000071, -12.41227409413852811, -64.10000000000000853 ) ) ;
#5284=CARTESIAN_POINT ( 'NONE',  ( -23.15000000000000213, -11.64999999998884483, -33.50000000000000000 ) ) ;
#5328=EDGE_CURVE ( 'NONE', #216196, #51264, #73472, .T. ) ;
#5334=ORIENTED_EDGE ( 'NONE', *, *, #186868, .F. ) ;
#5374=ORIENTED_EDGE ( 'NONE', *, *, #139850, .T. ) ;
#5411=EDGE_LOOP ( 'NONE', ( #58456, #83418, #41218, #62892 ) ) ;
#5437=ORIENTED_EDGE ( 'NONE', *, *, #247175, .T. ) ;
#5465=ADVANCED_FACE ( 'NONE', ( #39755 ), #110853, .F. ) ;
#5466=AXIS2_PLACEMENT_3D ( 'NONE', #229635, #129254, #77924 ) ;
#5470=CARTESIAN_POINT ( 'NONE',  ( -22.39999999999999858, 1.115600667400684642E-11, -25.70922040162659883 ) ) ;
#5490=FACE_OUTER_BOUND ( 'NONE', #234913, .T. ) ;
#5519=CARTESIAN_POINT ( 'NONE',  ( -18.47130263965439667, -9.471155585952800493, -73.68340476547700746 ) ) ;
#5536=AXIS2_PLACEMENT_3D ( 'NONE', #156306, #234515, #174613 ) ;
#5569=VERTEX_POINT ( 'NONE', #87812 ) ;
#5647=AXIS2_PLACEMENT_3D ( 'NONE', #119995, #164237, #200781 ) ;
#5668=LINE ( 'NONE', #203891, #204156 ) ;
#5670=CIRCLE ( 'NONE', #201331, 0.09999999999999824307 ) ;
#5686=CARTESIAN_POINT ( 'NONE',  ( 21.04999999999999716, 10.68430915749624077, -41.02669679032685224 ) ) ;
#5703=CARTESIAN_POINT ( 'NONE',  ( -20.54999999999999716, 1.115600667400684642E-11, -67.00000000000000000 ) ) ;
#5744=DIRECTION ( 'NONE',  ( 0.000000000000000000, -0.7397360091702744889, 0.6728971962616842051 ) ) ;
#5759=AXIS2_PLACEMENT_3D ( 'NONE', #241292, #245127, #63921 ) ;
#5780=ORIENTED_EDGE ( 'NONE', *, *, #101632, .F. ) ;
#5821=ADVANCED_FACE ( 'NONE', ( #49555 ), #245194, .T. ) ;
#5877=CARTESIAN_POINT ( 'NONE',  ( -22.43310005002225438, 0.005636942152031573783, -21.85033787286560525 ) ) ;
#5913=CARTESIAN_POINT ( 'NONE',  ( -21.05000000000000071, -1.835341550213255957, -45.05515129256298223 ) ) ;
#5916=ORIENTED_EDGE ( 'NONE', *, *, #213904, .T. ) ;
#5929=ORIENTED_EDGE ( 'NONE', *, *, #20813, .F. ) ;
#5930=DIRECTION ( 'NONE',  ( -1.000000000000000000, -7.304098846218134667E-16, 0.000000000000000000 ) ) ;
#5964=TOROIDAL_SURFACE ( 'NONE', #18467, 0.4000000000000005773, 0.1000000000000000056 ) ;
#5976=DIRECTION ( 'NONE',  ( 2.952720810173289112E-16, -1.000000000000000000, 0.000000000000000000 ) ) ;
#5998=ORIENTED_EDGE ( 'NONE', *, *, #178086, .F. ) ;
#6007=AXIS2_PLACEMENT_3D ( 'NONE', #40490, #136975, #58704 ) ;
#6014=ORIENTED_EDGE ( 'NONE', *, *, #146369, .F. ) ;
#6031=AXIS2_PLACEMENT_3D ( 'NONE', #77027, #156615, #236108 ) ;
#6049=ADVANCED_FACE ( 'NONE', ( #20713 ), #161507, .F. ) ;
#6076=CIRCLE ( 'NONE', #151868, 2.000000000000002665 ) ;
#6096=CARTESIAN_POINT ( 'NONE',  ( 22.49999999999999645, 0.1000000000111554016, -21.85042919245519855 ) ) ;
#6103=DIRECTION ( 'NONE',  ( 0.000000000000000000, 0.000000000000000000, -1.000000000000000000 ) ) ;
#6174=EDGE_CURVE ( 'NONE', #200635, #241925, #48845, .T. ) ;
#6214=CIRCLE ( 'NONE', #68600, 0.5000000000000004441 ) ;
#6222=CIRCLE ( 'NONE', #185306, 0.1000000000000028644 ) ;
#6223=DIRECTION ( 'NONE',  ( 0.000000000000000000, 0.000000000000000000, -1.000000000000000000 ) ) ;
#6241=FACE_OUTER_BOUND ( 'NONE', #244298, .T. ) ;
#6256=CARTESIAN_POINT ( 'NONE',  ( 21.14999999999999858, 1.115600667400684642E-11, -45.65000000000000568 ) ) ;
#6266=DIRECTION ( 'NONE',  ( 0.000000000000000000, 0.000000000000000000, 1.000000000000000000 ) ) ;
#6281=VERTEX_POINT ( 'NONE', #32615 ) ;
#6297=DIRECTION ( 'NONE',  ( 1.000000000000000000, 0.000000000000000000, 0.000000000000000000 ) ) ;
#6299=EDGE_LOOP ( 'NONE', ( #80627, #160268, #115535, #233046, #115487 ) ) ;
#6300=ORIENTED_EDGE ( 'NONE', *, *, #89382, .F. ) ;
#6306=CIRCLE ( 'NONE', #235253, 0.09999999999999693856 ) ;
#6330=AXIS2_PLACEMENT_3D ( 'NONE', #125937, #26882, #9854 ) ;
#6332=ORIENTED_EDGE ( 'NONE', *, *, #86956, .T. ) ;
#6361=CARTESIAN_POINT ( 'NONE',  ( 22.49999999999999645, 11.64957080755595520, -33.40000000000000568 ) ) ;
#6364=AXIS2_PLACEMENT_3D ( 'NONE', #189883, #156897, #71237 ) ;
#6366=LINE ( 'NONE', #104173, #108876 ) ;
#6368=VERTEX_POINT ( 'NONE', #255417 ) ;
#6372=CIRCLE ( 'NONE', #152152, 11.64999999999999325 ) ;
#6433=ORIENTED_EDGE ( 'NONE', *, *, #105260, .T. ) ;
#6439=DIRECTION ( 'NONE',  ( 1.000000000000000000, -0.000000000000000000, -0.000000000000000000 ) ) ;
#6453=AXIS2_PLACEMENT_3D ( 'NONE', #231278, #209118, #70930 ) ;
#6482=DIRECTION ( 'NONE',  ( 0.000000000000000000, -0.1350103645451876944, -0.9908441862701601321 ) ) ;
#6489=ORIENTED_EDGE ( 'NONE', *, *, #233999, .F. ) ;
#6492=DIRECTION ( 'NONE',  ( -3.469446951953635015E-14, 1.000000000000000000, 0.000000000000000000 ) ) ;
#6495=CARTESIAN_POINT ( 'NONE',  ( -21.55000000000000071, 7.150000000011155876, -54.75000000000000000 ) ) ;
#6516=COLOUR_RGB ( '', 0.31764706, 0.68627451, 0.89019608) ;
#6518=ORIENTED_EDGE ( 'NONE', *, *, #146395, .F. ) ;
#6519=LINE ( 'NONE', #87327, #113687 ) ;
#6523=EDGE_LOOP ( 'NONE', ( #72870, #3988, #143811, #185322 ) ) ;
#6529=FACE_OUTER_BOUND ( 'NONE', #118842, .T. ) ;
#6588=CARTESIAN_POINT ( 'NONE',  ( -21.14999999999999858, 1.115600667400684642E-11, -27.24142135623730354 ) ) ;
#6593=ADVANCED_FACE ( 'NONE', ( #161525 ), #226595, .T. ) ;
#6611=VECTOR ( 'NONE', #235610, 1000.000000000000000 ) ;
#6618=EDGE_LOOP ( 'NONE', ( #184516, #123347, #166057, #91264 ) ) ;
#6671=FACE_OUTER_BOUND ( 'NONE', #25142, .T. ) ;
#6695=DIRECTION ( 'NONE',  ( 0.000000000000000000, 1.000000000000000000, 0.000000000000000000 ) ) ;
#6697=EDGE_CURVE ( 'NONE', #116181, #165365, #27167, .T. ) ;
#6701=DIRECTION ( 'NONE',  ( -2.840903330521631775E-16, 0.8700118002898321601, -0.4930308989875230030 ) ) ;
#6714=CARTESIAN_POINT ( 'NONE',  ( 20.94999999999999574, 1.115600667400684642E-11, -33.50000000000000000 ) ) ;
#6723=AXIS2_PLACEMENT_3D ( 'NONE', #203649, #64142, #87531 ) ;
#6742=LINE ( 'NONE', #26321, #140859 ) ;
#6744=EDGE_LOOP ( 'NONE', ( #54289, #34267, #208333, #87364, #145522, #78735 ) ) ;
#6748=ORIENTED_EDGE ( 'NONE', *, *, #30880, .T. ) ;
#6764=FACE_OUTER_BOUND ( 'NONE', #239947, .T. ) ;
#6781=DIRECTION ( 'NONE',  ( -1.000000000000000000, 0.000000000000000000, 0.000000000000000000 ) ) ;
#6783=CARTESIAN_POINT ( 'NONE',  ( 20.90851465518106167, 10.32532329027886320, -72.56993430183595706 ) ) ;
#6788=ADVANCED_FACE ( 'NONE', ( #253861 ), #255107, .T. ) ;
#6789=CARTESIAN_POINT ( 'NONE',  ( -21.05000000000000071, -1.249999999988843369, -41.50000000000000000 ) ) ;
#6791=DIRECTION ( 'NONE',  ( 0.000000000000000000, 0.000000000000000000, -1.000000000000000000 ) ) ;
#6801=CARTESIAN_POINT ( 'NONE',  ( 21.05000000000000071, 1.115600667400684642E-11, -67.00000000000000000 ) ) ;
#6830=ORIENTED_EDGE ( 'NONE', *, *, #44908, .F. ) ;
#6853=EDGE_LOOP ( 'NONE', ( #84461, #227284, #112253 ) ) ;
#6866=EDGE_LOOP ( 'NONE', ( #147269, #228066 ) ) ;
#6873=VECTOR ( 'NONE', #147785, 1000.000000000000000 ) ;
#6893=DIRECTION ( 'NONE',  ( 1.000000000000000000, 0.000000000000000000, 0.000000000000000000 ) ) ;
#6941=CARTESIAN_POINT ( 'NONE',  ( -18.50000000000000000, -1.162701749926853712, -41.60000000000000142 ) ) ;
#6998=AXIS2_PLACEMENT_3D ( 'NONE', #111195, #87758, #90329 ) ;
#7043=FACE_OUTER_BOUND ( 'NONE', #25872, .T. ) ;
#7055=AXIS2_PLACEMENT_3D ( 'NONE', #169954, #113775, #70836 ) ;
#7056=CARTESIAN_POINT ( 'NONE',  ( 20.97107704358301916, 8.875478152032441059, -42.05897322938925953 ) ) ;
#7060=ORIENTED_EDGE ( 'NONE', *, *, #252807, .F. ) ;
#7069=DIRECTION ( 'NONE',  ( 0.000000000000000000, 0.000000000000000000, -1.000000000000000000 ) ) ;
#7072=ORIENTED_EDGE ( 'NONE', *, *, #31430, .T. ) ;
#7082=CIRCLE ( 'NONE', #2982, 0.1000000000000004496 ) ;
#7126=EDGE_LOOP ( 'NONE', ( #97862, #45176, #20917, #120791 ) ) ;
#7129=EDGE_CURVE ( 'NONE', #83334, #64314, #32966, .T. ) ;
#7138=CARTESIAN_POINT ( 'NONE',  ( -20.94999999999999929, 1.115600667400684642E-11, -41.40000000000000568 ) ) ;
#7145=VERTEX_POINT ( 'NONE', #193289 ) ;
#7183=CIRCLE ( 'NONE', #61372, 0.2000000000000057288 ) ;
#7223=ORIENTED_EDGE ( 'NONE', *, *, #194295, .T. ) ;
#7246=AXIS2_PLACEMENT_3D ( 'NONE', #244605, #183368, #7275 ) ;
#7247=CARTESIAN_POINT ( 'NONE',  ( -18.59999999999999787, 10.33248238083634440, -72.59484654391314962 ) ) ;
#7267=FACE_OUTER_BOUND ( 'NONE', #8250, .T. ) ;
#7275=DIRECTION ( 'NONE',  ( 0.000000000000000000, 1.000000000000000000, 0.000000000000000000 ) ) ;
#7284=VECTOR ( 'NONE', #81931, 1000.000000000000114 ) ;
#7310=CARTESIAN_POINT ( 'NONE',  ( -20.85000000000000142, 11.65000000001115232, -60.21613433702190576 ) ) ;
#7314=ORIENTED_EDGE ( 'NONE', *, *, #157983, .F. ) ;
#7316=CYLINDRICAL_SURFACE ( 'NONE', #164223, 4.049999999999998046 ) ;
#7325=VERTEX_POINT ( 'NONE', #45756 ) ;
#7333=CARTESIAN_POINT ( 'NONE',  ( 20.94999999999999929, 1.115600667400684642E-11, -67.00000000000000000 ) ) ;
#7358=DIRECTION ( 'NONE',  ( 0.000000000000000000, 0.000000000000000000, 1.000000000000000000 ) ) ;
#7368=CARTESIAN_POINT ( 'NONE',  ( -20.54999999999999716, -8.730841121484170131, -57.40192528101567149 ) ) ;
#7379=CARTESIAN_POINT ( 'NONE',  ( 21.05000000000000071, -8.730841121484166578, -57.40192528101567149 ) ) ;
#7415=EDGE_LOOP ( 'NONE', ( #78036, #87031, #93136, #49487 ) ) ;
#7433=ORIENTED_EDGE ( 'NONE', *, *, #233434, .F. ) ;
#7440=CARTESIAN_POINT ( 'NONE',  ( -21.64999999999999858, 7.350000000011155166, -45.85000000000000142 ) ) ;
#7450=AXIS2_PLACEMENT_3D ( 'NONE', #220181, #96354, #136775 ) ;
#7466=CARTESIAN_POINT ( 'NONE',  ( 21.07933241753356768, 6.328645948390905218, -33.40662040958070378 ) ) ;
#7485=FACE_OUTER_BOUND ( 'NONE', #186602, .T. ) ;
#7496=ADVANCED_FACE ( 'NONE', ( #246520 ), #208708, .F. ) ;
#7508=LINE ( 'NONE', #30960, #94603 ) ;
#7520=VERTEX_POINT ( 'NONE', #27526 ) ;
#7526=AXIS2_PLACEMENT_3D ( 'NONE', #84636, #144642, #125111 ) ;
#7532=EDGE_LOOP ( 'NONE', ( #140198, #128925, #234480, #166397 ) ) ;
#7562=ORIENTED_EDGE ( 'NONE', *, *, #47275, .T. ) ;
#7583=ORIENTED_EDGE ( 'NONE', *, *, #146163, .F. ) ;
#7603=ADVANCED_FACE ( 'NONE', ( #39056 ), #248763, .T. ) ;
#7607=LINE ( 'NONE', #44179, #34272 ) ;
#7627=DIRECTION ( 'NONE',  ( 0.000000000000000000, 0.000000000000000000, -1.000000000000000000 ) ) ;
#7650=EDGE_CURVE ( 'NONE', #31916, #195525, #71158, .T. ) ;
#7654=DIRECTION ( 'NONE',  ( 1.000000000000000000, 0.000000000000000000, -0.000000000000000000 ) ) ;
#7670=EDGE_CURVE ( 'NONE', #228463, #95688, #169696, .T. ) ;
#7685=DIRECTION ( 'NONE',  ( 0.000000000000000000, 0.000000000000000000, 1.000000000000000000 ) ) ;
#7695=CIRCLE ( 'NONE', #211716, 0.2000000000000057288 ) ;
#7713=CIRCLE ( 'NONE', #240928, 0.1999999999999999833 ) ;
#7724=CARTESIAN_POINT ( 'NONE',  ( -23.25000000000000000, 1.115600667400684642E-11, -74.90000000000000568 ) ) ;
#7778=CARTESIAN_POINT ( 'NONE',  ( -18.59999999999999787, 11.65000000001115232, -54.75000000000000000 ) ) ;
#7782=LINE ( 'NONE', #127729, #39398 ) ;
#7787=CARTESIAN_POINT ( 'NONE',  ( -18.59999999999999787, 1.340746217944851715, -23.22713749457881960 ) ) ;
#7794=ORIENTED_EDGE ( 'NONE', *, *, #219501, .F. ) ;
#7831=VECTOR ( 'NONE', #94934, 1000.000000000000000 ) ;
#7934=CARTESIAN_POINT ( 'NONE',  ( -20.64999999999999858, 2.000000000011154189, -53.77537807723790309 ) ) ;
#7947=DIRECTION ( 'NONE',  ( -0.000000000000000000, -0.000000000000000000, 1.000000000000000000 ) ) ;
#7956=DIRECTION ( 'NONE',  ( -1.000000000000000000, -7.304098846218134667E-16, 0.000000000000000000 ) ) ;
#7967=CARTESIAN_POINT ( 'NONE',  ( 18.59999999999998721, 6.933893972137497030, -70.78564583437358237 ) ) ;
#7977=LINE ( 'NONE', #109622, #218950 ) ;
#7997=CARTESIAN_POINT ( 'NONE',  ( 18.59999999999999076, 10.20857864377385127, -54.75000000000000000 ) ) ;
#8016=CARTESIAN_POINT ( 'NONE',  ( -18.59999999999999787, 11.65000000001115232, -45.65000000000000568 ) ) ;
#8021=ORIENTED_EDGE ( 'NONE', *, *, #91479, .F. ) ;
#8039=CARTESIAN_POINT ( 'NONE',  ( -21.05000000000000071, 1.162701749949165642, -41.40000000000000568 ) ) ;
#8051=CARTESIAN_POINT ( 'NONE',  ( 18.53317502108576775, 10.32263460347359896, -72.56059579686719019 ) ) ;
#8074=CARTESIAN_POINT ( 'NONE',  ( 21.05000000000000071, 8.776282895303632259, -42.05862899514094977 ) ) ;
#8083=CARTESIAN_POINT ( 'NONE',  ( 20.93975676684922504, 10.31104185824063180, -72.52045169831058047 ) ) ;
#8090=ADVANCED_FACE ( 'NONE', ( #255146 ), #74037, .F. ) ;
#8105=DIRECTION ( 'NONE',  ( 1.000000000000000000, 0.000000000000000000, 0.000000000000000000 ) ) ;
#8121=CARTESIAN_POINT ( 'NONE',  ( -18.48179518609235927, -9.518325300481611961, -73.88970557676125850 ) ) ;
#8145=CARTESIAN_POINT ( 'NONE',  ( 21.05000000000000071, 4.813084112160680661, -45.44151775652382952 ) ) ;
#8148=LINE ( 'NONE', #203771, #193827 ) ;
#8150=EDGE_CURVE ( 'NONE', #234522, #142401, #243335, .T. ) ;
#8192=EDGE_CURVE ( 'NONE', #186298, #39957, #211529, .T. ) ;
#8204=AXIS2_PLACEMENT_3D ( 'NONE', #110220, #51506, #30725 ) ;
#8222=ORIENTED_EDGE ( 'NONE', *, *, #162324, .T. ) ;
#8224=DIRECTION ( 'NONE',  ( 0.000000000000000000, 0.000000000000000000, -1.000000000000000000 ) ) ;
#8248=AXIS2_PLACEMENT_3D ( 'NONE', #43210, #122764, #202282 ) ;
#8250=EDGE_LOOP ( 'NONE', ( #41393, #142231, #124340, #101671, #151751 ) ) ;
#8279=DIRECTION ( 'NONE',  ( 0.000000000000000000, 0.000000000000000000, -1.000000000000000000 ) ) ;
#8318=CARTESIAN_POINT ( 'NONE',  ( -20.94999999999999929, 1.162701749949165642, -41.40000000000000568 ) ) ;
#8332=CARTESIAN_POINT ( 'NONE',  ( -23.24999999999999645, -9.599999999988845900, -73.70018939122203960 ) ) ;
#8344=DIRECTION ( 'NONE',  ( 1.000000000000000000, -0.000000000000000000, -0.000000000000000000 ) ) ;
#8361=FACE_OUTER_BOUND ( 'NONE', #85987, .T. ) ;
#8396=LINE ( 'NONE', #10960, #11744 ) ;
#8416=CARTESIAN_POINT ( 'NONE',  ( -20.64999999999999858, 4.250000000011156409, -45.85000000000000142 ) ) ;
#8471=DIRECTION ( 'NONE',  ( -1.000000000000000000, -0.000000000000000000, -0.000000000000000000 ) ) ;
#8477=CYLINDRICAL_SURFACE ( 'NONE', #210514, 0.09999999999999781286 ) ;
#8493=EDGE_CURVE ( 'NONE', #52785, #127250, #7713, .T. ) ;
#8503=DIRECTION ( 'NONE',  ( -4.701977403289178058E-30, 1.734723475976807094E-14, -1.000000000000000000 ) ) ;
#8511=DIRECTION ( 'NONE',  ( 0.000000000000000000, 0.000000000000000000, -1.000000000000000000 ) ) ;
#8520=AXIS2_PLACEMENT_3D ( 'NONE', #133955, #75308, #132695 ) ;
#8543=ORIENTED_EDGE ( 'NONE', *, *, #215253, .T. ) ;
#8603=EDGE_LOOP ( 'NONE', ( #183168, #202275, #45569, #145165 ) ) ;
#8669=CIRCLE ( 'NONE', #455, 0.1000000000000028644 ) ;
#8673=DIRECTION ( 'NONE',  ( -3.787827842127535236E-15, 0.7397360091702777085, 0.6728971962616808744 ) ) ;
#8687=EDGE_CURVE ( 'NONE', #80054, #177338, #126943, .T. ) ;
#8712=LINE ( 'NONE', #88213, #182042 ) ;
#8716=DIRECTION ( 'NONE',  ( 0.000000000000000000, 0.000000000000000000, -1.000000000000000000 ) ) ;
#8720=CIRCLE ( 'NONE', #187806, 0.1000000000000028644 ) ;
#8750=EDGE_LOOP ( 'NONE', ( #71673, #162290, #212872, #225772 ) ) ;
#8757=VECTOR ( 'NONE', #12999, 1000.000000000000000 ) ;
#8762=ORIENTED_EDGE ( 'NONE', *, *, #238929, .F. ) ;
#8772=CARTESIAN_POINT ( 'NONE',  ( 21.14999999999999858, 8.786607556611267356, -45.85000000000000142 ) ) ;
#8779=ORIENTED_EDGE ( 'NONE', *, *, #133673, .T. ) ;
#8820=DIRECTION ( 'NONE',  ( 0.000000000000000000, 1.000000000000000000, 0.000000000000000000 ) ) ;
#8825=CARTESIAN_POINT ( 'NONE',  ( 21.05933563467872105, 10.72452471209247626, -45.69364774895595360 ) ) ;
#8827=VERTEX_POINT ( 'NONE', #116062 ) ;
#8863=DIRECTION ( 'NONE',  ( 0.000000000000000000, 0.000000000000000000, -1.000000000000000000 ) ) ;
#8872=FACE_OUTER_BOUND ( 'NONE', #159097, .T. ) ;
#8879=CARTESIAN_POINT ( 'NONE',  ( -20.54999999999999716, 4.350000000011156054, -54.75000000000000000 ) ) ;
#8891=VECTOR ( 'NONE', #99785, 1000.000000000000000 ) ;
#8895=AXIS2_PLACEMENT_3D ( 'NONE', #156485, #57321, #136878 ) ;
#8931=AXIS2_PLACEMENT_3D ( 'NONE', #95889, #178029, #137576 ) ;
#8943=ORIENTED_EDGE ( 'NONE', *, *, #83176, .T. ) ;
#8944=CARTESIAN_POINT ( 'NONE',  ( 22.57320508075688892, 11.75000000001115552, -33.50000000000000000 ) ) ;
#8958=DIRECTION ( 'NONE',  ( 0.000000000000000000, 0.000000000000000000, -1.000000000000000000 ) ) ;
#8970=DIRECTION ( 'NONE',  ( 0.000000000000000000, -0.000000000000000000, -1.000000000000000000 ) ) ;
#9015=CYLINDRICAL_SURFACE ( 'NONE', #167160, 12.87499999999999822 ) ;
#9029=VERTEX_POINT ( 'NONE', #5052 ) ;
#9076=EDGE_CURVE ( 'NONE', #74863, #7145, #79854, .T. ) ;
#9077=DIRECTION ( 'NONE',  ( 3.265361837132813093E-16, -1.000000000000000000, -0.000000000000000000 ) ) ;
#9085=ORIENTED_EDGE ( 'NONE', *, *, #33521, .T. ) ;
#9102=AXIS2_PLACEMENT_3D ( 'NONE', #36327, #195406, #207587 ) ;
#9105=VERTEX_POINT ( 'NONE', #210995 ) ;
#9155=CARTESIAN_POINT ( 'NONE',  ( -20.94999999999999929, 7.031312794766356511, -70.60915093822731592 ) ) ;
#9178=ORIENTED_EDGE ( 'NONE', *, *, #172551, .F. ) ;
#9183=CARTESIAN_POINT ( 'NONE',  ( 21.14999999999999858, 11.75000000001116263, -45.65000000000000568 ) ) ;
#9191=VERTEX_POINT ( 'NONE', #97422 ) ;
#9270=VECTOR ( 'NONE', #192080, 1000.000000000000000 ) ;
#9280=ORIENTED_EDGE ( 'NONE', *, *, #193178, .T. ) ;
#9287=VERTEX_POINT ( 'NONE', #75358 ) ;
#9322=ORIENTED_EDGE ( 'NONE', *, *, #163419, .T. ) ;
#9367=ORIENTED_EDGE ( 'NONE', *, *, #29750, .T. ) ;
#9411=CARTESIAN_POINT ( 'NONE',  ( -21.05000000000000071, 1.115600667400684642E-11, -67.00000000000000000 ) ) ;
#9415=CIRCLE ( 'NONE', #234262, 0.5000000000000004441 ) ;
#9420=CIRCLE ( 'NONE', #84379, 0.1000000000000028644 ) ;
#9437=ORIENTED_EDGE ( 'NONE', *, *, #237116, .T. ) ;
#9453=DIRECTION ( 'NONE',  ( -1.000000000000000000, -0.000000000000000000, -0.000000000000000000 ) ) ;
#9481=CARTESIAN_POINT ( 'NONE',  ( 18.49713797159849094, -9.446482327567860438, -40.57145812161018483 ) ) ;
#9537=EDGE_LOOP ( 'NONE', ( #165368, #75255, #171496, #80000, #155976 ) ) ;
#9541=DIRECTION ( 'NONE',  ( 0.000000000000000000, 0.008583690987127922528, 0.9999631594459055250 ) ) ;
#9551=AXIS2_PLACEMENT_3D ( 'NONE', #28457, #45406, #253860 ) ;
#9585=CARTESIAN_POINT ( 'NONE',  ( -18.50000000000000000, 9.250000000011157297, -45.85000000000000142 ) ) ;
#9624=ORIENTED_EDGE ( 'NONE', *, *, #169884, .F. ) ;
#9642=AXIS2_PLACEMENT_3D ( 'NONE', #118101, #131576, #78943 ) ;
#9691=ORIENTED_EDGE ( 'NONE', *, *, #115004, .T. ) ;
#9707=CIRCLE ( 'NONE', #192889, 0.5000000000000004441 ) ;
#9718=VERTEX_POINT ( 'NONE', #163543 ) ;
#9723=CIRCLE ( 'NONE', #30605, 0.1000000000000028644 ) ;
#9749=CARTESIAN_POINT ( 'NONE',  ( 20.94999999999999929, -11.64999999998883595, -66.99999999999998579 ) ) ;
#9771=DIRECTION ( 'NONE',  ( -1.000000000000000000, 0.000000000000000000, 0.000000000000000000 ) ) ;
#9810=CYLINDRICAL_SURFACE ( 'NONE', #145737, 0.09999999999999939493 ) ;
#9823=DIRECTION ( 'NONE',  ( 0.000000000000000000, -1.000000000000000000, 0.000000000000000000 ) ) ;
#9829=ADVANCED_FACE ( 'NONE', ( #166152 ), #205217, .T. ) ;
#9832=CIRCLE ( 'NONE', #222196, 0.1000000000000028644 ) ;
#9854=DIRECTION ( 'NONE',  ( 0.000000000000000000, 0.000000000000000000, -1.000000000000000000 ) ) ;
#9906=ADVANCED_FACE ( 'NONE', ( #92989 ), #212949, .F. ) ;
#9923=LINE ( 'NONE', #71204, #78981 ) ;
#9924=CARTESIAN_POINT ( 'NONE',  ( 20.94999999999999929, -9.399999999988846611, -43.39396912265245021 ) ) ;
#9977=ORIENTED_EDGE ( 'NONE', *, *, #187753, .T. ) ;
#10003=CARTESIAN_POINT ( 'NONE',  ( -23.15000000000000213, 1.910280373842936141, -46.13136785519893834 ) ) ;
#10008=DIRECTION ( 'NONE',  ( 0.000000000000000000, -0.000000000000000000, -1.000000000000000000 ) ) ;
#10017=B_SPLINE_CURVE_WITH_KNOTS ( 'NONE', 3,
 ( #206799, #162559, #225052, #184655 ),
 .UNSPECIFIED., .F., .F.,
 ( 4, 4 ),
 ( 0.000000000000000000, 0.0002118541922231869474 ),
 .UNSPECIFIED. ) ;
#10036=CARTESIAN_POINT ( 'NONE',  ( 21.08134388332232234, 6.334680580529114202, -33.42418108249297859 ) ) ;
#10038=ADVANCED_FACE ( 'NONE', ( #141026 ), #100565, .T. ) ;
#10043=AXIS2_PLACEMENT_3D ( 'NONE', #169417, #248926, #205929 ) ;
#10051=CARTESIAN_POINT ( 'NONE',  ( -18.59999999999999787, -1.162701749926853712, -41.50000000000000000 ) ) ;
#10063=EDGE_CURVE ( 'NONE', #79373, #79923, #104426, .T. ) ;
#10076=DIRECTION ( 'NONE',  ( -0.000000000000000000, -0.8660254037844459241, -0.4999999999999873990 ) ) ;
#10100=DIRECTION ( 'NONE',  ( 1.000000000000000000, 0.000000000000000000, 0.000000000000000000 ) ) ;
#10105=EDGE_LOOP ( 'NONE', ( #90135, #149196, #205089 ) ) ;
#10155=ORIENTED_EDGE ( 'NONE', *, *, #9076, .T. ) ;
#10158=DIRECTION ( 'NONE',  ( -2.252264143451594314E-15, -0.1298341882520124002, -0.9915357197604841577 ) ) ;
#10167=CARTESIAN_POINT ( 'NONE',  ( 20.94999999999999574, 14.00000000001115730, -38.92709253038254502 ) ) ;
#10227=CIRCLE ( 'NONE', #105857, 0.09999999999999939493 ) ;
#10237=ORIENTED_EDGE ( 'NONE', *, *, #175533, .T. ) ;
#10246=ORIENTED_EDGE ( 'NONE', *, *, #89715, .F. ) ;
#10278=ORIENTED_EDGE ( 'NONE', *, *, #112126, .F. ) ;
#10295=DIRECTION ( 'NONE',  ( 0.000000000000000000, 0.9915357197604837136, -0.1298341882520134827 ) ) ;
#10314=EDGE_LOOP ( 'NONE', ( #635, #229159, #146735, #174698 ) ) ;
#10345=CARTESIAN_POINT ( 'NONE',  ( -21.14999999999999858, 1.115600667400684642E-11, -26.95934304829875927 ) ) ;
#10347=EDGE_CURVE ( 'NONE', #162149, #208880, #233416, .T. ) ;
#10404=CARTESIAN_POINT ( 'NONE',  ( 23.14999999999998437, 1.115600667400684642E-11, -33.50000000000000000 ) ) ;
#10417=CYLINDRICAL_SURFACE ( 'NONE', #33560, 0.1000000000000028644 ) ;
#10422=EDGE_LOOP ( 'NONE', ( #62459, #224548, #132059, #170278 ) ) ;
#10434=DIRECTION ( 'NONE',  ( -3.469446951953635015E-14, -1.000000000000000000, 0.000000000000000000 ) ) ;
#10439=CARTESIAN_POINT ( 'NONE',  ( 23.15000000000000213, -8.596261682231828516, -57.54987248284972168 ) ) ;
#10468=ORIENTED_EDGE ( 'NONE', *, *, #240463, .F. ) ;
#10475=CARTESIAN_POINT ( 'NONE',  ( -22.48660254037843487, 11.75000000001115730, -33.45000000000001705 ) ) ;
#10515=ORIENTED_EDGE ( 'NONE', *, *, #132208, .F. ) ;
#10557=ORIENTED_EDGE ( 'NONE', *, *, #81410, .T. ) ;
#10569=AXIS2_PLACEMENT_3D ( 'NONE', #141584, #2057, #222374 ) ;
#10590=CIRCLE ( 'NONE', #14703, 0.1000000000000028644 ) ;
#10614=DIRECTION ( 'NONE',  ( -0.000000000000000000, -0.000000000000000000, 1.000000000000000000 ) ) ;
#10637=DIRECTION ( 'NONE',  ( 0.000000000000000000, 0.000000000000000000, 1.000000000000000000 ) ) ;
#10645=ORIENTED_EDGE ( 'NONE', *, *, #85169, .T. ) ;
#10668=AXIS2_PLACEMENT_3D ( 'NONE', #27103, #244820, #66201 ) ;
#10669=CARTESIAN_POINT ( 'NONE',  ( 23.14999999999999503, 6.650000000011155876, -54.65000000000000568 ) ) ;
#10732=EDGE_LOOP ( 'NONE', ( #38691, #25118, #57792, #84019 ) ) ;
#10733=LINE ( 'NONE', #71998, #225700 ) ;
#10738=EDGE_CURVE ( 'NONE', #207975, #40042, #179945, .T. ) ;
#10770=B_SPLINE_CURVE_WITH_KNOTS ( 'NONE', 3,
 ( #205307, #167516, #26716, #226137, #166238, #127077 ),
 .UNSPECIFIED., .F., .F.,
 ( 4, 2, 4 ),
 ( 1.138412281109779656E-18, 0.0001569047307838639517, 0.0003138094615677267650 ),
 .UNSPECIFIED. ) ;
#10774=CARTESIAN_POINT ( 'NONE',  ( 20.04142135623730070, 11.75000000001115907, -58.15000000000000568 ) ) ;
#10780=CARTESIAN_POINT ( 'NONE',  ( 18.54147908293611735, -9.463261657916959280, -40.54894889675577474 ) ) ;
#10782=ORIENTED_EDGE ( 'NONE', *, *, #154940, .F. ) ;
#10815=FACE_OUTER_BOUND ( 'NONE', #217541, .T. ) ;
#10825=ORIENTED_EDGE ( 'NONE', *, *, #22648, .T. ) ;
#10828=AXIS2_PLACEMENT_3D ( 'NONE', #71289, #148229, #10008 ) ;
#10844=AXIS2_PLACEMENT_3D ( 'NONE', #48261, #89947, #132952 ) ;
#10845=ORIENTED_EDGE ( 'NONE', *, *, #227484, .F. ) ;
#10866=DIRECTION ( 'NONE',  ( 1.000000000000000000, -0.000000000000000000, -0.000000000000000000 ) ) ;
#10912=AXIS2_PLACEMENT_3D ( 'NONE', #34003, #112235, #230903 ) ;
#10913=DIRECTION ( 'NONE',  ( -1.000000000000000000, -0.000000000000000000, -0.000000000000000000 ) ) ;
#10942=AXIS2_PLACEMENT_3D ( 'NONE', #77212, #118937, #245 ) ;
#10960=CARTESIAN_POINT ( 'NONE',  ( -21.05000000000000071, -1.162701749926853712, -41.50000000000000000 ) ) ;
#10965=DIRECTION ( 'NONE',  ( 1.000000000000000000, 0.000000000000000000, -0.000000000000000000 ) ) ;
#10967=ORIENTED_EDGE ( 'NONE', *, *, #145010, .T. ) ;
#10982=EDGE_LOOP ( 'NONE', ( #67471, #42334, #246857, #1716 ) ) ;
#10989=EDGE_CURVE ( 'NONE', #205142, #2443, #38648, .T. ) ;
#10990=ORIENTED_EDGE ( 'NONE', *, *, #185402, .T. ) ;
#10993=EDGE_LOOP ( 'NONE', ( #167230, #119676, #164749, #16639 ) ) ;
#10995=LINE ( 'NONE', #184483, #101367 ) ;
#11094=DIRECTION ( 'NONE',  ( 7.304098846218134667E-16, -1.000000000000000000, 0.000000000000000000 ) ) ;
#11124=CARTESIAN_POINT ( 'NONE',  ( 18.49999999999996803, 7.070967871809997973, -70.74656422186831151 ) ) ;
#11131=CIRCLE ( 'NONE', #94321, 0.1000000000000028644 ) ;
#11164=CYLINDRICAL_SURFACE ( 'NONE', #116341, 0.5000000000000004441 ) ;
#11166=EDGE_CURVE ( 'NONE', #177338, #244896, #9415, .T. ) ;
#11167=AXIS2_PLACEMENT_3D ( 'NONE', #206063, #26160, #149962 ) ;
#11170=CARTESIAN_POINT ( 'NONE',  ( -18.50000000000000000, 11.65000000001115232, -45.75000000000000000 ) ) ;
#11237=ORIENTED_EDGE ( 'NONE', *, *, #84950, .F. ) ;
#11241=EDGE_CURVE ( 'NONE', #138871, #79373, #234447, .T. ) ;
#11273=ORIENTED_EDGE ( 'NONE', *, *, #158800, .T. ) ;
#11279=DIRECTION ( 'NONE',  ( 0.000000000000000000, 0.000000000000000000, -1.000000000000000000 ) ) ;
#11317=ORIENTED_EDGE ( 'NONE', *, *, #55809, .T. ) ;
#11325=CARTESIAN_POINT ( 'NONE',  ( 21.14250536705908345, 6.518172176891880554, -33.50000000000000000 ) ) ;
#11326=AXIS2_PLACEMENT_3D ( 'NONE', #176584, #215670, #17485 ) ;
#11341=FACE_OUTER_BOUND ( 'NONE', #53203, .T. ) ;
#11382=CARTESIAN_POINT ( 'NONE',  ( 20.85000000000000142, 1.115600667400684642E-11, -74.90000000000000568 ) ) ;
#11393=VECTOR ( 'NONE', #4022, 1000.000000000000227 ) ;
#11426=DIRECTION ( 'NONE',  ( -1.000000000000000000, -1.836970198721029934E-16, 0.000000000000000000 ) ) ;
#11431=AXIS2_PLACEMENT_3D ( 'NONE', #136407, #197686, #60738 ) ;
#11440=EDGE_CURVE ( 'NONE', #252850, #201612, #67870, .T. ) ;
#11448=CIRCLE ( 'NONE', #169702, 0.2000000000000057288 ) ;
#11459=DIRECTION ( 'NONE',  ( 0.000000000000000000, -0.8660254037844411501, -0.4999999999999956146 ) ) ;
#11481=CARTESIAN_POINT ( 'NONE',  ( -20.99749315643149217, 11.75000000001115197, -59.98519423124096761 ) ) ;
#11484=ORIENTED_EDGE ( 'NONE', *, *, #203124, .T. ) ;
#11492=CARTESIAN_POINT ( 'NONE',  ( -22.39999999999999858, 0.1000000000111554016, -25.70922040162659883 ) ) ;
#11499=EDGE_CURVE ( 'NONE', #163909, #126285, #78194, .T. ) ;
#11520=DIRECTION ( 'NONE',  ( 0.000000000000000000, -0.1350103645451876666, 0.9908441862701600211 ) ) ;
#11526=ORIENTED_EDGE ( 'NONE', *, *, #206611, .F. ) ;
#11552=ORIENTED_EDGE ( 'NONE', *, *, #55832, .T. ) ;
#11556=CIRCLE ( 'NONE', #15845, 0.09999999999999982514 ) ;
#11575=AXIS2_PLACEMENT_3D ( 'NONE', #167935, #110488, #32270 ) ;
#11590=VERTEX_POINT ( 'NONE', #112220 ) ;
#11598=AXIS2_PLACEMENT_3D ( 'NONE', #215582, #177776, #117775 ) ;
#11626=DIRECTION ( 'NONE',  ( -3.265361837132813093E-16, 1.000000000000000000, 0.000000000000000000 ) ) ;
#11666=EDGE_LOOP ( 'NONE', ( #237404, #79063, #224062, #25503, #213283 ) ) ;
#11682=EDGE_LOOP ( 'NONE', ( #197009, #165294, #137426 ) ) ;
#11698=EDGE_CURVE ( 'NONE', #161314, #256777, #197232, .T. ) ;
#11700=CARTESIAN_POINT ( 'NONE',  ( -21.14999999999999858, 1.115600667400684642E-11, -21.85042919245520210 ) ) ;
#11706=LINE ( 'NONE', #32576, #8757 ) ;
#11718=VERTEX_POINT ( 'NONE', #118640 ) ;
#11721=ADVANCED_FACE ( 'NONE', ( #198149 ), #76394, .T. ) ;
#11734=VERTEX_POINT ( 'NONE', #87174 ) ;
#11744=VECTOR ( 'NONE', #87888, 1000.000000000000000 ) ;
#11746=DIRECTION ( 'NONE',  ( -1.000000000000000000, 0.000000000000000000, 0.000000000000000000 ) ) ;
#11751=CARTESIAN_POINT ( 'NONE',  ( -23.15000000000000213, 11.65000000001115588, -59.98519422934606382 ) ) ;
#11774=ORIENTED_EDGE ( 'NONE', *, *, #70752, .T. ) ;
#11778=EDGE_CURVE ( 'NONE', #244896, #34405, #213805, .T. ) ;
#11784=ORIENTED_EDGE ( 'NONE', *, *, #65565, .T. ) ;
#11806=CARTESIAN_POINT ( 'NONE',  ( -21.93340585971692747, 7.324147022868200629, -33.50000000000000711 ) ) ;
#11827=AXIS2_PLACEMENT_3D ( 'NONE', #37801, #96439, #254234 ) ;
#11852=ORIENTED_EDGE ( 'NONE', *, *, #191270, .T. ) ;
#11929=EDGE_CURVE ( 'NONE', #183157, #67224, #163913, .T. ) ;
#11945=CARTESIAN_POINT ( 'NONE',  ( 20.94999999999999574, 1.261786168576181755, -41.58649896354548048 ) ) ;
#11957=ORIENTED_EDGE ( 'NONE', *, *, #200757, .F. ) ;
#11962=EDGE_CURVE ( 'NONE', #189515, #193526, #138922, .T. ) ;
#11967=ORIENTED_EDGE ( 'NONE', *, *, #245641, .T. ) ;
#11971=DIRECTION ( 'NONE',  ( 1.000000000000000000, 2.952720810173289112E-16, -0.000000000000000000 ) ) ;
#12017=AXIS2_PLACEMENT_3D ( 'NONE', #83044, #4804, #106467 ) ;
#12022=EDGE_CURVE ( 'NONE', #39510, #43703, #109734, .T. ) ;
#12027=ADVANCED_FACE ( 'NONE', ( #218674 ), #161305, .T. ) ;
#12043=CIRCLE ( 'NONE', #195389, 0.1000000000000028644 ) ;
#12070=ORIENTED_EDGE ( 'NONE', *, *, #76404, .T. ) ;
#12094=CARTESIAN_POINT ( 'NONE',  ( -20.07928932188135107, 9.220710678129810489, -45.85000000000000142 ) ) ;
#12099=CARTESIAN_POINT ( 'NONE',  ( -20.94999999999999929, 7.070967871809997973, -70.74656422186831151 ) ) ;
#12102=ORIENTED_EDGE ( 'NONE', *, *, #216926, .T. ) ;
#12118=ORIENTED_EDGE ( 'NONE', *, *, #242706, .T. ) ;
#12121=DIRECTION ( 'NONE',  ( -2.342056488767301376E-15, -0.1350103645451904977, 0.9908441862701596881 ) ) ;
#12132=DIRECTION ( 'NONE',  ( -0.000000000000000000, -0.000000000000000000, 1.000000000000000000 ) ) ;
#12177=DIRECTION ( 'NONE',  ( -1.000000000000000000, 0.000000000000000000, 0.000000000000000000 ) ) ;
#12182=CARTESIAN_POINT ( 'NONE',  ( 18.49999999999999289, 11.65000000001115943, -58.35000000000000142 ) ) ;
#12202=DIRECTION ( 'NONE',  ( 0.000000000000000000, 0.000000000000000000, -1.000000000000000000 ) ) ;
#12206=CARTESIAN_POINT ( 'NONE',  ( -21.05000000000000071, 1.162701749949165642, -41.60000000000000142 ) ) ;
#12215=CARTESIAN_POINT ( 'NONE',  ( -23.25000000000000000, 7.021664781911246322, -70.83356540189728889 ) ) ;
#12238=CARTESIAN_POINT ( 'NONE',  ( -18.59999999999999787, 11.65000000001115232, -40.51480577065400013 ) ) ;
#12248=AXIS2_PLACEMENT_3D ( 'NONE', #32677, #56010, #213834 ) ;
#12263=DIRECTION ( 'NONE',  ( -2.561896900575096011E-15, -0.5907332058517279494, 0.8068669527897025517 ) ) ;
#12323=ADVANCED_FACE ( 'NONE', ( #193694 ), #211981, .T. ) ;
#12378=ADVANCED_FACE ( 'NONE', ( #256155 ), #60577, .T. ) ;
#12391=ADVANCED_FACE ( 'NONE', ( #181827 ), #240516, .T. ) ;
#12423=CIRCLE ( 'NONE', #158200, 0.1000000000000008937 ) ;
#12436=DIRECTION ( 'NONE',  ( -1.000000000000000000, -0.000000000000000000, -0.000000000000000000 ) ) ;
#12445=VERTEX_POINT ( 'NONE', #17596 ) ;
#12448=VERTEX_POINT ( 'NONE', #179286 ) ;
#12449=CARTESIAN_POINT ( 'NONE',  ( 21.05000000000000071, -11.29603075032412640, -63.95210084033612929 ) ) ;
#12501=DIRECTION ( 'NONE',  ( 1.000000000000000000, 0.000000000000000000, -0.000000000000000000 ) ) ;
#12512=LINE ( 'NONE', #215800, #102707 ) ;
#12521=DIRECTION ( 'NONE',  ( 1.000000000000000000, 0.000000000000000000, 0.000000000000000000 ) ) ;
#12533=VECTOR ( 'NONE', #190441, 1000.000000000000000 ) ;
#12546=CARTESIAN_POINT ( 'NONE',  ( 21.04999999999999716, 8.894723818389001835, -41.98708432314988670 ) ) ;
#12579=LINE ( 'NONE', #28303, #213719 ) ;
#12595=ORIENTED_EDGE ( 'NONE', *, *, #23555, .F. ) ;
#12615=VERTEX_POINT ( 'NONE', #245655 ) ;
#12616=CARTESIAN_POINT ( 'NONE',  ( -21.05000000000000071, 0.03363273534480175353, -27.24118280531852321 ) ) ;
#12618=EDGE_LOOP ( 'NONE', ( #229654, #45752, #54759, #204208 ) ) ;
#12625=DIRECTION ( 'NONE',  ( -1.836970198721029934E-16, 1.000000000000000000, 0.000000000000000000 ) ) ;
#12632=ORIENTED_EDGE ( 'NONE', *, *, #130354, .F. ) ;
#12633=LINE ( 'NONE', #229096, #201087 ) ;
#12636=ORIENTED_EDGE ( 'NONE', *, *, #146302, .T. ) ;
#12658=CARTESIAN_POINT ( 'NONE',  ( -18.44448725179913851, -9.490081715472173940, -73.62896029406249454 ) ) ;
#12660=CIRCLE ( 'NONE', #20864, 0.1000000000000008799 ) ;
#12666=CARTESIAN_POINT ( 'NONE',  ( -20.94999999999999929, -11.64999999998884483, -67.00000000000000000 ) ) ;
#12700=EDGE_LOOP ( 'NONE', ( #220085, #47729, #135777, #225300 ) ) ;
#12726=DIRECTION ( 'NONE',  ( 1.000000000000000000, 0.000000000000000000, 0.000000000000000000 ) ) ;
#12767=VERTEX_POINT ( 'NONE', #149142 ) ;
#12783=CIRCLE ( 'NONE', #91858, 0.09999999999999939493 ) ;
#12786=CIRCLE ( 'NONE', #50151, 0.09999999999999939493 ) ;
#12794=CARTESIAN_POINT ( 'NONE',  ( -23.25000000000000000, -1.249999999988843369, -74.80048075441509070 ) ) ;
#12828=ORIENTED_EDGE ( 'NONE', *, *, #46792, .T. ) ;
#12840=CARTESIAN_POINT ( 'NONE',  ( -18.59999999999999787, 11.65000000001115232, -21.75000000000000355 ) ) ;
#12883=ORIENTED_EDGE ( 'NONE', *, *, #219270, .T. ) ;
#12995=ORIENTED_EDGE ( 'NONE', *, *, #87188, .F. ) ;
#12999=DIRECTION ( 'NONE',  ( -0.000000000000000000, -0.000000000000000000, 1.000000000000000000 ) ) ;
#13033=CARTESIAN_POINT ( 'NONE',  ( -21.05000000000000071, 1.115600667400684642E-11, -33.50000000000000000 ) ) ;
#13053=AXIS2_PLACEMENT_3D ( 'NONE', #105099, #244638, #67293 ) ;
#13057=ORIENTED_EDGE ( 'NONE', *, *, #227183, .T. ) ;
#13064=ORIENTED_EDGE ( 'NONE', *, *, #56105, .T. ) ;
#13068=CARTESIAN_POINT ( 'NONE',  ( 20.85000000000000142, -11.74999999998883560, -64.00000000000000000 ) ) ;
#13086=DIRECTION ( 'NONE',  ( 0.000000000000000000, 1.000000000000000000, 0.000000000000000000 ) ) ;
#13096=ADVANCED_FACE ( 'NONE', ( #108409 ), #55517, .T. ) ;
#13101=PLANE ( 'NONE',  #189063 ) ;
#13105=ORIENTED_EDGE ( 'NONE', *, *, #174275, .F. ) ;
#13115=CARTESIAN_POINT ( 'NONE',  ( -22.48660254037843487, 11.65000000001115588, -33.45000000000002416 ) ) ;
#13121=ORIENTED_EDGE ( 'NONE', *, *, #248982, .F. ) ;
#13136=CARTESIAN_POINT ( 'NONE',  ( -22.39999999999999858, 1.115600667400684642E-11, -33.39999999999999858 ) ) ;
#13164=EDGE_CURVE ( 'NONE', #9191, #63552, #188840, .T. ) ;
#13167=VECTOR ( 'NONE', #238833, 1000.000000000000000 ) ;
#13190=DIRECTION ( 'NONE',  ( 0.000000000000000000, -1.000000000000000000, -0.000000000000000000 ) ) ;
#13198=AXIS2_PLACEMENT_3D ( 'NONE', #104241, #125128, #67704 ) ;
#13209=DIRECTION ( 'NONE',  ( 0.000000000000000000, 0.000000000000000000, 1.000000000000000000 ) ) ;
#13231=CIRCLE ( 'NONE', #72048, 0.5000000000000004441 ) ;
#13254=ADVANCED_FACE ( 'NONE', ( #199167 ), #20552, .F. ) ;
#13266=ORIENTED_EDGE ( 'NONE', *, *, #194452, .T. ) ;
#13278=CARTESIAN_POINT ( 'NONE',  ( 21.05543885634738643, 8.775771046858691804, -45.68438447071469000 ) ) ;
#13295=EDGE_LOOP ( 'NONE', ( #252546, #212376, #100208, #53276 ) ) ;
#13301=CARTESIAN_POINT ( 'NONE',  ( 20.85000000000000142, -1.835859311432481045, -78.50443916879852679 ) ) ;
#13317=ORIENTED_EDGE ( 'NONE', *, *, #83640, .F. ) ;
#13337=ORIENTED_EDGE ( 'NONE', *, *, #14973, .F. ) ;
#13350=AXIS2_PLACEMENT_3D ( 'NONE', #247675, #248973, #172030 ) ;
#13373=CARTESIAN_POINT ( 'NONE',  ( -23.15000000000000213, 11.65000000001115588, -59.98519422934604961 ) ) ;
#13429=EDGE_CURVE ( 'NONE', #153815, #242609, #155734, .T. ) ;
#13523=B_SPLINE_CURVE_WITH_KNOTS ( 'NONE', 3,
 ( #218489, #121987, #119428, #102383, #219788, #200239, #180684, #2016, #81538, #202801, #161122, #84084, #3297, #159846, #82818, #162413, #163686, #243203, #241920 ),
 .UNSPECIFIED., .F., .F.,
 ( 4, 3, 3, 3, 3, 3, 4 ),
 ( -2.000416914658901521E-06, 0.000000000000000000, 4.714008503744565809E-05, 9.979203887777271477E-05, 0.0001372215519229478891, 0.0001635031576220937453, 0.0001900083748504128364 ),
 .UNSPECIFIED. ) ;
#13525=DIRECTION ( 'NONE',  ( 0.000000000000000000, 0.000000000000000000, -1.000000000000000000 ) ) ;
#13527=FACE_OUTER_BOUND ( 'NONE', #67741, .T. ) ;
#13546=CARTESIAN_POINT ( 'NONE',  ( 22.39999999999999858, 7.790779598384538929, -33.39999999999999858 ) ) ;
#13556=ORIENTED_EDGE ( 'NONE', *, *, #252807, .T. ) ;
#13611=DIRECTION ( 'NONE',  ( 0.000000000000000000, 1.000000000000000000, 0.000000000000000000 ) ) ;
#13628=DIRECTION ( 'NONE',  ( 1.000000000000000000, -0.000000000000000000, -0.000000000000000000 ) ) ;
#13636=ORIENTED_EDGE ( 'NONE', *, *, #82816, .F. ) ;
#13651=CIRCLE ( 'NONE', #121822, 0.09999999999999939493 ) ;
#13673=ORIENTED_EDGE ( 'NONE', *, *, #185696, .T. ) ;
#13700=CARTESIAN_POINT ( 'NONE',  ( -18.50000000000000000, 11.65000000001115232, -21.75000000000000355 ) ) ;
#13709=VECTOR ( 'NONE', #50487, 1000.000000000000000 ) ;
#13710=DIRECTION ( 'NONE',  ( 0.000000000000000000, 0.000000000000000000, 1.000000000000000000 ) ) ;
#13727=CARTESIAN_POINT ( 'NONE',  ( 18.59999999999999076, -1.149570369564537842, -74.81591248450196474 ) ) ;
#13750=CARTESIAN_POINT ( 'NONE',  ( 22.59999999999999787, 11.64957080755595520, -33.40000000000000568 ) ) ;
#13765=DIRECTION ( 'NONE',  ( 1.000000000000000000, -0.000000000000000000, -0.000000000000000000 ) ) ;
#13807=TOROIDAL_SURFACE ( 'NONE', #151391, 7.791421356237335338, 0.1000000000000000056 ) ;
#13845=CARTESIAN_POINT ( 'NONE',  ( 19.75857864376269291, 11.75000000001116440, -58.25000000000000711 ) ) ;
#13850=AXIS2_PLACEMENT_3D ( 'NONE', #86311, #128047, #200198 ) ;
#13880=ORIENTED_EDGE ( 'NONE', *, *, #46792, .F. ) ;
#13888=CARTESIAN_POINT ( 'NONE',  ( 21.14999999999999858, 11.75000000001116263, -33.60000000000000142 ) ) ;
#13890=AXIS2_PLACEMENT_3D ( 'NONE', #242404, #182461, #59901 ) ;
#13892=CARTESIAN_POINT ( 'NONE',  ( 20.94999999999999574, -11.64999999998883595, -36.39999999999999858 ) ) ;
#13900=CARTESIAN_POINT ( 'NONE',  ( 21.05000000000000071, 1.115625160336667635E-11, -65.00000000000000000 ) ) ;
#13947=AXIS2_PLACEMENT_3D ( 'NONE', #171696, #214623, #116825 ) ;
#13948=AXIS2_PLACEMENT_3D ( 'NONE', #98544, #115583, #94734 ) ;
#13953=LINE ( 'NONE', #249988, #154408 ) ;
#13956=ORIENTED_EDGE ( 'NONE', *, *, #69339, .T. ) ;
#13961=VERTEX_POINT ( 'NONE', #161686 ) ;
#13969=DIRECTION ( 'NONE',  ( 0.000000000000000000, 0.000000000000000000, -1.000000000000000000 ) ) ;
#13992=CARTESIAN_POINT ( 'NONE',  ( 20.95512820512820440, 10.62384868372303615, -41.16491356908760935 ) ) ;
#13995=ORIENTED_EDGE ( 'NONE', *, *, #15006, .T. ) ;
#14003=DIRECTION ( 'NONE',  ( 0.000000000000000000, -0.1455152366551522025, -0.9893560106964505163 ) ) ;
#14005=VERTEX_POINT ( 'NONE', #126384 ) ;
#14009=EDGE_CURVE ( 'NONE', #205018, #971, #81033, .T. ) ;
#14117=CARTESIAN_POINT ( 'NONE',  ( -21.14999999999999858, 0.09779029131994770863, -27.24218538952388613 ) ) ;
#14163=LINE ( 'NONE', #113231, #217553 ) ;
#14175=DIRECTION ( 'NONE',  ( 0.000000000000000000, -1.000000000000000000, 0.000000000000000000 ) ) ;
#14176=AXIS2_PLACEMENT_3D ( 'NONE', #104242, #24763, #100386 ) ;
#14190=AXIS2_PLACEMENT_3D ( 'NONE', #140799, #121276, #41711 ) ;
#14215=CARTESIAN_POINT ( 'NONE',  ( -20.85000000000000142, -1.164121893230052995, -74.71484808557160306 ) ) ;
#14219=VERTEX_POINT ( 'NONE', #211062 ) ;
#14235=DIRECTION ( 'NONE',  ( 0.000000000000000000, 0.000000000000000000, -1.000000000000000000 ) ) ;
#14240=AXIS2_PLACEMENT_3D ( 'NONE', #121610, #240257, #23795 ) ;
#14245=CARTESIAN_POINT ( 'NONE',  ( -18.59999999999999787, 11.65000000001115232, -40.51480577065400013 ) ) ;
#14253=ADVANCED_FACE ( 'NONE', ( #190221 ), #185112, .T. ) ;
#14261=CARTESIAN_POINT ( 'NONE',  ( -21.05000000000000071, -1.835341550213257733, -45.05515129256298223 ) ) ;
#14284=ORIENTED_EDGE ( 'NONE', *, *, #11929, .F. ) ;
#14344=CARTESIAN_POINT ( 'NONE',  ( -20.85000000000000142, 7.021664781911246322, -70.63356540189728605 ) ) ;
#14345=CARTESIAN_POINT ( 'NONE',  ( -20.07928932188135107, 9.220710678129810489, -54.65000000000000568 ) ) ;
#14351=CARTESIAN_POINT ( 'NONE',  ( -22.48660254037843487, 11.65000000001115588, -33.45000000000001705 ) ) ;
#14369=CARTESIAN_POINT ( 'NONE',  ( -18.60000000000001208, -9.364240527579751117, -40.68024858184076464 ) ) ;
#14374=CARTESIAN_POINT ( 'NONE',  ( -21.07094088545304089, 6.320167221927643020, -33.40110629744778237 ) ) ;
#14376=CARTESIAN_POINT ( 'NONE',  ( 20.95512820512820440, 10.62384868372303615, -45.65000000000000568 ) ) ;
#14377=CARTESIAN_POINT ( 'NONE',  ( 20.95512820512820440, 8.876151316299271343, -45.65000000000000568 ) ) ;
#14383=VECTOR ( 'NONE', #242227, 1000.000000000000000 ) ;
#14384=CYLINDRICAL_SURFACE ( 'NONE', #107146, 0.09999999999999939493 ) ;
#14397=DIRECTION ( 'NONE',  ( 0.000000000000000000, 0.8660254037844383745, -0.5000000000000003331 ) ) ;
#14404=DIRECTION ( 'NONE',  ( -3.265361837132813093E-16, 1.000000000000000000, 0.000000000000000000 ) ) ;
#14429=DIRECTION ( 'NONE',  ( 1.000000000000000000, 0.000000000000000000, 0.000000000000000000 ) ) ;
#14458=CARTESIAN_POINT ( 'NONE',  ( -21.05000000000000071, -11.48912529306489994, -63.89999999999999858 ) ) ;
#14511=CARTESIAN_POINT ( 'NONE',  ( 18.49999999999999289, 10.49142135624846439, -58.35000000000000142 ) ) ;
#14514=CARTESIAN_POINT ( 'NONE',  ( 18.33683296300444709, -9.511149971121596991, -73.90570741271007194 ) ) ;
#14530=ORIENTED_EDGE ( 'NONE', *, *, #138525, .T. ) ;
#14540=AXIS2_PLACEMENT_3D ( 'NONE', #175216, #36973, #116480 ) ;
#14565=VERTEX_POINT ( 'NONE', #51640 ) ;
#14577=AXIS2_PLACEMENT_3D ( 'NONE', #178816, #19718, #238755 ) ;
#14578=CARTESIAN_POINT ( 'NONE',  ( 21.07964655665547582, 8.774889614989714204, -45.72191658296406302 ) ) ;
#14582=FACE_OUTER_BOUND ( 'NONE', #59442, .T. ) ;
#14585=LINE ( 'NONE', #253159, #84005 ) ;
#14626=CARTESIAN_POINT ( 'NONE',  ( 20.02499999999999858, 9.750000000011153745, -54.65000000000000568 ) ) ;
#14632=AXIS2_PLACEMENT_3D ( 'NONE', #221346, #199255, #58417 ) ;
#14640=VERTEX_POINT ( 'NONE', #75119 ) ;
#14656=EDGE_CURVE ( 'NONE', #253488, #147289, #142519, .T. ) ;
#14685=CARTESIAN_POINT ( 'NONE',  ( 21.51976009735019346, 6.910458441670357388, -33.50000000000000000 ) ) ;
#14692=EDGE_CURVE ( 'NONE', #70987, #134912, #223617, .T. ) ;
#14703=AXIS2_PLACEMENT_3D ( 'NONE', #73660, #29409, #153202 ) ;
#14704=VERTEX_POINT ( 'NONE', #182881 ) ;
#14705=DIRECTION ( 'NONE',  ( -0.000000000000000000, -1.897661533703519897E-16, 1.000000000000000000 ) ) ;
#14719=ORIENTED_EDGE ( 'NONE', *, *, #173317, .T. ) ;
#14744=VECTOR ( 'NONE', #168678, 1000.000000000000114 ) ;
#14759=CYLINDRICAL_SURFACE ( 'NONE', #237124, 0.09999999999999939493 ) ;
#14760=DIRECTION ( 'NONE',  ( 1.000000000000000000, 0.000000000000000000, -0.000000000000000000 ) ) ;
#14771=VERTEX_POINT ( 'NONE', #11945 ) ;
#14781=FACE_OUTER_BOUND ( 'NONE', #43905, .T. ) ;
#14786=ADVANCED_FACE ( 'NONE', ( #173620 ), #106335, .T. ) ;
#14793=ORIENTED_EDGE ( 'NONE', *, *, #4582, .T. ) ;
#14799=VERTEX_POINT ( 'NONE', #251811 ) ;
#14826=CARTESIAN_POINT ( 'NONE',  ( 20.84999999999999787, 11.75000000001116085, -60.08085275404130243 ) ) ;
#14828=CIRCLE ( 'NONE', #60574, 0.1999999999999987899 ) ;
#14840=AXIS2_PLACEMENT_3D ( 'NONE', #210928, #184944, #165390 ) ;
#14863=CARTESIAN_POINT ( 'NONE',  ( -20.85000000000000142, 1.115600667400684642E-11, -67.00000000000000000 ) ) ;
#14890=CARTESIAN_POINT ( 'NONE',  ( -21.14999999999999858, 11.75000000001115552, -40.22613063605918882 ) ) ;
#14925=CARTESIAN_POINT ( 'NONE',  ( 23.14999999999999858, 1.115625160336667635E-11, -65.00000000000000000 ) ) ;
#14927=CARTESIAN_POINT ( 'NONE',  ( 18.59999999999998366, 1.115600667400684642E-11, -67.00000000000000000 ) ) ;
#14939=ADVANCED_FACE ( 'NONE', ( #159164 ), #219090, .F. ) ;
#14973=EDGE_CURVE ( 'NONE', #162457, #14005, #248297, .T. ) ;
#14983=CIRCLE ( 'NONE', #160753, 0.09999999999999907574 ) ;
#15001=CARTESIAN_POINT ( 'NONE',  ( 18.49999999999999289, 10.49142135624846617, -58.25000000000000711 ) ) ;
#15006=EDGE_CURVE ( 'NONE', #148274, #90674, #224234, .T. ) ;
#15035=CIRCLE ( 'NONE', #114974, 0.1000000000000028644 ) ;
#15057=LINE ( 'NONE', #94563, #17689 ) ;
#15074=DIRECTION ( 'NONE',  ( -0.000000000000000000, -1.000000000000000000, 6.308085367188393199E-16 ) ) ;
#15088=ORIENTED_EDGE ( 'NONE', *, *, #21799, .T. ) ;
#15098=VERTEX_POINT ( 'NONE', #147271 ) ;
#15100=CARTESIAN_POINT ( 'NONE',  ( 20.95429402530547591, 8.876194151113343977, -42.02308669793784901 ) ) ;
#15103=AXIS2_PLACEMENT_3D ( 'NONE', #80076, #16316, #158406 ) ;
#15108=EDGE_CURVE ( 'NONE', #171525, #8827, #14983, .T. ) ;
#15122=ORIENTED_EDGE ( 'NONE', *, *, #209530, .F. ) ;
#15134=CARTESIAN_POINT ( 'NONE',  ( 19.83283456528360489, 11.75000000001116263, -58.34999999942034776 ) ) ;
#15145=ORIENTED_EDGE ( 'NONE', *, *, #146126, .T. ) ;
#15163=CIRCLE ( 'NONE', #160915, 0.1000000000000028644 ) ;
#15170=CARTESIAN_POINT ( 'NONE',  ( -21.05000000000000426, -0.09999999998884338825, -27.02293297887525014 ) ) ;
#15187=CARTESIAN_POINT ( 'NONE',  ( 23.24999999999999645, 5.600000000011153389, -45.90526601891310321 ) ) ;
#15213=AXIS2_PLACEMENT_3D ( 'NONE', #223725, #63366, #202890 ) ;
#15218=CARTESIAN_POINT ( 'NONE',  ( -18.41418431465368855, -9.499999999989071853, -73.60018939122146264 ) ) ;
#15244=ORIENTED_EDGE ( 'NONE', *, *, #2245, .F. ) ;
#15299=ADVANCED_FACE ( 'NONE', ( #37614 ), #136680, .F. ) ;
#15322=ORIENTED_EDGE ( 'NONE', *, *, #10738, .T. ) ;
#15337=DIRECTION ( 'NONE',  ( 0.000000000000000000, -0.1495327102803689356, -0.9887567792719336168 ) ) ;
#15341=CARTESIAN_POINT ( 'NONE',  ( -20.85000000000000142, 11.75000000001115197, -60.21613433702190576 ) ) ;
#15416=EDGE_CURVE ( 'NONE', #15545, #139599, #223242, .T. ) ;
#15417=DIRECTION ( 'NONE',  ( 0.000000000000000000, 1.000000000000000000, 0.000000000000000000 ) ) ;
#15444=ORIENTED_EDGE ( 'NONE', *, *, #65169, .F. ) ;
#15475=CARTESIAN_POINT ( 'NONE',  ( -22.01447462590972748, 7.263800201241075172, -33.40096299994046092 ) ) ;
#15493=ORIENTED_EDGE ( 'NONE', *, *, #68181, .T. ) ;
#15529=ORIENTED_EDGE ( 'NONE', *, *, #69402, .F. ) ;
#15533=VERTEX_POINT ( 'NONE', #152120 ) ;
#15545=VERTEX_POINT ( 'NONE', #52984 ) ;
#15559=EDGE_LOOP ( 'NONE', ( #162881, #114282, #36473, #36130 ) ) ;
#15627=EDGE_CURVE ( 'NONE', #254522, #60369, #248379, .T. ) ;
#15635=CARTESIAN_POINT ( 'NONE',  ( -21.05000000000000071, 11.65000000001115232, -33.60000000000000142 ) ) ;
#15656=DIRECTION ( 'NONE',  ( 1.000000000000000000, -0.000000000000000000, -0.000000000000000000 ) ) ;
#15664=DIRECTION ( 'NONE',  ( -1.000000000000000000, -0.000000000000000000, -0.000000000000000000 ) ) ;
#15691=DIRECTION ( 'NONE',  ( 1.000000000000000000, 3.265361837132813093E-16, -0.000000000000000000 ) ) ;
#15747=ADVANCED_FACE ( 'NONE', ( #116824 ), #173433, .T. ) ;
#15764=EDGE_CURVE ( 'NONE', #171125, #125125, #94260, .T. ) ;
#15775=CARTESIAN_POINT ( 'NONE',  ( -23.25000000000000000, 1.115600667400684642E-11, -33.50000000000000000 ) ) ;
#15776=DIRECTION ( 'NONE',  ( 1.000000000000000000, -0.000000000000000000, -0.000000000000000000 ) ) ;
#15798=LINE ( 'NONE', #253077, #3770 ) ;
#15814=CARTESIAN_POINT ( 'NONE',  ( -22.39999999999999858, 11.65000000001115588, -33.40000000000000568 ) ) ;
#15831=ADVANCED_FACE ( 'NONE', ( #101049 ), #24158, .F. ) ;
#15843=AXIS2_PLACEMENT_3D ( 'NONE', #77458, #18787, #133602 ) ;
#15845=AXIS2_PLACEMENT_3D ( 'NONE', #252407, #54216, #213289 ) ;
#15889=ORIENTED_EDGE ( 'NONE', *, *, #195982, .T. ) ;
#15900=AXIS2_PLACEMENT_3D ( 'NONE', #70146, #28464, #8863 ) ;
#15903=EDGE_CURVE ( 'NONE', #126100, #131047, #90333, .T. ) ;
#15919=LINE ( 'NONE', #177570, #219483 ) ;
#15922=CARTESIAN_POINT ( 'NONE',  ( -21.05000000000000071, 6.540656951712397138, -33.60000000000000142 ) ) ;
#15937=FACE_OUTER_BOUND ( 'NONE', #120027, .T. ) ;
#15948=CARTESIAN_POINT ( 'NONE',  ( 18.46905048506369340, -9.473744257371235378, -73.67598629225537366 ) ) ;
#15959=CARTESIAN_POINT ( 'NONE',  ( 18.50000000000000000, -9.399999999988843058, -40.79725975966329798 ) ) ;
#15989=CARTESIAN_POINT ( 'NONE',  ( -22.39999999999999858, -0.09999999998884338825, -21.85042919245520210 ) ) ;
#15997=CARTESIAN_POINT ( 'NONE',  ( -23.15000000000000213, 11.75000000001115552, -59.98519422934606382 ) ) ;
#16000=ORIENTED_EDGE ( 'NONE', *, *, #147961, .T. ) ;
#16017=CARTESIAN_POINT ( 'NONE',  ( -21.05000000000000071, -0.2561057920810652089, -33.46510355832771211 ) ) ;
#16049=CARTESIAN_POINT ( 'NONE',  ( 23.14999999999999858, 6.650000000011155876, -45.85000000000000142 ) ) ;
#16068=CARTESIAN_POINT ( 'NONE',  ( -23.25000000000000000, 1.115649040949250830E-11, -63.10000000000000142 ) ) ;
#16122=DIRECTION ( 'NONE',  ( 0.000000000000000000, 0.000000000000000000, -1.000000000000000000 ) ) ;
#16131=CARTESIAN_POINT ( 'NONE',  ( 23.14999999999999858, 5.500000000011153745, -54.59473398108690390 ) ) ;
#16146=LINE ( 'NONE', #254678, #222156 ) ;
#16209=EDGE_CURVE ( 'NONE', #139486, #2368, #36388, .T. ) ;
#16211=DIRECTION ( 'NONE',  ( 7.304098846218134667E-16, -1.000000000000000000, 0.000000000000000000 ) ) ;
#16218=CARTESIAN_POINT ( 'NONE',  ( 20.94999999999999574, 1.750000000011155743, -45.16951155790165018 ) ) ;
#16238=DIRECTION ( 'NONE',  ( 0.000000000000000000, -0.8700118002898359348, 0.4930308989875165082 ) ) ;
#16250=VERTEX_POINT ( 'NONE', #160811 ) ;
#16258=ADVANCED_FACE ( 'NONE', ( #194164 ), #248013, .F. ) ;
#16287=DIRECTION ( 'NONE',  ( 0.000000000000000000, 0.000000000000000000, -1.000000000000000000 ) ) ;
#16301=FACE_OUTER_BOUND ( 'NONE', #107670, .T. ) ;
#16316=DIRECTION ( 'NONE',  ( 1.000000000000000000, 0.000000000000000000, -0.000000000000000000 ) ) ;
#16318=CARTESIAN_POINT ( 'NONE',  ( 21.14999999999999858, 11.65000000001116298, -45.75000000000000711 ) ) ;
#16322=FACE_OUTER_BOUND ( 'NONE', #141089, .T. ) ;
#16330=DIRECTION ( 'NONE',  ( 0.000000000000000000, 1.000000000000000000, 0.000000000000000000 ) ) ;
#16333=PLANE ( 'NONE',  #83987 ) ;
#16339=DIRECTION ( 'NONE',  ( 3.469446951953635015E-14, -0.000000000000000000, 1.000000000000000000 ) ) ;
#16344=DIRECTION ( 'NONE',  ( 0.000000000000000000, 0.000000000000000000, -1.000000000000000000 ) ) ;
#16348=AXIS2_PLACEMENT_3D ( 'NONE', #56313, #116322, #118893 ) ;
#16355=DIRECTION ( 'NONE',  ( 0.000000000000000000, 0.000000000000000000, -1.000000000000000000 ) ) ;
#16361=DIRECTION ( 'NONE',  ( 0.000000000000000000, 1.000000000000000000, 0.000000000000000000 ) ) ;
#16370=DIRECTION ( 'NONE',  ( -4.391705002472929091E-16, 1.000000000000000000, 0.000000000000000000 ) ) ;
#16386=DIRECTION ( 'NONE',  ( -1.000000000000000000, 0.000000000000000000, 0.000000000000000000 ) ) ;
#16405=CARTESIAN_POINT ( 'NONE',  ( -20.85000000000000497, 11.75000000001115019, -60.08085275404129533 ) ) ;
#16408=CARTESIAN_POINT ( 'NONE',  ( -23.15000000000000213, 5.950000000011163692, -56.69429769496518645 ) ) ;
#16416=CARTESIAN_POINT ( 'NONE',  ( -23.15000000000000213, 1.115600667400684642E-11, -54.12500000000000711 ) ) ;
#16421=CARTESIAN_POINT ( 'NONE',  ( 20.85882249326303040, 10.33248238083634796, -72.59484654391314962 ) ) ;
#16431=CARTESIAN_POINT ( 'NONE',  ( 19.96984138294285671, 11.75000000001126921, -58.22457207120090317 ) ) ;
#16435=AXIS2_PLACEMENT_3D ( 'NONE', #195715, #256888, #178729 ) ;
#16446=DIRECTION ( 'NONE',  ( 1.000000000000000000, 0.000000000000000000, 0.000000000000000000 ) ) ;
#16458=DIRECTION ( 'NONE',  ( -0.7071067811865388020, 0.7071067811865561215, 0.000000000000000000 ) ) ;
#16459=AXIS2_PLACEMENT_3D ( 'NONE', #95377, #113650, #212769 ) ;
#16460=DIRECTION ( 'NONE',  ( 0.000000000000000000, -0.000000000000000000, 1.000000000000000000 ) ) ;
#16483=EDGE_LOOP ( 'NONE', ( #223056, #107679, #130941, #176405 ) ) ;
#16501=DIRECTION ( 'NONE',  ( 1.000000000000000000, 0.000000000000000000, 0.000000000000000000 ) ) ;
#16520=AXIS2_PLACEMENT_3D ( 'NONE', #246518, #251661, #197774 ) ;
#16531=DIRECTION ( 'NONE',  ( 1.000000000000000000, 0.000000000000000000, 0.000000000000000000 ) ) ;
#16557=ORIENTED_EDGE ( 'NONE', *, *, #128949, .T. ) ;
#16577=AXIS2_PLACEMENT_3D ( 'NONE', #229556, #105710, #185286 ) ;
#16580=ORIENTED_EDGE ( 'NONE', *, *, #146163, .T. ) ;
#16583=FILL_AREA_STYLE ('',( #76524 ) ) ;
#16590=CIRCLE ( 'NONE', #45790, 0.1000000000000008799 ) ;
#16591=VECTOR ( 'NONE', #92388, 1000.000000000000000 ) ;
#16639=ORIENTED_EDGE ( 'NONE', *, *, #87554, .T. ) ;
#16642=ADVANCED_FACE ( 'NONE', ( #70063 ), #128135, .F. ) ;
#16647=FACE_OUTER_BOUND ( 'NONE', #38562, .T. ) ;
#16687=CIRCLE ( 'NONE', #33458, 12.87499999999999822 ) ;
#16740=ORIENTED_EDGE ( 'NONE', *, *, #248990, .F. ) ;
#16752=DIRECTION ( 'NONE',  ( -1.000000000000000000, -2.952720810173289112E-16, 0.000000000000000000 ) ) ;
#16755=DIRECTION ( 'NONE',  ( -0.000000000000000000, 0.8660254037844411501, 0.4999999999999956701 ) ) ;
#16756=ORIENTED_EDGE ( 'NONE', *, *, #213121, .T. ) ;
#16786=ADVANCED_FACE ( 'NONE', ( #37347 ), #193843, .T. ) ;
#16798=CARTESIAN_POINT ( 'NONE',  ( -21.05000000000000071, -11.48912529306489994, -64.00000000000000000 ) ) ;
#16805=VERTEX_POINT ( 'NONE', #174324 ) ;
#16821=CARTESIAN_POINT ( 'NONE',  ( 20.94999999999999929, -1.135018845899022466, -74.71697688343232358 ) ) ;
#16830=DIRECTION ( 'NONE',  ( 0.000000000000000000, 1.000000000000000000, 0.000000000000000000 ) ) ;
#16832=ORIENTED_EDGE ( 'NONE', *, *, #134045, .F. ) ;
#16856=B_SPLINE_CURVE_WITH_KNOTS ( 'NONE', 3,
 ( #247425, #205731, #45381, #145751, #124930, #27141, #203168, #49228 ),
 .UNSPECIFIED., .F., .F.,
 ( 4, 2, 2, 4 ),
 ( 0.000000000000000000, 0.0002181133598169129764, 0.0003271700397253546246, 0.0004362267196337962999 ),
 .UNSPECIFIED. ) ;
#16861=VERTEX_POINT ( 'NONE', #118149 ) ;
#16941=ADVANCED_FACE ( 'NONE', ( #62039 ), #245804, .T. ) ;
#16944=ORIENTED_EDGE ( 'NONE', *, *, #250398, .F. ) ;
#16965=DIRECTION ( 'NONE',  ( 0.000000000000000000, 0.000000000000000000, -1.000000000000000000 ) ) ;
#16993=LINE ( 'NONE', #256809, #82188 ) ;
#16994=EDGE_LOOP ( 'NONE', ( #96701, #187121, #212255, #29009 ) ) ;
#17009=CIRCLE ( 'NONE', #212640, 0.09999999999999867328 ) ;
#17010=EDGE_CURVE ( 'NONE', #3674, #205356, #87978, .T. ) ;
#17039=EDGE_LOOP ( 'NONE', ( #153258, #127188, #2782, #232813 ) ) ;
#17051=AXIS2_PLACEMENT_3D ( 'NONE', #228733, #192174, #13525 ) ;
#17073=CARTESIAN_POINT ( 'NONE',  ( 18.46163235739470920, -9.480150806907120753, -73.65761053987772300 ) ) ;
#17085=FACE_OUTER_BOUND ( 'NONE', #68079, .T. ) ;
#17109=DIRECTION ( 'NONE',  ( 1.000000000000000000, 0.000000000000000000, 0.000000000000000000 ) ) ;
#17119=AXIS2_PLACEMENT_3D ( 'NONE', #54875, #191871, #106179 ) ;
#17123=CARTESIAN_POINT ( 'NONE',  ( -18.40904629823847216, -9.499999999988851584, -73.60018956248165978 ) ) ;
#17124=CIRCLE ( 'NONE', #254396, 11.70000000000000284 ) ;
#17141=VECTOR ( 'NONE', #133161, 1000.000000000000000 ) ;
#17195=DIRECTION ( 'NONE',  ( -7.304098846218134667E-16, -1.000000000000000000, 0.000000000000000000 ) ) ;
#17196=DIRECTION ( 'NONE',  ( 0.000000000000000000, 0.000000000000000000, -1.000000000000000000 ) ) ;
#17219=DIRECTION ( 'NONE',  ( 0.000000000000000000, -0.8660254037844384856, 0.5000000000000002220 ) ) ;
#17236=DIRECTION ( 'NONE',  ( 0.000000000000000000, 1.000000000000000000, -6.938893903907270030E-14 ) ) ;
#17237=CIRCLE ( 'NONE', #46421, 0.09999999999999761857 ) ;
#17240=DIRECTION ( 'NONE',  ( 1.000000000000000000, 1.836970198721029934E-16, 0.000000000000000000 ) ) ;
#17261=DIRECTION ( 'NONE',  ( -0.000000000000000000, -0.000000000000000000, 1.000000000000000000 ) ) ;
#17283=EDGE_LOOP ( 'NONE', ( #74086, #36358, #11967, #24862 ) ) ;
#17305=CIRCLE ( 'NONE', #175522, 0.4000000000000045186 ) ;
#17363=DIRECTION ( 'NONE',  ( -1.000000000000000000, -0.000000000000000000, 0.000000000000000000 ) ) ;
#17371=ORIENTED_EDGE ( 'NONE', *, *, #203827, .F. ) ;
#17391=CARTESIAN_POINT ( 'NONE',  ( 20.94999999999999574, -1.162701749926853712, -41.60000000000000142 ) ) ;
#17418=DIRECTION ( 'NONE',  ( 1.000000000000000000, 0.000000000000000000, -0.000000000000000000 ) ) ;
#17420=VERTEX_POINT ( 'NONE', #35504 ) ;
#17430=VECTOR ( 'NONE', #136849, 1000.000000000000000 ) ;
#17436=VERTEX_POINT ( 'NONE', #52441 ) ;
#17485=DIRECTION ( 'NONE',  ( 1.000000000000000000, 1.875376730785737719E-16, 0.000000000000000000 ) ) ;
#17530=DIRECTION ( 'NONE',  ( -7.304098846218134667E-16, -1.000000000000000000, 0.000000000000000000 ) ) ;
#17560=CIRCLE ( 'NONE', #30089, 0.1000000000000028644 ) ;
#17561=AXIS2_PLACEMENT_3D ( 'NONE', #66991, #206503, #109964 ) ;
#17568=CARTESIAN_POINT ( 'NONE',  ( 18.49999999999999289, 11.65000000001115588, -67.00000000000000000 ) ) ;
#17572=CARTESIAN_POINT ( 'NONE',  ( -23.15000000000000213, 4.150000000011156764, -21.75000000000000355 ) ) ;
#17585=CARTESIAN_POINT ( 'NONE',  ( 20.94999999999999929, 5.000000000011153745, -45.90526601891310321 ) ) ;
#17588=AXIS2_PLACEMENT_3D ( 'NONE', #163112, #122703, #137111 ) ;
#17595=DIRECTION ( 'NONE',  ( -0.000000000000000000, 0.000000000000000000, -1.000000000000000000 ) ) ;
#17596=CARTESIAN_POINT ( 'NONE',  ( -23.25000000000000000, -11.64999999998884483, -33.50000000000000000 ) ) ;
#17610=CARTESIAN_POINT ( 'NONE',  ( -21.05000000000000071, 0.09779029131994597390, -27.24218538952387902 ) ) ;
#17613=ORIENTED_EDGE ( 'NONE', *, *, #69120, .F. ) ;
#17630=AXIS2_PLACEMENT_3D ( 'NONE', #103343, #122939, #219440 ) ;
#17651=CARTESIAN_POINT ( 'NONE',  ( 21.05000000000000071, 8.776282889879928106, -45.67621514106831171 ) ) ;
#17658=DIRECTION ( 'NONE',  ( -0.000000000000000000, -0.000000000000000000, -1.000000000000000000 ) ) ;
#17689=VECTOR ( 'NONE', #136236, 1000.000000000000000 ) ;
#17700=VERTEX_POINT ( 'NONE', #234645 ) ;
#17709=DIRECTION ( 'NONE',  ( 0.000000000000000000, 1.000000000000000000, 0.000000000000000000 ) ) ;
#17716=AXIS2_PLACEMENT_3D ( 'NONE', #38917, #95019, #118457 ) ;
#17741=VERTEX_POINT ( 'NONE', #14345 ) ;
#17774=ORIENTED_EDGE ( 'NONE', *, *, #224895, .T. ) ;
#17783=AXIS2_PLACEMENT_3D ( 'NONE', #238241, #40082, #175736 ) ;
#17785=VECTOR ( 'NONE', #234489, 1000.000000000000000 ) ;
#17879=EDGE_CURVE ( 'NONE', #16805, #48144, #44916, .T. ) ;
#17902=ORIENTED_EDGE ( 'NONE', *, *, #99216, .T. ) ;
#17910=ORIENTED_EDGE ( 'NONE', *, *, #239462, .T. ) ;
#17914=EDGE_LOOP ( 'NONE', ( #170686, #185163, #99423, #224636 ) ) ;
#17915=AXIS2_PLACEMENT_3D ( 'NONE', #226494, #88264, #49163 ) ;
#17938=DIRECTION ( 'NONE',  ( 0.000000000000000000, 0.000000000000000000, -1.000000000000000000 ) ) ;
#17948=CARTESIAN_POINT ( 'NONE',  ( 20.96937028524355640, 10.62446937163783289, -40.99142610116961549 ) ) ;
#17952=CARTESIAN_POINT ( 'NONE',  ( -22.39999999999999858, 7.790779598384560245, -33.39999999999999858 ) ) ;
#17976=DIRECTION ( 'NONE',  ( 1.000000000000000000, -0.000000000000000000, -0.000000000000000000 ) ) ;
#17993=ADVANCED_FACE ( 'NONE', ( #8872 ), #53089, .T. ) ;
#18006=AXIS2_PLACEMENT_3D ( 'NONE', #214221, #237635, #18586 ) ;
#18012=CARTESIAN_POINT ( 'NONE',  ( -21.07928932188134041, 6.328516656404449492, -33.40110485434561127 ) ) ;
#18026=AXIS2_PLACEMENT_3D ( 'NONE', #34438, #56506, #193490 ) ;
#18042=DIRECTION ( 'NONE',  ( 0.000000000000000000, 1.000000000000000000, 0.000000000000000000 ) ) ;
#18057=DIRECTION ( 'NONE',  ( 0.000000000000000000, 0.000000000000000000, -1.000000000000000000 ) ) ;
#18058=CARTESIAN_POINT ( 'NONE',  ( -22.50000000000000000, 11.75000000001115552, -33.50000000000000000 ) ) ;
#18087=CARTESIAN_POINT ( 'NONE',  ( 18.59999999999999787, 1.851028230152016674, -45.15391326942249606 ) ) ;
#18122=FACE_OUTER_BOUND ( 'NONE', #11666, .T. ) ;
#18163=DIRECTION ( 'NONE',  ( -1.000000000000000000, -3.265361837132813093E-16, 0.000000000000000000 ) ) ;
#18190=DIRECTION ( 'NONE',  ( 0.000000000000000000, -1.000000000000000000, 0.000000000000000000 ) ) ;
#18222=CARTESIAN_POINT ( 'NONE',  ( 22.43288208788031568, 0.004899854896538678728, -21.85034815628092630 ) ) ;
#18252=DIRECTION ( 'NONE',  ( 7.304098846218134667E-16, -1.000000000000000000, 0.000000000000000000 ) ) ;
#18276=ORIENTED_EDGE ( 'NONE', *, *, #1607, .T. ) ;
#18288=AXIS2_PLACEMENT_3D ( 'NONE', #172790, #213148, #76196 ) ;
#18305=CARTESIAN_POINT ( 'NONE',  ( -21.53752568622133268, 0.09897446127756706624, -26.71319212545143174 ) ) ;
#18344=DIRECTION ( 'NONE',  ( 0.000000000000000000, 0.9999631594459058581, 0.008583690987093516023 ) ) ;
#18357=AXIS2_PLACEMENT_3D ( 'NONE', #132432, #13765, #16355 ) ;
#18367=ORIENTED_EDGE ( 'NONE', *, *, #185402, .F. ) ;
#18396=CIRCLE ( 'NONE', #172004, 0.09999999999999939493 ) ;
#18415=ORIENTED_EDGE ( 'NONE', *, *, #60317, .T. ) ;
#18421=CIRCLE ( 'NONE', #14176, 0.3999999999999975797 ) ;
#18426=EDGE_CURVE ( 'NONE', #162457, #26532, #140766, .T. ) ;
#18439=ORIENTED_EDGE ( 'NONE', *, *, #20638, .T. ) ;
#18467=AXIS2_PLACEMENT_3D ( 'NONE', #138892, #21569, #218449 ) ;
#18481=FACE_BOUND ( 'NONE', #110793, .T. ) ;
#18494=ADVANCED_FACE ( 'NONE', ( #168962 ), #146453, .F. ) ;
#18498=CARTESIAN_POINT ( 'NONE',  ( -18.59999999999999787, 11.75000000001115197, -21.75000000000000355 ) ) ;
#18508=VECTOR ( 'NONE', #214536, 1000.000000000000114 ) ;
#18521=CIRCLE ( 'NONE', #151814, 0.1000000000000028644 ) ;
#18531=EDGE_CURVE ( 'NONE', #197537, #41243, #45267, .T. ) ;
#18540=CARTESIAN_POINT ( 'NONE',  ( -21.14999999999999858, 11.75000000001115552, -40.28386566297815108 ) ) ;
#18548=DIRECTION ( 'NONE',  ( 1.000000000000000000, 0.000000000000000000, 0.000000000000000000 ) ) ;
#18549=AXIS2_PLACEMENT_3D ( 'NONE', #51589, #231557, #230254 ) ;
#18566=CARTESIAN_POINT ( 'NONE',  ( -20.85000000000000142, 1.115600667400684642E-11, -67.00000000000000000 ) ) ;
#18586=DIRECTION ( 'NONE',  ( -1.000000000000000000, 0.000000000000000000, 0.000000000000000000 ) ) ;
#18621=VERTEX_POINT ( 'NONE', #100882 ) ;
#18629=AXIS2_PLACEMENT_3D ( 'NONE', #86013, #243831, #191601 ) ;
#18644=CIRCLE ( 'NONE', #60323, 0.1000000000000028644 ) ;
#18666=VERTEX_POINT ( 'NONE', #163476 ) ;
#18673=DIRECTION ( 'NONE',  ( -0.000000000000000000, -0.1298341882520022694, -0.9915357197604853789 ) ) ;
#18678=DIRECTION ( 'NONE',  ( 0.000000000000000000, 0.000000000000000000, -1.000000000000000000 ) ) ;
#18695=ORIENTED_EDGE ( 'NONE', *, *, #143026, .T. ) ;
#18706=VECTOR ( 'NONE', #78452, 1000.000000000000000 ) ;
#18736=ORIENTED_EDGE ( 'NONE', *, *, #123635, .F. ) ;
#18739=ORIENTED_EDGE ( 'NONE', *, *, #237753, .F. ) ;
#18762=FACE_OUTER_BOUND ( 'NONE', #200068, .T. ) ;
#18787=DIRECTION ( 'NONE',  ( 0.000000000000000000, -1.000000000000000000, 0.000000000000000000 ) ) ;
#18802=EDGE_CURVE ( 'NONE', #64202, #192209, #140966, .T. ) ;
#18803=EDGE_CURVE ( 'NONE', #108455, #201436, #216129, .T. ) ;
#18860=DIRECTION ( 'NONE',  ( 1.000000000000000000, 0.000000000000000000, 0.000000000000000000 ) ) ;
#18866=EDGE_CURVE ( 'NONE', #3656, #131987, #150785, .T. ) ;
#18894=DIRECTION ( 'NONE',  ( 0.000000000000000000, 1.000000000000000000, 0.000000000000000000 ) ) ;
#18897=AXIS2_PLACEMENT_3D ( 'NONE', #52027, #127583, #105411 ) ;
#18906=LINE ( 'NONE', #218376, #18508 ) ;
#18923=DIRECTION ( 'NONE',  ( 0.000000000000000000, 0.000000000000000000, -1.000000000000000000 ) ) ;
#18934=ADVANCED_FACE ( 'NONE', ( #242377 ), #203680, .T. ) ;
#18945=DIRECTION ( 'NONE',  ( -1.000000000000000000, 0.000000000000000000, 0.000000000000000000 ) ) ;
#18953=CARTESIAN_POINT ( 'NONE',  ( 20.87600722750343252, 10.33112638556969465, -72.59012289269746532 ) ) ;
#18969=DIRECTION ( 'NONE',  ( 1.000000000000000000, 0.000000000000000000, -0.000000000000000000 ) ) ;
#18996=AXIS2_PLACEMENT_3D ( 'NONE', #126179, #8820, #10100 ) ;
#19013=ORIENTED_EDGE ( 'NONE', *, *, #197365, .F. ) ;
#19027=CARTESIAN_POINT ( 'NONE',  ( -21.14999999999999858, 6.257814610487270279, -33.40220970869120265 ) ) ;
#19031=VERTEX_POINT ( 'NONE', #125023 ) ;
#19052=B_SPLINE_CURVE_WITH_KNOTS ( 'NONE', 3,
 ( #134403, #71905, #112316, #35373, #152747, #194430, #232272, #114867, #174899, #185745 ),
 .UNSPECIFIED., .F., .F.,
 ( 4, 3, 3, 4 ),
 ( 4.906538933386797396E-18, 0.0002000000000002859679, 0.001000000000045107602, 0.001967863649472130407 ),
 .UNSPECIFIED. ) ;
#19058=CARTESIAN_POINT ( 'NONE',  ( 20.95443524775735256, 8.878554263883968289, -42.03372227560014807 ) ) ;
#19063=CARTESIAN_POINT ( 'NONE',  ( 18.50000000000000000, -9.399999999988843058, -40.79725975966329798 ) ) ;
#19086=AXIS2_PLACEMENT_3D ( 'NONE', #197995, #217548, #158907 ) ;
#19098=CARTESIAN_POINT ( 'NONE',  ( 20.87155475150661132, 11.75000000001115907, -60.09558652915745114 ) ) ;
#19125=DIRECTION ( 'NONE',  ( 1.000000000000000000, 0.000000000000000000, -0.000000000000000000 ) ) ;
#19166=VERTEX_POINT ( 'NONE', #191438 ) ;
#19207=CARTESIAN_POINT ( 'NONE',  ( -20.64999999999999858, -8.730841121484171907, -43.09807471898432851 ) ) ;
#19210=FACE_OUTER_BOUND ( 'NONE', #31289, .T. ) ;
#19232=TOROIDAL_SURFACE ( 'NONE', #86398, 12.97499999999999609, 0.1000000000000000056 ) ;
#19233=DIRECTION ( 'NONE',  ( -0.000000000000000000, 0.000000000000000000, 1.000000000000000000 ) ) ;
#19239=CARTESIAN_POINT ( 'NONE',  ( 20.51284917709620359, 10.31088662285602275, -41.17247318559201830 ) ) ;
#19271=ORIENTED_EDGE ( 'NONE', *, *, #11962, .T. ) ;
#19275=CARTESIAN_POINT ( 'NONE',  ( -20.94999999999999929, -11.64999999998884483, -36.50000000000000711 ) ) ;
#19295=VERTEX_POINT ( 'NONE', #157445 ) ;
#19323=AXIS2_PLACEMENT_3D ( 'NONE', #231277, #51300, #72198 ) ;
#19326=ADVANCED_FACE ( 'NONE', ( #137824 ), #191895, .F. ) ;
#19338=DIRECTION ( 'NONE',  ( 0.000000000000000000, 0.000000000000000000, -1.000000000000000000 ) ) ;
#19383=CARTESIAN_POINT ( 'NONE',  ( -20.00857864376270001, 9.350000000011156942, -54.65000000000000568 ) ) ;
#19410=VECTOR ( 'NONE', #20522, 1000.000000000000000 ) ;
#19414=ORIENTED_EDGE ( 'NONE', *, *, #146782, .F. ) ;
#19442=LINE ( 'NONE', #2416, #7284 ) ;
#19457=CARTESIAN_POINT ( 'NONE',  ( 18.59999999999999787, -1.835341550213255957, -45.05515129256298223 ) ) ;
#19478=DIRECTION ( 'NONE',  ( 0.000000000000000000, 0.000000000000000000, -1.000000000000000000 ) ) ;
#19484=EDGE_LOOP ( 'NONE', ( #22136, #23310, #84002, #185400 ) ) ;
#19493=CARTESIAN_POINT ( 'NONE',  ( 20.95512820512820440, 8.876151316299271343, -42.05862899514094977 ) ) ;
#19498=CARTESIAN_POINT ( 'NONE',  ( 18.59999999999999076, 6.450000000011156587, -54.75000000000000000 ) ) ;
#19505=DIRECTION ( 'NONE',  ( -1.000000000000000000, 0.000000000000000000, 0.000000000000000000 ) ) ;
#19525=LINE ( 'NONE', #176043, #30310 ) ;
#19547=CARTESIAN_POINT ( 'NONE',  ( 23.15000000000000213, -9.599999999988845900, -43.39396912265245021 ) ) ;
#19551=DIRECTION ( 'NONE',  ( 1.000000000000000000, 0.000000000000000000, 0.000000000000000000 ) ) ;
#19557=ORIENTED_EDGE ( 'NONE', *, *, #149206, .T. ) ;
#19564=DIRECTION ( 'NONE',  ( 0.000000000000000000, 0.000000000000000000, -1.000000000000000000 ) ) ;
#19607=ADVANCED_FACE ( 'NONE', ( #16322 ), #237653, .F. ) ;
#19617=ORIENTED_EDGE ( 'NONE', *, *, #24666, .T. ) ;
#19636=CARTESIAN_POINT ( 'NONE',  ( -21.14999999999999858, 6.540656951712397138, -33.50000000000000000 ) ) ;
#19641=VECTOR ( 'NONE', #241333, 1000.000000000000000 ) ;
#19648=ORIENTED_EDGE ( 'NONE', *, *, #23580, .F. ) ;
#19663=VERTEX_POINT ( 'NONE', #17568 ) ;
#19697=TOROIDAL_SURFACE ( 'NONE', #102865, 4.099999999999999645, 0.1000000000000000056 ) ;
#19718=DIRECTION ( 'NONE',  ( -1.000000000000000000, -0.000000000000000000, 0.000000000000000000 ) ) ;
#19748=VERTEX_POINT ( 'NONE', #124401 ) ;
#19761=CARTESIAN_POINT ( 'NONE',  ( 23.14999999999999858, 4.000000000011155521, -67.00000000000000000 ) ) ;
#19768=CIRCLE ( 'NONE', #123808, 7.791421356237338003 ) ;
#19785=CARTESIAN_POINT ( 'NONE',  ( -23.25000000000000000, 5.950000000011167245, -56.69429769496518645 ) ) ;
#19832=DIRECTION ( 'NONE',  ( -7.304098846218134667E-16, 1.000000000000000000, -0.000000000000000000 ) ) ;
#19834=EDGE_LOOP ( 'NONE', ( #33258, #140547, #41856, #46276 ) ) ;
#19845=DIRECTION ( 'NONE',  ( 0.000000000000000000, 0.000000000000000000, -1.000000000000000000 ) ) ;
#19851=CARTESIAN_POINT ( 'NONE',  ( 23.14999999999999858, 5.500000000011153745, -45.90526601891310321 ) ) ;
#19928=ORIENTED_EDGE ( 'NONE', *, *, #147508, .T. ) ;
#19948=CARTESIAN_POINT ( 'NONE',  ( -18.59999999999999787, -1.835859311432481045, -78.50443916879852679 ) ) ;
#19953=EDGE_CURVE ( 'NONE', #65618, #113714, #90391, .T. ) ;
#19987=EDGE_CURVE ( 'NONE', #192209, #119332, #136255, .T. ) ;
#20053=DIRECTION ( 'NONE',  ( 0.000000000000000000, 1.000000000000000000, 0.000000000000000000 ) ) ;
#20065=CARTESIAN_POINT ( 'NONE',  ( 20.94999999999999929, 5.900000000011162093, -56.78090023534362984 ) ) ;
#20067=ORIENTED_EDGE ( 'NONE', *, *, #40806, .F. ) ;
#20102=CIRCLE ( 'NONE', #78519, 0.09999999999999939493 ) ;
#20108=ORIENTED_EDGE ( 'NONE', *, *, #226570, .T. ) ;
#20113=EDGE_LOOP ( 'NONE', ( #122982, #193652, #175135, #60700 ) ) ;
#20126=AXIS2_PLACEMENT_3D ( 'NONE', #96675, #35493, #17196 ) ;
#20136=ADVANCED_FACE ( 'NONE', ( #237623 ), #160679, .T. ) ;
#20142=CARTESIAN_POINT ( 'NONE',  ( 20.04142135623730070, 11.65000000001115943, -21.75000000000000355 ) ) ;
#20306=EDGE_CURVE ( 'NONE', #125125, #28235, #16856, .T. ) ;
#20337=DIRECTION ( 'NONE',  ( 0.000000000000000000, 0.9998779222360102414, 0.01562499999996356907 ) ) ;
#20340=FACE_OUTER_BOUND ( 'NONE', #192444, .T. ) ;
#20358=ORIENTED_EDGE ( 'NONE', *, *, #60303, .T. ) ;
#20375=CARTESIAN_POINT ( 'NONE',  ( 18.49505832270840600, -9.438028062771733673, -40.69847317489385574 ) ) ;
#20405=CARTESIAN_POINT ( 'NONE',  ( -20.85000000000000142, -1.835859311432479268, -78.50443916879852679 ) ) ;
#20415=FACE_OUTER_BOUND ( 'NONE', #5411, .T. ) ;
#20480=AXIS2_PLACEMENT_3D ( 'NONE', #215490, #218035, #158138 ) ;
#20484=ORIENTED_EDGE ( 'NONE', *, *, #74976, .T. ) ;
#20487=LINE ( 'NONE', #175716, #250170 ) ;
#20522=DIRECTION ( 'NONE',  ( 1.000000000000000000, -0.000000000000000000, -0.000000000000000000 ) ) ;
#20524=ORIENTED_EDGE ( 'NONE', *, *, #203450, .T. ) ;
#20539=CARTESIAN_POINT ( 'NONE',  ( 20.85000000000000142, 1.115600667400684642E-11, -67.00000000000000000 ) ) ;
#20548=CARTESIAN_POINT ( 'NONE',  ( 20.54374330479337374, 10.50501031423420351, -41.22568363488881715 ) ) ;
#20552=CYLINDRICAL_SURFACE ( 'NONE', #84744, 0.1000000000000028644 ) ;
#20558=DIRECTION ( 'NONE',  ( 1.000000000000000000, -0.000000000000000000, -0.000000000000000000 ) ) ;
#20559=EDGE_CURVE ( 'NONE', #35027, #227982, #186562, .T. ) ;
#20636=ORIENTED_EDGE ( 'NONE', *, *, #186307, .F. ) ;
#20638=EDGE_CURVE ( 'NONE', #121226, #28056, #165920, .T. ) ;
#20646=CARTESIAN_POINT ( 'NONE',  ( -20.94999999999999929, 11.75000000001115552, -40.51480577065400013 ) ) ;
#20652=DIRECTION ( 'NONE',  ( 0.000000000000000000, -6.308085367188393199E-16, -1.000000000000000000 ) ) ;
#20675=DIRECTION ( 'NONE',  ( 0.000000000000000000, -0.9915357197604792727, 0.1298341882520475943 ) ) ;
#20713=FACE_OUTER_BOUND ( 'NONE', #80382, .T. ) ;
#20725=VECTOR ( 'NONE', #120211, 1000.000000000000000 ) ;
#20759=B_SPLINE_CURVE_WITH_KNOTS ( 'NONE', 3,
 ( #178638, #196876, #255518, #177359, #13278, #70705, #211470, #193206, #14578, #94075, #92789, #32875, #233613, #253151, #212766, #34154 ),
 .UNSPECIFIED., .F., .F.,
 ( 4, 3, 3, 3, 3, 4 ),
 ( 0.000000000000000000, 2.372700795693551704E-05, 5.739057815866934116E-05, 9.073899019179910389E-05, 0.0001243544287365693814, 0.0001585386695601165850 ),
 .UNSPECIFIED. ) ;
#20761=ORIENTED_EDGE ( 'NONE', *, *, #186557, .T. ) ;
#20762=EDGE_CURVE ( 'NONE', #73682, #121226, #95016, .T. ) ;
#20797=CARTESIAN_POINT ( 'NONE',  ( 20.95265033839679347, 10.51225083247831371, -41.06576375602996620 ) ) ;
#20813=EDGE_CURVE ( 'NONE', #204139, #173018, #203298, .T. ) ;
#20817=DIRECTION ( 'NONE',  ( -1.000000000000000000, 7.304098846218134667E-16, 4.217023435051625732E-16 ) ) ;
#20864=AXIS2_PLACEMENT_3D ( 'NONE', #245601, #166094, #9541 ) ;
#20874=ORIENTED_EDGE ( 'NONE', *, *, #134045, .T. ) ;
#20878=CIRCLE ( 'NONE', #95833, 0.09999999999999939493 ) ;
#20890=CARTESIAN_POINT ( 'NONE',  ( 20.94999999999999929, -11.29603075032412995, -36.54789915966387071 ) ) ;
#20891=CARTESIAN_POINT ( 'NONE',  ( -23.25000000000000000, 11.65000000001115588, -21.75000000000000355 ) ) ;
#20893=DIRECTION ( 'NONE',  ( 0.000000000000000000, 0.000000000000000000, 1.000000000000000000 ) ) ;
#20917=ORIENTED_EDGE ( 'NONE', *, *, #152364, .T. ) ;
#20920=CIRCLE ( 'NONE', #174885, 0.1000000000000017958 ) ;
#20929=DIRECTION ( 'NONE',  ( 1.000000000000000000, 0.000000000000000000, 0.000000000000000000 ) ) ;
#20950=DIRECTION ( 'NONE',  ( 0.000000000000000000, 0.000000000000000000, 1.000000000000000000 ) ) ;
#20963=EDGE_CURVE ( 'NONE', #208880, #247553, #165905, .T. ) ;
#20986=ORIENTED_EDGE ( 'NONE', *, *, #201182, .F. ) ;
#21019=ORIENTED_EDGE ( 'NONE', *, *, #132080, .F. ) ;
#21021=ORIENTED_EDGE ( 'NONE', *, *, #159730, .T. ) ;
#21165=EDGE_CURVE ( 'NONE', #217509, #137157, #219650, .T. ) ;
#21172=DIRECTION ( 'NONE',  ( 1.000000000000000000, 0.000000000000000000, 0.000000000000000000 ) ) ;
#21189=ADVANCED_FACE ( 'NONE', ( #238059 ), #140229, .T. ) ;
#21191=ORIENTED_EDGE ( 'NONE', *, *, #243459, .F. ) ;
#21192=CARTESIAN_POINT ( 'NONE',  ( -21.05000000000000071, 1.115600667400684642E-11, -33.50000000000000000 ) ) ;
#21200=CARTESIAN_POINT ( 'NONE',  ( -20.94999999999999929, -11.64999999998884483, -36.39999999999999858 ) ) ;
#21221=CARTESIAN_POINT ( 'NONE',  ( -18.50000000000000000, 5.950000000011100632, -43.80570230503486329 ) ) ;
#21237=EDGE_CURVE ( 'NONE', #135639, #117247, #25456, .T. ) ;
#21249=AXIS2_PLACEMENT_3D ( 'NONE', #66299, #42881, #102826 ) ;
#21306=CIRCLE ( 'NONE', #225443, 11.90000000000000391 ) ;
#21349=FACE_OUTER_BOUND ( 'NONE', #73879, .T. ) ;
#21375=ORIENTED_EDGE ( 'NONE', *, *, #45711, .F. ) ;
#21397=CARTESIAN_POINT ( 'NONE',  ( -21.05000000000000071, 11.65000000001115232, -40.28386566297815108 ) ) ;
#21410=DIRECTION ( 'NONE',  ( -1.000000000000000000, -2.952720810173289112E-16, 0.000000000000000000 ) ) ;
#21411=CYLINDRICAL_SURFACE ( 'NONE', #198464, 0.09999999999999939493 ) ;
#21486=CARTESIAN_POINT ( 'NONE',  ( 21.00000000000000000, 9.750000000011153745, -54.75000000000000000 ) ) ;
#21533=DIRECTION ( 'NONE',  ( -1.000000000000000000, -0.000000000000000000, -0.000000000000000000 ) ) ;
#21544=EDGE_LOOP ( 'NONE', ( #36391, #145440, #143929, #136186, #145637 ) ) ;
#21550=ORIENTED_EDGE ( 'NONE', *, *, #97323, .T. ) ;
#21569=DIRECTION ( 'NONE',  ( 1.000000000000000000, 0.000000000000000000, 0.000000000000000000 ) ) ;
#21594=CARTESIAN_POINT ( 'NONE',  ( 23.14999999999999858, 4.813084112160684214, -55.05848224347618469 ) ) ;
#21604=DIRECTION ( 'NONE',  ( 0.000000000000000000, 0.000000000000000000, -1.000000000000000000 ) ) ;
#21618=ORIENTED_EDGE ( 'NONE', *, *, #56877, .T. ) ;
#21619=DIRECTION ( 'NONE',  ( 1.000000000000000000, -0.000000000000000000, -0.000000000000000000 ) ) ;
#21638=DIRECTION ( 'NONE',  ( -0.7071067811865388020, 0.7071067811865561215, 0.000000000000000000 ) ) ;
#21644=AXIS2_PLACEMENT_3D ( 'NONE', #238542, #143291, #139423 ) ;
#21706=DIRECTION ( 'NONE',  ( 0.000000000000000000, 2.664535259100315349E-15, -1.000000000000000000 ) ) ;
#21709=ORIENTED_EDGE ( 'NONE', *, *, #4805, .F. ) ;
#21749=EDGE_LOOP ( 'NONE', ( #152439, #86766, #220408, #142154 ) ) ;
#21783=ORIENTED_EDGE ( 'NONE', *, *, #30463, .F. ) ;
#21797=CARTESIAN_POINT ( 'NONE',  ( -18.59999999999999787, 1.115600667400684642E-11, -67.00000000000000000 ) ) ;
#21799=EDGE_CURVE ( 'NONE', #163909, #193526, #45054, .T. ) ;
#21842=FACE_OUTER_BOUND ( 'NONE', #75070, .T. ) ;
#21845=CARTESIAN_POINT ( 'NONE',  ( -18.49719636458551264, -9.446365359216914115, -40.57161386988322249 ) ) ;
#21855=CARTESIAN_POINT ( 'NONE',  ( -18.50000000000000000, 11.65000000001115232, -21.75000000000000355 ) ) ;
#21860=TOROIDAL_SURFACE ( 'NONE', #113622, 0.2000000000000000111, 0.1000000000000000056 ) ;
#21870=CARTESIAN_POINT ( 'NONE',  ( 21.07928932188134041, 0.09889514566578937182, -27.17148334360129169 ) ) ;
#21895=CARTESIAN_POINT ( 'NONE',  ( -23.15000000000000213, 4.350000000011156054, -54.64999999999999858 ) ) ;
#21964=CARTESIAN_POINT ( 'NONE',  ( -23.25000000000000000, 1.115600667400684642E-11, -37.65000000000000568 ) ) ;
#21971=ORIENTED_EDGE ( 'NONE', *, *, #44792, .T. ) ;
#21973=EDGE_CURVE ( 'NONE', #213025, #67212, #193482, .T. ) ;
#21977=DIRECTION ( 'NONE',  ( 1.000000000000000000, 0.000000000000000000, 0.000000000000000000 ) ) ;
#21983=VERTEX_POINT ( 'NONE', #173955 ) ;
#22001=CARTESIAN_POINT ( 'NONE',  ( 20.97468175916167610, 10.62526516438217783, -45.75476143541259688 ) ) ;
#22024=AXIS2_PLACEMENT_3D ( 'NONE', #226770, #70305, #48132 ) ;
#22053=ORIENTED_EDGE ( 'NONE', *, *, #196152, .T. ) ;
#22072=EDGE_CURVE ( 'NONE', #168194, #161272, #31851, .T. ) ;
#22077=CARTESIAN_POINT ( 'NONE',  ( 20.95378194480896639, 10.53491199155394220, -41.06505414814786548 ) ) ;
#22082=ORIENTED_EDGE ( 'NONE', *, *, #109820, .T. ) ;
#22092=ORIENTED_EDGE ( 'NONE', *, *, #157665, .F. ) ;
#22101=CARTESIAN_POINT ( 'NONE',  ( 21.97500000000000497, 9.750000000011153745, -45.85000000000000142 ) ) ;
#22111=DIRECTION ( 'NONE',  ( 1.000000000000000000, 0.000000000000000000, 0.000000000000000000 ) ) ;
#22136=ORIENTED_EDGE ( 'NONE', *, *, #165745, .T. ) ;
#22137=DIRECTION ( 'NONE',  ( 1.000000000000000000, 0.000000000000000000, 0.000000000000000000 ) ) ;
#22165=DIRECTION ( 'NONE',  ( 0.000000000000000000, 0.000000000000000000, -1.000000000000000000 ) ) ;
#22176=ORIENTED_EDGE ( 'NONE', *, *, #86115, .F. ) ;
#22202=DIRECTION ( 'NONE',  ( 0.000000000000000000, 0.000000000000000000, -1.000000000000000000 ) ) ;
#22203=EDGE_LOOP ( 'NONE', ( #28089, #190265, #187805, #114897 ) ) ;
#22210=VERTEX_POINT ( 'NONE', #137220 ) ;
#22221=EDGE_CURVE ( 'NONE', #187737, #195077, #141082, .T. ) ;
#22248=VECTOR ( 'NONE', #104298, 1000.000000000000000 ) ;
#22269=AXIS2_PLACEMENT_3D ( 'NONE', #88818, #186677, #247910 ) ;
#22288=CIRCLE ( 'NONE', #88889, 0.1000000000000028644 ) ;
#22291=VERTEX_POINT ( 'NONE', #7997 ) ;
#22336=CARTESIAN_POINT ( 'NONE',  ( -20.54999999999999716, -8.999999999988846255, -43.39396912265245021 ) ) ;
#22348=ORIENTED_EDGE ( 'NONE', *, *, #229748, .F. ) ;
#22368=LINE ( 'NONE', #18498, #18706 ) ;
#22375=EDGE_CURVE ( 'NONE', #131987, #161055, #251730, .T. ) ;
#22379=DIRECTION ( 'NONE',  ( -0.000000000000000000, -0.9875055080513799322, 0.1575844902526464253 ) ) ;
#22416=DIRECTION ( 'NONE',  ( 0.000000000000000000, 0.000000000000000000, 1.000000000000000000 ) ) ;
#22426=VERTEX_POINT ( 'NONE', #88779 ) ;
#22462=CIRCLE ( 'NONE', #76594, 0.09999999999999484301 ) ;
#22467=ORIENTED_EDGE ( 'NONE', *, *, #138807, .F. ) ;
#22490=CYLINDRICAL_SURFACE ( 'NONE', #157229, 12.87499999999999822 ) ;
#22500=FACE_OUTER_BOUND ( 'NONE', #158968, .T. ) ;
#22525=ADVANCED_FACE ( 'NONE', ( #156520 ), #215169, .F. ) ;
#22562=CARTESIAN_POINT ( 'NONE',  ( -18.50000000000000000, -1.835859311432484375, -78.50443916879852679 ) ) ;
#22567=CARTESIAN_POINT ( 'NONE',  ( -18.50000000000000000, -1.835341550213255957, -45.05515129256298223 ) ) ;
#22595=CARTESIAN_POINT ( 'NONE',  ( -20.94999999999999929, -11.48912529306490349, -36.60000000000000142 ) ) ;
#22599=ADVANCED_FACE ( 'NONE', ( #237309 ), #191190, .F. ) ;
#22601=VECTOR ( 'NONE', #183863, 1000.000000000000000 ) ;
#22605=ORIENTED_EDGE ( 'NONE', *, *, #79120, .F. ) ;
#22614=VECTOR ( 'NONE', #149460, 1000.000000000000000 ) ;
#22628=ADVANCED_FACE ( 'NONE', ( #101600 ), #122503, .T. ) ;
#22648=EDGE_CURVE ( 'NONE', #139488, #80050, #116183, .T. ) ;
#22756=CARTESIAN_POINT ( 'NONE',  ( -20.94999999999999929, -1.162701749926853712, -41.60000000000000142 ) ) ;
#22762=ORIENTED_EDGE ( 'NONE', *, *, #86115, .T. ) ;
#22793=CIRCLE ( 'NONE', #214309, 0.1000000000000000472 ) ;
#22808=ORIENTED_EDGE ( 'NONE', *, *, #214462, .T. ) ;
#22832=CARTESIAN_POINT ( 'NONE',  ( 21.05000005001280172, 8.871279691782060439, -45.67794758824611279 ) ) ;
#22884=AXIS2_PLACEMENT_3D ( 'NONE', #99884, #2087, #235568 ) ;
#22910=EDGE_CURVE ( 'NONE', #43174, #134638, #75382, .T. ) ;
#22952=VERTEX_POINT ( 'NONE', #195330 ) ;
#22961=ORIENTED_EDGE ( 'NONE', *, *, #180464, .T. ) ;
#22974=CIRCLE ( 'NONE', #127006, 11.65000000000000036 ) ;
#23023=DIRECTION ( 'NONE',  ( 0.000000000000000000, 0.000000000000000000, -1.000000000000000000 ) ) ;
#23024=CARTESIAN_POINT ( 'NONE',  ( -23.15000000000000213, 2.000000000011154189, -46.72462192276210402 ) ) ;
#23072=EDGE_CURVE ( 'NONE', #190117, #28056, #241434, .T. ) ;
#23107=CIRCLE ( 'NONE', #168877, 0.1000000000000028644 ) ;
#23113=ORIENTED_EDGE ( 'NONE', *, *, #171032, .T. ) ;
#23116=EDGE_CURVE ( 'NONE', #38982, #165098, #82981, .T. ) ;
#23131=DIRECTION ( 'NONE',  ( 0.000000000000000000, 0.1350103645451904977, -0.9908441862701596881 ) ) ;
#23135=DIRECTION ( 'NONE',  ( 0.000000000000000000, 0.000000000000000000, -1.000000000000000000 ) ) ;
#23141=VECTOR ( 'NONE', #108546, 1000.000000000000000 ) ;
#23146=CARTESIAN_POINT ( 'NONE',  ( -18.43599941264909603, -9.519327428583617134, -40.47297678952136124 ) ) ;
#23251=DIRECTION ( 'NONE',  ( 1.000000000000000000, 2.952720810173289112E-16, -0.000000000000000000 ) ) ;
#23259=DIRECTION ( 'NONE',  ( 0.000000000000000000, 0.000000000000000000, -1.000000000000000000 ) ) ;
#23275=CARTESIAN_POINT ( 'NONE',  ( 18.59999999999999076, 10.20857864377385127, -58.15000000000000568 ) ) ;
#23307=CARTESIAN_POINT ( 'NONE',  ( 21.05000000000000071, 1.115600667400684642E-11, -71.00000000000001421 ) ) ;
#23310=ORIENTED_EDGE ( 'NONE', *, *, #177808, .F. ) ;
#23331=DIRECTION ( 'NONE',  ( 0.000000000000000000, 0.000000000000000000, 1.000000000000000000 ) ) ;
#23335=DIRECTION ( 'NONE',  ( -1.000000000000000000, 0.000000000000000000, 0.000000000000000000 ) ) ;
#23354=CIRCLE ( 'NONE', #98115, 0.3999999999999975797 ) ;
#23385=CONICAL_SURFACE ( 'NONE', #56624, 6.249999999999998224, 0.7853981633974431720 ) ;
#23388=EDGE_CURVE ( 'NONE', #125075, #110138, #41712, .T. ) ;
#23393=B_SPLINE_CURVE_WITH_KNOTS ( 'NONE', 3,
 ( #127806, #249046, #49545, #30008, #109499, #207348 ),
 .UNSPECIFIED., .F., .F.,
 ( 4, 2, 4 ),
 ( 0.000000000000000000, 0.0001895189928937402997, 0.0003790379857874805994 ),
 .UNSPECIFIED. ) ;
#23408=ORIENTED_EDGE ( 'NONE', *, *, #112642, .T. ) ;
#23423=CARTESIAN_POINT ( 'NONE',  ( 20.04142135623730070, 11.65000000001115943, -54.85000000000000142 ) ) ;
#23432=CARTESIAN_POINT ( 'NONE',  ( -18.50000000000000355, -1.263275465206102233, -74.90186466674640542 ) ) ;
#23511=CARTESIAN_POINT ( 'NONE',  ( -21.08035267497491816, 0.08268862478717949049, -27.16829316021696172 ) ) ;
#23543=ORIENTED_EDGE ( 'NONE', *, *, #115004, .F. ) ;
#23544=DIRECTION ( 'NONE',  ( 1.000000000000000000, -7.304098846218133681E-16, -2.111765289898285610E-31 ) ) ;
#23551=CARTESIAN_POINT ( 'NONE',  ( 21.07016717456946253, 6.320940838111409832, -33.50000000000000711 ) ) ;
#23555=EDGE_CURVE ( 'NONE', #233092, #111434, #113544, .T. ) ;
#23558=LINE ( 'NONE', #105585, #68987 ) ;
#23577=EDGE_LOOP ( 'NONE', ( #22762, #87887, #254692, #100399 ) ) ;
#23580=EDGE_CURVE ( 'NONE', #230427, #182014, #254070, .T. ) ;
#23581=DIRECTION ( 'NONE',  ( 1.000000000000000000, 3.265361837132813093E-16, -0.000000000000000000 ) ) ;
#23618=VECTOR ( 'NONE', #28138, 1000.000000000000000 ) ;
#23639=AXIS2_PLACEMENT_3D ( 'NONE', #83425, #142142, #20950 ) ;
#23640=ORIENTED_EDGE ( 'NONE', *, *, #45784, .F. ) ;
#23656=VERTEX_POINT ( 'NONE', #58679 ) ;
#23665=CIRCLE ( 'NONE', #7055, 0.1999999999999987899 ) ;
#23693=CARTESIAN_POINT ( 'NONE',  ( 22.39999999999999503, 11.65000000001116298, -33.40000000000000568 ) ) ;
#23716=FACE_OUTER_BOUND ( 'NONE', #53170, .T. ) ;
#23720=DIRECTION ( 'NONE',  ( 1.000000000000000000, 0.000000000000000000, -0.000000000000000000 ) ) ;
#23740=DIRECTION ( 'NONE',  ( 1.000000000000000000, 0.000000000000000000, 0.000000000000000000 ) ) ;
#23754=VECTOR ( 'NONE', #191393, 1000.000000000000000 ) ;
#23768=DIRECTION ( 'NONE',  ( 0.000000000000000000, 0.1298341882520022694, 0.9915357197604852679 ) ) ;
#23776=ORIENTED_EDGE ( 'NONE', *, *, #226570, .F. ) ;
#23780=ORIENTED_EDGE ( 'NONE', *, *, #15108, .F. ) ;
#23795=DIRECTION ( 'NONE',  ( -1.000000000000000000, -1.836970198721029934E-16, 0.000000000000000000 ) ) ;
#23805=CARTESIAN_POINT ( 'NONE',  ( -18.59999999999999787, -1.149570369564537842, -74.81591248450196474 ) ) ;
#23809=EDGE_CURVE ( 'NONE', #95921, #100505, #79270, .T. ) ;
#23815=CARTESIAN_POINT ( 'NONE',  ( 18.59999999999999076, -1.835859311432481045, -78.50443916879852679 ) ) ;
#23881=ORIENTED_EDGE ( 'NONE', *, *, #239800, .F. ) ;
#23892=CARTESIAN_POINT ( 'NONE',  ( 21.05000000000000071, 11.75000000001116263, -59.98519422934605672 ) ) ;
#24012=CARTESIAN_POINT ( 'NONE',  ( -22.50875500270928598, -0.1008579137641475443, -21.75043287260211144 ) ) ;
#24023=VECTOR ( 'NONE', #199033, 1000.000000000000000 ) ;
#24062=CARTESIAN_POINT ( 'NONE',  ( -18.50000000000000000, 1.340746217944851715, -23.22713749457881960 ) ) ;
#24071=ADVANCED_FACE ( 'NONE', ( #230994 ), #108459, .F. ) ;
#24077=DIRECTION ( 'NONE',  ( 0.000000000000000000, 0.000000000000000000, -1.000000000000000000 ) ) ;
#24088=EDGE_CURVE ( 'NONE', #203545, #109174, #111025, .T. ) ;
#24092=CIRCLE ( 'NONE', #132393, 4.049999999999998934 ) ;
#24103=VERTEX_POINT ( 'NONE', #130575 ) ;
#24106=EDGE_CURVE ( 'NONE', #216121, #163280, #246080, .T. ) ;
#24121=FACE_OUTER_BOUND ( 'NONE', #232614, .T. ) ;
#24124=DIRECTION ( 'NONE',  ( -1.000000000000000000, -3.265361837132813093E-16, 0.000000000000000000 ) ) ;
#24144=AXIS2_PLACEMENT_3D ( 'NONE', #201659, #199097, #81673 ) ;
#24158=CYLINDRICAL_SURFACE ( 'NONE', #32106, 2.000000000000001776 ) ;
#24165=EDGE_CURVE ( 'NONE', #86684, #213775, #71115, .T. ) ;
#24240=B_SPLINE_CURVE_WITH_KNOTS ( 'NONE', 3,
 ( #257220, #251688, #32694, #36529, #91348, #213848 ),
 .UNSPECIFIED., .F., .F.,
 ( 4, 2, 4 ),
 ( 0.000000000000000000, 0.0001496588209255839900, 0.0002993176418511679800 ),
 .UNSPECIFIED. ) ;
#24261=CARTESIAN_POINT ( 'NONE',  ( 20.85000000000000142, 11.75000000001115907, -60.21613433702191287 ) ) ;
#24304=CARTESIAN_POINT ( 'NONE',  ( -20.94684162641900116, 11.75000000001115374, -40.34164400167171038 ) ) ;
#24349=FACE_OUTER_BOUND ( 'NONE', #123937, .T. ) ;
#24354=AXIS2_PLACEMENT_3D ( 'NONE', #166655, #246159, #226572 ) ;
#24369=AXIS2_PLACEMENT_3D ( 'NONE', #23024, #45124, #199066 ) ;
#24378=CIRCLE ( 'NONE', #107738, 12.77499999999999503 ) ;
#24381=DIRECTION ( 'NONE',  ( -1.000000000000000000, -3.265361837132813093E-16, 0.000000000000000000 ) ) ;
#24420=EDGE_CURVE ( 'NONE', #75871, #104039, #246261, .T. ) ;
#24423=FACE_OUTER_BOUND ( 'NONE', #39579, .T. ) ;
#24425=UNCERTAINTY_MEASURE_WITH_UNIT (LENGTH_MEASURE( 1.000000000000000082E-05 ), #216032, 'distance_accuracy_value', 'NONE');
#24459=CARTESIAN_POINT ( 'NONE',  ( 21.07954640115348965, 0.06600770715080908624, -27.17071230397564463 ) ) ;
#24462=AXIS2_PLACEMENT_3D ( 'NONE', #43812, #123351, #202873 ) ;
#24496=ORIENTED_EDGE ( 'NONE', *, *, #25515, .F. ) ;
#24499=DIRECTION ( 'NONE',  ( 1.000000000000000000, 0.000000000000000000, 0.000000000000000000 ) ) ;
#24510=CARTESIAN_POINT ( 'NONE',  ( -20.64999999999999858, 2.500000000011156409, -46.72462192276210402 ) ) ;
#24511=VERTEX_POINT ( 'NONE', #7778 ) ;
#24527=AXIS2_PLACEMENT_3D ( 'NONE', #206100, #67865, #225629 ) ;
#24592=CARTESIAN_POINT ( 'NONE',  ( -23.25000000000000000, 5.950000000011163692, -56.69429769496518645 ) ) ;
#24612=CARTESIAN_POINT ( 'NONE',  ( -21.29999999999995808, 1.115600667400684642E-11, -33.50000000000000000 ) ) ;
#24614=CARTESIAN_POINT ( 'NONE',  ( -21.05000000000000071, 1.115600667400684642E-11, -67.00000000000000000 ) ) ;
#24660=VERTEX_POINT ( 'NONE', #33794 ) ;
#24666=EDGE_CURVE ( 'NONE', #15533, #127486, #104568, .T. ) ;
#24720=FACE_BOUND ( 'NONE', #133502, .T. ) ;
#24763=DIRECTION ( 'NONE',  ( -1.000000000000000000, -0.000000000000000000, -0.000000000000000000 ) ) ;
#24776=DIRECTION ( 'NONE',  ( 0.000000000000000000, 0.000000000000000000, -1.000000000000000000 ) ) ;
#24789=CARTESIAN_POINT ( 'NONE',  ( -23.15000000000000213, 11.75000000001115552, -21.75000000000000355 ) ) ;
#24820=ORIENTED_EDGE ( 'NONE', *, *, #93551, .T. ) ;
#24862=ORIENTED_EDGE ( 'NONE', *, *, #207836, .T. ) ;
#24869=DIRECTION ( 'NONE',  ( 0.000000000000000000, 1.000000000000000000, -1.224646799147353207E-16 ) ) ;
#24889=CIRCLE ( 'NONE', #187191, 3.999999999999999112 ) ;
#24941=ADVANCED_FACE ( 'NONE', ( #146944 ), #206942, .T. ) ;
#24948=CARTESIAN_POINT ( 'NONE',  ( -20.54999999999999716, -8.999999999988846255, -42.89396912265245021 ) ) ;
#24967=AXIS2_PLACEMENT_3D ( 'NONE', #46387, #23023, #183361 ) ;
#24975=ORIENTED_EDGE ( 'NONE', *, *, #37800, .T. ) ;
#24977=DIRECTION ( 'NONE',  ( -0.000000000000000000, -0.000000000000000000, -1.000000000000000000 ) ) ;
#25014=ORIENTED_EDGE ( 'NONE', *, *, #85453, .T. ) ;
#25025=CARTESIAN_POINT ( 'NONE',  ( -20.85000000000000142, -1.851617760457748618, -78.60318971960367662 ) ) ;
#25041=ORIENTED_EDGE ( 'NONE', *, *, #193395, .T. ) ;
#25093=CARTESIAN_POINT ( 'NONE',  ( -23.25000000000000000, 1.115600667400684642E-11, -67.00000000000000000 ) ) ;
#25101=DIRECTION ( 'NONE',  ( 1.000000000000000000, 0.000000000000000000, 0.000000000000000000 ) ) ;
#25113=CARTESIAN_POINT ( 'NONE',  ( 21.05000000000000071, -1.360870587180885716, -41.57299792709095954 ) ) ;
#25116=CARTESIAN_POINT ( 'NONE',  ( -2.995603634470884209E-16, 6.650000000011155876, -54.75000000000000000 ) ) ;
#25118=ORIENTED_EDGE ( 'NONE', *, *, #194218, .T. ) ;
#25142=EDGE_LOOP ( 'NONE', ( #257027, #200407, #177844, #59229, #7583, #182004, #131561 ) ) ;
#25155=ORIENTED_EDGE ( 'NONE', *, *, #150339, .T. ) ;
#25165=ORIENTED_EDGE ( 'NONE', *, *, #78451, .T. ) ;
#25190=FACE_OUTER_BOUND ( 'NONE', #68593, .T. ) ;
#25197=CARTESIAN_POINT ( 'NONE',  ( 22.39999999999999503, 11.75000000001116263, -33.60000000000000142 ) ) ;
#25215=DIRECTION ( 'NONE',  ( 1.000000000000000000, 0.000000000000000000, 0.000000000000000000 ) ) ;
#25222=AXIS2_PLACEMENT_3D ( 'NONE', #173631, #210145, #31532 ) ;
#25227=EDGE_CURVE ( 'NONE', #55518, #48144, #47236, .T. ) ;
#25256=EDGE_CURVE ( 'NONE', #126699, #201739, #69708, .T. ) ;
#25260=ORIENTED_EDGE ( 'NONE', *, *, #205937, .F. ) ;
#25261=EDGE_CURVE ( 'NONE', #132417, #27454, #10995, .T. ) ;
#25280=DIRECTION ( 'NONE',  ( -1.000000000000000000, 0.000000000000000000, 0.000000000000000000 ) ) ;
#25285=AXIS2_PLACEMENT_3D ( 'NONE', #227420, #206580, #48784 ) ;
#25288=ORIENTED_EDGE ( 'NONE', *, *, #79664, .F. ) ;
#25302=ADVANCED_FACE ( 'NONE', ( #133511 ), #1458, .F. ) ;
#25313=CARTESIAN_POINT ( 'NONE',  ( -21.05000000000000426, 6.440770893673126274, -33.51759718700845525 ) ) ;
#25327=AXIS2_PLACEMENT_3D ( 'NONE', #187340, #244711, #46510 ) ;
#25332=CARTESIAN_POINT ( 'NONE',  ( 22.50000000000000000, 0.1000000000111554016, -21.85042919245520210 ) ) ;
#25363=SPHERICAL_SURFACE ( 'NONE', #162246, 0.1000000000000000056 ) ;
#25368=CARTESIAN_POINT ( 'NONE',  ( 20.77766267348356166, 10.44904239062990570, -41.09270891587767238 ) ) ;
#25445=CIRCLE ( 'NONE', #50537, 0.1000000000000000472 ) ;
#25456=LINE ( 'NONE', #103666, #95334 ) ;
#25469=EDGE_LOOP ( 'NONE', ( #135038, #166176, #98378, #74125, #66885 ) ) ;
#25475=DIRECTION ( 'NONE',  ( -0.7071067811865475727, -0.7071067811865475727, 0.000000000000000000 ) ) ;
#25503=ORIENTED_EDGE ( 'NONE', *, *, #74632, .F. ) ;
#25507=DIRECTION ( 'NONE',  ( 1.000000000000000000, 0.000000000000000000, 0.000000000000000000 ) ) ;
#25514=FACE_OUTER_BOUND ( 'NONE', #223137, .T. ) ;
#25515=EDGE_CURVE ( 'NONE', #250000, #61108, #164159, .T. ) ;
#25516=ORIENTED_EDGE ( 'NONE', *, *, #184264, .T. ) ;
#25540=DIRECTION ( 'NONE',  ( -1.000000000000000000, -2.952720810173289112E-16, 0.000000000000000000 ) ) ;
#25548=ORIENTED_EDGE ( 'NONE', *, *, #221357, .F. ) ;
#25570=DIRECTION ( 'NONE',  ( -1.000000000000000000, -0.000000000000000000, -0.000000000000000000 ) ) ;
#25577=CARTESIAN_POINT ( 'NONE',  ( -21.05000000000000071, 11.75000000001115197, -40.28386566297815108 ) ) ;
#25628=AXIS2_PLACEMENT_3D ( 'NONE', #12840, #251427, #226715 ) ;
#25637=VERTEX_POINT ( 'NONE', #76354 ) ;
#25655=CYLINDRICAL_SURFACE ( 'NONE', #256116, 0.5000000000000004441 ) ;
#25667=AXIS2_PLACEMENT_3D ( 'NONE', #124196, #83726, #244115 ) ;
#25677=VERTEX_POINT ( 'NONE', #80065 ) ;
#25684=CARTESIAN_POINT ( 'NONE',  ( 22.49999999999999645, 0.04562336060752137518, -21.84949566144972621 ) ) ;
#25701=AXIS2_PLACEMENT_3D ( 'NONE', #199711, #122739, #217939 ) ;
#25748=DIRECTION ( 'NONE',  ( 0.000000000000000000, -1.000000000000000000, 0.000000000000000000 ) ) ;
#25795=EDGE_LOOP ( 'NONE', ( #191251, #9367, #60859, #221843 ) ) ;
#25800=CARTESIAN_POINT ( 'NONE',  ( -22.50000000000000000, 1.115600667400684642E-11, -21.85042919245520210 ) ) ;
#25803=CIRCLE ( 'NONE', #179940, 0.1000000000000028644 ) ;
#25824=ADVANCED_FACE ( 'NONE', ( #188201 ), #221992, .T. ) ;
#25848=CARTESIAN_POINT ( 'NONE',  ( 21.78635804494511419, 0.09900506551883611617, -26.46433851484681909 ) ) ;
#25871=EDGE_CURVE ( 'NONE', #140969, #65925, #226097, .T. ) ;
#25872=EDGE_LOOP ( 'NONE', ( #69429, #47215, #111462, #26766 ) ) ;
#25892=ORIENTED_EDGE ( 'NONE', *, *, #197278, .T. ) ;
#25939=CARTESIAN_POINT ( 'NONE',  ( -18.50000000000000711, 11.75000000001115197, -40.51480577065400013 ) ) ;
#25971=DIRECTION ( 'NONE',  ( -1.000000000000000000, 0.000000000000000000, 0.000000000000000000 ) ) ;
#25990=ADVANCED_FACE ( 'NONE', ( #203601 ), #82336, .F. ) ;
#26029=DIRECTION ( 'NONE',  ( 0.000000000000000000, -1.000000000000000000, -1.734723475976807292E-15 ) ) ;
#26048=ADVANCED_FACE ( 'NONE', ( #23716 ), #72012, .T. ) ;
#26049=DIRECTION ( 'NONE',  ( 0.000000000000000000, 0.000000000000000000, 1.000000000000000000 ) ) ;
#26066=CIRCLE ( 'NONE', #167723, 0.09999999999999939493 ) ;
#26094=CARTESIAN_POINT ( 'NONE',  ( -23.15000000000000213, 11.65000000001115588, -59.98519422934605672 ) ) ;
#26103=CARTESIAN_POINT ( 'NONE',  ( -23.15000000000000213, 11.65000000001115588, -45.75000000000000000 ) ) ;
#26127=ORIENTED_EDGE ( 'NONE', *, *, #237002, .F. ) ;
#26140=EDGE_LOOP ( 'NONE', ( #94462, #93458, #242591, #144337 ) ) ;
#26160=DIRECTION ( 'NONE',  ( 1.000000000000000000, 0.000000000000000000, 0.000000000000000000 ) ) ;
#26169=DIRECTION ( 'NONE',  ( 0.000000000000000000, 0.000000000000000000, 1.000000000000000000 ) ) ;
#26185=ORIENTED_EDGE ( 'NONE', *, *, #164164, .T. ) ;
#26214=DIRECTION ( 'NONE',  ( 1.000000000000000000, 0.000000000000000000, 0.000000000000000000 ) ) ;
#26278=CARTESIAN_POINT ( 'NONE',  ( 18.59999999999999076, 6.550000000011156231, -43.51702717044002355 ) ) ;
#26295=EDGE_LOOP ( 'NONE', ( #26562, #124446, #207243, #9178 ) ) ;
#26314=DIRECTION ( 'NONE',  ( 1.000000000000000000, 0.000000000000000000, 0.000000000000000000 ) ) ;
#26321=CARTESIAN_POINT ( 'NONE',  ( -21.55000000000000426, 7.750000000011155521, -45.85000000000000142 ) ) ;
#26347=CARTESIAN_POINT ( 'NONE',  ( 21.05000000000000071, 1.360870587203197646, -41.57299792709095954 ) ) ;
#26351=CARTESIAN_POINT ( 'NONE',  ( 23.14999999999999858, 4.775700934590584090, -45.34876810404598046 ) ) ;
#26352=AXIS2_PLACEMENT_3D ( 'NONE', #136608, #91413, #216149 ) ;
#26358=CARTESIAN_POINT ( 'NONE',  ( -21.14999999999999858, 1.115600667400684642E-11, -26.95934304829875927 ) ) ;
#26388=FACE_OUTER_BOUND ( 'NONE', #32493, .T. ) ;
#26433=ORIENTED_EDGE ( 'NONE', *, *, #36139, .T. ) ;
#26463=ADVANCED_FACE ( 'NONE', ( #189835 ), #243221, .T. ) ;
#26499=TOROIDAL_SURFACE ( 'NONE', #101257, 0.2000000000000000111, 0.1000000000000000056 ) ;
#26511=VERTEX_POINT ( 'NONE', #73760 ) ;
#26532=VERTEX_POINT ( 'NONE', #153310 ) ;
#26543=ORIENTED_EDGE ( 'NONE', *, *, #227215, .F. ) ;
#26562=ORIENTED_EDGE ( 'NONE', *, *, #103501, .F. ) ;
#26564=AXIS2_PLACEMENT_3D ( 'NONE', #115742, #57018, #192720 ) ;
#26574=CIRCLE ( 'NONE', #101533, 0.1000000000000028644 ) ;
#26598=CARTESIAN_POINT ( 'NONE',  ( -21.09107601085566586, 6.363877975371106999, -33.46069283528267846 ) ) ;
#26601=DIRECTION ( 'NONE',  ( 7.589415207398576792E-15, -1.000000000000000000, -0.000000000000000000 ) ) ;
#26611=ORIENTED_EDGE ( 'NONE', *, *, #97300, .F. ) ;
#26614=LINE ( 'NONE', #8332, #71242 ) ;
#26623=ORIENTED_EDGE ( 'NONE', *, *, #44908, .T. ) ;
#26638=DIRECTION ( 'NONE',  ( 0.000000000000000000, 0.000000000000000000, -1.000000000000000000 ) ) ;
#26650=CARTESIAN_POINT ( 'NONE',  ( 20.13684514580102913, 9.495855392761558988, -41.64303168568470426 ) ) ;
#26675=ORIENTED_EDGE ( 'NONE', *, *, #69637, .F. ) ;
#26707=CARTESIAN_POINT ( 'NONE',  ( -21.05000000000000071, 1.750000000011155743, -45.16951155790164307 ) ) ;
#26711=ORIENTED_EDGE ( 'NONE', *, *, #243435, .T. ) ;
#26716=CARTESIAN_POINT ( 'NONE',  ( 22.57856590037848576, -0.004128330053175033321, -21.74994153732456326 ) ) ;
#26724=LINE ( 'NONE', #128377, #52563 ) ;
#26766=ORIENTED_EDGE ( 'NONE', *, *, #129542, .T. ) ;
#26835=CARTESIAN_POINT ( 'NONE',  ( -18.50211644919735576, 10.30207779525983014, -72.48955207167824710 ) ) ;
#26840=DIRECTION ( 'NONE',  ( 0.000000000000000000, 0.9654727137038726648, -0.2605042016806632943 ) ) ;
#26843=VECTOR ( 'NONE', #126036, 1000.000000000000000 ) ;
#26852=ORIENTED_EDGE ( 'NONE', *, *, #221831, .T. ) ;
#26868=CARTESIAN_POINT ( 'NONE',  ( -21.44999999999999929, 7.350000000011155166, -54.65000000000000568 ) ) ;
#26880=ORIENTED_EDGE ( 'NONE', *, *, #205937, .T. ) ;
#26882=DIRECTION ( 'NONE',  ( 1.000000000000000000, -0.000000000000000000, 0.000000000000000000 ) ) ;
#26887=AXIS2_PLACEMENT_3D ( 'NONE', #153371, #149499, #129896 ) ;
#26926=VECTOR ( 'NONE', #106854, 1000.000000000000000 ) ;
#26970=AXIS2_PLACEMENT_3D ( 'NONE', #48413, #187943, #208791 ) ;
#26982=AXIS2_PLACEMENT_3D ( 'NONE', #40627, #200939, #143526 ) ;
#27035=PLANE ( 'NONE',  #10828 ) ;
#27074=AXIS2_PLACEMENT_3D ( 'NONE', #118119, #198930, #197645 ) ;
#27103=CARTESIAN_POINT ( 'NONE',  ( 21.05000000000000071, 1.115600667400684642E-11, -67.00000000000000000 ) ) ;
#27109=AXIS2_PLACEMENT_3D ( 'NONE', #112012, #91144, #130259 ) ;
#27117=VECTOR ( 'NONE', #59056, 1000.000000000000000 ) ;
#27121=PLANE ( 'NONE',  #132882 ) ;
#27136=ORIENTED_EDGE ( 'NONE', *, *, #94184, .T. ) ;
#27141=CARTESIAN_POINT ( 'NONE',  ( 18.47149038651510722, -9.671457157995549281, -73.67278633473839022 ) ) ;
#27156=EDGE_LOOP ( 'NONE', ( #254889, #26543, #118272, #157676 ) ) ;
#27158=CARTESIAN_POINT ( 'NONE',  ( 21.14999999999999858, 10.71339244341104013, -45.75000000000000000 ) ) ;
#27167=LINE ( 'NONE', #106639, #144124 ) ;
#27223=AXIS2_PLACEMENT_3D ( 'NONE', #96627, #219161, #197028 ) ;
#27266=EDGE_CURVE ( 'NONE', #86605, #27579, #164514, .T. ) ;
#27295=ORIENTED_EDGE ( 'NONE', *, *, #225532, .F. ) ;
#27297=AXIS2_PLACEMENT_3D ( 'NONE', #118744, #199575, #56164 ) ;
#27329=VERTEX_POINT ( 'NONE', #250466 ) ;
#27340=DIRECTION ( 'NONE',  ( 0.000000000000000000, 0.000000000000000000, 1.000000000000000000 ) ) ;
#27353=EDGE_CURVE ( 'NONE', #36405, #3656, #222739, .T. ) ;
#27359=DIRECTION ( 'NONE',  ( 1.000000000000000000, -0.000000000000000000, -0.000000000000000000 ) ) ;
#27380=CARTESIAN_POINT ( 'NONE',  ( -21.64999999999999858, 7.250000000011148416, -54.75000000000000000 ) ) ;
#27383=TOROIDAL_SURFACE ( 'NONE', #173130, 2.100000000000002309, 0.1000000000000000056 ) ;
#27400=DIRECTION ( 'NONE',  ( 0.000000000000000000, -1.000000000000000000, 6.308085367188393199E-16 ) ) ;
#27406=CARTESIAN_POINT ( 'NONE',  ( 22.39999999999999503, 1.115600667400684642E-11, -21.85042919245520210 ) ) ;
#27417=DIRECTION ( 'NONE',  ( -2.827886303505248766E-16, 0.8660254037844411501, 0.4999999999999956146 ) ) ;
#27435=ORIENTED_EDGE ( 'NONE', *, *, #215196, .F. ) ;
#27438=ORIENTED_EDGE ( 'NONE', *, *, #223980, .T. ) ;
#27449=EDGE_CURVE ( 'NONE', #166959, #154073, #232221, .T. ) ;
#27454=VERTEX_POINT ( 'NONE', #193082 ) ;
#27471=CARTESIAN_POINT ( 'NONE',  ( -23.25000000000000000, 1.115600667400684642E-11, -67.00000000000000000 ) ) ;
#27515=DIRECTION ( 'NONE',  ( 0.000000000000000000, -0.8660254037844411501, -0.4999999999999956146 ) ) ;
#27526=CARTESIAN_POINT ( 'NONE',  ( -20.64999999999999858, -9.499999999988848032, -43.39396912265245021 ) ) ;
#27538=CARTESIAN_POINT ( 'NONE',  ( -21.05000000000000071, 1.115600667400684642E-11, -33.50000000000000000 ) ) ;
#27549=CYLINDRICAL_SURFACE ( 'NONE', #237930, 0.09999999999999939493 ) ;
#27553=ORIENTED_EDGE ( 'NONE', *, *, #154312, .F. ) ;
#27579=VERTEX_POINT ( 'NONE', #72499 ) ;
#27581=VERTEX_POINT ( 'NONE', #209414 ) ;
#27597=DIRECTION ( 'NONE',  ( 0.000000000000000000, 0.000000000000000000, 1.000000000000000000 ) ) ;
#27604=DIRECTION ( 'NONE',  ( 1.000000000000000000, 0.000000000000000000, 0.000000000000000000 ) ) ;
#27676=CARTESIAN_POINT ( 'NONE',  ( 20.89878130938411616, 10.32747123227773045, -72.57740328502492844 ) ) ;
#27710=AXIS2_PLACEMENT_3D ( 'NONE', #164767, #107346, #169947 ) ;
#27736=EDGE_LOOP ( 'NONE', ( #136155, #214590, #116737, #44758, #255640, #2099, #104867 ) ) ;
#27752=ORIENTED_EDGE ( 'NONE', *, *, #131464, .T. ) ;
#27761=ADVANCED_FACE ( 'NONE', ( #85292 ), #193722, .F. ) ;
#27805=CARTESIAN_POINT ( 'NONE',  ( 18.48536876927986583, -9.463527249856113599, -40.54861826508263789 ) ) ;
#27816=ORIENTED_EDGE ( 'NONE', *, *, #116831, .F. ) ;
#27855=DIRECTION ( 'NONE',  ( 0.000000000000000000, -1.000000000000000000, 0.000000000000000000 ) ) ;
#27861=EDGE_CURVE ( 'NONE', #12448, #241925, #231332, .T. ) ;
#27881=ORIENTED_EDGE ( 'NONE', *, *, #88848, .F. ) ;
#27886=LINE ( 'NONE', #183085, #224401 ) ;
#27902=ORIENTED_EDGE ( 'NONE', *, *, #87220, .F. ) ;
#27914=ORIENTED_EDGE ( 'NONE', *, *, #233434, .T. ) ;
#27926=CARTESIAN_POINT ( 'NONE',  ( 21.05000000000000071, -1.736257131586239844, -45.06865232901750318 ) ) ;
#27939=EDGE_CURVE ( 'NONE', #12767, #116556, #56499, .T. ) ;
#27996=CIRCLE ( 'NONE', #82101, 0.09999999999999939493 ) ;
#28038=B_SPLINE_CURVE_WITH_KNOTS ( 'NONE', 3,
 ( #82886, #162482, #63345, #68504, #166350, #189734, #107618, #227565, #205424, #72370, #89326, #48924, #208028, #26835, #28115, #91903, #131034, #125889, #191040 ),
 .UNSPECIFIED., .F., .F.,
 ( 4, 3, 3, 3, 3, 3, 4 ),
 ( 0.000000000000000000, 2.646747978908405501E-05, 5.271166642128941309E-05, 9.008788829884216409E-05, 0.0001426648776561083808, 0.0001897378458659868894, 0.0001917382627806458214 ),
 .UNSPECIFIED. ) ;
#28056=VERTEX_POINT ( 'NONE', #57738 ) ;
#28061=ORIENTED_EDGE ( 'NONE', *, *, #183596, .T. ) ;
#28089=ORIENTED_EDGE ( 'NONE', *, *, #180395, .T. ) ;
#28090=VECTOR ( 'NONE', #214303, 1000.000000000000000 ) ;
#28094=( BOUNDED_SURFACE ( )  B_SPLINE_SURFACE ( 3, 2, ( 
 ( #78143, #25577, #136842 ),
 ( #216378, #37773, #237238 ),
 ( #58574, #116020, #138112 ),
 ( #195564, #59852, #142917 ),
 ( #43850, #24304, #84189 ),
 ( #204187, #105053, #184633 ) ),
 .UNSPECIFIED., .F., .F., .F. ) 
 B_SPLINE_SURFACE_WITH_KNOTS ( ( 4, 2, 4 ),
 ( 3, 3 ),
 ( 1.570796326794895448, 2.356194490192343505, 3.141592653589791784 ),
 ( 0.000000000000000000, 1.000000000000000000 ),
 .UNSPECIFIED. ) 
 GEOMETRIC_REPRESENTATION_ITEM ( )  RATIONAL_B_SPLINE_SURFACE ( (
 ( 1.000000000000000000, 0.7071067811865475727, 1.000000000000000000),
 ( 1.000000000000000000, 0.6611148371778921007, 1.000000000000000000),
 ( 1.000000000000000000, 0.6092287576696249207, 1.000000000000000000),
 ( 1.000000000000000000, 0.5278258667057440512, 1.000000000000000000),
 ( 1.000000000000000000, 0.4993418825334574596, 1.000000000000000000),
 ( 1.000000000000000000, 0.4999999999999960587, 1.000000000000000000) ) ) 
 REPRESENTATION_ITEM ( '' )  SURFACE ( )  );
#28115=CARTESIAN_POINT ( 'NONE',  ( -18.50016250449483479, 10.29766095125286895, -72.47436639332757125 ) ) ;
#28138=DIRECTION ( 'NONE',  ( 1.000000000000000000, -0.000000000000000000, -0.000000000000000000 ) ) ;
#28144=EDGE_LOOP ( 'NONE', ( #220064, #55554 ) ) ;
#28156=CARTESIAN_POINT ( 'NONE',  ( 20.85000000000000142, 7.021664781911246322, -70.83356540189728889 ) ) ;
#28174=CARTESIAN_POINT ( 'NONE',  ( 23.15000000000000213, -9.499999999988844479, -57.10603087734755690 ) ) ;
#28181=ADVANCED_FACE ( 'NONE', ( #22500 ), #119026, .F. ) ;
#28235=VERTEX_POINT ( 'NONE', #210116 ) ;
#28238=ORIENTED_EDGE ( 'NONE', *, *, #191972, .F. ) ;
#28303=CARTESIAN_POINT ( 'NONE',  ( 18.59999999999999787, -1.249999999988843369, -74.80048075441507649 ) ) ;
#28332=DIRECTION ( 'NONE',  ( -1.000000000000000000, 0.000000000000000000, 0.000000000000000000 ) ) ;
#28398=DIRECTION ( 'NONE',  ( 0.000000000000000000, -8.673617379883786823E-14, 1.000000000000000000 ) ) ;
#28408=ADVANCED_FACE ( 'NONE', ( #172309, #213952 ), #35352, .T. ) ;
#28437=DIRECTION ( 'NONE',  ( -1.000000000000000000, -0.000000000000000000, -0.000000000000000000 ) ) ;
#28457=CARTESIAN_POINT ( 'NONE',  ( 20.94999999999999929, -8.999999999988842703, -57.10603087734755690 ) ) ;
#28464=DIRECTION ( 'NONE',  ( 0.000000000000000000, -1.000000000000000000, -0.000000000000000000 ) ) ;
#28506=ORIENTED_EDGE ( 'NONE', *, *, #193578, .F. ) ;
#28509=VERTEX_POINT ( 'NONE', #79549 ) ;
#28528=ORIENTED_EDGE ( 'NONE', *, *, #82816, .T. ) ;
#28530=EDGE_CURVE ( 'NONE', #96628, #210104, #256566, .T. ) ;
#28567=ORIENTED_EDGE ( 'NONE', *, *, #162734, .F. ) ;
#28571=DIRECTION ( 'NONE',  ( 0.000000000000000000, -1.000000000000000000, -2.891205793294679805E-16 ) ) ;
#28598=DIRECTION ( 'NONE',  ( 1.000000000000000000, 0.000000000000000000, 0.000000000000000000 ) ) ;
#28615=PLANE ( 'NONE',  #41163 ) ;
#28621=CARTESIAN_POINT ( 'NONE',  ( -20.94999999999999929, -1.849153571964891274, -78.60596661979704436 ) ) ;
#28634=FACE_OUTER_BOUND ( 'NONE', #99177, .T. ) ;
#28642=ADVANCED_FACE ( 'NONE', ( #125133 ), #225474, .F. ) ;
#28652=CARTESIAN_POINT ( 'NONE',  ( -23.25000000000000000, 6.933893972137497030, -70.78564583437358237 ) ) ;
#28659=ORIENTED_EDGE ( 'NONE', *, *, #184003, .F. ) ;
#28681=ORIENTED_EDGE ( 'NONE', *, *, #256036, .T. ) ;
#28698=CYLINDRICAL_SURFACE ( 'NONE', #68167, 0.1000000000000028644 ) ;
#28732=CARTESIAN_POINT ( 'NONE',  ( 20.94999999999999574, -11.41227409413852989, -36.50000000000000711 ) ) ;
#28745=ORIENTED_EDGE ( 'NONE', *, *, #210599, .F. ) ;
#28766=CIRCLE ( 'NONE', #224523, 0.09999999999999949207 ) ;
#28779=CARTESIAN_POINT ( 'NONE',  ( -20.85000000000000142, 7.021664781911246322, -70.83356540189728889 ) ) ;
#28780=CARTESIAN_POINT ( 'NONE',  ( -23.25000000000000000, -1.851617760457748618, -78.60318971960367662 ) ) ;
#28781=CARTESIAN_POINT ( 'NONE',  ( -18.50000000000000000, 1.637172712981535883, -45.08215336547201701 ) ) ;
#28782=CARTESIAN_POINT ( 'NONE',  ( -20.85000000000000142, 10.33248238083634440, -72.59484654391314962 ) ) ;
#28802=DIRECTION ( 'NONE',  ( 0.000000000000000000, 0.000000000000000000, -1.000000000000000000 ) ) ;
#28804=CARTESIAN_POINT ( 'NONE',  ( -23.25000000000000000, 11.65000000001115588, -54.84999999999999432 ) ) ;
#28821=CARTESIAN_POINT ( 'NONE',  ( 21.05000000000000071, 1.115600667400684642E-11, -33.50000000000000000 ) ) ;
#28867=DIRECTION ( 'NONE',  ( 0.000000000000000000, 0.000000000000000000, -1.000000000000000000 ) ) ;
#28931=VERTEX_POINT ( 'NONE', #222267 ) ;
#28939=EDGE_LOOP ( 'NONE', ( #103357, #20358, #185600, #187539 ) ) ;
#28986=ORIENTED_EDGE ( 'NONE', *, *, #165647, .F. ) ;
#29009=ORIENTED_EDGE ( 'NONE', *, *, #85843, .F. ) ;
#29028=DIRECTION ( 'NONE',  ( -1.000000000000000000, -0.000000000000000000, -0.000000000000000000 ) ) ;
#29032=DIRECTION ( 'NONE',  ( 0.000000000000000000, 0.000000000000000000, 1.000000000000000000 ) ) ;
#29049=ORIENTED_EDGE ( 'NONE', *, *, #184231, .F. ) ;
#29060=CARTESIAN_POINT ( 'NONE',  ( -23.15000000000000213, 1.115600667400684642E-11, -33.50000000000000000 ) ) ;
#29065=CARTESIAN_POINT ( 'NONE',  ( -21.05000000000000071, 1.115600667400684642E-11, -55.19999999999999574 ) ) ;
#29078=EDGE_LOOP ( 'NONE', ( #236940, #88961, #231994, #147626 ) ) ;
#29100=CARTESIAN_POINT ( 'NONE',  ( 18.39999999999999858, -9.519327731081279609, -40.47297637655933755 ) ) ;
#29121=EDGE_CURVE ( 'NONE', #47498, #252850, #233864, .T. ) ;
#29148=VERTEX_POINT ( 'NONE', #194761 ) ;
#29151=DIRECTION ( 'NONE',  ( 1.000000000000000000, 2.952720810173289112E-16, -0.000000000000000000 ) ) ;
#29165=CARTESIAN_POINT ( 'NONE',  ( -21.13614978966381841, 6.499104701844946597, -33.49999999999999289 ) ) ;
#29183=CARTESIAN_POINT ( 'NONE',  ( 20.94999999999999929, 1.115649653272650466E-11, -63.00000000000000000 ) ) ;
#29212=DIRECTION ( 'NONE',  ( 0.000000000000000000, 1.000000000000000000, -6.308085367188393199E-16 ) ) ;
#29227=ADVANCED_FACE ( 'NONE', ( #5490 ), #102847, .F. ) ;
#29228=CARTESIAN_POINT ( 'NONE',  ( -18.59999999999999787, 7.021664781911246322, -70.73356540189729458 ) ) ;
#29251=CIRCLE ( 'NONE', #203982, 0.09999999999999939493 ) ;
#29254=DIRECTION ( 'NONE',  ( 0.000000000000000000, -0.000000000000000000, 1.000000000000000000 ) ) ;
#29262=AXIS2_PLACEMENT_3D ( 'NONE', #117937, #236593, #138750 ) ;
#29282=CARTESIAN_POINT ( 'NONE',  ( -20.64999999999999858, -8.999999999988846255, -42.89396912265245021 ) ) ;
#29306=DIRECTION ( 'NONE',  ( 0.000000000000000000, -1.000000000000000000, 0.000000000000000000 ) ) ;
#29332=LINE ( 'NONE', #130961, #131153 ) ;
#29375=CARTESIAN_POINT ( 'NONE',  ( 20.94999999999999574, -1.835341550213255957, -45.05515129256298223 ) ) ;
#29409=DIRECTION ( 'NONE',  ( 0.000000000000000000, -1.000000000000000000, 0.000000000000000000 ) ) ;
#29410=ORIENTED_EDGE ( 'NONE', *, *, #147637, .F. ) ;
#29424=EDGE_LOOP ( 'NONE', ( #125533, #59805, #38896, #44223 ) ) ;
#29451=CYLINDRICAL_SURFACE ( 'NONE', #137347, 11.79999999999999716 ) ;
#29467=DIRECTION ( 'NONE',  ( 0.000000000000000000, 1.000000000000000000, 0.000000000000000000 ) ) ;
#29555=ORIENTED_EDGE ( 'NONE', *, *, #222072, .T. ) ;
#29592=FACE_OUTER_BOUND ( 'NONE', #248749, .T. ) ;
#29609=LINE ( 'NONE', #167834, #250696 ) ;
#29652=CARTESIAN_POINT ( 'NONE',  ( -20.94999999999999929, 11.60000000001115161, -40.42820323027555673 ) ) ;
#29658=ORIENTED_EDGE ( 'NONE', *, *, #231644, .F. ) ;
#29681=ORIENTED_EDGE ( 'NONE', *, *, #229858, .F. ) ;
#29687=EDGE_LOOP ( 'NONE', ( #222293, #3414, #164074, #3807 ) ) ;
#29692=FACE_OUTER_BOUND ( 'NONE', #95361, .T. ) ;
#29693=CARTESIAN_POINT ( 'NONE',  ( 20.94999999999999574, -1.835341550213255957, -45.05515129256298223 ) ) ;
#29710=DIRECTION ( 'NONE',  ( 0.000000000000000000, 0.000000000000000000, -1.000000000000000000 ) ) ;
#29747=ORIENTED_EDGE ( 'NONE', *, *, #95857, .F. ) ;
#29750=EDGE_CURVE ( 'NONE', #101473, #145358, #67756, .T. ) ;
#29818=ORIENTED_EDGE ( 'NONE', *, *, #141008, .F. ) ;
#29835=DIRECTION ( 'NONE',  ( 1.000000000000000000, -0.000000000000000000, -0.000000000000000000 ) ) ;
#29850=CARTESIAN_POINT ( 'NONE',  ( -23.15000000000000213, 11.75000000001115552, -45.75000000000000000 ) ) ;
#29864=CIRCLE ( 'NONE', #129777, 0.1000000000000028644 ) ;
#29905=CARTESIAN_POINT ( 'NONE',  ( -20.94999999999999929, 0.2561057921033771945, -33.46510355832771211 ) ) ;
#29914=FACE_OUTER_BOUND ( 'NONE', #190567, .T. ) ;
#29927=ADVANCED_FACE ( 'NONE', ( #173326 ), #196669, .T. ) ;
#29936=CARTESIAN_POINT ( 'NONE',  ( -18.50000000000000000, 1.115600667400684642E-11, -67.00000000000000000 ) ) ;
#29938=CARTESIAN_POINT ( 'NONE',  ( 18.50000000000000000, -9.499999999988842703, -73.60018939122204529 ) ) ;
#29944=AXIS2_PLACEMENT_3D ( 'NONE', #168826, #170109, #147937 ) ;
#29989=CARTESIAN_POINT ( 'NONE',  ( 22.39999999999999858, 0.1000000000111554016, -25.70922040162662014 ) ) ;
#29996=LINE ( 'NONE', #28732, #31679 ) ;
#30008=CARTESIAN_POINT ( 'NONE',  ( 21.04999999999999716, 6.304455821958818262, -33.52103547654012772 ) ) ;
#30011=DIRECTION ( 'NONE',  ( 0.000000000000000000, 0.000000000000000000, -1.000000000000000000 ) ) ;
#30035=DIRECTION ( 'NONE',  ( -0.000000000000000000, -0.000000000000000000, 1.000000000000000000 ) ) ;
#30088=CARTESIAN_POINT ( 'NONE',  ( 23.14999999999999858, 1.115600667400684642E-11, -67.00000000000000000 ) ) ;
#30089=AXIS2_PLACEMENT_3D ( 'NONE', #245646, #162272, #103543 ) ;
#30159=ORIENTED_EDGE ( 'NONE', *, *, #20963, .F. ) ;
#30191=CARTESIAN_POINT ( 'NONE',  ( 18.55121869061587958, 10.32747123227773400, -72.57740328502492844 ) ) ;
#30225=ORIENTED_EDGE ( 'NONE', *, *, #92323, .F. ) ;
#30236=ADVANCED_FACE ( 'NONE', ( #107845 ), #239257, .F. ) ;
#30254=VECTOR ( 'NONE', #237331, 1000.000000000000000 ) ;
#30310=VECTOR ( 'NONE', #20817, 1000.000000000000000 ) ;
#30318=AXIS2_PLACEMENT_3D ( 'NONE', #84737, #122648, #178789 ) ;
#30326=CYLINDRICAL_SURFACE ( 'NONE', #59440, 0.1000000000000028644 ) ;
#30359=ORIENTED_EDGE ( 'NONE', *, *, #23116, .F. ) ;
#30388=ORIENTED_EDGE ( 'NONE', *, *, #204835, .T. ) ;
#30397=LINE ( 'NONE', #32999, #121177 ) ;
#30399=AXIS2_PLACEMENT_3D ( 'NONE', #182215, #243454, #161373 ) ;
#30400=FACE_OUTER_BOUND ( 'NONE', #237720, .T. ) ;
#30462=ORIENTED_EDGE ( 'NONE', *, *, #134829, .T. ) ;
#30463=EDGE_CURVE ( 'NONE', #235258, #194903, #114541, .T. ) ;
#30524=CIRCLE ( 'NONE', #205452, 0.1000000000000028644 ) ;
#30605=AXIS2_PLACEMENT_3D ( 'NONE', #176430, #96832, #73487 ) ;
#30611=ORIENTED_EDGE ( 'NONE', *, *, #118475, .F. ) ;
#30619=DIRECTION ( 'NONE',  ( 0.000000000000000000, -0.1350103645451904977, -0.9908441862701596881 ) ) ;
#30628=EDGE_CURVE ( 'NONE', #207108, #46223, #78353, .T. ) ;
#30657=AXIS2_PLACEMENT_3D ( 'NONE', #19207, #236976, #139114 ) ;
#30660=AXIS2_PLACEMENT_3D ( 'NONE', #154413, #55234, #213051 ) ;
#30664=AXIS2_PLACEMENT_3D ( 'NONE', #78055, #160200, #100163 ) ;
#30680=FACE_OUTER_BOUND ( 'NONE', #45109, .T. ) ;
#30689=DIRECTION ( 'NONE',  ( 0.000000000000000000, 0.000000000000000000, -1.000000000000000000 ) ) ;
#30725=DIRECTION ( 'NONE',  ( -1.000000000000000000, 0.000000000000000000, 0.000000000000000000 ) ) ;
#30727=CARTESIAN_POINT ( 'NONE',  ( 18.49999999999999645, 10.25000000263022670, -58.18717194963260653 ) ) ;
#30728=DIRECTION ( 'NONE',  ( 1.000000000000000000, -0.000000000000000000, -0.000000000000000000 ) ) ;
#30732=CARTESIAN_POINT ( 'NONE',  ( -20.15000000000000568, 9.291421356248463326, -54.75000000000000000 ) ) ;
#30739=CARTESIAN_POINT ( 'NONE',  ( -20.00857864376270001, 9.150000000011157653, -45.75000000000000000 ) ) ;
#30746=DIRECTION ( 'NONE',  ( -0.000000000000000000, 0.8660254037844502539, 0.4999999999999799050 ) ) ;
#30812=CARTESIAN_POINT ( 'NONE',  ( -20.94999999999999929, -1.360870587180885716, -41.57299792709095954 ) ) ;
#30827=DIRECTION ( 'NONE',  ( 0.000000000000000000, 0.000000000000000000, -1.000000000000000000 ) ) ;
#30860=VERTEX_POINT ( 'NONE', #117055 ) ;
#30864=VECTOR ( 'NONE', #199272, 1000.000000000000000 ) ;
#30880=EDGE_CURVE ( 'NONE', #237399, #193788, #96184, .T. ) ;
#30913=ADVANCED_FACE ( 'NONE', ( #75386 ), #31377, .T. ) ;
#30940=DIRECTION ( 'NONE',  ( 0.000000000000000000, 0.000000000000000000, 1.000000000000000000 ) ) ;
#30950=CARTESIAN_POINT ( 'NONE',  ( -18.42637059832564006, -9.496945461878546269, -73.60907730979984365 ) ) ;
#30953=ORIENTED_EDGE ( 'NONE', *, *, #203339, .T. ) ;
#30960=CARTESIAN_POINT ( 'NONE',  ( -21.55000000000000426, 7.708578643773852157, -54.75000000000000000 ) ) ;
#30973=ORIENTED_EDGE ( 'NONE', *, *, #218311, .T. ) ;
#30974=CARTESIAN_POINT ( 'NONE',  ( 20.84999999999999432, 7.021664781911246322, -70.83356540189728889 ) ) ;
#30996=CARTESIAN_POINT ( 'NONE',  ( 21.05000000000000071, 5.000000000011153745, -54.59473398108690390 ) ) ;
#31005=CARTESIAN_POINT ( 'NONE',  ( -21.14999999999999858, 6.540656951712397138, -33.60000000000000142 ) ) ;
#31007=ADVANCED_FACE ( 'NONE', ( #219994 ), #25655, .F. ) ;
#31026=CIRCLE ( 'NONE', #189220, 0.09999999999999939493 ) ;
#31078=CARTESIAN_POINT ( 'NONE',  ( 23.15000000000000213, -8.596261682231833845, -42.95012751715027832 ) ) ;
#31100=AXIS2_PLACEMENT_3D ( 'NONE', #124287, #163410, #123003 ) ;
#31111=EDGE_LOOP ( 'NONE', ( #177741, #256669, #117207, #251985 ) ) ;
#31118=AXIS2_PLACEMENT_3D ( 'NONE', #161074, #18969, #138888 ) ;
#31129=DIRECTION ( 'NONE',  ( 0.000000000000000000, 0.000000000000000000, -1.000000000000000000 ) ) ;
#31140=ORIENTED_EDGE ( 'NONE', *, *, #113628, .F. ) ;
#31144=CARTESIAN_POINT ( 'NONE',  ( 23.14999999999999147, -4.149999999988843058, -33.50000000000000000 ) ) ;
#31154=EDGE_LOOP ( 'NONE', ( #195786, #188978, #137263, #234740 ) ) ;
#31162=ORIENTED_EDGE ( 'NONE', *, *, #232783, .F. ) ;
#31169=CARTESIAN_POINT ( 'NONE',  ( 18.59999999999999076, 11.65000000001115943, -58.35000000000000142 ) ) ;
#31186=EDGE_LOOP ( 'NONE', ( #131540, #15244, #11273, #93517 ) ) ;
#31209=CARTESIAN_POINT ( 'NONE',  ( 22.49806830649814060, 11.64988965485023620, -33.42253568367449645 ) ) ;
#31217=AXIS2_PLACEMENT_3D ( 'NONE', #186375, #239929, #203362 ) ;
#31225=ORIENTED_EDGE ( 'NONE', *, *, #152309, .F. ) ;
#31260=FACE_OUTER_BOUND ( 'NONE', #31983, .T. ) ;
#31278=DIRECTION ( 'NONE',  ( -1.000000000000000000, 0.000000000000000000, 0.000000000000000000 ) ) ;
#31289=EDGE_LOOP ( 'NONE', ( #141431, #18415, #154100, #91178, #224190, #166767 ) ) ;
#31300=ORIENTED_EDGE ( 'NONE', *, *, #82594, .T. ) ;
#31342=ADVANCED_FACE ( 'NONE', ( #119971 ), #114909, .T. ) ;
#31346=CIRCLE ( 'NONE', #243689, 0.1000000000000028644 ) ;
#31365=ORIENTED_EDGE ( 'NONE', *, *, #253911, .F. ) ;
#31377=TOROIDAL_SURFACE ( 'NONE', #135555, 7.800000000000000711, 0.1000000000000000056 ) ;
#31382=CARTESIAN_POINT ( 'NONE',  ( -22.47071067811865674, 7.720074744509219045, -33.40090754529740025 ) ) ;
#31402=CARTESIAN_POINT ( 'NONE',  ( 21.05000000000000071, 1.115650877919449575E-11, -62.90000000000001279 ) ) ;
#31430=EDGE_CURVE ( 'NONE', #167819, #139486, #106492, .T. ) ;
#31431=ADVANCED_FACE ( 'NONE', ( #203333 ), #40441, .F. ) ;
#31458=VERTEX_POINT ( 'NONE', #126355 ) ;
#31485=CARTESIAN_POINT ( 'NONE',  ( -20.85000000000000142, 11.75000000001115197, -60.21613433702190576 ) ) ;
#31496=EDGE_CURVE ( 'NONE', #88400, #205142, #85913, .T. ) ;
#31516=ADVANCED_FACE ( 'NONE', ( #5088 ), #229322, .T. ) ;
#31528=CIRCLE ( 'NONE', #231409, 4.099999999999992539 ) ;
#31532=DIRECTION ( 'NONE',  ( 0.000000000000000000, 0.000000000000000000, -1.000000000000000000 ) ) ;
#31596=DIRECTION ( 'NONE',  ( -1.000000000000000000, 0.000000000000000000, 0.000000000000000000 ) ) ;
#31610=VERTEX_POINT ( 'NONE', #57057 ) ;
#31618=CIRCLE ( 'NONE', #123353, 11.65000000000000036 ) ;
#31630=CARTESIAN_POINT ( 'NONE',  ( -20.64999999999999858, 1.115600667400684642E-11, -46.47500000000000142 ) ) ;
#31633=CARTESIAN_POINT ( 'NONE',  ( 19.75857864376268935, 11.65000000001115943, -58.25000000000000000 ) ) ;
#31639=EDGE_CURVE ( 'NONE', #171197, #231120, #175773, .T. ) ;
#31654=CARTESIAN_POINT ( 'NONE',  ( 18.39999999999999858, -9.499999999988844479, -40.53206939669966857 ) ) ;
#31679=VECTOR ( 'NONE', #190339, 1000.000000000000000 ) ;
#31683=AXIS2_PLACEMENT_3D ( 'NONE', #248301, #227444, #110068 ) ;
#31706=DIRECTION ( 'NONE',  ( 0.000000000000000000, -1.000000000000000000, 0.000000000000000000 ) ) ;
#31713=ADVANCED_FACE ( 'NONE', ( #145273 ), #241664, .T. ) ;
#31717=CARTESIAN_POINT ( 'NONE',  ( -21.37071067811865532, 8.070710678129811910, -54.75000000000000000 ) ) ;
#31760=CARTESIAN_POINT ( 'NONE',  ( -20.94999999999999929, -1.162701749926853712, -41.50000000000000000 ) ) ;
#31773=AXIS2_PLACEMENT_3D ( 'NONE', #200555, #103992, #46594 ) ;
#31794=EDGE_LOOP ( 'NONE', ( #234845, #21021, #37421, #161276 ) ) ;
#31795=DIRECTION ( 'NONE',  ( 0.000000000000000000, -1.000000000000000000, 0.000000000000000000 ) ) ;
#31801=CARTESIAN_POINT ( 'NONE',  ( -18.39999999999999858, -9.519327731081281385, -40.47297637655933045 ) ) ;
#31802=ORIENTED_EDGE ( 'NONE', *, *, #187721, .T. ) ;
#31820=AXIS2_PLACEMENT_3D ( 'NONE', #66626, #144862, #202286 ) ;
#31851=LINE ( 'NONE', #112650, #249094 ) ;
#31862=ADVANCED_FACE ( 'NONE', ( #8361 ), #167451, .F. ) ;
#31874=ORIENTED_EDGE ( 'NONE', *, *, #191260, .F. ) ;
#31897=CARTESIAN_POINT ( 'NONE',  ( -21.52071067811865746, 7.779289321892505882, -45.85000000000000142 ) ) ;
#31901=AXIS2_PLACEMENT_3D ( 'NONE', #197381, #236508, #57859 ) ;
#31905=FACE_OUTER_BOUND ( 'NONE', #33107, .T. ) ;
#31916=VERTEX_POINT ( 'NONE', #31801 ) ;
#31917=DIRECTION ( 'NONE',  ( 0.7071359030027766224, -0.7070776581709024011, 0.000000000000000000 ) ) ;
#31946=ORIENTED_EDGE ( 'NONE', *, *, #45711, .T. ) ;
#31953=ORIENTED_EDGE ( 'NONE', *, *, #35767, .F. ) ;
#31983=EDGE_LOOP ( 'NONE', ( #69653, #5032, #154763, #56078 ) ) ;
#32003=CARTESIAN_POINT ( 'NONE',  ( 18.49999999999988276, 10.28015861706820466, -58.22457207120090317 ) ) ;
#32021=DIRECTION ( 'NONE',  ( 1.000000000000000000, 1.734723475976817507E-14, 0.000000000000000000 ) ) ;
#32040=ORIENTED_EDGE ( 'NONE', *, *, #74702, .F. ) ;
#32045=ORIENTED_EDGE ( 'NONE', *, *, #87908, .T. ) ;
#32048=DIRECTION ( 'NONE',  ( 0.000000000000000000, 0.000000000000000000, -1.000000000000000000 ) ) ;
#32065=ORIENTED_EDGE ( 'NONE', *, *, #114509, .F. ) ;
#32066=AXIS2_PLACEMENT_3D ( 'NONE', #130736, #91613, #53769 ) ;
#32074=DIRECTION ( 'NONE',  ( 0.000000000000000000, -1.000000000000000000, 6.308085367188393199E-16 ) ) ;
#32087=DIRECTION ( 'NONE',  ( -0.000000000000000000, -0.000000000000000000, -1.000000000000000000 ) ) ;
#32093=FACE_OUTER_BOUND ( 'NONE', #26295, .T. ) ;
#32106=AXIS2_PLACEMENT_3D ( 'NONE', #1989, #46256, #142774 ) ;
#32117=FACE_OUTER_BOUND ( 'NONE', #50529, .T. ) ;
#32154=DIRECTION ( 'NONE',  ( 0.000000000000000000, 1.224646799142015331E-16, 1.000000000000000000 ) ) ;
#32155=EDGE_CURVE ( 'NONE', #9287, #96922, #142413, .T. ) ;
#32176=CARTESIAN_POINT ( 'NONE',  ( -20.94999999999999929, -11.48912529306489994, -63.89999999999999858 ) ) ;
#32194=CARTESIAN_POINT ( 'NONE',  ( 21.11101077988997332, 6.423684734737197921, -33.48471473108569540 ) ) ;
#32222=CARTESIAN_POINT ( 'NONE',  ( -18.50000000000000355, -9.419084502802135717, -73.82990780702543532 ) ) ;
#32225=DIRECTION ( 'NONE',  ( -1.000000000000000000, -0.000000000000000000, -0.000000000000000000 ) ) ;
#32244=ORIENTED_EDGE ( 'NONE', *, *, #133673, .F. ) ;
#32246=ORIENTED_EDGE ( 'NONE', *, *, #45943, .T. ) ;
#32270=DIRECTION ( 'NONE',  ( -1.000000000000000000, -8.673617379884087537E-15, 0.000000000000000000 ) ) ;
#32344=VERTEX_POINT ( 'NONE', #96540 ) ;
#32346=CARTESIAN_POINT ( 'NONE',  ( -20.96077737575326694, 11.62390063401586282, -60.14079195710661452 ) ) ;
#32375=FACE_OUTER_BOUND ( 'NONE', #249669, .T. ) ;
#32397=AXIS2_PLACEMENT_3D ( 'NONE', #57817, #132240, #253458 ) ;
#32408=DIRECTION ( 'NONE',  ( 0.000000000000000000, 0.9998779222360096863, -0.01562500000001061998 ) ) ;
#32443=CARTESIAN_POINT ( 'NONE',  ( 20.94999999999999929, 1.115600667400684642E-11, -67.00000000000000000 ) ) ;
#32454=CARTESIAN_POINT ( 'NONE',  ( -18.49499033040907037, -9.438148771733517961, -40.69815322592344131 ) ) ;
#32464=CARTESIAN_POINT ( 'NONE',  ( -20.54999999999999716, 7.250000000011155521, -54.65000000000000568 ) ) ;
#32466=CIRCLE ( 'NONE', #103140, 0.1000000000000029476 ) ;
#32483=DIRECTION ( 'NONE',  ( 0.000000000000000000, 0.9908441862701596881, 0.1350103645451904977 ) ) ;
#32491=EDGE_CURVE ( 'NONE', #127487, #233728, #247969, .T. ) ;
#32493=EDGE_LOOP ( 'NONE', ( #61118, #76097, #128086 ) ) ;
#32509=FACE_OUTER_BOUND ( 'NONE', #69390, .T. ) ;
#32556=CARTESIAN_POINT ( 'NONE',  ( 20.94999999999999929, 6.650000000011155876, -54.75000000000000000 ) ) ;
#32559=DIRECTION ( 'NONE',  ( 1.000000000000000000, -0.000000000000000000, 0.000000000000000000 ) ) ;
#32564=DIRECTION ( 'NONE',  ( 0.000000000000000000, -0.9999176327611369874, 0.01283462868041987913 ) ) ;
#32576=CARTESIAN_POINT ( 'NONE',  ( -23.25000000000000000, -11.64999999998884483, -21.75000000000000355 ) ) ;
#32599=CARTESIAN_POINT ( 'NONE',  ( 18.39999999999999858, -9.499999999988842703, -73.91465834296967330 ) ) ;
#32615=CARTESIAN_POINT ( 'NONE',  ( 20.94999999999999574, -1.835341550213255957, -45.15515129256298366 ) ) ;
#32624=DIRECTION ( 'NONE',  ( -0.000000000000000000, -0.8700118002898321601, 0.4930308989875230030 ) ) ;
#32671=CARTESIAN_POINT ( 'NONE',  ( -21.53752568617666441, 6.786807874515170980, -33.40102553874074687 ) ) ;
#32677=CARTESIAN_POINT ( 'NONE',  ( -18.50000000000000000, 9.350000000011156942, -45.85000000000000142 ) ) ;
#32694=CARTESIAN_POINT ( 'NONE',  ( 20.97239005616515328, 8.874843841361279573, -45.75015280215318825 ) ) ;
#32699=LINE ( 'NONE', #131746, #211728 ) ;
#32704=ORIENTED_EDGE ( 'NONE', *, *, #100716, .T. ) ;
#32715=EDGE_LOOP ( 'NONE', ( #214285, #238107, #240047, #201951 ) ) ;
#32762=CYLINDRICAL_SURFACE ( 'NONE', #4248, 0.1000000000000028644 ) ;
#32765=CARTESIAN_POINT ( 'NONE',  ( -20.64999999999999858, 1.925233644870967487, -54.26975646687386501 ) ) ;
#32801=CARTESIAN_POINT ( 'NONE',  ( 18.49999999999999289, 10.20857864377385127, -58.15000000000000568 ) ) ;
#32807=CARTESIAN_POINT ( 'NONE',  ( 18.39999999999999858, -9.499999999988844479, -73.60018939122204529 ) ) ;
#32812=CARTESIAN_POINT ( 'NONE',  ( -23.25000000000000000, 11.65000000001115588, -59.98519422934604961 ) ) ;
#32817=DIRECTION ( 'NONE',  ( 1.000000000000000000, 0.000000000000000000, 0.000000000000000000 ) ) ;
#32839=ORIENTED_EDGE ( 'NONE', *, *, #50521, .F. ) ;
#32843=CARTESIAN_POINT ( 'NONE',  ( -20.64999999999999858, 1.115600667400684642E-11, -46.37500000000000000 ) ) ;
#32848=AXIS2_PLACEMENT_3D ( 'NONE', #254813, #198741, #16287 ) ;
#32852=CIRCLE ( 'NONE', #70265, 0.1000000000000013933 ) ;
#32875=CARTESIAN_POINT ( 'NONE',  ( 21.10710606213542206, 8.776894023904366904, -45.74099652639942093 ) ) ;
#32879=CYLINDRICAL_SURFACE ( 'NONE', #153196, 0.09999999999999939493 ) ;
#32880=ORIENTED_EDGE ( 'NONE', *, *, #144939, .F. ) ;
#32909=VERTEX_POINT ( 'NONE', #4823 ) ;
#32918=EDGE_CURVE ( 'NONE', #189223, #201612, #127545, .T. ) ;
#32950=CARTESIAN_POINT ( 'NONE',  ( 18.42595409746875035, -9.499999812554021261, -40.49936235174737220 ) ) ;
#32966=LINE ( 'NONE', #188143, #148449 ) ;
#32970=DIRECTION ( 'NONE',  ( -1.000000000000000000, 0.000000000000000000, 0.000000000000000000 ) ) ;
#32976=CARTESIAN_POINT ( 'NONE',  ( -23.25000000000000000, 1.910280373842930812, -54.36863214480106166 ) ) ;
#32991=CARTESIAN_POINT ( 'NONE',  ( -20.85000000000000142, -1.835859311432481045, -78.60443916879853532 ) ) ;
#32999=CARTESIAN_POINT ( 'NONE',  ( 21.05000000000000071, -11.74999999998883560, -36.39999999999999858 ) ) ;
#33013=CARTESIAN_POINT ( 'NONE',  ( 20.94999999999999574, -11.48912529306490349, -36.60000000000000142 ) ) ;
#33023=DIRECTION ( 'NONE',  ( 1.000000000000000000, 0.000000000000000000, 0.000000000000000000 ) ) ;
#33049=ORIENTED_EDGE ( 'NONE', *, *, #109380, .F. ) ;
#33050=LINE ( 'NONE', #248198, #39432 ) ;
#33073=ORIENTED_EDGE ( 'NONE', *, *, #141803, .T. ) ;
#33107=EDGE_LOOP ( 'NONE', ( #140263, #184304, #30359, #170638 ) ) ;
#33112=ORIENTED_EDGE ( 'NONE', *, *, #84347, .F. ) ;
#33127=CARTESIAN_POINT ( 'NONE',  ( -20.99142135623731065, 11.60000000001115161, -60.07179676972450721 ) ) ;
#33133=EDGE_CURVE ( 'NONE', #28931, #214564, #40271, .T. ) ;
#33136=CARTESIAN_POINT ( 'NONE',  ( 21.07954763557419042, 6.329290990048669130, -33.43412408138156167 ) ) ;
#33137=CARTESIAN_POINT ( 'NONE',  ( -21.05000000000000071, 1.162701749949165642, -41.60000000000000142 ) ) ;
#33138=LINE ( 'NONE', #130902, #28090 ) ;
#33148=ADVANCED_FACE ( 'NONE', ( #136320 ), #173667, .T. ) ;
#33163=AXIS2_PLACEMENT_3D ( 'NONE', #149465, #32087, #111603 ) ;
#33248=ORIENTED_EDGE ( 'NONE', *, *, #21165, .T. ) ;
#33258=ORIENTED_EDGE ( 'NONE', *, *, #223923, .T. ) ;
#33267=DIRECTION ( 'NONE',  ( -1.000000000000000000, 0.000000000000000000, 0.000000000000000000 ) ) ;
#33279=AXIS2_PLACEMENT_3D ( 'NONE', #217678, #15691, #14404 ) ;
#33312=DIRECTION ( 'NONE',  ( 0.000000000000000000, 0.000000000000000000, -1.000000000000000000 ) ) ;
#33322=ORIENTED_EDGE ( 'NONE', *, *, #57069, .T. ) ;
#33328=EDGE_CURVE ( 'NONE', #66671, #146761, #94386, .T. ) ;
#33347=DIRECTION ( 'NONE',  ( -1.000000000000000000, -0.000000000000000000, -0.000000000000000000 ) ) ;
#33354=VERTEX_POINT ( 'NONE', #103619 ) ;
#33357=CARTESIAN_POINT ( 'NONE',  ( 19.75857864376268935, 11.75000000001115907, -58.35000000000000142 ) ) ;
#33370=DIRECTION ( 'NONE',  ( 0.000000000000000000, 0.000000000000000000, -1.000000000000000000 ) ) ;
#33386=CARTESIAN_POINT ( 'NONE',  ( 21.05000000000000071, 1.115600667400684642E-11, -33.50000000000000000 ) ) ;
#33406=EDGE_CURVE ( 'NONE', #163151, #38982, #244220, .T. ) ;
#33407=AXIS2_PLACEMENT_3D ( 'NONE', #88305, #242266, #68783 ) ;
#33430=DIRECTION ( 'NONE',  ( 0.000000000000000000, -1.000000000000000000, 0.000000000000000000 ) ) ;
#33447=CARTESIAN_POINT ( 'NONE',  ( 20.01093837587850288, 11.75000000001116263, -58.25439743459698150 ) ) ;
#33449=CARTESIAN_POINT ( 'NONE',  ( -23.25000000000000000, -11.64999999998884483, -63.89999999999999858 ) ) ;
#33451=CARTESIAN_POINT ( 'NONE',  ( -20.94999999999999929, 1.250000000011155299, -41.50000000000000000 ) ) ;
#33457=CIRCLE ( 'NONE', #174943, 12.87499999999999822 ) ;
#33458=AXIS2_PLACEMENT_3D ( 'NONE', #238177, #38720, #118247 ) ;
#33462=DIRECTION ( 'NONE',  ( 0.000000000000000000, 0.1495327102803689356, -0.9887567792719336168 ) ) ;
#33477=EDGE_LOOP ( 'NONE', ( #189488, #188076, #10246, #4936 ) ) ;
#33491=CARTESIAN_POINT ( 'NONE',  ( -22.50000000000000000, 11.64957080755595520, -33.40000000000000568 ) ) ;
#33503=EDGE_LOOP ( 'NONE', ( #201096, #233425, #204017, #101452 ) ) ;
#33510=CIRCLE ( 'NONE', #8520, 0.1000000000000017958 ) ;
#33516=EDGE_CURVE ( 'NONE', #173018, #31916, #137019, .T. ) ;
#33521=EDGE_CURVE ( 'NONE', #27329, #16250, #216550, .T. ) ;
#33540=DIRECTION ( 'NONE',  ( -1.000000000000000000, 0.000000000000000000, 0.000000000000000000 ) ) ;
#33543=CARTESIAN_POINT ( 'NONE',  ( 20.84999999999998721, -11.74999999998884448, -67.00000000000000000 ) ) ;
#33560=AXIS2_PLACEMENT_3D ( 'NONE', #5237, #207339, #245171 ) ;
#33577=LINE ( 'NONE', #202858, #170872 ) ;
#33579=DIRECTION ( 'NONE',  ( -0.000000000000000000, 0.8660254037844411501, 0.4999999999999956701 ) ) ;
#33594=CARTESIAN_POINT ( 'NONE',  ( 20.46382478191414833, 10.59862044130854031, -41.17781446934547063 ) ) ;
#33622=DIRECTION ( 'NONE',  ( 0.000000000000000000, 1.000000000000000000, 0.000000000000000000 ) ) ;
#33639=DIRECTION ( 'NONE',  ( 0.000000000000000000, -4.336808689941893885E-15, 1.000000000000000000 ) ) ;
#33648=CARTESIAN_POINT ( 'NONE',  ( -21.05315837350849506, 11.74999999738093059, -60.15835599785489052 ) ) ;
#33655=CIRCLE ( 'NONE', #241698, 0.09999999999999761857 ) ;
#33673=AXIS2_PLACEMENT_3D ( 'NONE', #100607, #202315, #134922 ) ;
#33678=DIRECTION ( 'NONE',  ( 1.734723475976817507E-14, 0.000000000000000000, -1.000000000000000000 ) ) ;
#33690=DIRECTION ( 'NONE',  ( -1.000000000000000000, 0.000000000000000000, 0.000000000000000000 ) ) ;
#33706=CARTESIAN_POINT ( 'NONE',  ( -21.29999999999995808, 1.115600667400684642E-11, -33.50000000000000000 ) ) ;
#33707=DIRECTION ( 'NONE',  ( 0.000000000000000000, 1.776356839400254803E-15, -1.000000000000000000 ) ) ;
#33741=ORIENTED_EDGE ( 'NONE', *, *, #27266, .F. ) ;
#33757=ORIENTED_EDGE ( 'NONE', *, *, #192494, .T. ) ;
#33794=CARTESIAN_POINT ( 'NONE',  ( 20.94999999999999929, -1.835859311432481045, -78.50443916879852679 ) ) ;
#33802=DIRECTION ( 'NONE',  ( 0.000000000000000000, -1.000000000000000000, 0.000000000000000000 ) ) ;
#33834=DIRECTION ( 'NONE',  ( 1.000000000000000000, 0.000000000000000000, 0.000000000000000000 ) ) ;
#33846=CIRCLE ( 'NONE', #154453, 0.09999999999999939493 ) ;
#33859=ORIENTED_EDGE ( 'NONE', *, *, #203904, .T. ) ;
#33863=DIRECTION ( 'NONE',  ( -0.7071067811865474617, -0.7071067811865474617, -2.044391222244499837E-16 ) ) ;
#33877=ORIENTED_EDGE ( 'NONE', *, *, #169884, .T. ) ;
#33920=CARTESIAN_POINT ( 'NONE',  ( -18.59999999999999787, 6.982009704867601307, -70.69615211825629331 ) ) ;
#33934=DIRECTION ( 'NONE',  ( 0.000000000000000000, -1.000000000000000000, 0.000000000000000000 ) ) ;
#33939=VERTEX_POINT ( 'NONE', #152452 ) ;
#33943=DIRECTION ( 'NONE',  ( -0.000000000000000000, -0.000000000000000000, 1.000000000000000000 ) ) ;
#33962=PLANE ( 'NONE',  #141495 ) ;
#33967=FACE_OUTER_BOUND ( 'NONE', #236206, .T. ) ;
#34003=CARTESIAN_POINT ( 'NONE',  ( -20.94999999999999929, -1.835341550213255957, -45.05515129256298223 ) ) ;
#34024=DIRECTION ( 'NONE',  ( -1.000000000000000000, -0.000000000000000000, 0.000000000000000000 ) ) ;
#34036=DIRECTION ( 'NONE',  ( 2.952720810173289112E-16, -1.000000000000000000, -0.000000000000000000 ) ) ;
#34043=CARTESIAN_POINT ( 'NONE',  ( 21.05000000000000426, -0.01681986837451829309, -27.19257478043459386 ) ) ;
#34050=ORIENTED_EDGE ( 'NONE', *, *, #216960, .F. ) ;
#34085=CARTESIAN_POINT ( 'NONE',  ( 18.49999999999999289, 10.20857864377384239, -58.26715728752538581 ) ) ;
#34096=CARTESIAN_POINT ( 'NONE',  ( 20.94999999999999929, 6.650000000011155876, -45.65000000000000568 ) ) ;
#34134=CARTESIAN_POINT ( 'NONE',  ( -18.36527282682041928, -9.500000599987968641, -73.92214896449833361 ) ) ;
#34154=CARTESIAN_POINT ( 'NONE',  ( 21.14999999999999858, 8.786607556611267356, -45.75000000000000711 ) ) ;
#34157=( BOUNDED_SURFACE ( )  B_SPLINE_SURFACE ( 3, 2, ( 
 ( #238308, #101317, #201750 ),
 ( #220038, #257823, #23146 ),
 ( #60953, #38849, #163921 ),
 ( #41423, #59647, #183484 ),
 ( #139189, #21845, #141769 ),
 ( #119667, #161363, #42682 ),
 ( #242160, #84317, #218731 ),
 ( #180917, #118382, #62249 ) ),
 .UNSPECIFIED., .F., .F., .F. ) 
 B_SPLINE_SURFACE_WITH_KNOTS ( ( 4, 2, 2, 4 ),
 ( 3, 3 ),
 ( 0.0001723339234021445073, 0.0002782939632049937244, 0.0003842540030078429956, 0.0005961740826135415380 ),
 ( 0.000000000000000000, 1.000000000000000000 ),
 .UNSPECIFIED. ) 
 GEOMETRIC_REPRESENTATION_ITEM ( )  RATIONAL_B_SPLINE_SURFACE ( (
 ( 1.000000000000000000, 0.9504532311154628710, 1.000000000000000000),
 ( 1.000000000000000000, 0.9506023220710051458, 1.000000000000000000),
 ( 1.000000000000000000, 0.9395774818181180654, 1.000000000000000000),
 ( 1.000000000000000000, 0.9079328464647721253, 1.000000000000000000),
 ( 1.000000000000000000, 0.8875702416205415446, 1.000000000000000000),
 ( 1.000000000000000000, 0.8205919608040560531, 1.000000000000000000),
 ( 1.000000000000000000, 0.7666842783598126765, 1.000000000000000000),
 ( 1.000000000000000000, 0.7071067811864651942, 1.000000000000000000) ) ) 
 REPRESENTATION_ITEM ( '' )  SURFACE ( )  );
#34158=CARTESIAN_POINT ( 'NONE',  ( 20.94999999999999929, 4.850467289730776344, -54.96573259099832143 ) ) ;
#34188=ORIENTED_EDGE ( 'NONE', *, *, #246657, .F. ) ;
#34216=CARTESIAN_POINT ( 'NONE',  ( 22.57320508075688537, 11.65000000001115588, -33.50000000000000000 ) ) ;
#34220=AXIS2_PLACEMENT_3D ( 'NONE', #152288, #250082, #96119 ) ;
#34223=DIRECTION ( 'NONE',  ( -0.000000000000000000, -0.000000000000000000, -1.000000000000000000 ) ) ;
#34231=CARTESIAN_POINT ( 'NONE',  ( 23.24999999999999289, 6.650000000011155876, -54.65000000000000568 ) ) ;
#34257=ORIENTED_EDGE ( 'NONE', *, *, #182313, .F. ) ;
#34267=ORIENTED_EDGE ( 'NONE', *, *, #69669, .T. ) ;
#34272=VECTOR ( 'NONE', #65004, 1000.000000000000000 ) ;
#34278=ORIENTED_EDGE ( 'NONE', *, *, #40806, .T. ) ;
#34333=EDGE_LOOP ( 'NONE', ( #175858, #161721, #28986, #66460 ) ) ;
#34343=DIRECTION ( 'NONE',  ( 0.000000000000000000, 0.9654727137038715545, -0.2605042016806676242 ) ) ;
#34398=DIRECTION ( 'NONE',  ( 0.000000000000000000, -0.8068669527896844551, -0.5907332058517525963 ) ) ;
#34405=VERTEX_POINT ( 'NONE', #21594 ) ;
#34409=AXIS2_PLACEMENT_3D ( 'NONE', #186499, #225585, #30011 ) ;
#34412=CIRCLE ( 'NONE', #230195, 12.87500000000000000 ) ;
#34435=ORIENTED_EDGE ( 'NONE', *, *, #191270, .F. ) ;
#34438=CARTESIAN_POINT ( 'NONE',  ( 20.94999999999999574, -11.48912529306490349, -36.60000000000000142 ) ) ;
#34447=DIRECTION ( 'NONE',  ( 1.000000000000000000, 0.000000000000000000, 0.000000000000000000 ) ) ;
#34496=CARTESIAN_POINT ( 'NONE',  ( 18.59999999999999076, 1.250000000011167511, -41.50000000000000000 ) ) ;
#34509=ORIENTED_EDGE ( 'NONE', *, *, #154940, .T. ) ;
#34524=CARTESIAN_POINT ( 'NONE',  ( -21.05000000000000071, -11.29603075032412463, -63.95210084033612929 ) ) ;
#34527=AXIS2_PLACEMENT_3D ( 'NONE', #145531, #47709, #225055 ) ;
#34534=FACE_OUTER_BOUND ( 'NONE', #98229, .T. ) ;
#34538=DIRECTION ( 'NONE',  ( 1.000000000000000000, 0.000000000000000000, 0.000000000000000000 ) ) ;
#34563=AXIS2_PLACEMENT_3D ( 'NONE', #87695, #185534, #85105 ) ;
#34573=ORIENTED_EDGE ( 'NONE', *, *, #146510, .T. ) ;
#34588=CARTESIAN_POINT ( 'NONE',  ( 21.05000000000000071, 10.72371710471867701, -41.16491356908760935 ) ) ;
#34609=LINE ( 'NONE', #35892, #184525 ) ;
#34618=CARTESIAN_POINT ( 'NONE',  ( 23.14999999999999147, 1.115600667400684642E-11, -33.50000000000000000 ) ) ;
#34621=CARTESIAN_POINT ( 'NONE',  ( 23.14999999999999503, 11.75000000001116263, -21.75000000000000355 ) ) ;
#34637=FACE_OUTER_BOUND ( 'NONE', #134484, .T. ) ;
#34644=CARTESIAN_POINT ( 'NONE',  ( -20.94999999999999929, -1.835341550213257733, -45.05515129256298223 ) ) ;
#34662=VECTOR ( 'NONE', #190252, 1000.000000000000000 ) ;
#34676=CARTESIAN_POINT ( 'NONE',  ( 21.05000000000000071, 8.926614585098253229, -41.97168301922312850 ) ) ;
#34729=EDGE_CURVE ( 'NONE', #96922, #203545, #221101, .T. ) ;
#34733=CARTESIAN_POINT ( 'NONE',  ( -20.94999999999999929, 1.115600667400684642E-11, -55.20000000000000284 ) ) ;
#34739=ORIENTED_EDGE ( 'NONE', *, *, #131679, .F. ) ;
#34797=TOROIDAL_SURFACE ( 'NONE', #151322, 0.9750000000000019762, 0.1000000000000000056 ) ;
#34821=CARTESIAN_POINT ( 'NONE',  ( 21.05000000000000071, 5.500000000011153745, -54.59473398108690390 ) ) ;
#34841=ORIENTED_EDGE ( 'NONE', *, *, #134740, .T. ) ;
#34844=CARTESIAN_POINT ( 'NONE',  ( -18.59999999999999787, 14.05000000001115623, -39.01369507076099552 ) ) ;
#34869=DIRECTION ( 'NONE',  ( 0.000000000000000000, -0.9893560106964500722, 0.1455152366551550613 ) ) ;
#34874=( NAMED_UNIT ( * ) PLANE_ANGLE_UNIT ( ) SI_UNIT ( $, .RADIAN. ) );
#34882=EDGE_CURVE ( 'NONE', #245137, #40042, #191003, .T. ) ;
#34883=DIRECTION ( 'NONE',  ( -0.000000000000000000, -1.000000000000000000, 6.308085367188393199E-16 ) ) ;
#34889=DIRECTION ( 'NONE',  ( 0.000000000000000000, 0.000000000000000000, 1.000000000000000000 ) ) ;
#34914=CARTESIAN_POINT ( 'NONE',  ( -23.15000000000000213, 1.910280373842930812, -54.36863214480106166 ) ) ;
#34956=VECTOR ( 'NONE', #201922, 999.9999999999998863 ) ;
#34965=EDGE_CURVE ( 'NONE', #14771, #61206, #194855, .T. ) ;
#34970=EDGE_CURVE ( 'NONE', #225834, #47428, #119152, .T. ) ;
#34974=( BOUNDED_SURFACE ( )  B_SPLINE_SURFACE ( 3, 2, ( 
 ( #49894, #66893, #72045 ),
 ( #52448, #132004, #186859 ),
 ( #248093, #147722, #208970 ),
 ( #90290, #9481, #10780 ),
 ( #168619, #27805, #189419 ),
 ( #206405, #249397, #169901 ),
 ( #211551, #32950, #108589 ),
 ( #31654, #130714, #29100 ) ),
 .UNSPECIFIED., .F., .F., .F. ) 
 B_SPLINE_SURFACE_WITH_KNOTS ( ( 4, 2, 2, 4 ),
 ( 3, 3 ),
 ( 0.0001704874539069835152, 0.0003809798300636603702, 0.0004862260181419988383, 0.0005914722062203372523 ),
 ( 0.000000000000000000, 1.000000000000000000 ),
 .UNSPECIFIED. ) 
 GEOMETRIC_REPRESENTATION_ITEM ( )  RATIONAL_B_SPLINE_SURFACE ( (
 ( 1.000000000000000000, 0.7071067811864942820, 1.000000000000000000),
 ( 1.000000000000000000, 0.7670648383578960727, 1.000000000000000000),
 ( 1.000000000000000000, 0.8204820770248829609, 1.000000000000000000),
 ( 1.000000000000000000, 0.8877218296115439999, 1.000000000000000000),
 ( 1.000000000000000000, 0.9080815932664635381, 1.000000000000000000),
 ( 1.000000000000000000, 0.9395541505862817777, 1.000000000000000000),
 ( 1.000000000000000000, 0.9506520335378265685, 1.000000000000000000),
 ( 1.000000000000000000, 0.9504532311154628710, 1.000000000000000000) ) ) 
 REPRESENTATION_ITEM ( '' )  SURFACE ( )  );
#35027=VERTEX_POINT ( 'NONE', #14925 ) ;
#35052=ORIENTED_EDGE ( 'NONE', *, *, #67735, .F. ) ;
#35056=EDGE_CURVE ( 'NONE', #129370, #146650, #196121, .T. ) ;
#35060=CARTESIAN_POINT ( 'NONE',  ( -21.17356465864818205, 6.422803126252873973, -33.40108875898613405 ) ) ;
#35082=ORIENTED_EDGE ( 'NONE', *, *, #110628, .T. ) ;
#35092=CYLINDRICAL_SURFACE ( 'NONE', #215759, 0.1000000000000006162 ) ;
#35121=VERTEX_POINT ( 'NONE', #179150 ) ;
#35124=CIRCLE ( 'NONE', #184927, 0.1999999999999987899 ) ;
#35180=DIRECTION ( 'NONE',  ( 0.000000000000000000, 0.000000000000000000, -1.000000000000000000 ) ) ;
#35188=ORIENTED_EDGE ( 'NONE', *, *, #160241, .F. ) ;
#35192=DIRECTION ( 'NONE',  ( 1.000000000000000000, 0.000000000000000000, 0.000000000000000000 ) ) ;
#35215=DIRECTION ( 'NONE',  ( 1.734723475976817507E-14, 0.000000000000000000, -1.000000000000000000 ) ) ;
#35221=CARTESIAN_POINT ( 'NONE',  ( -21.14999999999999858, 11.65000000001115232, -33.50000000000000000 ) ) ;
#35235=TOROIDAL_SURFACE ( 'NONE', #68513, 0.2000000000000000111, 0.1000000000000000056 ) ;
#35242=ORIENTED_EDGE ( 'NONE', *, *, #141732, .F. ) ;
#35256=VECTOR ( 'NONE', #134042, 1000.000000000000114 ) ;
#35272=AXIS2_PLACEMENT_3D ( 'NONE', #32443, #70281, #54531 ) ;
#35274=AXIS2_PLACEMENT_3D ( 'NONE', #101001, #180596, #75104 ) ;
#35293=DIRECTION ( 'NONE',  ( -0.7071067811865475727, -0.7071067811865475727, 0.000000000000000000 ) ) ;
#35330=DIRECTION ( 'NONE',  ( 1.000000000000000000, -0.000000000000000000, -0.000000000000000000 ) ) ;
#35344=FACE_OUTER_BOUND ( 'NONE', #1152, .T. ) ;
#35352=PLANE ( 'NONE',  #148294 ) ;
#35373=CARTESIAN_POINT ( 'NONE',  ( -22.32929514600008503, 0.09907567812507747651, -25.92135243462349692 ) ) ;
#35374=DIRECTION ( 'NONE',  ( -0.000000000000000000, 0.000000000000000000, 1.000000000000000000 ) ) ;
#35389=AXIS2_PLACEMENT_3D ( 'NONE', #169677, #189201, #66683 ) ;
#35412=CIRCLE ( 'NONE', #201981, 0.1000000000000002554 ) ;
#35429=ORIENTED_EDGE ( 'NONE', *, *, #127975, .T. ) ;
#35453=VERTEX_POINT ( 'NONE', #19761 ) ;
#35464=SPHERICAL_SURFACE ( 'NONE', #138221, 0.1000000000000000056 ) ;
#35493=DIRECTION ( 'NONE',  ( -1.000000000000000000, -0.000000000000000000, -0.000000000000000000 ) ) ;
#35504=CARTESIAN_POINT ( 'NONE',  ( -18.50000000000000000, 7.120270961708746960, -70.65956304183933412 ) ) ;
#35511=DIRECTION ( 'NONE',  ( 0.000000000000000000, 0.000000000000000000, -1.000000000000000000 ) ) ;
#35564=ADVANCED_FACE ( 'NONE', ( #127509 ), #238797, .T. ) ;
#35584=DIRECTION ( 'NONE',  ( -0.000000000000000000, 0.1350103645451876666, 0.9908441862701600211 ) ) ;
#35604=( GEOMETRIC_REPRESENTATION_CONTEXT ( 3 ) GLOBAL_UNCERTAINTY_ASSIGNED_CONTEXT ( ( #251122 ) ) GLOBAL_UNIT_ASSIGNED_CONTEXT ( ( #169260, #34874, #94809 ) ) REPRESENTATION_CONTEXT ( 'NONE', 'WORKASPACE' ) );
#35610=FACE_OUTER_BOUND ( 'NONE', #202536, .T. ) ;
#35617=ORIENTED_EDGE ( 'NONE', *, *, #229369, .T. ) ;
#35641=CARTESIAN_POINT ( 'NONE',  ( 23.24999999999999289, 11.65000000001116298, -59.98519422934606382 ) ) ;
#35644=ORIENTED_EDGE ( 'NONE', *, *, #161338, .F. ) ;
#35689=DIRECTION ( 'NONE',  ( -1.000000000000000000, -0.000000000000000000, -0.000000000000000000 ) ) ;
#35729=ORIENTED_EDGE ( 'NONE', *, *, #245653, .T. ) ;
#35752=AXIS2_PLACEMENT_3D ( 'NONE', #162575, #51239, #89104 ) ;
#35767=EDGE_CURVE ( 'NONE', #4740, #14640, #4104, .T. ) ;
#35785=AXIS2_PLACEMENT_3D ( 'NONE', #82813, #48858, #43728 ) ;
#35810=AXIS2_PLACEMENT_3D ( 'NONE', #222879, #238603, #44266 ) ;
#35831=VECTOR ( 'NONE', #220756, 1000.000000000000000 ) ;
#35843=CARTESIAN_POINT ( 'NONE',  ( -21.14999999999999858, -0.09999999998884338825, -21.85042919245520210 ) ) ;
#35881=VECTOR ( 'NONE', #184922, 1000.000000000000000 ) ;
#35892=CARTESIAN_POINT ( 'NONE',  ( 20.94999999999999929, -8.663551401857999323, -57.47589888193269303 ) ) ;
#35964=FACE_OUTER_BOUND ( 'NONE', #206554, .T. ) ;
#35988=DIRECTION ( 'NONE',  ( -1.000000000000000000, -0.000000000000000000, -0.000000000000000000 ) ) ;
#36040=ORIENTED_EDGE ( 'NONE', *, *, #22221, .F. ) ;
#36062=ADVANCED_FACE ( 'NONE', ( #227571 ), #9810, .T. ) ;
#36064=DIRECTION ( 'NONE',  ( 0.000000000000000000, -0.1350103645451904977, 0.9908441862701596881 ) ) ;
#36072=CARTESIAN_POINT ( 'NONE',  ( 20.95392731769792150, 8.883061479199918509, -42.02222797957130496 ) ) ;
#36100=ORIENTED_EDGE ( 'NONE', *, *, #141381, .T. ) ;
#36119=DIRECTION ( 'NONE',  ( 0.000000000000000000, 0.000000000000000000, -1.000000000000000000 ) ) ;
#36130=ORIENTED_EDGE ( 'NONE', *, *, #34882, .F. ) ;
#36137=LINE ( 'NONE', #79065, #185129 ) ;
#36139=EDGE_CURVE ( 'NONE', #43027, #230716, #87478, .T. ) ;
#36165=VERTEX_POINT ( 'NONE', #196150 ) ;
#36310=CIRCLE ( 'NONE', #157111, 0.09999999999999939493 ) ;
#36312=ORIENTED_EDGE ( 'NONE', *, *, #46602, .F. ) ;
#36327=CARTESIAN_POINT ( 'NONE',  ( 21.05000000000000071, 5.000000000011153745, -54.99473398108690958 ) ) ;
#36356=DIRECTION ( 'NONE',  ( -0.000000000000000000, 0.000000000000000000, 1.000000000000000000 ) ) ;
#36358=ORIENTED_EDGE ( 'NONE', *, *, #74980, .T. ) ;
#36388=CIRCLE ( 'NONE', #178034, 0.1999999999999987899 ) ;
#36391=ORIENTED_EDGE ( 'NONE', *, *, #74829, .F. ) ;
#36392=EDGE_LOOP ( 'NONE', ( #11784, #189946, #197623 ) ) ;
#36405=VERTEX_POINT ( 'NONE', #51172 ) ;
#36408=VERTEX_POINT ( 'NONE', #32976 ) ;
#36420=CARTESIAN_POINT ( 'NONE',  ( -20.64999999999999858, 4.350000000011156054, -54.64999999999999858 ) ) ;
#36472=AXIS2_PLACEMENT_3D ( 'NONE', #93057, #10965, #213008 ) ;
#36473=ORIENTED_EDGE ( 'NONE', *, *, #225442, .F. ) ;
#36493=DIRECTION ( 'NONE',  ( 0.000000000000000000, 0.000000000000000000, -1.000000000000000000 ) ) ;
#36497=CARTESIAN_POINT ( 'NONE',  ( -18.52139480978223318, -9.481358845055737561, -40.52455656711906329 ) ) ;
#36514=DIRECTION ( 'NONE',  ( 0.000000000000000000, 1.265107689135680095E-16, -1.000000000000000000 ) ) ;
#36517=CIRCLE ( 'NONE', #128629, 0.5000000000000004441 ) ;
#36522=CARTESIAN_POINT ( 'NONE',  ( 20.95052659398289308, 10.47982436779105875, -41.07523875586560536 ) ) ;
#36529=CARTESIAN_POINT ( 'NONE',  ( 21.03675099975491136, 8.875180032795963569, -45.82554213677805421 ) ) ;
#36537=CARTESIAN_POINT ( 'NONE',  ( -18.50000000000000000, 11.75000000001115197, -21.75000000000000355 ) ) ;
#36564=EDGE_LOOP ( 'NONE', ( #136153, #206172, #49780, #93433 ) ) ;
#36579=CARTESIAN_POINT ( 'NONE',  ( -18.59999999999999787, 9.350000000011156942, -45.85000000000000142 ) ) ;
#36585=CARTESIAN_POINT ( 'NONE',  ( 23.24999999999999645, 5.600000000011153389, -54.59473398108690390 ) ) ;
#36593=EDGE_LOOP ( 'NONE', ( #178185, #176724 ) ) ;
#36623=DIRECTION ( 'NONE',  ( 0.000000000000000000, 0.000000000000000000, -1.000000000000000000 ) ) ;
#36626=ORIENTED_EDGE ( 'NONE', *, *, #166485, .T. ) ;
#36652=VERTEX_POINT ( 'NONE', #173781 ) ;
#36656=CARTESIAN_POINT ( 'NONE',  ( -21.07928932188134041, 0.09889514566555068775, -27.17148334360670958 ) ) ;
#36691=EDGE_CURVE ( 'NONE', #197787, #183680, #1494, .T. ) ;
#36768=EDGE_CURVE ( 'NONE', #55828, #66671, #41344, .T. ) ;
#36769=DIRECTION ( 'NONE',  ( 0.000000000000000000, 0.000000000000000000, -1.000000000000000000 ) ) ;
#36792=DIRECTION ( 'NONE',  ( 1.000000000000000000, 0.000000000000000000, 0.000000000000000000 ) ) ;
#36797=DIRECTION ( 'NONE',  ( 0.000000000000000000, 0.000000000000000000, -1.000000000000000000 ) ) ;
#36802=ORIENTED_EDGE ( 'NONE', *, *, #67398, .T. ) ;
#36804=AXIS2_PLACEMENT_3D ( 'NONE', #76988, #156570, #217764 ) ;
#36816=EDGE_CURVE ( 'NONE', #135854, #35027, #249789, .T. ) ;
#36838=ORIENTED_EDGE ( 'NONE', *, *, #36768, .F. ) ;
#36845=CARTESIAN_POINT ( 'NONE',  ( -18.50000000000000000, 9.350000000011156942, -45.65000000000000568 ) ) ;
#36849=DIRECTION ( 'NONE',  ( 1.000000000000000000, 3.265361837132813093E-16, -0.000000000000000000 ) ) ;
#36868=AXIS2_PLACEMENT_3D ( 'NONE', #103229, #27604, #184066 ) ;
#36907=FACE_OUTER_BOUND ( 'NONE', #128744, .T. ) ;
#36910=VERTEX_POINT ( 'NONE', #14377 ) ;
#36911=CIRCLE ( 'NONE', #144996, 0.1000000000000016709 ) ;
#36926=FACE_OUTER_BOUND ( 'NONE', #84054, .T. ) ;
#36929=ORIENTED_EDGE ( 'NONE', *, *, #199095, .F. ) ;
#36939=ORIENTED_EDGE ( 'NONE', *, *, #69746, .T. ) ;
#36973=DIRECTION ( 'NONE',  ( 1.000000000000000000, 0.000000000000000000, 0.000000000000000000 ) ) ;
#36974=CARTESIAN_POINT ( 'NONE',  ( 21.05000000000000071, 6.304516329275108077, -33.52110330805914629 ) ) ;
#36978=CARTESIAN_POINT ( 'NONE',  ( -18.59999999999999787, 11.75000000001115197, -21.75000000000000355 ) ) ;
#36983=DIRECTION ( 'NONE',  ( 0.000000000000000000, 0.000000000000000000, -1.000000000000000000 ) ) ;
#36994=ORIENTED_EDGE ( 'NONE', *, *, #173324, .T. ) ;
#37000=CARTESIAN_POINT ( 'NONE',  ( 20.99999999999997868, 1.115600667400684642E-11, -33.50000000000000000 ) ) ;
#37021=EDGE_CURVE ( 'NONE', #9718, #80932, #245517, .T. ) ;
#37024=DIRECTION ( 'NONE',  ( -1.000000000000000000, -7.304098846218134667E-16, 0.000000000000000000 ) ) ;
#37033=ORIENTED_EDGE ( 'NONE', *, *, #145546, .F. ) ;
#37078=AXIS2_PLACEMENT_3D ( 'NONE', #62521, #221562, #45520 ) ;
#37106=ADVANCED_FACE ( 'NONE', ( #122441 ), #138122, .T. ) ;
#37119=CYLINDRICAL_SURFACE ( 'NONE', #202632, 0.1000000000000028644 ) ;
#37123=VECTOR ( 'NONE', #47383, 1000.000000000000000 ) ;
#37161=CYLINDRICAL_SURFACE ( 'NONE', #148377, 0.09999999999999781286 ) ;
#37166=ADVANCED_FACE ( 'NONE', ( #183700 ), #62467, .T. ) ;
#37208=FACE_OUTER_BOUND ( 'NONE', #28939, .T. ) ;
#37277=ADVANCED_FACE ( 'NONE', ( #166728 ), #37606, .T. ) ;
#37329=EDGE_CURVE ( 'NONE', #9718, #187977, #120821, .T. ) ;
#37337=CARTESIAN_POINT ( 'NONE',  ( 18.57071067811864040, 10.17928932189250091, -54.85000000000000142 ) ) ;
#37343=CIRCLE ( 'NONE', #53907, 0.1000000000000028644 ) ;
#37347=FACE_OUTER_BOUND ( 'NONE', #93393, .T. ) ;
#37389=CARTESIAN_POINT ( 'NONE',  ( -21.44999999999999929, 7.350000000011155166, -54.75000000000000000 ) ) ;
#37401=FACE_OUTER_BOUND ( 'NONE', #231220, .T. ) ;
#37421=ORIENTED_EDGE ( 'NONE', *, *, #254499, .T. ) ;
#37433=ORIENTED_EDGE ( 'NONE', *, *, #96368, .F. ) ;
#37469=FACE_OUTER_BOUND ( 'NONE', #51061, .T. ) ;
#37488=CIRCLE ( 'NONE', #183218, 0.09999999999999943656 ) ;
#37502=EDGE_CURVE ( 'NONE', #83073, #131237, #104208, .T. ) ;
#37508=CIRCLE ( 'NONE', #212298, 0.1000000000000028644 ) ;
#37531=DIRECTION ( 'NONE',  ( -1.000000000000000000, -0.000000000000000000, -0.000000000000000000 ) ) ;
#37562=DIRECTION ( 'NONE',  ( 0.000000000000000000, 0.000000000000000000, -1.000000000000000000 ) ) ;
#37567=CARTESIAN_POINT ( 'NONE',  ( -18.50000000000000000, -9.399999999988850163, -40.79725975966329088 ) ) ;
#37578=EDGE_CURVE ( 'NONE', #120355, #14005, #210442, .T. ) ;
#37602=DIRECTION ( 'NONE',  ( 1.000000000000000000, -0.000000000000000000, -0.000000000000000000 ) ) ;
#37606=TOROIDAL_SURFACE ( 'NONE', #195834, 0.2000000000000000111, 0.1000000000000000056 ) ;
#37607=CARTESIAN_POINT ( 'NONE',  ( 18.59999999999999076, 1.835341550235567887, -45.05515129256298223 ) ) ;
#37614=FACE_OUTER_BOUND ( 'NONE', #131182, .T. ) ;
#37621=FACE_OUTER_BOUND ( 'NONE', #113662, .T. ) ;
#37633=LINE ( 'NONE', #157605, #168567 ) ;
#37634=VECTOR ( 'NONE', #215017, 1000.000000000000000 ) ;
#37644=EDGE_CURVE ( 'NONE', #82553, #253318, #37798, .T. ) ;
#37660=ADVANCED_FACE ( 'NONE', ( #132072 ), #208486, .T. ) ;
#37661=ORIENTED_EDGE ( 'NONE', *, *, #83808, .T. ) ;
#37666=ORIENTED_EDGE ( 'NONE', *, *, #207799, .F. ) ;
#37680=VECTOR ( 'NONE', #39016, 1000.000000000000000 ) ;
#37709=ORIENTED_EDGE ( 'NONE', *, *, #248273, .T. ) ;
#37723=VECTOR ( 'NONE', #188591, 1000.000000000000000 ) ;
#37760=ORIENTED_EDGE ( 'NONE', *, *, #225671, .T. ) ;
#37773=CARTESIAN_POINT ( 'NONE',  ( -21.03571358705787020, 11.75000000001115197, -40.32510682205884933 ) ) ;
#37796=CARTESIAN_POINT ( 'NONE',  ( -20.85000000000000142, -1.835859311432481045, -78.50443916879852679 ) ) ;
#37798=CIRCLE ( 'NONE', #129346, 0.09999999999999939493 ) ;
#37800=EDGE_CURVE ( 'NONE', #126560, #216334, #235031, .T. ) ;
#37801=CARTESIAN_POINT ( 'NONE',  ( -20.85000000000000142, -1.164121893230052995, -74.91484808557160591 ) ) ;
#37856=EDGE_CURVE ( 'NONE', #138330, #226447, #116871, .T. ) ;
#37926=DIRECTION ( 'NONE',  ( 0.000000000000000000, 0.5000000000000144329, 0.8660254037844302699 ) ) ;
#37929=CARTESIAN_POINT ( 'NONE',  ( -22.39999999999999858, 7.790779598384560245, -33.50000000000000000 ) ) ;
#37972=ORIENTED_EDGE ( 'NONE', *, *, #147360, .F. ) ;
#38057=VERTEX_POINT ( 'NONE', #200574 ) ;
#38100=CARTESIAN_POINT ( 'NONE',  ( 20.94999999999999929, 8.876614585098254295, -41.88508047884467800 ) ) ;
#38118=CARTESIAN_POINT ( 'NONE',  ( -21.14999999999999858, 11.75000000001115552, -40.28386566297815108 ) ) ;
#38142=VECTOR ( 'NONE', #130231, 1000.000000000000114 ) ;
#38144=FACE_OUTER_BOUND ( 'NONE', #248839, .T. ) ;
#38187=FACE_OUTER_BOUND ( 'NONE', #17039, .T. ) ;
#38191=TOROIDAL_SURFACE ( 'NONE', #171474, 11.65000000000000036, 0.1000000000000000056 ) ;
#38197=DIRECTION ( 'NONE',  ( 1.000000000000000000, 0.000000000000000000, 0.000000000000000000 ) ) ;
#38201=DIRECTION ( 'NONE',  ( 0.000000000000000000, -0.5000000000000078826, 0.8660254037844340447 ) ) ;
#38222=AXIS2_PLACEMENT_3D ( 'NONE', #38100, #117619, #197144 ) ;
#38284=EDGE_LOOP ( 'NONE', ( #235790, #165673, #98591, #225878 ) ) ;
#38286=ORIENTED_EDGE ( 'NONE', *, *, #2706, .F. ) ;
#38326=LINE ( 'NONE', #136094, #163734 ) ;
#38330=DIRECTION ( 'NONE',  ( 1.000000000000000000, 0.000000000000000000, 0.000000000000000000 ) ) ;
#38371=EDGE_CURVE ( 'NONE', #200872, #250359, #96840, .T. ) ;
#38373=CYLINDRICAL_SURFACE ( 'NONE', #145552, 0.09999999999999939493 ) ;
#38422=ORIENTED_EDGE ( 'NONE', *, *, #3560, .F. ) ;
#38426=EDGE_CURVE ( 'NONE', #96705, #200797, #51537, .T. ) ;
#38446=FACE_OUTER_BOUND ( 'NONE', #110211, .T. ) ;
#38463=ADVANCED_FACE ( 'NONE', ( #209358 ), #129820, .F. ) ;
#38468=EDGE_CURVE ( 'NONE', #224599, #140260, #84335, .T. ) ;
#38472=EDGE_CURVE ( 'NONE', #61003, #68228, #230135, .T. ) ;
#38482=CARTESIAN_POINT ( 'NONE',  ( -21.05000000000000071, 0.05132743235267277215, -27.19981666373291773 ) ) ;
#38501=CIRCLE ( 'NONE', #46849, 0.5999999999999998668 ) ;
#38518=CIRCLE ( 'NONE', #171830, 12.87499999999999822 ) ;
#38529=CARTESIAN_POINT ( 'NONE',  ( 20.94999999999999929, 1.115624548013267999E-11, -65.10000000000000853 ) ) ;
#38562=EDGE_LOOP ( 'NONE', ( #138606, #51692, #163599, #62692 ) ) ;
#38605=ADVANCED_FACE ( 'NONE', ( #215765 ), #21860, .F. ) ;
#38648=CIRCLE ( 'NONE', #84377, 0.1000000000000028644 ) ;
#38678=CARTESIAN_POINT ( 'NONE',  ( -20.54999999999999716, -8.999999999988846255, -43.39396912265245021 ) ) ;
#38681=DIRECTION ( 'NONE',  ( 0.000000000000000000, 4.440892098500631684E-15, -1.000000000000000000 ) ) ;
#38683=CIRCLE ( 'NONE', #30318, 0.1000000000000028644 ) ;
#38687=CIRCLE ( 'NONE', #184420, 0.1000000000000028644 ) ;
#38691=ORIENTED_EDGE ( 'NONE', *, *, #204426, .F. ) ;
#38701=PRESENTATION_STYLE_ASSIGNMENT (( #197761 ) ) ;
#38720=DIRECTION ( 'NONE',  ( 1.000000000000000000, 0.000000000000000000, 0.000000000000000000 ) ) ;
#38726=DIRECTION ( 'NONE',  ( 0.000000000000000000, -1.000000000000000000, 0.000000000000000000 ) ) ;
#38734=CARTESIAN_POINT ( 'NONE',  ( -23.25000000000000000, 6.982009704867601307, -70.69615211825629331 ) ) ;
#38762=FACE_OUTER_BOUND ( 'NONE', #38856, .T. ) ;
#38801=FACE_OUTER_BOUND ( 'NONE', #52399, .T. ) ;
#38818=CARTESIAN_POINT ( 'NONE',  ( 20.11144452914042091, 9.933610851134151432, -41.39029345395471893 ) ) ;
#38838=EDGE_CURVE ( 'NONE', #231120, #175831, #92944, .T. ) ;
#38849=CARTESIAN_POINT ( 'NONE',  ( -18.45037301276669339, -9.490200447530787287, -40.51267413641429727 ) ) ;
#38856=EDGE_LOOP ( 'NONE', ( #88927, #53878, #118832 ) ) ;
#38887=CARTESIAN_POINT ( 'NONE',  ( 20.94999999999999929, 1.115600667400684642E-11, -67.00000000000000000 ) ) ;
#38896=ORIENTED_EDGE ( 'NONE', *, *, #83781, .T. ) ;
#38917=CARTESIAN_POINT ( 'NONE',  ( 20.85000000000000142, -1.835859311432481045, -78.50443916879852679 ) ) ;
#38958=AXIS2_PLACEMENT_3D ( 'NONE', #124040, #101868, #219263 ) ;
#38982=VERTEX_POINT ( 'NONE', #215475 ) ;
#38984=DIRECTION ( 'NONE',  ( 0.000000000000000000, 1.000000000000000000, 0.000000000000000000 ) ) ;
#38990=DIRECTION ( 'NONE',  ( 1.000000000000000000, -0.000000000000000000, 0.000000000000000000 ) ) ;
#39016=DIRECTION ( 'NONE',  ( 6.938893903907224433E-15, -1.000000000000000000, -2.891205793294679805E-16 ) ) ;
#39049=CARTESIAN_POINT ( 'NONE',  ( -23.15000000000000213, -11.64999999998884483, -63.89999999999999858 ) ) ;
#39056=FACE_OUTER_BOUND ( 'NONE', #135533, .T. ) ;
#39078=CARTESIAN_POINT ( 'NONE',  ( 20.95203847575071521, 10.50106053928516303, -41.06707134862356412 ) ) ;
#39081=DIRECTION ( 'NONE',  ( -1.000000000000000000, 0.000000000000000000, 0.000000000000000000 ) ) ;
#39092=CIRCLE ( 'NONE', #184805, 12.87499999999999822 ) ;
#39097=FACE_OUTER_BOUND ( 'NONE', #142826, .T. ) ;
#39104=ORIENTED_EDGE ( 'NONE', *, *, #13164, .F. ) ;
#39115=EDGE_CURVE ( 'NONE', #94226, #84007, #234797, .T. ) ;
#39127=DIRECTION ( 'NONE',  ( 1.000000000000000000, -0.000000000000000000, -0.000000000000000000 ) ) ;
#39138=CARTESIAN_POINT ( 'NONE',  ( 20.94999999999999929, 1.115600667400684642E-11, -67.00000000000000000 ) ) ;
#39144=ORIENTED_EDGE ( 'NONE', *, *, #81410, .F. ) ;
#39168=DIRECTION ( 'NONE',  ( -1.000000000000000000, 0.000000000000000000, -0.000000000000000000 ) ) ;
#39181=CARTESIAN_POINT ( 'NONE',  ( -21.07094088545368749, 0.09889370256337755294, -27.17983277808286857 ) ) ;
#39216=CARTESIAN_POINT ( 'NONE',  ( -21.51976009735018991, 6.910458441670358276, -33.50000000000000000 ) ) ;
#39227=AXIS2_PLACEMENT_3D ( 'NONE', #47968, #104073, #6266 ) ;
#39243=EDGE_LOOP ( 'NONE', ( #119869, #40535, #68603, #90090 ) ) ;
#39284=DIRECTION ( 'NONE',  ( 0.000000000000000000, -1.000000000000000000, 0.000000000000000000 ) ) ;
#39308=ORIENTED_EDGE ( 'NONE', *, *, #136590, .T. ) ;
#39314=AXIS2_PLACEMENT_3D ( 'NONE', #187328, #246006, #248561 ) ;
#39388=DIRECTION ( 'NONE',  ( -1.000000000000000000, -0.000000000000000000, -0.000000000000000000 ) ) ;
#39398=VECTOR ( 'NONE', #87288, 1000.000000000000000 ) ;
#39432=VECTOR ( 'NONE', #51245, 1000.000000000000000 ) ;
#39457=SPHERICAL_SURFACE ( 'NONE', #53481, 0.1000000000000000056 ) ;
#39479=EDGE_CURVE ( 'NONE', #3284, #116043, #16993, .T. ) ;
#39489=DIRECTION ( 'NONE',  ( -1.000000000000000000, -1.836970198721029934E-16, 0.000000000000000000 ) ) ;
#39506=DIRECTION ( 'NONE',  ( 0.000000000000000000, 0.9908441862701596881, -0.1350103645451904977 ) ) ;
#39510=VERTEX_POINT ( 'NONE', #5079 ) ;
#39535=CARTESIAN_POINT ( 'NONE',  ( -21.05000000000000071, -11.39257802169451672, -36.57394957983193251 ) ) ;
#39579=EDGE_LOOP ( 'NONE', ( #100467, #210871, #40036, #255029 ) ) ;
#39615=ORIENTED_EDGE ( 'NONE', *, *, #165592, .F. ) ;
#39645=DIRECTION ( 'NONE',  ( 1.000000000000000000, -0.000000000000000000, -0.000000000000000000 ) ) ;
#39658=DIRECTION ( 'NONE',  ( 1.000000000000000000, 0.000000000000000000, -0.000000000000000000 ) ) ;
#39662=AXIS2_PLACEMENT_3D ( 'NONE', #156009, #78978, #98526 ) ;
#39670=DIRECTION ( 'NONE',  ( 1.836970198721029934E-16, -1.000000000000000000, -0.000000000000000000 ) ) ;
#39673=CYLINDRICAL_SURFACE ( 'NONE', #58328, 0.1000000000000028644 ) ;
#39701=EDGE_LOOP ( 'NONE', ( #101210, #77159, #200581, #244767, #187786 ) ) ;
#39705=DIRECTION ( 'NONE',  ( 0.000000000000000000, 0.008583690987124399305, -0.9999631594459055250 ) ) ;
#39731=VECTOR ( 'NONE', #171275, 1000.000000000000000 ) ;
#39749=CARTESIAN_POINT ( 'NONE',  ( 18.49999999999999645, -1.866714910046153308, -45.25267524628200988 ) ) ;
#39755=FACE_OUTER_BOUND ( 'NONE', #119806, .T. ) ;
#39764=CARTESIAN_POINT ( 'NONE',  ( -18.50000000000000000, 9.150000000011157653, -54.65000000000000568 ) ) ;
#39796=CARTESIAN_POINT ( 'NONE',  ( -21.07954763557430056, 0.06587591862962487166, -27.17070900996239047 ) ) ;
#39833=CARTESIAN_POINT ( 'NONE',  ( 23.25000000000000000, -11.74999999998883560, -21.75000000000000355 ) ) ;
#39876=CARTESIAN_POINT ( 'NONE',  ( -18.59999999999999787, 7.021664781911246322, -70.83356540189728889 ) ) ;
#39888=CIRCLE ( 'NONE', #185613, 0.09999999999999939493 ) ;
#39900=CARTESIAN_POINT ( 'NONE',  ( 18.59999999999999432, -1.299733671219632791, -23.52812952286940273 ) ) ;
#39957=VERTEX_POINT ( 'NONE', #29228 ) ;
#39970=CARTESIAN_POINT ( 'NONE',  ( -21.05000000000000071, 1.115600667400684642E-11, -37.79999999999996163 ) ) ;
#39972=CIRCLE ( 'NONE', #185704, 0.1000000000000028644 ) ;
#39980=DIRECTION ( 'NONE',  ( 0.000000000000000000, 0.000000000000000000, 1.000000000000000000 ) ) ;
#40005=ORIENTED_EDGE ( 'NONE', *, *, #241089, .F. ) ;
#40009=ADVANCED_FACE ( 'NONE', ( #7043 ), #86554, .F. ) ;
#40036=ORIENTED_EDGE ( 'NONE', *, *, #139850, .F. ) ;
#40042=VERTEX_POINT ( 'NONE', #35641 ) ;
#40074=AXIS2_PLACEMENT_3D ( 'NONE', #197484, #138765, #98347 ) ;
#40082=DIRECTION ( 'NONE',  ( -1.000000000000000000, 0.000000000000000000, 0.000000000000000000 ) ) ;
#40104=ADVANCED_FACE ( 'NONE', ( #36926 ), #140666, .F. ) ;
#40123=CARTESIAN_POINT ( 'NONE',  ( 20.30466543256828160, 9.304236939266303352, -41.75366265139219024 ) ) ;
#40137=SPHERICAL_SURFACE ( 'NONE', #73054, 0.1000000000000000056 ) ;
#40141=DIRECTION ( 'NONE',  ( -1.000000000000000000, -0.000000000000000000, -0.000000000000000000 ) ) ;
#40183=DIRECTION ( 'NONE',  ( -1.000000000000000000, 0.000000000000000000, 0.000000000000000000 ) ) ;
#40221=ADVANCED_FACE ( 'NONE', ( #160722 ), #237660, .T. ) ;
#40223=CARTESIAN_POINT ( 'NONE',  ( -21.05000000000000071, 1.835341550235567887, -45.05515129256298223 ) ) ;
#40225=FACE_OUTER_BOUND ( 'NONE', #10993, .T. ) ;
#40235=ORIENTED_EDGE ( 'NONE', *, *, #99413, .T. ) ;
#40239=DIRECTION ( 'NONE',  ( -1.000000000000000000, 0.000000000000000000, 0.000000000000000000 ) ) ;
#40271=CIRCLE ( 'NONE', #173567, 12.97499999999999964 ) ;
#40277=EDGE_CURVE ( 'NONE', #15545, #147029, #6742, .T. ) ;
#40340=CARTESIAN_POINT ( 'NONE',  ( 20.85000000000000142, 11.75000000001115907, -67.00000000000000000 ) ) ;
#40357=CARTESIAN_POINT ( 'NONE',  ( -20.64999999999999858, -8.999999999988844479, -57.10603087734755690 ) ) ;
#40358=EDGE_LOOP ( 'NONE', ( #98339, #48148, #166881, #114940, #159191 ) ) ;
#40373=DIRECTION ( 'NONE',  ( -1.000000000000000000, -0.000000000000000000, -0.000000000000000000 ) ) ;
#40393=CIRCLE ( 'NONE', #144361, 0.1000000000000028644 ) ;
#40400=EDGE_LOOP ( 'NONE', ( #210496, #21191, #193928, #215997 ) ) ;
#40441=CYLINDRICAL_SURFACE ( 'NONE', #56594, 0.1000000000000028644 ) ;
#40471=ORIENTED_EDGE ( 'NONE', *, *, #2706, .T. ) ;
#40487=EDGE_LOOP ( 'NONE', ( #105220, #128449, #27816, #161491 ) ) ;
#40490=CARTESIAN_POINT ( 'NONE',  ( 20.94999999999999929, 6.450000000011156587, -43.51702717044002355 ) ) ;
#40496=DIRECTION ( 'NONE',  ( 0.000000000000000000, 0.9915357197604792727, -0.1298341882520473722 ) ) ;
#40503=FACE_OUTER_BOUND ( 'NONE', #188985, .T. ) ;
#40521=EDGE_LOOP ( 'NONE', ( #77756, #160034, #83489, #191312, #162061, #170126 ) ) ;
#40535=ORIENTED_EDGE ( 'NONE', *, *, #54712, .T. ) ;
#40537=PRODUCT_DEFINITION ( 'UNKNOWN', '', #248677, #199189 ) ;
#40541=VERTEX_POINT ( 'NONE', #43008 ) ;
#40550=VERTEX_POINT ( 'NONE', #122552 ) ;
#40600=ORIENTED_EDGE ( 'NONE', *, *, #229178, .F. ) ;
#40627=CARTESIAN_POINT ( 'NONE',  ( -20.64999999999999858, 7.250000000011155521, -54.65000000000000568 ) ) ;
#40631=FACE_OUTER_BOUND ( 'NONE', #29424, .T. ) ;
#40635=DIRECTION ( 'NONE',  ( 0.000000000000000000, 0.9998779222360102414, 0.01562499999996356907 ) ) ;
#40647=ORIENTED_EDGE ( 'NONE', *, *, #115299, .T. ) ;
#40679=LINE ( 'NONE', #156760, #20725 ) ;
#40724=DIRECTION ( 'NONE',  ( -0.000000000000000000, -0.000000000000000000, -1.000000000000000000 ) ) ;
#40730=AXIS2_PLACEMENT_3D ( 'NONE', #175730, #255177, #119602 ) ;
#40779=DIRECTION ( 'NONE',  ( 0.000000000000000000, 1.000000000000000000, -0.000000000000000000 ) ) ;
#40782=DIRECTION ( 'NONE',  ( 0.000000000000000000, 0.000000000000000000, 1.000000000000000000 ) ) ;
#40792=AXIS2_PLACEMENT_3D ( 'NONE', #13546, #134742, #53941 ) ;
#40806=EDGE_CURVE ( 'NONE', #191837, #103845, #246336, .T. ) ;
#40832=FACE_OUTER_BOUND ( 'NONE', #126165, .T. ) ;
#40845=LINE ( 'NONE', #78637, #27117 ) ;
#40860=ORIENTED_EDGE ( 'NONE', *, *, #160629, .F. ) ;
#40897=DIRECTION ( 'NONE',  ( 0.000000000000000000, 0.000000000000000000, -1.000000000000000000 ) ) ;
#40919=FACE_OUTER_BOUND ( 'NONE', #110525, .T. ) ;
#40922=AXIS2_PLACEMENT_3D ( 'NONE', #145218, #103516, #147811 ) ;
#40930=EDGE_CURVE ( 'NONE', #156961, #127685, #240993, .T. ) ;
#40934=FACE_OUTER_BOUND ( 'NONE', #17914, .T. ) ;
#40938=DIRECTION ( 'NONE',  ( 0.000000000000000000, 0.000000000000000000, -1.000000000000000000 ) ) ;
#40942=AXIS2_PLACEMENT_3D ( 'NONE', #242345, #225330, #121157 ) ;
#40955=CARTESIAN_POINT ( 'NONE',  ( 20.94999999999999574, -11.74999999998883560, -36.39999999999999858 ) ) ;
#41013=CARTESIAN_POINT ( 'NONE',  ( -22.39999999999999858, 1.115488181425289271E-11, -21.85042919245520210 ) ) ;
#41033=ORIENTED_EDGE ( 'NONE', *, *, #143030, .T. ) ;
#41101=VECTOR ( 'NONE', #175984, 1000.000000000000000 ) ;
#41114=DIRECTION ( 'NONE',  ( 0.000000000000000000, -1.734723475983068283E-15, 1.000000000000000000 ) ) ;
#41120=DIRECTION ( 'NONE',  ( 0.000000000000000000, -1.000000000000000000, 0.000000000000000000 ) ) ;
#41129=DIRECTION ( 'NONE',  ( 0.000000000000000000, -1.000000000000000000, -1.897661533703519897E-16 ) ) ;
#41139=ORIENTED_EDGE ( 'NONE', *, *, #33133, .F. ) ;
#41146=DIRECTION ( 'NONE',  ( -1.000000000000000000, 0.000000000000000000, 0.000000000000000000 ) ) ;
#41154=CARTESIAN_POINT ( 'NONE',  ( 20.94999999999999574, 1.250000000011155299, -41.50000000000000000 ) ) ;
#41159=DIRECTION ( 'NONE',  ( -1.000000000000000000, 0.000000000000000000, 0.000000000000000000 ) ) ;
#41163=AXIS2_PLACEMENT_3D ( 'NONE', #170690, #188919, #248903 ) ;
#41165=ORIENTED_EDGE ( 'NONE', *, *, #37502, .F. ) ;
#41218=ORIENTED_EDGE ( 'NONE', *, *, #166895, .T. ) ;
#41232=EDGE_CURVE ( 'NONE', #134638, #72318, #124655, .T. ) ;
#41243=VERTEX_POINT ( 'NONE', #92075 ) ;
#41246=EDGE_CURVE ( 'NONE', #12448, #201039, #213301, .T. ) ;
#41271=CARTESIAN_POINT ( 'NONE',  ( -20.94999999999999929, 11.65000000001115232, -67.00000000000000000 ) ) ;
#41277=DIRECTION ( 'NONE',  ( 0.000000000000000000, 1.000000000000000000, 0.000000000000000000 ) ) ;
#41293=CARTESIAN_POINT ( 'NONE',  ( 22.39999999999999503, -0.09999999998884338825, -21.85042919245520210 ) ) ;
#41325=CIRCLE ( 'NONE', #162119, 0.1000000000000028644 ) ;
#41337=AXIS2_PLACEMENT_3D ( 'NONE', #218063, #199830, #39489 ) ;
#41344=CIRCLE ( 'NONE', #16577, 12.97499999999999964 ) ;
#41387=DIRECTION ( 'NONE',  ( 1.000000000000000000, 0.000000000000000000, 0.000000000000000000 ) ) ;
#41393=ORIENTED_EDGE ( 'NONE', *, *, #250932, .T. ) ;
#41415=CARTESIAN_POINT ( 'NONE',  ( -21.14999999999999858, 1.115600667400684642E-11, -33.50000000000000000 ) ) ;
#41423=CARTESIAN_POINT ( 'NONE',  ( -18.46093223321773280, -9.480682968263375088, -40.58455051392668622 ) ) ;
#41505=EDGE_CURVE ( 'NONE', #43099, #146650, #62287, .T. ) ;
#41569=ORIENTED_EDGE ( 'NONE', *, *, #51428, .F. ) ;
#41571=AXIS2_PLACEMENT_3D ( 'NONE', #114559, #216205, #179674 ) ;
#41608=LINE ( 'NONE', #121154, #42666 ) ;
#41662=DIRECTION ( 'NONE',  ( 1.000000000000000000, 0.000000000000000000, -0.000000000000000000 ) ) ;
#41675=VECTOR ( 'NONE', #138857, 1000.000000000000000 ) ;
#41678=AXIS2_PLACEMENT_3D ( 'NONE', #39049, #35215, #114714 ) ;
#41711=DIRECTION ( 'NONE',  ( 0.000000000000000000, 0.000000000000000000, 1.000000000000000000 ) ) ;
#41712=CIRCLE ( 'NONE', #179101, 4.099999999999992539 ) ;
#41748=ORIENTED_EDGE ( 'NONE', *, *, #225442, .T. ) ;
#41761=DIRECTION ( 'NONE',  ( 1.000000000000000000, -0.000000000000000000, -0.000000000000000000 ) ) ;
#41782=CIRCLE ( 'NONE', #204055, 0.1000000000000028644 ) ;
#41789=CIRCLE ( 'NONE', #91825, 7.900000000000003908 ) ;
#41819=CIRCLE ( 'NONE', #195932, 4.300000000000032685 ) ;
#41833=ADVANCED_FACE ( 'NONE', ( #55840 ), #72907, .F. ) ;
#41850=CYLINDRICAL_SURFACE ( 'NONE', #217504, 0.09999999999999939493 ) ;
#41856=ORIENTED_EDGE ( 'NONE', *, *, #15416, .F. ) ;
#41896=CARTESIAN_POINT ( 'NONE',  ( -23.25000000000000000, -8.596261682231835621, -42.95012751715027832 ) ) ;
#41950=VERTEX_POINT ( 'NONE', #53085 ) ;
#41986=VERTEX_POINT ( 'NONE', #54368 ) ;
#42004=DIRECTION ( 'NONE',  ( 1.000000000000000000, 0.000000000000000000, 0.000000000000000000 ) ) ;
#42006=DIRECTION ( 'NONE',  ( 0.000000000000000000, -1.000000000000000000, 0.000000000000000000 ) ) ;
#42023=DIRECTION ( 'NONE',  ( 0.000000000000000000, 0.000000000000000000, -1.000000000000000000 ) ) ;
#42026=EDGE_CURVE ( 'NONE', #197787, #7520, #154298, .T. ) ;
#42041=ORIENTED_EDGE ( 'NONE', *, *, #239190, .T. ) ;
#42048=FACE_OUTER_BOUND ( 'NONE', #172501, .T. ) ;
#42067=EDGE_CURVE ( 'NONE', #2443, #128224, #33577, .T. ) ;
#42085=AXIS2_PLACEMENT_3D ( 'NONE', #90154, #171053, #71914 ) ;
#42092=CARTESIAN_POINT ( 'NONE',  ( -20.94999999999999929, -11.29603075032412995, -36.54789915966387071 ) ) ;
#42106=ORIENTED_EDGE ( 'NONE', *, *, #110975, .F. ) ;
#42107=DIRECTION ( 'NONE',  ( -1.000000000000000000, 0.000000000000000000, 0.000000000000000000 ) ) ;
#42143=ORIENTED_EDGE ( 'NONE', *, *, #64497, .T. ) ;
#42145=DIRECTION ( 'NONE',  ( 1.000000000000000000, -0.000000000000000000, -0.000000000000000000 ) ) ;
#42156=VERTEX_POINT ( 'NONE', #102445 ) ;
#42170=AXIS2_PLACEMENT_3D ( 'NONE', #124190, #147588, #162038 ) ;
#42172=TOROIDAL_SURFACE ( 'NONE', #187915, 2.100000000000002309, 0.1000000000000000056 ) ;
#42177=ADVANCED_FACE ( 'NONE', ( #127189 ), #125885, .F. ) ;
#42192=DIRECTION ( 'NONE',  ( 0.000000000000000000, 0.000000000000000000, -1.000000000000000000 ) ) ;
#42333=EDGE_CURVE ( 'NONE', #100083, #254522, #245273, .T. ) ;
#42334=ORIENTED_EDGE ( 'NONE', *, *, #175684, .F. ) ;
#42379=CARTESIAN_POINT ( 'NONE',  ( 20.94999999999999574, -1.261786168553869603, -41.58649896354548048 ) ) ;
#42429=DIRECTION ( 'NONE',  ( 0.000000000000000000, -0.9893560106964500722, 0.1455152366551550613 ) ) ;
#42457=VERTEX_POINT ( 'NONE', #62745 ) ;
#42469=DIRECTION ( 'NONE',  ( 0.000000000000000000, -1.000000000000000000, -0.000000000000000000 ) ) ;
#42510=FACE_OUTER_BOUND ( 'NONE', #227697, .T. ) ;
#42534=CIRCLE ( 'NONE', #63373, 0.5000000000000004441 ) ;
#42536=VERTEX_POINT ( 'NONE', #9183 ) ;
#42563=VECTOR ( 'NONE', #234896, 1000.000000000000000 ) ;
#42564=CIRCLE ( 'NONE', #188312, 4.299999999999956302 ) ;
#42566=CARTESIAN_POINT ( 'NONE',  ( -18.50000000000000000, 9.350000000011156942, -54.85000000000000142 ) ) ;
#42571=CARTESIAN_POINT ( 'NONE',  ( 23.24999999999999289, 11.65000000001116298, -21.75000000000000355 ) ) ;
#42646=ADVANCED_FACE ( 'NONE', ( #230824 ), #87198, .T. ) ;
#42658=CARTESIAN_POINT ( 'NONE',  ( 18.59999999999999076, 6.450000000011156587, -43.51702717044002355 ) ) ;
#42666=VECTOR ( 'NONE', #200661, 1000.000000000000114 ) ;
#42667=EDGE_CURVE ( 'NONE', #35453, #47428, #24889, .T. ) ;
#42679=CARTESIAN_POINT ( 'NONE',  ( 21.05000000000000071, 1.115600667400684642E-11, -67.00000000000000000 ) ) ;
#42681=CARTESIAN_POINT ( 'NONE',  ( 18.59999999999999432, 1.162701749949165642, -41.60000000000000142 ) ) ;
#42682=CARTESIAN_POINT ( 'NONE',  ( -18.58693740092145319, -9.406432150241794687, -40.62481645650139939 ) ) ;
#42698=VECTOR ( 'NONE', #166424, 1000.000000000000000 ) ;
#42742=DIRECTION ( 'NONE',  ( 0.000000000000000000, 1.000000000000000000, 0.000000000000000000 ) ) ;
#42778=ORIENTED_EDGE ( 'NONE', *, *, #220191, .T. ) ;
#42824=EDGE_CURVE ( 'NONE', #251013, #86684, #120557, .T. ) ;
#42835=ORIENTED_EDGE ( 'NONE', *, *, #74610, .F. ) ;
#42836=CARTESIAN_POINT ( 'NONE',  ( 21.11344571971309136, 10.61787902352891066, -45.74602089239949265 ) ) ;
#42879=CARTESIAN_POINT ( 'NONE',  ( 22.47071067811865319, 0.09909245471376171288, -25.77992525550195424 ) ) ;
#42881=DIRECTION ( 'NONE',  ( -1.000000000000000000, -3.265361837132813093E-16, 0.000000000000000000 ) ) ;
#42883=CIRCLE ( 'NONE', #221907, 0.5000000000000004441 ) ;
#42914=DIRECTION ( 'NONE',  ( 0.000000000000000000, 1.000000000000000000, -6.308085367188393199E-16 ) ) ;
#42949=DIRECTION ( 'NONE',  ( 0.000000000000000000, -1.000000000000000000, 0.000000000000000000 ) ) ;
#42950=DIRECTION ( 'NONE',  ( -1.000000000000000000, 0.000000000000000000, 0.000000000000000000 ) ) ;
#42960=AXIS2_PLACEMENT_3D ( 'NONE', #120106, #117504, #256958 ) ;
#42987=VECTOR ( 'NONE', #96227, 1000.000000000000114 ) ;
#42993=ORIENTED_EDGE ( 'NONE', *, *, #233866, .F. ) ;
#43000=FACE_OUTER_BOUND ( 'NONE', #215298, .T. ) ;
#43008=CARTESIAN_POINT ( 'NONE',  ( 18.59999999999999787, -1.736705739456431807, -78.51742258762372728 ) ) ;
#43021=CARTESIAN_POINT ( 'NONE',  ( 18.59999999999999432, -1.637172712959223952, -45.08215336547201701 ) ) ;
#43027=VERTEX_POINT ( 'NONE', #236904 ) ;
#43058=CARTESIAN_POINT ( 'NONE',  ( -20.94999999999999929, 7.120270961708750512, -70.65956304183931991 ) ) ;
#43066=AXIS2_PLACEMENT_3D ( 'NONE', #56534, #78677, #55248 ) ;
#43092=EDGE_CURVE ( 'NONE', #146761, #133244, #16687, .T. ) ;
#43099=VERTEX_POINT ( 'NONE', #158690 ) ;
#43148=LINE ( 'NONE', #240061, #194360 ) ;
#43154=FACE_OUTER_BOUND ( 'NONE', #234429, .T. ) ;
#43163=LINE ( 'NONE', #6588, #157158 ) ;
#43174=VERTEX_POINT ( 'NONE', #222449 ) ;
#43175=VERTEX_POINT ( 'NONE', #45129 ) ;
#43210=CARTESIAN_POINT ( 'NONE',  ( -20.64999999999999858, 7.150000000011155876, -54.65000000000000568 ) ) ;
#43226=ORIENTED_EDGE ( 'NONE', *, *, #18866, .F. ) ;
#43233=ORIENTED_EDGE ( 'NONE', *, *, #222469, .T. ) ;
#43241=CIRCLE ( 'NONE', #251517, 12.87499999999999822 ) ;
#43255=VECTOR ( 'NONE', #245110, 1000.000000000000000 ) ;
#43292=VERTEX_POINT ( 'NONE', #149390 ) ;
#43310=CIRCLE ( 'NONE', #193162, 4.049999999999998046 ) ;
#43316=DIRECTION ( 'NONE',  ( 0.000000000000000000, 1.000000000000000000, 0.000000000000000000 ) ) ;
#43337=ORIENTED_EDGE ( 'NONE', *, *, #88053, .T. ) ;
#43349=DIRECTION ( 'NONE',  ( 1.000000000000000000, -0.000000000000000000, -0.000000000000000000 ) ) ;
#43356=CARTESIAN_POINT ( 'NONE',  ( 20.92356734117541706, 10.31973158071402175, -72.55053347133544150 ) ) ;
#43375=ORIENTED_EDGE ( 'NONE', *, *, #61310, .F. ) ;
#43429=AXIS2_PLACEMENT_3D ( 'NONE', #44659, #240294, #124205 ) ;
#43446=ORIENTED_EDGE ( 'NONE', *, *, #109130, .T. ) ;
#43450=EDGE_LOOP ( 'NONE', ( #90150, #160060, #5104, #219725 ) ) ;
#43516=EDGE_CURVE ( 'NONE', #113714, #22952, #12786, .T. ) ;
#43519=ORIENTED_EDGE ( 'NONE', *, *, #107150, .T. ) ;
#43520=CARTESIAN_POINT ( 'NONE',  ( 21.14999999999999858, 1.115600667400684642E-11, -26.95934304829875927 ) ) ;
#43533=ORIENTED_EDGE ( 'NONE', *, *, #175827, .F. ) ;
#43556=DIRECTION ( 'NONE',  ( 0.000000000000000000, 0.000000000000000000, -1.000000000000000000 ) ) ;
#43581=PLANE ( 'NONE',  #171459 ) ;
#43583=ORIENTED_EDGE ( 'NONE', *, *, #120066, .F. ) ;
#43604=EDGE_LOOP ( 'NONE', ( #256595, #194482, #225425, #109662 ) ) ;
#43623=DIRECTION ( 'NONE',  ( 1.000000000000000000, 0.000000000000000000, 0.000000000000000000 ) ) ;
#43661=ORIENTED_EDGE ( 'NONE', *, *, #134171, .T. ) ;
#43691=AXIS2_PLACEMENT_3D ( 'NONE', #66711, #50963, #126677 ) ;
#43693=ORIENTED_EDGE ( 'NONE', *, *, #243235, .F. ) ;
#43698=ORIENTED_EDGE ( 'NONE', *, *, #148768, .T. ) ;
#43703=VERTEX_POINT ( 'NONE', #164773 ) ;
#43708=AXIS2_PLACEMENT_3D ( 'NONE', #217276, #116920, #39980 ) ;
#43728=DIRECTION ( 'NONE',  ( 0.000000000000000000, -2.255140518769784599E-13, 1.000000000000000000 ) ) ;
#43764=CARTESIAN_POINT ( 'NONE',  ( -23.15000000000000213, 2.000000000011154189, -53.77537807723790309 ) ) ;
#43773=CARTESIAN_POINT ( 'NONE',  ( -18.39999999999999858, -9.599999999988849453, -73.60018939122203108 ) ) ;
#43812=CARTESIAN_POINT ( 'NONE',  ( -20.94999999999999929, 1.835341550235569663, -45.05515129256298223 ) ) ;
#43826=CARTESIAN_POINT ( 'NONE',  ( 20.94999999999999929, -11.48912529306489994, -64.10000000000000853 ) ) ;
#43850=CARTESIAN_POINT ( 'NONE',  ( -20.97625342178428554, 11.60000000083159755, -40.42820322980187342 ) ) ;
#43882=ORIENTED_EDGE ( 'NONE', *, *, #122672, .T. ) ;
#43896=CARTESIAN_POINT ( 'NONE',  ( 18.49999999999999289, 10.20857864377385127, -21.75000000000000355 ) ) ;
#43898=ORIENTED_EDGE ( 'NONE', *, *, #139760, .T. ) ;
#43905=EDGE_LOOP ( 'NONE', ( #54589, #112405, #158293, #226881 ) ) ;
#43973=FACE_OUTER_BOUND ( 'NONE', #56359, .T. ) ;
#44062=CARTESIAN_POINT ( 'NONE',  ( -20.54999999999999716, -8.663551401858004652, -43.02410111806730697 ) ) ;
#44077=VECTOR ( 'NONE', #48621, 1000.000000000000000 ) ;
#44092=DIRECTION ( 'NONE',  ( 0.000000000000000000, 0.000000000000000000, 1.000000000000000000 ) ) ;
#44099=CARTESIAN_POINT ( 'NONE',  ( 21.07888907270776002, 10.72506921352637654, -45.72119358683318779 ) ) ;
#44107=LINE ( 'NONE', #243587, #49146 ) ;
#44116=ORIENTED_EDGE ( 'NONE', *, *, #224739, .F. ) ;
#44122=CARTESIAN_POINT ( 'NONE',  ( 21.12400247839509504, 10.72148804404154454, -45.75000000000000000 ) ) ;
#44125=AXIS2_PLACEMENT_3D ( 'NONE', #208608, #32559, #88614 ) ;
#44136=CARTESIAN_POINT ( 'NONE',  ( -20.85000000000000142, -1.249999999988843369, -74.80048075441509070 ) ) ;
#44179=CARTESIAN_POINT ( 'NONE',  ( -21.05000000000000071, -1.851028230129704522, -45.15391326942249606 ) ) ;
#44223=ORIENTED_EDGE ( 'NONE', *, *, #116114, .F. ) ;
#44249=DIRECTION ( 'NONE',  ( 0.000000000000000000, 0.000000000000000000, -1.000000000000000000 ) ) ;
#44253=AXIS2_PLACEMENT_3D ( 'NONE', #207762, #29151, #27855 ) ;
#44261=FACE_OUTER_BOUND ( 'NONE', #12618, .T. ) ;
#44266=DIRECTION ( 'NONE',  ( 0.000000000000000000, 0.1568667991644863147, 0.9876197685951252359 ) ) ;
#44272=ORIENTED_EDGE ( 'NONE', *, *, #253362, .F. ) ;
#44294=EDGE_LOOP ( 'NONE', ( #207319, #35242, #114001, #234120 ) ) ;
#44306=DIRECTION ( 'NONE',  ( 1.000000000000000000, 0.000000000000000000, 0.000000000000000000 ) ) ;
#44335=CARTESIAN_POINT ( 'NONE',  ( 18.60000000000000142, -9.399999999988782662, -40.79725975966329798 ) ) ;
#44380=EDGE_LOOP ( 'NONE', ( #99270, #80910, #31225 ) ) ;
#44388=AXIS2_PLACEMENT_3D ( 'NONE', #32176, #191250, #77669 ) ;
#44434=ORIENTED_EDGE ( 'NONE', *, *, #22375, .F. ) ;
#44461=CIRCLE ( 'NONE', #202654, 0.2000000000000005107 ) ;
#44552=TOROIDAL_SURFACE ( 'NONE', #144473, 11.70000000000000462, 0.1000000000000000056 ) ;
#44562=LINE ( 'NONE', #142360, #232571 ) ;
#44595=ADVANCED_FACE ( 'NONE', ( #174147 ), #16333, .F. ) ;
#44619=AXIS2_PLACEMENT_3D ( 'NONE', #246839, #12121, #130752 ) ;
#44643=CYLINDRICAL_SURFACE ( 'NONE', #42170, 0.5000000000000004441 ) ;
#44659=CARTESIAN_POINT ( 'NONE',  ( -23.15000000000000213, -8.999999999988844479, -57.10603087734755690 ) ) ;
#44700=VECTOR ( 'NONE', #40724, 1000.000000000000000 ) ;
#44747=FACE_OUTER_BOUND ( 'NONE', #158575, .T. ) ;
#44756=CARTESIAN_POINT ( 'NONE',  ( -20.94999999999999929, 1.115600667400684642E-11, -33.50000000000000000 ) ) ;
#44758=ORIENTED_EDGE ( 'NONE', *, *, #60994, .T. ) ;
#44784=CARTESIAN_POINT ( 'NONE',  ( -18.59999999999999787, -1.263275465206102233, -74.90186466674640542 ) ) ;
#44792=EDGE_CURVE ( 'NONE', #14005, #3179, #209075, .T. ) ;
#44796=VECTOR ( 'NONE', #143277, 1000.000000000000000 ) ;
#44828=ORIENTED_EDGE ( 'NONE', *, *, #104904, .T. ) ;
#44857=CARTESIAN_POINT ( 'NONE',  ( -21.07954640115336531, 6.329287696035376776, -33.43399229286031726 ) ) ;
#44863=ADVANCED_FACE ( 'NONE', ( #246903 ), #231229, .T. ) ;
#44908=EDGE_CURVE ( 'NONE', #61206, #42457, #255854, .T. ) ;
#44913=CARTESIAN_POINT ( 'NONE',  ( 20.12481660106788084, 9.526343992285099205, -41.72614166909304600 ) ) ;
#44916=CIRCLE ( 'NONE', #232185, 0.1000000000000000472 ) ;
#44920=AXIS2_PLACEMENT_3D ( 'NONE', #257993, #122393, #241070 ) ;
#44972=ORIENTED_EDGE ( 'NONE', *, *, #64188, .T. ) ;
#45011=VERTEX_POINT ( 'NONE', #99371 ) ;
#45024=CARTESIAN_POINT ( 'NONE',  ( -22.48479450179659977, 0.04699158119804078271, -21.85000155374838826 ) ) ;
#45034=VERTEX_POINT ( 'NONE', #79806 ) ;
#45054=CIRCLE ( 'NONE', #211678, 0.1999999999999987899 ) ;
#45100=FACE_OUTER_BOUND ( 'NONE', #176688, .T. ) ;
#45109=EDGE_LOOP ( 'NONE', ( #95963, #108301, #6748, #111089, #182884, #201647, #232627, #103646, #116654, #101740, #25516, #62353, #223872, #12070, #167818, #197005, #102779, #32880 ) ) ;
#45124=DIRECTION ( 'NONE',  ( 1.000000000000000000, 0.000000000000000000, -0.000000000000000000 ) ) ;
#45129=CARTESIAN_POINT ( 'NONE',  ( 18.59999999999999076, 6.650000000011155876, -54.75000000000000000 ) ) ;
#45141=DIRECTION ( 'NONE',  ( -0.000000000000000000, -0.000000000000000000, 1.000000000000000000 ) ) ;
#45149=DIRECTION ( 'NONE',  ( -0.000000000000000000, -0.1350103645451904977, 0.9908441862701596881 ) ) ;
#45176=ORIENTED_EDGE ( 'NONE', *, *, #30880, .F. ) ;
#45190=AXIS2_PLACEMENT_3D ( 'NONE', #214538, #115438, #16370 ) ;
#45200=DIRECTION ( 'NONE',  ( 0.000000000000000000, 0.000000000000000000, 1.000000000000000000 ) ) ;
#45219=SHAPE_REPRESENTATION ( 'Injection Molded Chain Links 2', ( #2425 ), #35604 ) ;
#45267=CIRCLE ( 'NONE', #32848, 0.1000000000000028644 ) ;
#45276=CARTESIAN_POINT ( 'NONE',  ( 21.13435531349788832, 1.115486826172573664E-11, -27.00627893640781352 ) ) ;
#45321=CARTESIAN_POINT ( 'NONE',  ( -21.05000000000000071, -0.09999999998884338825, -26.95934304829875927 ) ) ;
#45323=FACE_OUTER_BOUND ( 'NONE', #155671, .T. ) ;
#45333=CARTESIAN_POINT ( 'NONE',  ( -18.59999999999999787, -1.164121893230052995, -74.91484808557160591 ) ) ;
#45366=CARTESIAN_POINT ( 'NONE',  ( 20.94999999999999929, -8.999999999988844479, -43.39396912265245021 ) ) ;
#45371=DIRECTION ( 'NONE',  ( 0.000000000000000000, 0.000000000000000000, -1.000000000000000000 ) ) ;
#45373=AXIS2_PLACEMENT_3D ( 'NONE', #187951, #45860, #204920 ) ;
#45381=CARTESIAN_POINT ( 'NONE',  ( 18.58719872626879877, -9.566644397587475979, -73.82247819639700026 ) ) ;
#45390=VERTEX_POINT ( 'NONE', #184898 ) ;
#45399=CARTESIAN_POINT ( 'NONE',  ( 21.09793522318416592, 10.72462451022393282, -45.73929087097716462 ) ) ;
#45406=DIRECTION ( 'NONE',  ( 1.000000000000000000, -0.000000000000000000, -0.000000000000000000 ) ) ;
#45413=VECTOR ( 'NONE', #220558, 1000.000000000000000 ) ;
#45415=PLANE ( 'NONE',  #44920 ) ;
#45422=ORIENTED_EDGE ( 'NONE', *, *, #92443, .F. ) ;
#45428=CARTESIAN_POINT ( 'NONE',  ( 21.76363531954645936, 7.012936547882880234, -33.40099812570054638 ) ) ;
#45430=CARTESIAN_POINT ( 'NONE',  ( -18.50000000000000000, -1.736257131586239844, -45.06865232901750318 ) ) ;
#45520=DIRECTION ( 'NONE',  ( 0.000000000000000000, 0.000000000000000000, -1.000000000000000000 ) ) ;
#45569=ORIENTED_EDGE ( 'NONE', *, *, #31430, .F. ) ;
#45580=VECTOR ( 'NONE', #17219, 1000.000000000000114 ) ;
#45593=CARTESIAN_POINT ( 'NONE',  ( -23.25000000000000000, 2.600000000011156054, -53.77537807723790309 ) ) ;
#45595=EDGE_LOOP ( 'NONE', ( #103415, #13057, #6830, #5122 ) ) ;
#45601=CARTESIAN_POINT ( 'NONE',  ( -20.94999999999999929, 1.115600667400684642E-11, -67.00000000000000000 ) ) ;
#45604=AXIS2_PLACEMENT_3D ( 'NONE', #30088, #130437, #147438 ) ;
#45613=DIRECTION ( 'NONE',  ( 1.000000000000000000, -0.000000000000000000, -0.000000000000000000 ) ) ;
#45634=EDGE_LOOP ( 'NONE', ( #199665, #165807, #22808, #212676, #19617, #166538, #215244, #147861, #253144, #95436 ) ) ;
#45636=CARTESIAN_POINT ( 'NONE',  ( -18.59999999999999787, 1.115600667400684642E-11, -67.00000000000000000 ) ) ;
#45644=DIRECTION ( 'NONE',  ( 0.000000000000000000, -8.881784197001832136E-16, -1.000000000000000000 ) ) ;
#45650=DIRECTION ( 'NONE',  ( 0.000000000000000000, 0.000000000000000000, -1.000000000000000000 ) ) ;
#45656=ADVANCED_FACE ( 'NONE', ( #89414 ), #143001, .F. ) ;
#45702=DIRECTION ( 'NONE',  ( 0.000000000000000000, -0.8660254037844411501, -0.4999999999999956146 ) ) ;
#45710=ORIENTED_EDGE ( 'NONE', *, *, #186063, .T. ) ;
#45711=EDGE_CURVE ( 'NONE', #96815, #244896, #34609, .T. ) ;
#45721=FACE_OUTER_BOUND ( 'NONE', #253781, .T. ) ;
#45726=FACE_OUTER_BOUND ( 'NONE', #252811, .T. ) ;
#45742=DIRECTION ( 'NONE',  ( 1.000000000000000000, 3.265361837132813093E-16, -0.000000000000000000 ) ) ;
#45752=ORIENTED_EDGE ( 'NONE', *, *, #32918, .F. ) ;
#45756=CARTESIAN_POINT ( 'NONE',  ( -20.64999999999999858, 4.350000000011156054, -45.75000000000000711 ) ) ;
#45784=EDGE_CURVE ( 'NONE', #121232, #189010, #75029, .T. ) ;
#45787=VECTOR ( 'NONE', #173574, 1000.000000000000000 ) ;
#45790=AXIS2_PLACEMENT_3D ( 'NONE', #20405, #84149, #179484 ) ;
#45791=AXIS2_PLACEMENT_3D ( 'NONE', #244725, #188612, #54233 ) ;
#45834=DIRECTION ( 'NONE',  ( 1.000000000000000000, -0.000000000000000000, -0.000000000000000000 ) ) ;
#45840=DIRECTION ( 'NONE',  ( 1.000000000000000000, 0.000000000000000000, -0.000000000000000000 ) ) ;
#45848=CIRCLE ( 'NONE', #33407, 0.1999999999999987899 ) ;
#45860=DIRECTION ( 'NONE',  ( 0.000000000000000000, -1.000000000000000000, 0.000000000000000000 ) ) ;
#45868=CARTESIAN_POINT ( 'NONE',  ( 22.48660254037844197, 11.65000000001116298, -33.45000000000000995 ) ) ;
#45873=VERTEX_POINT ( 'NONE', #100924 ) ;
#45882=EDGE_CURVE ( 'NONE', #127734, #234879, #76369, .T. ) ;
#45943=EDGE_CURVE ( 'NONE', #160723, #32344, #130366, .T. ) ;
#46011=DIRECTION ( 'NONE',  ( 0.000000000000000000, 0.000000000000000000, -1.000000000000000000 ) ) ;
#46059=AXIS2_PLACEMENT_3D ( 'NONE', #7934, #87444, #112180 ) ;
#46072=CARTESIAN_POINT ( 'NONE',  ( 18.59999999999999432, 1.162701749949165642, -41.50000000000000000 ) ) ;
#46138=EDGE_LOOP ( 'NONE', ( #118964, #164037, #80537, #157527 ) ) ;
#46204=ADVANCED_FACE ( 'NONE', ( #204575 ), #125061, .T. ) ;
#46223=VERTEX_POINT ( 'NONE', #205862 ) ;
#46256=DIRECTION ( 'NONE',  ( -1.000000000000000000, 0.000000000000000000, 0.000000000000000000 ) ) ;
#46276=ORIENTED_EDGE ( 'NONE', *, *, #186307, .T. ) ;
#46283=CYLINDRICAL_SURFACE ( 'NONE', #27223, 0.09999999999999939493 ) ;
#46286=VERTEX_POINT ( 'NONE', #152346 ) ;
#46318=AXIS2_PLACEMENT_3D ( 'NONE', #194966, #16330, #95819 ) ;
#46320=AXIS2_PLACEMENT_3D ( 'NONE', #233263, #255305, #134113 ) ;
#46321=CIRCLE ( 'NONE', #112985, 11.79999999999999716 ) ;
#46326=VERTEX_POINT ( 'NONE', #50624 ) ;
#46348=CIRCLE ( 'NONE', #196382, 0.09999999999999907574 ) ;
#46363=CARTESIAN_POINT ( 'NONE',  ( -20.54999999999999716, 1.115600667400684642E-11, -65.00000000000000000 ) ) ;
#46387=CARTESIAN_POINT ( 'NONE',  ( 20.94999999999999929, 6.650000000011155876, -43.51702717044002355 ) ) ;
#46406=B_SPLINE_CURVE_WITH_KNOTS ( 'NONE', 3,
 ( #191523, #115807, #96228, #175798, #211059, #255257, #156246, #32454, #136633, #37567 ),
 .UNSPECIFIED., .F., .F.,
 ( 4, 2, 2, 2, 4 ),
 ( 0.000000000000000000, 3.990160268012908580E-05, 7.980320536025817160E-05, 0.0001596064107205132261, 0.0003192128214410382158 ),
 .UNSPECIFIED. ) ;
#46421=AXIS2_PLACEMENT_3D ( 'NONE', #188815, #145826, #5017 ) ;
#46430=DIRECTION ( 'NONE',  ( 0.000000000000000000, 1.000000000000000000, 0.000000000000000000 ) ) ;
#46464=EDGE_LOOP ( 'NONE', ( #101378, #82916, #23780, #253165 ) ) ;
#46510=DIRECTION ( 'NONE',  ( 0.000000000000000000, 3.552713678800509607E-15, 1.000000000000000000 ) ) ;
#46551=DIRECTION ( 'NONE',  ( -1.000000000000000000, -0.000000000000000000, -0.000000000000000000 ) ) ;
#46590=DIRECTION ( 'NONE',  ( 0.000000000000000000, -0.4999999999999949485, 0.8660254037844415942 ) ) ;
#46593=DIRECTION ( 'NONE',  ( 1.000000000000000000, 0.000000000000000000, 0.000000000000000000 ) ) ;
#46594=DIRECTION ( 'NONE',  ( -1.000000000000000000, 0.000000000000000000, 0.000000000000000000 ) ) ;
#46602=EDGE_CURVE ( 'NONE', #180750, #225961, #134991, .T. ) ;
#46624=ORIENTED_EDGE ( 'NONE', *, *, #207460, .T. ) ;
#46626=VECTOR ( 'NONE', #257943, 1000.000000000000000 ) ;
#46627=DIRECTION ( 'NONE',  ( 0.000000000000000000, 0.000000000000000000, -1.000000000000000000 ) ) ;
#46641=CARTESIAN_POINT ( 'NONE',  ( 21.11701782572533048, 10.72160911601861244, -45.74503742951121410 ) ) ;
#46650=EDGE_CURVE ( 'NONE', #103845, #67554, #50312, .T. ) ;
#46701=FACE_OUTER_BOUND ( 'NONE', #70610, .T. ) ;
#46792=EDGE_CURVE ( 'NONE', #233728, #136029, #18906, .T. ) ;
#46848=LINE ( 'NONE', #169426, #93813 ) ;
#46849=AXIS2_PLACEMENT_3D ( 'NONE', #232495, #248189, #91677 ) ;
#46901=CARTESIAN_POINT ( 'NONE',  ( 22.00356870141551724, 7.254242362499355501, -33.50000000000000711 ) ) ;
#46903=FACE_OUTER_BOUND ( 'NONE', #194082, .T. ) ;
#46927=CIRCLE ( 'NONE', #22024, 0.1000000000000028644 ) ;
#46948=ORIENTED_EDGE ( 'NONE', *, *, #92709, .T. ) ;
#46995=ADVANCED_FACE ( 'NONE', ( #63163 ), #124450, .F. ) ;
#47005=DIRECTION ( 'NONE',  ( -3.265361837132813093E-16, 1.000000000000000000, 0.000000000000000000 ) ) ;
#47057=ADVANCED_FACE ( 'NONE', ( #70919 ), #150741, .F. ) ;
#47059=DIRECTION ( 'NONE',  ( 1.000000000000000000, 0.000000000000000000, 0.000000000000000000 ) ) ;
#47088=LINE ( 'NONE', #187921, #210146 ) ;
#47091=AXIS2_PLACEMENT_3D ( 'NONE', #21192, #86235, #42023 ) ;
#47109=ORIENTED_EDGE ( 'NONE', *, *, #135821, .T. ) ;
#47120=CARTESIAN_POINT ( 'NONE',  ( -18.50000000000000000, 5.341242990002803559, -23.69334979351197745 ) ) ;
#47136=CARTESIAN_POINT ( 'NONE',  ( 18.50211644919734866, 10.30207779525984790, -72.48955207167824710 ) ) ;
#47215=ORIENTED_EDGE ( 'NONE', *, *, #175980, .T. ) ;
#47218=CARTESIAN_POINT ( 'NONE',  ( -18.31572283045152361, -9.548437830874650700, -73.85062565105830856 ) ) ;
#47236=CIRCLE ( 'NONE', #80542, 0.1000000000000001860 ) ;
#47275=EDGE_CURVE ( 'NONE', #79923, #31610, #9723, .T. ) ;
#47307=ADVANCED_FACE ( 'NONE', ( #241516 ), #159770, .T. ) ;
#47342=ADVANCED_FACE ( 'NONE', ( #103262 ), #62875, .T. ) ;
#47360=AXIS2_PLACEMENT_3D ( 'NONE', #66766, #182878, #4204 ) ;
#47372=AXIS2_PLACEMENT_3D ( 'NONE', #201382, #121862, #80110 ) ;
#47383=DIRECTION ( 'NONE',  ( 1.000000000000000000, -0.000000000000000000, -0.000000000000000000 ) ) ;
#47394=TOROIDAL_SURFACE ( 'NONE', #1618, 0.4000000000000012990, 0.1000000000000000056 ) ;
#47406=CARTESIAN_POINT ( 'NONE',  ( -21.05000000000000071, 6.304961112695785630, -33.52138556593774155 ) ) ;
#47420=CARTESIAN_POINT ( 'NONE',  ( -20.94999999999999929, 1.851028230152016674, -45.15391326942249606 ) ) ;
#47428=VERTEX_POINT ( 'NONE', #90122 ) ;
#47448=CARTESIAN_POINT ( 'NONE',  ( -18.59999999999999787, 1.115600667400684642E-11, -74.90000000000000568 ) ) ;
#47454=DIRECTION ( 'NONE',  ( 0.000000000000000000, -0.9915357197604792727, 0.1298341882520475943 ) ) ;
#47498=VERTEX_POINT ( 'NONE', #136965 ) ;
#47499=AXIS2_PLACEMENT_3D ( 'NONE', #156574, #15776, #152721 ) ;
#47524=DIRECTION ( 'NONE',  ( 4.336808689942128177E-15, 0.8660254037844330455, -0.5000000000000096589 ) ) ;
#47535=ADVANCED_FACE ( 'NONE', ( #53588 ), #92699, .T. ) ;
#47628=CYLINDRICAL_SURFACE ( 'NONE', #132326, 0.1000000000000028644 ) ;
#47650=ORIENTED_EDGE ( 'NONE', *, *, #178012, .F. ) ;
#47651=CIRCLE ( 'NONE', #193445, 0.1999999999999987899 ) ;
#47674=CYLINDRICAL_SURFACE ( 'NONE', #7246, 0.09999999999999939493 ) ;
#47681=CIRCLE ( 'NONE', #155872, 0.1000000000000028644 ) ;
#47707=CARTESIAN_POINT ( 'NONE',  ( 18.59999999999999076, 1.115600667400684642E-11, -67.00000000000000000 ) ) ;
#47709=DIRECTION ( 'NONE',  ( 1.000000000000000000, 0.000000000000000000, -0.000000000000000000 ) ) ;
#47729=ORIENTED_EDGE ( 'NONE', *, *, #185696, .F. ) ;
#47786=DIRECTION ( 'NONE',  ( 0.000000000000000000, 0.000000000000000000, -1.000000000000000000 ) ) ;
#47861=CARTESIAN_POINT ( 'NONE',  ( 20.94999999999999929, -8.999999999988842703, -57.10603087734755690 ) ) ;
#47863=ADVANCED_FACE ( 'NONE', ( #72522 ), #152064, .T. ) ;
#47865=DIRECTION ( 'NONE',  ( 2.952720810173289112E-16, -1.000000000000000000, -0.000000000000000000 ) ) ;
#47882=CARTESIAN_POINT ( 'NONE',  ( -20.94999999999999929, 5.850000000011105428, -43.63249722427797650 ) ) ;
#47899=ORIENTED_EDGE ( 'NONE', *, *, #193638, .T. ) ;
#47905=DIRECTION ( 'NONE',  ( 0.000000000000000000, 0.000000000000000000, 1.000000000000000000 ) ) ;
#47913=AXIS2_PLACEMENT_3D ( 'NONE', #232317, #251845, #91502 ) ;
#47917=LINE ( 'NONE', #25800, #182769 ) ;
#47937=DIRECTION ( 'NONE',  ( 1.000000000000000000, 0.000000000000000000, 0.000000000000000000 ) ) ;
#47938=CARTESIAN_POINT ( 'NONE',  ( 18.59999999999999076, -1.164121893230052995, -74.91484808557160591 ) ) ;
#47968=CARTESIAN_POINT ( 'NONE',  ( 20.94999999999999929, -1.162701749926853712, -41.40000000000000568 ) ) ;
#47969=ORIENTED_EDGE ( 'NONE', *, *, #144972, .F. ) ;
#47973=FACE_OUTER_BOUND ( 'NONE', #10314, .T. ) ;
#47987=LINE ( 'NONE', #45430, #184040 ) ;
#47995=ORIENTED_EDGE ( 'NONE', *, *, #226399, .F. ) ;
#47996=DIRECTION ( 'NONE',  ( 0.000000000000000000, 0.000000000000000000, -1.000000000000000000 ) ) ;
#48018=EDGE_CURVE ( 'NONE', #127278, #113415, #72663, .T. ) ;
#48049=CARTESIAN_POINT ( 'NONE',  ( -2.995603634470884209E-16, -11.74999999998884448, -45.75000000000000711 ) ) ;
#48061=AXIS2_PLACEMENT_3D ( 'NONE', #108733, #228700, #90439 ) ;
#48070=AXIS2_PLACEMENT_3D ( 'NONE', #9411, #185495, #29032 ) ;
#48074=CARTESIAN_POINT ( 'NONE',  ( -18.59999999999999787, 9.250000000011157297, -45.75000000000000000 ) ) ;
#48092=DIRECTION ( 'NONE',  ( -0.000000000000000000, 1.000000000000000000, 2.891205793294679805E-16 ) ) ;
#48124=VERTEX_POINT ( 'NONE', #241844 ) ;
#48132=DIRECTION ( 'NONE',  ( 0.000000000000000000, 0.000000000000000000, -1.000000000000000000 ) ) ;
#48144=VERTEX_POINT ( 'NONE', #162334 ) ;
#48148=ORIENTED_EDGE ( 'NONE', *, *, #167238, .F. ) ;
#48179=EDGE_CURVE ( 'NONE', #203988, #61003, #223836, .T. ) ;
#48203=ORIENTED_EDGE ( 'NONE', *, *, #153343, .F. ) ;
#48249=CARTESIAN_POINT ( 'NONE',  ( 21.05000000000000071, 5.000000000011153745, -54.59473398108690390 ) ) ;
#48261=CARTESIAN_POINT ( 'NONE',  ( -23.25000000000000000, 1.115600667400684642E-11, -33.50000000000000000 ) ) ;
#48272=EDGE_CURVE ( 'NONE', #127486, #45873, #136005, .T. ) ;
#48297=AXIS2_PLACEMENT_3D ( 'NONE', #226143, #47524, #207930 ) ;
#48308=CARTESIAN_POINT ( 'NONE',  ( -22.49999999999999645, 11.74956712350054744, -33.39914163090129051 ) ) ;
#48372=CARTESIAN_POINT ( 'NONE',  ( -21.05000000000000071, 1.115600667400684642E-11, -33.50000000000000000 ) ) ;
#48379=CARTESIAN_POINT ( 'NONE',  ( -23.15000000000000213, 4.350000000011156054, -45.65000000000000568 ) ) ;
#48385=DIRECTION ( 'NONE',  ( 0.7071067811865474617, 0.7071067811865474617, -0.000000000000000000 ) ) ;
#48388=CARTESIAN_POINT ( 'NONE',  ( 18.59999999999999076, 6.982009704867611077, -70.69615211825629331 ) ) ;
#48403=EDGE_CURVE ( 'NONE', #127486, #217509, #114520, .T. ) ;
#48413=CARTESIAN_POINT ( 'NONE',  ( 20.94999999999999574, 10.42338541492406279, -40.99205192387010044 ) ) ;
#48414=VECTOR ( 'NONE', #254967, 1000.000000000000000 ) ;
#48439=CARTESIAN_POINT ( 'NONE',  ( 18.57399277249656322, 10.33112638556969820, -72.59012289269746532 ) ) ;
#48443=CARTESIAN_POINT ( 'NONE',  ( 18.59999999999999076, 7.120270961708750512, -70.65956304183931991 ) ) ;
#48461=DIRECTION ( 'NONE',  ( -0.000000000000000000, -1.000000000000000000, 6.308085367188393199E-16 ) ) ;
#48468=AXIS2_PLACEMENT_3D ( 'NONE', #231342, #211768, #192214 ) ;
#48478=FACE_OUTER_BOUND ( 'NONE', #157079, .T. ) ;
#48490=AXIS2_PLACEMENT_3D ( 'NONE', #134938, #33347, #112843 ) ;
#48517=CARTESIAN_POINT ( 'NONE',  ( -18.33682934331516279, -9.511185591082417901, -73.90565476867330119 ) ) ;
#48530=ORIENTED_EDGE ( 'NONE', *, *, #149164, .T. ) ;
#48541=CARTESIAN_POINT ( 'NONE',  ( 23.14999999999999858, 5.950000000011160139, -56.69429769496518645 ) ) ;
#48568=ORIENTED_EDGE ( 'NONE', *, *, #240395, .T. ) ;
#48569=CIRCLE ( 'NONE', #173533, 0.1000000000000028644 ) ;
#48576=DIRECTION ( 'NONE',  ( 0.000000000000000000, 0.000000000000000000, -1.000000000000000000 ) ) ;
#48594=ORIENTED_EDGE ( 'NONE', *, *, #162324, .F. ) ;
#48621=DIRECTION ( 'NONE',  ( -1.000000000000000000, 0.000000000000000000, 0.000000000000000000 ) ) ;
#48624=ORIENTED_EDGE ( 'NONE', *, *, #184003, .T. ) ;
#48634=ORIENTED_EDGE ( 'NONE', *, *, #10063, .T. ) ;
#48687=PLANE ( 'NONE',  #40922 ) ;
#48689=AXIS2_PLACEMENT_3D ( 'NONE', #6801, #180308, #122914 ) ;
#48715=AXIS2_PLACEMENT_3D ( 'NONE', #107354, #186933, #8279 ) ;
#48753=CARTESIAN_POINT ( 'NONE',  ( -18.59999999999999787, -1.362429037182155023, -74.88888124792120493 ) ) ;
#48757=CARTESIAN_POINT ( 'NONE',  ( -18.59999999999999787, 1.162701749949165642, -41.60000000000000142 ) ) ;
#48779=CIRCLE ( 'NONE', #32066, 0.09999999999999939493 ) ;
#48784=DIRECTION ( 'NONE',  ( 0.000000000000000000, 0.000000000000000000, -1.000000000000000000 ) ) ;
#48824=ORIENTED_EDGE ( 'NONE', *, *, #46650, .F. ) ;
#48834=EDGE_CURVE ( 'NONE', #36165, #110094, #131927, .T. ) ;
#48845=CIRCLE ( 'NONE', #177867, 0.09999999999999939493 ) ;
#48858=DIRECTION ( 'NONE',  ( 1.000000000000000000, -0.000000000000000000, -0.000000000000000000 ) ) ;
#48924=CARTESIAN_POINT ( 'NONE',  ( -18.51024323315077424, 10.31104185824062647, -72.52045169831058047 ) ) ;
#48932=DIRECTION ( 'NONE',  ( -0.000000000000000000, -0.2605042016806452532, -0.9654727137038777718 ) ) ;
#48953=ORIENTED_EDGE ( 'NONE', *, *, #72211, .F. ) ;
#48999=DIRECTION ( 'NONE',  ( 1.000000000000000000, -0.000000000000000000, -0.000000000000000000 ) ) ;
#49029=ORIENTED_EDGE ( 'NONE', *, *, #213092, .T. ) ;
#49091=EDGE_LOOP ( 'NONE', ( #13266, #104463, #43693, #230926 ) ) ;
#49143=CIRCLE ( 'NONE', #215722, 0.2000000000000057288 ) ;
#49146=VECTOR ( 'NONE', #64940, 1000.000000000000000 ) ;
#49156=DIRECTION ( 'NONE',  ( -1.000000000000000000, 0.000000000000000000, 0.000000000000000000 ) ) ;
#49157=ADVANCED_FACE ( 'NONE', ( #171266 ), #19697, .F. ) ;
#49163=DIRECTION ( 'NONE',  ( 0.000000000000000000, -1.224646799142015331E-16, 1.000000000000000000 ) ) ;
#49200=DIRECTION ( 'NONE',  ( 0.000000000000000000, 0.000000000000000000, 1.000000000000000000 ) ) ;
#49222=ORIENTED_EDGE ( 'NONE', *, *, #107691, .T. ) ;
#49228=CARTESIAN_POINT ( 'NONE',  ( 18.39999999999999858, -9.682403433465241349, -73.65684337741279819 ) ) ;
#49237=ORIENTED_EDGE ( 'NONE', *, *, #194218, .F. ) ;
#49284=CARTESIAN_POINT ( 'NONE',  ( -20.64999999999999858, 2.000000000011154189, -46.72462192276210402 ) ) ;
#49310=CARTESIAN_POINT ( 'NONE',  ( 22.39999999999999503, 11.65000000001116298, -33.40000000000000568 ) ) ;
#49322=ORIENTED_EDGE ( 'NONE', *, *, #140112, .T. ) ;
#49346=CARTESIAN_POINT ( 'NONE',  ( 22.59999999999999432, 11.74987124438766273, -33.43457040898632471 ) ) ;
#49349=EDGE_CURVE ( 'NONE', #83073, #140260, #186093, .T. ) ;
#49365=EDGE_CURVE ( 'NONE', #158454, #216204, #96775, .T. ) ;
#49370=FACE_OUTER_BOUND ( 'NONE', #3526, .T. ) ;
#49407=DIRECTION ( 'NONE',  ( 4.239556034732056743E-17, -0.1298341882520022972, -0.9915357197604853789 ) ) ;
#49436=ORIENTED_EDGE ( 'NONE', *, *, #239023, .F. ) ;
#49444=( BOUNDED_SURFACE ( )  B_SPLINE_SURFACE ( 3, 2, ( 
 ( #41013, #164791, #63100 ),
 ( #121823, #162240, #24012 ),
 ( #1834, #100908, #66966 ),
 ( #3120, #85207, #120547 ) ),
 .UNSPECIFIED., .F., .F., .F. ) 
 B_SPLINE_SURFACE_WITH_KNOTS ( ( 4, 4 ),
 ( 3, 3 ),
 ( -1.355252715606880543E-20, 0.0003124336117481267463 ),
 ( 0.000000000000000000, 1.000000000000000000 ),
 .UNSPECIFIED. ) 
 GEOMETRIC_REPRESENTATION_ITEM ( )  RATIONAL_B_SPLINE_SURFACE ( (
 ( 1.000000000000000000, 0.7040654476016099395, 1.000000000000000000),
 ( 1.000000000000000000, 0.7039193538781852721, 1.000000000000000000),
 ( 1.000000000000000000, 0.7089171279145316529, 1.000000000000000000),
 ( 1.000000000000000000, 0.7071067811865506814, 1.000000000000000000) ) ) 
 REPRESENTATION_ITEM ( '' )  SURFACE ( )  );
#49446=CIRCLE ( 'NONE', #57790, 0.8750000000000007772 ) ;
#49463=DIRECTION ( 'NONE',  ( 0.000000000000000000, 0.000000000000000000, -1.000000000000000000 ) ) ;
#49466=ADVANCED_FACE ( 'NONE', ( #221864 ), #157712, .F. ) ;
#49472=DIRECTION ( 'NONE',  ( 0.000000000000000000, 0.9908441862701596881, -0.1350103645451904977 ) ) ;
#49487=ORIENTED_EDGE ( 'NONE', *, *, #65169, .T. ) ;
#49511=ORIENTED_EDGE ( 'NONE', *, *, #224691, .T. ) ;
#49514=DIRECTION ( 'NONE',  ( -1.000000000000000000, 0.000000000000000000, 0.000000000000000000 ) ) ;
#49541=AXIS2_PLACEMENT_3D ( 'NONE', #94572, #114136, #33370 ) ;
#49542=ORIENTED_EDGE ( 'NONE', *, *, #214841, .F. ) ;
#49545=CARTESIAN_POINT ( 'NONE',  ( 21.05000000000000426, 6.413826288824131083, -33.58574093703341390 ) ) ;
#49555=FACE_OUTER_BOUND ( 'NONE', #6523, .T. ) ;
#49589=ORIENTED_EDGE ( 'NONE', *, *, #219270, .F. ) ;
#49646=DIRECTION ( 'NONE',  ( 0.000000000000000000, -0.000000000000000000, -1.000000000000000000 ) ) ;
#49665=EDGE_CURVE ( 'NONE', #202789, #9029, #61799, .T. ) ;
#49684=EDGE_LOOP ( 'NONE', ( #232364, #140022, #243425, #136516 ) ) ;
#49780=ORIENTED_EDGE ( 'NONE', *, *, #55809, .F. ) ;
#49798=CARTESIAN_POINT ( 'NONE',  ( -20.64999999999999858, 1.115600667400684642E-11, -67.00000000000000000 ) ) ;
#49803=CARTESIAN_POINT ( 'NONE',  ( -18.58744394320938653, -9.566385154537710989, -73.82284805387557469 ) ) ;
#49831=LINE ( 'NONE', #189354, #195227 ) ;
#49852=ORIENTED_EDGE ( 'NONE', *, *, #231528, .F. ) ;
#49860=CARTESIAN_POINT ( 'NONE',  ( -18.59999999999999787, 1.162701749949165642, -41.60000000000000142 ) ) ;
#49879=AXIS2_PLACEMENT_3D ( 'NONE', #244677, #183446, #41387 ) ;
#49894=CARTESIAN_POINT ( 'NONE',  ( 18.50000000000000000, -9.399999999988823518, -40.79725975966326246 ) ) ;
#49924=TOROIDAL_SURFACE ( 'NONE', #166667, 2.100000000000002309, 0.1000000000000000056 ) ;
#49962=DIRECTION ( 'NONE',  ( -1.000000000000000000, -2.952720810173289112E-16, 0.000000000000000000 ) ) ;
#49971=CARTESIAN_POINT ( 'NONE',  ( 21.05000000000000426, 10.56275983746218117, -40.95681395791864077 ) ) ;
#50004=DIRECTION ( 'NONE',  ( 1.000000000000000000, 0.000000000000000000, 0.000000000000000000 ) ) ;
#50048=CIRCLE ( 'NONE', #79057, 0.1000000000000028644 ) ;
#50070=CARTESIAN_POINT ( 'NONE',  ( 21.05000000000000071, 5.500000000011153745, -45.90526601891310321 ) ) ;
#50080=AXIS2_PLACEMENT_3D ( 'NONE', #170153, #250910, #210521 ) ;
#50134=ORIENTED_EDGE ( 'NONE', *, *, #179428, .F. ) ;
#50140=EDGE_LOOP ( 'NONE', ( #202935, #155893, #28745, #120860 ) ) ;
#50151=AXIS2_PLACEMENT_3D ( 'NONE', #218293, #123085, #239171 ) ;
#50184=DIRECTION ( 'NONE',  ( 0.000000000000000000, 0.000000000000000000, -1.000000000000000000 ) ) ;
#50192=ADVANCED_FACE ( 'NONE', ( #38801 ), #161321, .T. ) ;
#50198=CARTESIAN_POINT ( 'NONE',  ( -21.05000000000000071, 1.115600667400684642E-11, -33.50000000000000000 ) ) ;
#50233=CARTESIAN_POINT ( 'NONE',  ( 21.05000000000000071, 10.56271494673968725, -40.95680210564469803 ) ) ;
#50246=DIRECTION ( 'NONE',  ( 0.000000000000000000, 0.000000000000000000, -1.000000000000000000 ) ) ;
#50265=CARTESIAN_POINT ( 'NONE',  ( 21.14999999999999858, -11.74999999998884448, -45.75000000000000711 ) ) ;
#50266=DIRECTION ( 'NONE',  ( 0.000000000000000000, 0.000000000000000000, 1.000000000000000000 ) ) ;
#50307=DIRECTION ( 'NONE',  ( -0.000000000000000000, 1.000000000000000000, 2.891205793294679805E-16 ) ) ;
#50312=LINE ( 'NONE', #107736, #22614 ) ;
#50355=CARTESIAN_POINT ( 'NONE',  ( -20.64999999999999858, 2.000000000011154189, -53.77537807723790309 ) ) ;
#50396=DIRECTION ( 'NONE',  ( 0.000000000000000000, 0.000000000000000000, 1.000000000000000000 ) ) ;
#50398=ORIENTED_EDGE ( 'NONE', *, *, #145404, .T. ) ;
#50431=CARTESIAN_POINT ( 'NONE',  ( 18.52928932188133970, 10.27928932189249878, -58.20857864376269930 ) ) ;
#50441=LINE ( 'NONE', #187426, #235724 ) ;
#50445=EDGE_CURVE ( 'NONE', #47498, #100761, #145542, .T. ) ;
#50450=DIRECTION ( 'NONE',  ( 0.000000000000000000, 0.000000000000000000, -1.000000000000000000 ) ) ;
#50459=ADVANCED_FACE ( 'NONE', ( #92028 ), #171609, .T. ) ;
#50487=DIRECTION ( 'NONE',  ( -0.000000000000000000, -0.1350103645451876666, 0.9908441862701600211 ) ) ;
#50495=DIRECTION ( 'NONE',  ( -1.000000000000000000, 0.000000000000000000, 0.000000000000000000 ) ) ;
#50506=ORIENTED_EDGE ( 'NONE', *, *, #234695, .T. ) ;
#50521=EDGE_CURVE ( 'NONE', #162149, #86723, #70754, .T. ) ;
#50529=EDGE_LOOP ( 'NONE', ( #243298, #209635, #141306, #86480 ) ) ;
#50536=DIRECTION ( 'NONE',  ( 1.000000000000000000, 0.000000000000000000, 0.000000000000000000 ) ) ;
#50537=AXIS2_PLACEMENT_3D ( 'NONE', #170662, #71533, #51914 ) ;
#50573=DIRECTION ( 'NONE',  ( -1.000000000000000000, -7.304098846218133681E-16, 4.217023435051677994E-16 ) ) ;
#50581=EDGE_CURVE ( 'NONE', #16250, #3179, #128999, .T. ) ;
#50589=CIRCLE ( 'NONE', #138080, 0.5000000000000013323 ) ;
#50624=CARTESIAN_POINT ( 'NONE',  ( -20.54999999999999716, 2.400000000011155432, -46.72462192276210402 ) ) ;
#50625=CARTESIAN_POINT ( 'NONE',  ( 23.14999999999999858, 1.115600667400684642E-11, -33.50000000000000000 ) ) ;
#50646=LINE ( 'NONE', #217419, #83512 ) ;
#50648=DIRECTION ( 'NONE',  ( 0.000000000000000000, 0.000000000000000000, -1.000000000000000000 ) ) ;
#50663=DIRECTION ( 'NONE',  ( 0.000000000000000000, -0.000000000000000000, -1.000000000000000000 ) ) ;
#50694=CARTESIAN_POINT ( 'NONE',  ( 22.48660254037844197, 11.65000000001116298, -33.45000000000000995 ) ) ;
#50696=CARTESIAN_POINT ( 'NONE',  ( -20.64999999999999858, -9.499999999988846255, -57.10603087734755690 ) ) ;
#50703=DIRECTION ( 'NONE',  ( 1.000000000000000000, 3.265361837132813093E-16, -0.000000000000000000 ) ) ;
#50740=AXIS2_PLACEMENT_3D ( 'NONE', #94870, #33678, #256448 ) ;
#50752=CIRCLE ( 'NONE', #117428, 6.258578643762710669 ) ;
#50807=LINE ( 'NONE', #32599, #244175 ) ;
#50815=ADVANCED_FACE ( 'NONE', ( #196922 ), #32762, .T. ) ;
#50818=FACE_OUTER_BOUND ( 'NONE', #70344, .T. ) ;
#50856=VECTOR ( 'NONE', #226214, 1000.000000000000000 ) ;
#50864=DIRECTION ( 'NONE',  ( -0.7071067811865474617, 0.7071067811865474617, 0.000000000000000000 ) ) ;
#50905=EDGE_LOOP ( 'NONE', ( #116887, #122372, #20636, #35188 ) ) ;
#50924=EDGE_CURVE ( 'NONE', #209893, #190117, #63841, .T. ) ;
#50963=DIRECTION ( 'NONE',  ( 1.000000000000000000, -0.000000000000000000, -0.000000000000000000 ) ) ;
#50972=CARTESIAN_POINT ( 'NONE',  ( -22.39999999999999858, 7.790779598384560245, -33.39999999999999858 ) ) ;
#51000=CARTESIAN_POINT ( 'NONE',  ( 23.14999999999999858, 5.000000000011153745, -55.09473398108690390 ) ) ;
#51003=CYLINDRICAL_SURFACE ( 'NONE', #255741, 2.000000000000001776 ) ;
#51024=ADVANCED_FACE ( 'NONE', ( #89802 ), #126376, .F. ) ;
#51061=EDGE_LOOP ( 'NONE', ( #34435, #216451, #232574, #171801 ) ) ;
#51075=CARTESIAN_POINT ( 'NONE',  ( 20.94999999999999929, 5.000000000011153745, -54.59473398108690390 ) ) ;
#51087=AXIS2_PLACEMENT_3D ( 'NONE', #19383, #177201, #256643 ) ;
#51091=VERTEX_POINT ( 'NONE', #76661 ) ;
#51097=AXIS2_PLACEMENT_3D ( 'NONE', #146927, #223897, #225174 ) ;
#51107=AXIS2_PLACEMENT_3D ( 'NONE', #35843, #256086, #39705 ) ;
#51134=CARTESIAN_POINT ( 'NONE',  ( -21.05000000000000071, 6.307425219576558995, -33.51681986838567440 ) ) ;
#51144=ORIENTED_EDGE ( 'NONE', *, *, #115859, .T. ) ;
#51150=ORIENTED_EDGE ( 'NONE', *, *, #166206, .T. ) ;
#51172=CARTESIAN_POINT ( 'NONE',  ( 21.05000000000000071, 10.42338541492406279, -40.99205192387010044 ) ) ;
#51184=ADVANCED_FACE ( 'NONE', ( #214894 ), #187637, .T. ) ;
#51195=EDGE_CURVE ( 'NONE', #96922, #42536, #141635, .T. ) ;
#51222=CARTESIAN_POINT ( 'NONE',  ( -22.47071067811865319, 0.09909245471376171288, -25.77992525550194003 ) ) ;
#51239=DIRECTION ( 'NONE',  ( 0.000000000000000000, 1.734723475976807292E-15, -1.000000000000000000 ) ) ;
#51245=DIRECTION ( 'NONE',  ( -0.000000000000000000, -1.000000000000000000, -0.000000000000000000 ) ) ;
#51251=DIRECTION ( 'NONE',  ( 0.000000000000000000, 1.000000000000000000, -6.308085367188393199E-16 ) ) ;
#51264=VERTEX_POINT ( 'NONE', #160083 ) ;
#51300=DIRECTION ( 'NONE',  ( -0.000000000000000000, 1.000000000000000000, -1.224646799147352961E-16 ) ) ;
#51331=CARTESIAN_POINT ( 'NONE',  ( 21.05000000000000071, 6.299230910098046365, -33.40156250000000426 ) ) ;
#51355=ORIENTED_EDGE ( 'NONE', *, *, #196005, .T. ) ;
#51403=AXIS2_PLACEMENT_3D ( 'NONE', #511, #216991, #237856 ) ;
#51428=EDGE_CURVE ( 'NONE', #100505, #135153, #96008, .T. ) ;
#51451=CARTESIAN_POINT ( 'NONE',  ( -20.85000000000000142, -11.74999999998884448, -67.00000000000000000 ) ) ;
#51455=DIRECTION ( 'NONE',  ( 1.000000000000000000, 0.000000000000000000, 0.000000000000000000 ) ) ;
#51471=DIRECTION ( 'NONE',  ( 0.000000000000000000, 0.8700118002898322711, -0.4930308989875231696 ) ) ;
#51479=CARTESIAN_POINT ( 'NONE',  ( -21.05000000000000071, -1.261786168553869603, -41.58649896354548048 ) ) ;
#51486=ORIENTED_EDGE ( 'NONE', *, *, #79162, .F. ) ;
#51498=AXIS2_PLACEMENT_3D ( 'NONE', #198669, #20053, #99539 ) ;
#51502=CARTESIAN_POINT ( 'NONE',  ( 21.05000000000000071, 10.72371710471868056, -41.16491356908760935 ) ) ;
#51506=DIRECTION ( 'NONE',  ( 0.000000000000000000, -0.000000000000000000, -1.000000000000000000 ) ) ;
#51516=DIRECTION ( 'NONE',  ( 1.000000000000000000, 0.000000000000000000, -0.000000000000000000 ) ) ;
#51532=FACE_OUTER_BOUND ( 'NONE', #236483, .T. ) ;
#51537=LINE ( 'NONE', #11170, #42698 ) ;
#51538=AXIS2_PLACEMENT_3D ( 'NONE', #158644, #59472, #80323 ) ;
#51571=CIRCLE ( 'NONE', #201442, 11.74999999999999645 ) ;
#51589=CARTESIAN_POINT ( 'NONE',  ( -20.64999999999999858, 7.150000000011155876, -45.85000000000000142 ) ) ;
#51612=CIRCLE ( 'NONE', #5647, 0.09999999999999907574 ) ;
#51619=ADVANCED_FACE ( 'NONE', ( #180603, #240574, #1939 ), #197582, .F. ) ;
#51640=CARTESIAN_POINT ( 'NONE',  ( 20.95512820512820440, 8.876151316299271343, -42.05862899514094977 ) ) ;
#51652=ADVANCED_FACE ( 'NONE', ( #220994 ), #82742, .F. ) ;
#51692=ORIENTED_EDGE ( 'NONE', *, *, #77341, .F. ) ;
#51703=ORIENTED_EDGE ( 'NONE', *, *, #166281, .F. ) ;
#51723=AXIS2_PLACEMENT_3D ( 'NONE', #205996, #27400, #121368 ) ;
#51745=CYLINDRICAL_SURFACE ( 'NONE', #52721, 0.1000000000000028644 ) ;
#51799=DIRECTION ( 'NONE',  ( 0.000000000000000000, 0.000000000000000000, -1.000000000000000000 ) ) ;
#51811=VECTOR ( 'NONE', #62619, 1000.000000000000000 ) ;
#51828=EDGE_LOOP ( 'NONE', ( #198949, #23881, #128491, #221927 ) ) ;
#51850=CARTESIAN_POINT ( 'NONE',  ( -20.99551997958364069, 11.75000000001110756, -60.15165913768996120 ) ) ;
#51887=CARTESIAN_POINT ( 'NONE',  ( 20.94999999999999574, 1.849084418638171856, -45.15601052144712213 ) ) ;
#51893=DIRECTION ( 'NONE',  ( -0.000000000000000000, 1.000000000000000000, -0.000000000000000000 ) ) ;
#51914=DIRECTION ( 'NONE',  ( 0.000000000000000000, 1.000000000000000000, 0.000000000000000000 ) ) ;
#51924=EDGE_CURVE ( 'NONE', #147068, #9191, #75586, .T. ) ;
#51926=DIRECTION ( 'NONE',  ( 1.000000000000000000, 0.000000000000000000, 0.000000000000000000 ) ) ;
#51975=ADVANCED_FACE ( 'NONE', ( #216848 ), #96201, .T. ) ;
#51987=CARTESIAN_POINT ( 'NONE',  ( 22.50000000000000000, 11.64957080755595520, -33.40000000000000568 ) ) ;
#52016=FACE_BOUND ( 'NONE', #148133, .T. ) ;
#52027=CARTESIAN_POINT ( 'NONE',  ( 18.59999999999999076, 11.65000000001115943, -67.00000000000000000 ) ) ;
#52030=LINE ( 'NONE', #172040, #76900 ) ;
#52063=ADVANCED_FACE ( 'NONE', ( #236419 ), #128040, .F. ) ;
#52096=DIRECTION ( 'NONE',  ( 0.000000000000000000, 1.776356839400310418E-15, -1.000000000000000000 ) ) ;
#52145=DIRECTION ( 'NONE',  ( 1.000000000000000000, 0.000000000000000000, -0.000000000000000000 ) ) ;
#52162=DIRECTION ( 'NONE',  ( 0.000000000000000000, -0.000000000000000000, -1.000000000000000000 ) ) ;
#52184=EDGE_CURVE ( 'NONE', #34405, #235569, #50589, .T. ) ;
#52202=FACE_OUTER_BOUND ( 'NONE', #151693, .T. ) ;
#52214=ORIENTED_EDGE ( 'NONE', *, *, #142428, .T. ) ;
#52216=FACE_OUTER_BOUND ( 'NONE', #162292, .T. ) ;
#52258=DIRECTION ( 'NONE',  ( 0.000000000000000000, 0.1495327102803689356, 0.9887567792719336168 ) ) ;
#52300=CARTESIAN_POINT ( 'NONE',  ( 18.49999999999999289, 10.32573593129922607, -58.35000000000001563 ) ) ;
#52303=CARTESIAN_POINT ( 'NONE',  ( 18.48413544395648600, -9.664304033616620160, -73.68310499303828465 ) ) ;
#52315=CIRCLE ( 'NONE', #160707, 7.900000000000003908 ) ;
#52343=ORIENTED_EDGE ( 'NONE', *, *, #169442, .T. ) ;
#52346=EDGE_CURVE ( 'NONE', #145730, #26511, #150564, .T. ) ;
#52360=ORIENTED_EDGE ( 'NONE', *, *, #181825, .T. ) ;
#52368=AXIS2_PLACEMENT_3D ( 'NONE', #187383, #28332, #50396 ) ;
#52381=DIRECTION ( 'NONE',  ( 1.000000000000000000, -0.000000000000000000, -0.000000000000000000 ) ) ;
#52399=EDGE_LOOP ( 'NONE', ( #136726, #17774, #127234, #66016, #110359, #247913, #49511, #211177 ) ) ;
#52403=VERTEX_POINT ( 'NONE', #986 ) ;
#52412=AXIS2_PLACEMENT_3D ( 'NONE', #228897, #12436, #108934 ) ;
#52441=CARTESIAN_POINT ( 'NONE',  ( -20.54999999999999716, -9.399999999988848387, -43.39396912265245021 ) ) ;
#52444=CARTESIAN_POINT ( 'NONE',  ( 21.05000000000000071, 1.115600667400684642E-11, -67.00000000000000000 ) ) ;
#52448=CARTESIAN_POINT ( 'NONE',  ( 18.50000000000000355, -9.421456145484386369, -40.74198208401926991 ) ) ;
#52504=DIRECTION ( 'NONE',  ( 0.000000000000000000, -1.000000000000000000, 0.000000000000000000 ) ) ;
#52556=CARTESIAN_POINT ( 'NONE',  ( -23.15000000000000213, 4.350000000011156054, -45.75000000000000711 ) ) ;
#52563=VECTOR ( 'NONE', #146624, 1000.000000000000000 ) ;
#52569=EDGE_CURVE ( 'NONE', #85875, #201436, #29609, .T. ) ;
#52629=CIRCLE ( 'NONE', #198389, 0.1000000000000028644 ) ;
#52669=FACE_OUTER_BOUND ( 'NONE', #31794, .T. ) ;
#52675=DIRECTION ( 'NONE',  ( -2.952720810173288619E-16, 1.000000000000000000, 0.000000000000000000 ) ) ;
#52710=ORIENTED_EDGE ( 'NONE', *, *, #243861, .F. ) ;
#52717=CARTESIAN_POINT ( 'NONE',  ( 23.15000000000000213, -11.64999999998883595, -63.89999999999999858 ) ) ;
#52721=AXIS2_PLACEMENT_3D ( 'NONE', #231712, #210852, #113032 ) ;
#52728=CARTESIAN_POINT ( 'NONE',  ( -21.05000000000000071, 1.115600667400684642E-11, -41.40000000000000568 ) ) ;
#52760=AXIS2_PLACEMENT_3D ( 'NONE', #128139, #222056, #244202 ) ;
#52785=VERTEX_POINT ( 'NONE', #215988 ) ;
#52809=DIRECTION ( 'NONE',  ( 0.000000000000000000, 0.000000000000000000, -1.000000000000000000 ) ) ;
#52818=CARTESIAN_POINT ( 'NONE',  ( -18.59999999999999787, -9.499999999988849808, -41.60000000000000142 ) ) ;
#52861=CARTESIAN_POINT ( 'NONE',  ( 20.94999999999999574, -11.48912529306490349, -36.50000000000000711 ) ) ;
#52929=DIRECTION ( 'NONE',  ( 0.000000000000000000, 0.000000000000000000, -1.000000000000000000 ) ) ;
#52957=DIRECTION ( 'NONE',  ( 1.000000000000000000, -0.000000000000000000, -0.000000000000000000 ) ) ;
#52984=CARTESIAN_POINT ( 'NONE',  ( -21.55000000000000071, 7.350000000011155166, -45.85000000000000142 ) ) ;
#52991=ORIENTED_EDGE ( 'NONE', *, *, #236251, .T. ) ;
#53000=DIRECTION ( 'NONE',  ( 0.000000000000000000, 0.000000000000000000, -1.000000000000000000 ) ) ;
#53005=CARTESIAN_POINT ( 'NONE',  ( 21.11927991906888025, 6.448493118502572230, -33.49091632052610379 ) ) ;
#53029=DIRECTION ( 'NONE',  ( 0.000000000000000000, 0.000000000000000000, -1.000000000000000000 ) ) ;
#53046=CARTESIAN_POINT ( 'NONE',  ( 21.87500000000000355, 9.750000000011153745, -54.65000000000000568 ) ) ;
#53050=CARTESIAN_POINT ( 'NONE',  ( -21.55000000000000071, 7.350000000011155166, -54.65000000000000568 ) ) ;
#53085=CARTESIAN_POINT ( 'NONE',  ( -21.05000000000000071, 1.360870587203197646, -41.57299792709095954 ) ) ;
#53087=LINE ( 'NONE', #34844, #195443 ) ;
#53089=TOROIDAL_SURFACE ( 'NONE', #244802, 11.90000000000000391, 0.1000000000000000056 ) ;
#53098=CARTESIAN_POINT ( 'NONE',  ( 20.12500000000000355, 10.24195072709382970, -41.36020372708612314 ) ) ;
#53099=ORIENTED_EDGE ( 'NONE', *, *, #162021, .F. ) ;
#53133=ORIENTED_EDGE ( 'NONE', *, *, #107528, .F. ) ;
#53153=DIRECTION ( 'NONE',  ( 1.000000000000000000, 0.000000000000000000, 0.000000000000000000 ) ) ;
#53169=AXIS2_PLACEMENT_3D ( 'NONE', #11492, #93576, #111870 ) ;
#53170=EDGE_LOOP ( 'NONE', ( #70408, #119439, #40860, #97553, #7072 ) ) ;
#53203=EDGE_LOOP ( 'NONE', ( #218591, #69736, #72757, #2182, #202484 ) ) ;
#53276=ORIENTED_EDGE ( 'NONE', *, *, #158826, .F. ) ;
#53351=ORIENTED_EDGE ( 'NONE', *, *, #56746, .T. ) ;
#53394=ORIENTED_EDGE ( 'NONE', *, *, #76572, .F. ) ;
#53433=EDGE_CURVE ( 'NONE', #39957, #95339, #54682, .T. ) ;
#53449=CARTESIAN_POINT ( 'NONE',  ( -22.49544290803785174, 11.74987023786834506, -33.43468804074269940 ) ) ;
#53456=CARTESIAN_POINT ( 'NONE',  ( 20.85000000000000142, -1.263275465206102233, -74.90186466674640542 ) ) ;
#53459=AXIS2_PLACEMENT_3D ( 'NONE', #47861, #109122, #126116 ) ;
#53467=CARTESIAN_POINT ( 'NONE',  ( -18.59999999999999787, -9.321008403350132809, -40.73593824907788274 ) ) ;
#53481=AXIS2_PLACEMENT_3D ( 'NONE', #215481, #78532, #21172 ) ;
#53488=DIRECTION ( 'NONE',  ( 0.000000000000000000, 0.000000000000000000, -1.000000000000000000 ) ) ;
#53505=CYLINDRICAL_SURFACE ( 'NONE', #84026, 0.1000000000000028644 ) ;
#53546=ORIENTED_EDGE ( 'NONE', *, *, #246995, .F. ) ;
#53562=CARTESIAN_POINT ( 'NONE',  ( 23.24999999999999289, 6.550000000011156231, -54.85000000000000142 ) ) ;
#53567=EDGE_CURVE ( 'NONE', #9105, #87561, #1144, .T. ) ;
#53587=CARTESIAN_POINT ( 'NONE',  ( 18.59999999999996945, 10.33248238083634440, -72.59484654391314962 ) ) ;
#53588=FACE_OUTER_BOUND ( 'NONE', #212461, .T. ) ;
#53602=VECTOR ( 'NONE', #250219, 1000.000000000000000 ) ;
#53613=AXIS2_PLACEMENT_3D ( 'NONE', #216980, #138705, #55322 ) ;
#53625=DIRECTION ( 'NONE',  ( -1.000000000000000000, 0.000000000000000000, 0.000000000000000000 ) ) ;
#53627=AXIS2_PLACEMENT_3D ( 'NONE', #173437, #252907, #134235 ) ;
#53653=CIRCLE ( 'NONE', #232728, 0.09999999999999911737 ) ;
#53656=CIRCLE ( 'NONE', #70451, 0.1000000000000028644 ) ;
#53657=ORIENTED_EDGE ( 'NONE', *, *, #87908, .F. ) ;
#53665=ORIENTED_EDGE ( 'NONE', *, *, #32491, .F. ) ;
#53682=FACE_OUTER_BOUND ( 'NONE', #137433, .T. ) ;
#53724=EDGE_CURVE ( 'NONE', #28509, #132417, #196514, .T. ) ;
#53726=CARTESIAN_POINT ( 'NONE',  ( 19.97071067811865674, 11.72071067812981759, -58.20857864376270641 ) ) ;
#53733=VECTOR ( 'NONE', #67695, 1000.000000000000000 ) ;
#53749=EDGE_CURVE ( 'NONE', #201739, #102509, #47987, .T. ) ;
#53755=VERTEX_POINT ( 'NONE', #145799 ) ;
#53762=VERTEX_POINT ( 'NONE', #126239 ) ;
#53769=DIRECTION ( 'NONE',  ( -1.000000000000000000, 0.000000000000000000, 0.000000000000000000 ) ) ;
#53792=EDGE_CURVE ( 'NONE', #174796, #205763, #226617, .T. ) ;
#53801=CARTESIAN_POINT ( 'NONE',  ( 18.49999999999999645, 1.115600667400684642E-11, -67.00000000000000000 ) ) ;
#53839=CARTESIAN_POINT ( 'NONE',  ( -18.59999999999999787, 1.835341550235567887, -45.05515129256298223 ) ) ;
#53859=DIRECTION ( 'NONE',  ( 1.000000000000000000, -0.000000000000000000, -0.000000000000000000 ) ) ;
#53878=ORIENTED_EDGE ( 'NONE', *, *, #231976, .T. ) ;
#53906=CIRCLE ( 'NONE', #241352, 11.80000000000000426 ) ;
#53907=AXIS2_PLACEMENT_3D ( 'NONE', #241064, #256707, #201926 ) ;
#53921=TOROIDAL_SURFACE ( 'NONE', #174608, 7.800000000000000711, 0.1000000000000000056 ) ;
#53928=DIRECTION ( 'NONE',  ( 0.000000000000000000, 0.000000000000000000, -1.000000000000000000 ) ) ;
#53929=EDGE_LOOP ( 'NONE', ( #231988, #15122, #126695, #10515 ) ) ;
#53941=DIRECTION ( 'NONE',  ( -6.938893903907209445E-14, -0.9999176327611370985, -0.01283462868040260302 ) ) ;
#53949=TOROIDAL_SURFACE ( 'NONE', #253852, 12.77499999999999858, 0.1000000000000000056 ) ;
#54022=DIRECTION ( 'NONE',  ( 0.000000000000000000, 0.000000000000000000, -1.000000000000000000 ) ) ;
#54064=DIRECTION ( 'NONE',  ( 0.000000000000000000, 0.4930308989875313852, 0.8700118002898274971 ) ) ;
#54084=EDGE_CURVE ( 'NONE', #72361, #197038, #246758, .T. ) ;
#54091=VECTOR ( 'NONE', #81645, 1000.000000000000000 ) ;
#54100=CARTESIAN_POINT ( 'NONE',  ( 18.49999999999999289, 10.41716543472751688, -58.34999999942034776 ) ) ;
#54120=DIRECTION ( 'NONE',  ( 1.000000000000000000, 2.952720810173289112E-16, -0.000000000000000000 ) ) ;
#54155=EDGE_CURVE ( 'NONE', #129105, #250227, #225889, .T. ) ;
#54196=ORIENTED_EDGE ( 'NONE', *, *, #196329, .F. ) ;
#54216=DIRECTION ( 'NONE',  ( 3.616040088954497272E-32, -1.224646799147352961E-16, 1.000000000000000000 ) ) ;
#54232=ORIENTED_EDGE ( 'NONE', *, *, #24420, .F. ) ;
#54233=DIRECTION ( 'NONE',  ( 0.000000000000000000, 0.8660254037844411501, 0.4999999999999956701 ) ) ;
#54236=DIRECTION ( 'NONE',  ( 0.000000000000000000, 1.776356839400244943E-15, -1.000000000000000000 ) ) ;
#54243=VECTOR ( 'NONE', #205113, 1000.000000000000000 ) ;
#54256=ORIENTED_EDGE ( 'NONE', *, *, #13429, .F. ) ;
#54279=DIRECTION ( 'NONE',  ( -0.000000000000000000, -0.8700118002898321601, 0.4930308989875230030 ) ) ;
#54289=ORIENTED_EDGE ( 'NONE', *, *, #209430, .T. ) ;
#54304=DIRECTION ( 'NONE',  ( 0.000000000000000000, -0.000000000000000000, 1.000000000000000000 ) ) ;
#54324=DIRECTION ( 'NONE',  ( -0.000000000000000000, -0.000000000000000000, -1.000000000000000000 ) ) ;
#54368=CARTESIAN_POINT ( 'NONE',  ( -18.50000000000000000, -9.399999999988850163, -40.79725975966329088 ) ) ;
#54382=EDGE_CURVE ( 'NONE', #193788, #199100, #213633, .T. ) ;
#54398=CIRCLE ( 'NONE', #87699, 0.1000000000000028644 ) ;
#54413=DIRECTION ( 'NONE',  ( -1.000000000000000000, 0.000000000000000000, 0.000000000000000000 ) ) ;
#54435=CARTESIAN_POINT ( 'NONE',  ( -20.94999999999999929, 11.75000000001115019, -60.21613433702190576 ) ) ;
#54440=CIRCLE ( 'NONE', #225103, 2.100000000000002309 ) ;
#54526=AXIS2_PLACEMENT_3D ( 'NONE', #70650, #150170, #18344 ) ;
#54531=DIRECTION ( 'NONE',  ( 0.000000000000000000, 0.000000000000000000, -1.000000000000000000 ) ) ;
#54552=DIRECTION ( 'NONE',  ( 0.000000000000000000, 0.000000000000000000, -1.000000000000000000 ) ) ;
#54567=CARTESIAN_POINT ( 'NONE',  ( 22.49436431346199683, 11.64995094766461392, -33.43309647027773934 ) ) ;
#54589=ORIENTED_EDGE ( 'NONE', *, *, #25871, .T. ) ;
#54595=CARTESIAN_POINT ( 'NONE',  ( 23.25000000000000000, -11.74999999998883560, -21.75000000000000355 ) ) ;
#54634=ADVANCED_FACE ( 'NONE', ( #30400 ), #70826, .T. ) ;
#54646=CARTESIAN_POINT ( 'NONE',  ( 20.94999999999999574, -1.162701749926853712, -41.50000000000000000 ) ) ;
#54659=AXIS2_PLACEMENT_3D ( 'NONE', #133800, #210776, #110388 ) ;
#54662=ORIENTED_EDGE ( 'NONE', *, *, #85843, .T. ) ;
#54682=CIRCLE ( 'NONE', #229666, 0.1000000000000028644 ) ;
#54692=AXIS2_PLACEMENT_3D ( 'NONE', #186414, #127717, #84684 ) ;
#54702=CARTESIAN_POINT ( 'NONE',  ( 20.94999999999999929, 4.813084112160684214, -55.05848224347618469 ) ) ;
#54712=EDGE_CURVE ( 'NONE', #168194, #86723, #96744, .T. ) ;
#54735=CARTESIAN_POINT ( 'NONE',  ( -20.64999999999999858, 1.115600667400684642E-11, -67.00000000000000000 ) ) ;
#54738=CYLINDRICAL_SURFACE ( 'NONE', #235276, 0.09999999999999939493 ) ;
#54754=VERTEX_POINT ( 'NONE', #58900 ) ;
#54759=ORIENTED_EDGE ( 'NONE', *, *, #192042, .F. ) ;
#54762=EDGE_CURVE ( 'NONE', #82771, #173389, #238767, .T. ) ;
#54773=FACE_OUTER_BOUND ( 'NONE', #228539, .T. ) ;
#54775=DIRECTION ( 'NONE',  ( 0.000000000000000000, 0.000000000000000000, -1.000000000000000000 ) ) ;
#54785=DIRECTION ( 'NONE',  ( 1.000000000000000000, 0.000000000000000000, -0.000000000000000000 ) ) ;
#54865=ORIENTED_EDGE ( 'NONE', *, *, #222530, .T. ) ;
#54875=CARTESIAN_POINT ( 'NONE',  ( 21.30000000000002558, 1.115600667400684642E-11, -33.50000000000000000 ) ) ;
#54889=AXIS2_PLACEMENT_3D ( 'NONE', #54735, #251658, #36493 ) ;
#54941=DIRECTION ( 'NONE',  ( 0.000000000000000000, 0.000000000000000000, -1.000000000000000000 ) ) ;
#54944=VERTEX_POINT ( 'NONE', #67921 ) ;
#55004=DIRECTION ( 'NONE',  ( 0.000000000000000000, 0.000000000000000000, -1.000000000000000000 ) ) ;
#55016=ORIENTED_EDGE ( 'NONE', *, *, #257450, .T. ) ;
#55038=CARTESIAN_POINT ( 'NONE',  ( 21.10257677756356287, 0.02495074957913891861, -27.10161825746727260 ) ) ;
#55040=CARTESIAN_POINT ( 'NONE',  ( 21.93642651522410603, 7.327166239336949438, -33.50000000000000000 ) ) ;
#55047=DIRECTION ( 'NONE',  ( 1.000000000000000000, 0.000000000000000000, 0.000000000000000000 ) ) ;
#55070=DIRECTION ( 'NONE',  ( -1.000000000000000000, 0.000000000000000000, 0.000000000000000000 ) ) ;
#55113=ORIENTED_EDGE ( 'NONE', *, *, #68031, .T. ) ;
#55121=VERTEX_POINT ( 'NONE', #232148 ) ;
#55125=TOROIDAL_SURFACE ( 'NONE', #155160, 0.6000000000000004219, 0.1000000000000000056 ) ;
#55173=ADVANCED_FACE ( 'NONE', ( #76899 ), #13101, .T. ) ;
#55186=AXIS2_PLACEMENT_3D ( 'NONE', #29989, #32564, #230739 ) ;
#55234=DIRECTION ( 'NONE',  ( 0.000000000000000000, -0.000000000000000000, 1.000000000000000000 ) ) ;
#55248=DIRECTION ( 'NONE',  ( 0.000000000000000000, 0.3738317757009345654, 0.9274965247785492695 ) ) ;
#55249=ORIENTED_EDGE ( 'NONE', *, *, #159946, .F. ) ;
#55250=ORIENTED_EDGE ( 'NONE', *, *, #159496, .T. ) ;
#55280=DIRECTION ( 'NONE',  ( 1.000000000000000000, -0.000000000000000000, -0.000000000000000000 ) ) ;
#55287=CIRCLE ( 'NONE', #30399, 11.89999999999999325 ) ;
#55310=CARTESIAN_POINT ( 'NONE',  ( -23.15000000000000213, 1.115600667400684642E-11, -55.19999999999999574 ) ) ;
#55322=DIRECTION ( 'NONE',  ( 0.000000000000000000, 5.329070518200807403E-15, -1.000000000000000000 ) ) ;
#55352=VERTEX_POINT ( 'NONE', #185001 ) ;
#55390=DIRECTION ( 'NONE',  ( -1.000000000000000000, 0.000000000000000000, 0.000000000000000000 ) ) ;
#55402=VERTEX_POINT ( 'NONE', #172861 ) ;
#55410=CARTESIAN_POINT ( 'NONE',  ( -18.50000000000000000, 11.65000000001115232, -54.85000000000000142 ) ) ;
#55426=CARTESIAN_POINT ( 'NONE',  ( -20.54999999999999716, -11.74999999998884626, -45.85000000000000853 ) ) ;
#55452=EDGE_CURVE ( 'NONE', #173035, #126285, #184969, .T. ) ;
#55459=FACE_OUTER_BOUND ( 'NONE', #244039, .T. ) ;
#55475=EDGE_CURVE ( 'NONE', #135639, #127734, #126707, .T. ) ;
#55493=CARTESIAN_POINT ( 'NONE',  ( 19.75857864376269646, 11.65000000001116476, -58.25000000000000000 ) ) ;
#55517=TOROIDAL_SURFACE ( 'NONE', #5466, 11.65000000000000036, 0.1000000000000000056 ) ;
#55518=VERTEX_POINT ( 'NONE', #39749 ) ;
#55538=AXIS2_PLACEMENT_3D ( 'NONE', #29060, #228518, #48576 ) ;
#55550=ORIENTED_EDGE ( 'NONE', *, *, #203848, .F. ) ;
#55554=ORIENTED_EDGE ( 'NONE', *, *, #194000, .T. ) ;
#55583=DIRECTION ( 'NONE',  ( -1.000000000000000000, 0.000000000000000000, 0.000000000000000000 ) ) ;
#55584=CIRCLE ( 'NONE', #18026, 0.1000000000000028644 ) ;
#55585=CARTESIAN_POINT ( 'NONE',  ( 18.45068634130097252, -9.486506073331602451, -40.56877843116809856 ) ) ;
#55603=ADVANCED_FACE ( 'NONE', ( #143943 ), #64171, .T. ) ;
#55626=ADVANCED_FACE ( 'NONE', ( #125670 ), #239086, .T. ) ;
#55630=LINE ( 'NONE', #120806, #126693 ) ;
#55674=ORIENTED_EDGE ( 'NONE', *, *, #235803, .F. ) ;
#55683=CARTESIAN_POINT ( 'NONE',  ( -20.96428641294228612, 11.75000000001149125, -60.17489317794078119 ) ) ;
#55721=EDGE_CURVE ( 'NONE', #175831, #165098, #160966, .T. ) ;
#55727=AXIS2_PLACEMENT_3D ( 'NONE', #149647, #224013, #50495 ) ;
#55732=VECTOR ( 'NONE', #220528, 1000.000000000000000 ) ;
#55742=DIRECTION ( 'NONE',  ( -0.000000000000000000, 0.9876197685951276783, 0.1568667991644721316 ) ) ;
#55766=ORIENTED_EDGE ( 'NONE', *, *, #74976, .F. ) ;
#55772=CIRCLE ( 'NONE', #109976, 11.65000000000000036 ) ;
#55775=ORIENTED_EDGE ( 'NONE', *, *, #84104, .F. ) ;
#55778=EDGE_CURVE ( 'NONE', #100761, #168461, #33050, .T. ) ;
#55785=DIRECTION ( 'NONE',  ( -1.000000000000000000, -0.000000000000000000, -0.000000000000000000 ) ) ;
#55809=EDGE_CURVE ( 'NONE', #201418, #89935, #247689, .T. ) ;
#55827=CARTESIAN_POINT ( 'NONE',  ( -21.05000000000000071, 5.850000000011108092, -43.63249722427796939 ) ) ;
#55828=VERTEX_POINT ( 'NONE', #98069 ) ;
#55832=EDGE_CURVE ( 'NONE', #64423, #16861, #218027, .T. ) ;
#55840=FACE_OUTER_BOUND ( 'NONE', #113637, .T. ) ;
#55853=PLANE ( 'NONE',  #230412 ) ;
#55883=DIRECTION ( 'NONE',  ( -1.000000000000000000, -0.000000000000000000, 0.000000000000000000 ) ) ;
#55908=ORIENTED_EDGE ( 'NONE', *, *, #257450, .F. ) ;
#55964=LINE ( 'NONE', #54702, #234646 ) ;
#55990=ORIENTED_EDGE ( 'NONE', *, *, #62928, .T. ) ;
#56010=DIRECTION ( 'NONE',  ( 1.000000000000000000, -0.000000000000000000, -0.000000000000000000 ) ) ;
#56013=CARTESIAN_POINT ( 'NONE',  ( -20.64999999999999858, -9.399999999988846611, -57.10603087734755690 ) ) ;
#56023=EDGE_CURVE ( 'NONE', #228463, #35453, #201896, .T. ) ;
#56055=DIRECTION ( 'NONE',  ( 0.000000000000000000, 0.000000000000000000, -1.000000000000000000 ) ) ;
#56069=DIRECTION ( 'NONE',  ( 0.7071067811865388020, -0.7071067811865561215, 0.000000000000000000 ) ) ;
#56078=ORIENTED_EDGE ( 'NONE', *, *, #79457, .F. ) ;
#56091=AXIS2_PLACEMENT_3D ( 'NONE', #14215, #190273, #250233 ) ;
#56105=EDGE_CURVE ( 'NONE', #253318, #14640, #210113, .T. ) ;
#56116=CIRCLE ( 'NONE', #64516, 0.09999999999999939493 ) ;
#56147=VECTOR ( 'NONE', #34036, 1000.000000000000000 ) ;
#56158=CARTESIAN_POINT ( 'NONE',  ( 18.48197441911643324, -9.517954794694091447, -73.89021164220768867 ) ) ;
#56164=DIRECTION ( 'NONE',  ( 0.000000000000000000, 0.000000000000000000, -1.000000000000000000 ) ) ;
#56170=DIRECTION ( 'NONE',  ( 1.000000000000000000, 0.000000000000000000, 0.000000000000000000 ) ) ;
#56231=( BOUNDED_SURFACE ( )  B_SPLINE_SURFACE ( 3, 2, ( 
 ( #213508, #54435, #15341 ),
 ( #74043, #55683, #152286 ),
 ( #32346, #51850, #170596 ),
 ( #250080, #193969, #150983 ),
 ( #190112, #33648, #11481 ),
 ( #71464, #230523, #251348 ) ),
 .UNSPECIFIED., .F., .F., .F. ) 
 B_SPLINE_SURFACE_WITH_KNOTS ( ( 4, 2, 4 ),
 ( 3, 3 ),
 ( 1.570796326794897668, 2.356194490192346169, 3.141592653589794448 ),
 ( 0.000000000000000000, 1.000000000000000000 ),
 .UNSPECIFIED. ) 
 GEOMETRIC_REPRESENTATION_ITEM ( )  RATIONAL_B_SPLINE_SURFACE ( (
 ( 1.000000000000000000, 0.7071067811865597852, 1.000000000000000000),
 ( 1.000000000000000000, 0.6611148371776427446, 1.000000000000000000),
 ( 1.000000000000000000, 0.6092287576699335627, 1.000000000000000000),
 ( 1.000000000000000000, 0.5278258667054436248, 1.000000000000000000),
 ( 1.000000000000000000, 0.4993418825336356504, 1.000000000000000000),
 ( 1.000000000000000000, 0.4999999999999960587, 1.000000000000000000) ) ) 
 REPRESENTATION_ITEM ( '' )  SURFACE ( )  );
#56241=CARTESIAN_POINT ( 'NONE',  ( 21.05000000000000071, 1.115600667400684642E-11, -29.19999999999996732 ) ) ;
#56243=EDGE_CURVE ( 'NONE', #127278, #27329, #218633, .T. ) ;
#56247=ORIENTED_EDGE ( 'NONE', *, *, #110331, .T. ) ;
#56258=EDGE_CURVE ( 'NONE', #213775, #237327, #164496, .T. ) ;
#56267=ORIENTED_EDGE ( 'NONE', *, *, #257941, .T. ) ;
#56303=DIRECTION ( 'NONE',  ( 1.000000000000000000, 0.000000000000000000, 0.000000000000000000 ) ) ;
#56313=CARTESIAN_POINT ( 'NONE',  ( 20.94999999999999929, 1.115600667400684642E-11, -67.00000000000000000 ) ) ;
#56351=CARTESIAN_POINT ( 'NONE',  ( 20.94999999999999574, 1.162701749949165642, -41.40000000000000568 ) ) ;
#56359=EDGE_LOOP ( 'NONE', ( #212880, #145028, #227056, #215647 ) ) ;
#56382=DIRECTION ( 'NONE',  ( 1.000000000000000000, 0.000000000000000000, 0.000000000000000000 ) ) ;
#56396=DIRECTION ( 'NONE',  ( 0.000000000000000000, 0.000000000000000000, -1.000000000000000000 ) ) ;
#56408=EDGE_CURVE ( 'NONE', #135166, #202789, #29332, .T. ) ;
#56420=EDGE_LOOP ( 'NONE', ( #19271, #183801, #183093, #164249 ) ) ;
#56428=CYLINDRICAL_SURFACE ( 'NONE', #128805, 0.09999999999999939493 ) ;
#56471=CARTESIAN_POINT ( 'NONE',  ( -22.50485643085239928, -0.07878633906603055292, -21.75020506082759653 ) ) ;
#56480=CARTESIAN_POINT ( 'NONE',  ( 21.05000000000000071, 6.258847123090218290, -33.46824164694449877 ) ) ;
#56499=CIRCLE ( 'NONE', #223122, 0.1000000000000000472 ) ;
#56506=DIRECTION ( 'NONE',  ( 1.000000000000000000, 0.000000000000000000, 0.000000000000000000 ) ) ;
#56524=FACE_OUTER_BOUND ( 'NONE', #147970, .T. ) ;
#56533=ORIENTED_EDGE ( 'NONE', *, *, #79664, .T. ) ;
#56534=CARTESIAN_POINT ( 'NONE',  ( 21.05000000000000071, 4.850467289730776344, -54.96573259099832143 ) ) ;
#56545=CARTESIAN_POINT ( 'NONE',  ( -21.14999999999999858, -11.64999999998884483, -36.39999999999999858 ) ) ;
#56559=DIRECTION ( 'NONE',  ( 0.000000000000000000, 0.000000000000000000, -1.000000000000000000 ) ) ;
#56575=CARTESIAN_POINT ( 'NONE',  ( -18.59999999999999787, -1.687074390080403941, -20.68542703345834965 ) ) ;
#56594=AXIS2_PLACEMENT_3D ( 'NONE', #78233, #237326, #108088 ) ;
#56605=DIRECTION ( 'NONE',  ( -0.000000000000000000, 1.000000000000000000, -0.000000000000000000 ) ) ;
#56620=FACE_OUTER_BOUND ( 'NONE', #133201, .T. ) ;
#56624=AXIS2_PLACEMENT_3D ( 'NONE', #37000, #156947, #136043 ) ;
#56647=ORIENTED_EDGE ( 'NONE', *, *, #103038, .T. ) ;
#56658=CARTESIAN_POINT ( 'NONE',  ( -20.94999999999999929, 11.70000000001115126, -60.24500185048138690 ) ) ;
#56660=EDGE_CURVE ( 'NONE', #11590, #217175, #115249, .T. ) ;
#56686=DIRECTION ( 'NONE',  ( -1.000000000000000000, -2.952720810173289112E-16, 0.000000000000000000 ) ) ;
#56715=FACE_OUTER_BOUND ( 'NONE', #145978, .T. ) ;
#56723=ORIENTED_EDGE ( 'NONE', *, *, #244451, .F. ) ;
#56742=CYLINDRICAL_SURFACE ( 'NONE', #188967, 0.09999999999999939493 ) ;
#56744=CARTESIAN_POINT ( 'NONE',  ( 21.05000000000000071, 8.776282895303630482, -42.05862899514094977 ) ) ;
#56746=EDGE_CURVE ( 'NONE', #138742, #104053, #69013, .T. ) ;
#56761=CIRCLE ( 'NONE', #102558, 7.720710678118663850 ) ;
#56763=ADVANCED_FACE ( 'NONE', ( #135451 ), #233310, .F. ) ;
#56788=ORIENTED_EDGE ( 'NONE', *, *, #94184, .F. ) ;
#56810=DIRECTION ( 'NONE',  ( 0.000000000000000000, -0.5907332058517320572, 0.8068669527896995541 ) ) ;
#56816=CIRCLE ( 'NONE', #86039, 11.90000000000000391 ) ;
#56820=CARTESIAN_POINT ( 'NONE',  ( 18.59999999999999076, 1.835341550235567887, -45.05515129256298223 ) ) ;
#56822=AXIS2_PLACEMENT_3D ( 'NONE', #191044, #51471, #54064 ) ;
#56844=EDGE_CURVE ( 'NONE', #113969, #248271, #248050, .T. ) ;
#56851=DIRECTION ( 'NONE',  ( 0.000000000000000000, 1.000000000000000000, 0.000000000000000000 ) ) ;
#56877=EDGE_CURVE ( 'NONE', #30860, #207476, #231499, .T. ) ;
#56886=EDGE_CURVE ( 'NONE', #52785, #100962, #119066, .T. ) ;
#56917=AXIS2_PLACEMENT_3D ( 'NONE', #10439, #229487, #166977 ) ;
#56923=EDGE_CURVE ( 'NONE', #67212, #224490, #202448, .T. ) ;
#56932=SHAPE_REPRESENTATION_RELATIONSHIP ( 'NONE' , 'NONE' ,  #45219, #228621 ) ;
#56942=LINE ( 'NONE', #233076, #200712 ) ;
#56971=ORIENTED_EDGE ( 'NONE', *, *, #61310, .T. ) ;
#57018=DIRECTION ( 'NONE',  ( 1.000000000000000000, -0.000000000000000000, -0.000000000000000000 ) ) ;
#57057=CARTESIAN_POINT ( 'NONE',  ( 23.15000000000000213, -11.74999999998883560, -63.89999999999999858 ) ) ;
#57069=EDGE_CURVE ( 'NONE', #209893, #110094, #235752, .T. ) ;
#57080=EDGE_CURVE ( 'NONE', #139128, #51091, #39972, .T. ) ;
#57081=DIRECTION ( 'NONE',  ( -1.000000000000000000, 0.000000000000000000, 0.000000000000000000 ) ) ;
#57122=ORIENTED_EDGE ( 'NONE', *, *, #253432, .T. ) ;
#57160=DIRECTION ( 'NONE',  ( 0.000000000000000000, 0.000000000000000000, 1.000000000000000000 ) ) ;
#57187=DIRECTION ( 'NONE',  ( 0.000000000000000000, 0.000000000000000000, -1.000000000000000000 ) ) ;
#57190=LINE ( 'NONE', #96322, #122444 ) ;
#57195=VERTEX_POINT ( 'NONE', #53046 ) ;
#57197=DIRECTION ( 'NONE',  ( 1.000000000000000000, 0.000000000000000000, 0.000000000000000000 ) ) ;
#57243=VERTEX_POINT ( 'NONE', #94739 ) ;
#57289=ORIENTED_EDGE ( 'NONE', *, *, #156021, .T. ) ;
#57300=DIRECTION ( 'NONE',  ( 0.000000000000000000, 0.000000000000000000, 1.000000000000000000 ) ) ;
#57310=AXIS2_PLACEMENT_3D ( 'NONE', #124300, #159572, #99559 ) ;
#57321=DIRECTION ( 'NONE',  ( -2.578261006436900068E-14, 0.1350103645451904977, -0.9908441862701597991 ) ) ;
#57329=VECTOR ( 'NONE', #219093, 1000.000000000000000 ) ;
#57336=ORIENTED_EDGE ( 'NONE', *, *, #160720, .T. ) ;
#57342=DIRECTION ( 'NONE',  ( -1.000000000000000000, 0.000000000000000000, 0.000000000000000000 ) ) ;
#57364=DIRECTION ( 'NONE',  ( 0.000000000000000000, 0.000000000000000000, 1.000000000000000000 ) ) ;
#57373=EDGE_CURVE ( 'NONE', #217175, #55402, #190168, .T. ) ;
#57386=DIRECTION ( 'NONE',  ( 1.000000000000000000, -0.000000000000000000, -0.000000000000000000 ) ) ;
#57387=AXIS2_PLACEMENT_3D ( 'NONE', #5913, #224959, #62067 ) ;
#57430=ORIENTED_EDGE ( 'NONE', *, *, #188916, .T. ) ;
#57448=ORIENTED_EDGE ( 'NONE', *, *, #56258, .F. ) ;
#57450=CARTESIAN_POINT ( 'NONE',  ( -22.16821283564876666, 7.558973340791935058, -33.50000000000000000 ) ) ;
#57457=DIRECTION ( 'NONE',  ( 0.000000000000000000, 0.000000000000000000, 1.000000000000000000 ) ) ;
#57483=CIRCLE ( 'NONE', #74111, 0.09999999999999939493 ) ;
#57502=AXIS2_PLACEMENT_3D ( 'NONE', #133418, #124750, #34343 ) ;
#57507=CIRCLE ( 'NONE', #120107, 0.1000000000000028644 ) ;
#57549=CIRCLE ( 'NONE', #115833, 0.09999999999999939493 ) ;
#57571=AXIS2_PLACEMENT_3D ( 'NONE', #149923, #130322, #31278 ) ;
#57603=CARTESIAN_POINT ( 'NONE',  ( 20.94999999999999929, 8.776282895303632259, -45.65000000000000568 ) ) ;
#57649=TOROIDAL_SURFACE ( 'NONE', #24369, 0.6000000000000017542, 0.1000000000000000056 ) ;
#57666=AXIS2_PLACEMENT_3D ( 'NONE', #254989, #76405, #157271 ) ;
#57667=AXIS2_PLACEMENT_3D ( 'NONE', #77181, #215412, #135858 ) ;
#57675=CARTESIAN_POINT ( 'NONE',  ( 20.84999999999999432, -1.164121893230052995, -74.91484808557160591 ) ) ;
#57694=DIRECTION ( 'NONE',  ( -1.000000000000000000, -2.952720810173289112E-16, 0.000000000000000000 ) ) ;
#57738=CARTESIAN_POINT ( 'NONE',  ( -23.15000000000000213, 11.60000000001115517, -60.07179676972450011 ) ) ;
#57790=AXIS2_PLACEMENT_3D ( 'NONE', #225983, #163482, #104752 ) ;
#57792=ORIENTED_EDGE ( 'NONE', *, *, #203808, .F. ) ;
#57796=ORIENTED_EDGE ( 'NONE', *, *, #159730, .F. ) ;
#57807=AXIS2_PLACEMENT_3D ( 'NONE', #257827, #200482, #255260 ) ;
#57817=CARTESIAN_POINT ( 'NONE',  ( -18.59999999999999787, 9.150000000011157653, -21.75000000000000355 ) ) ;
#57834=ORIENTED_EDGE ( 'NONE', *, *, #23072, .T. ) ;
#57859=DIRECTION ( 'NONE',  ( -1.000000000000000000, -1.836970198721029934E-16, 0.000000000000000000 ) ) ;
#57873=EDGE_CURVE ( 'NONE', #142401, #21983, #73654, .T. ) ;
#57937=PLANE ( 'NONE',  #137533 ) ;
#57962=CIRCLE ( 'NONE', #3826, 2.000000000000002665 ) ;
#57986=FACE_OUTER_BOUND ( 'NONE', #205361, .T. ) ;
#58015=CIRCLE ( 'NONE', #253838, 0.1000000000000028644 ) ;
#58022=DIRECTION ( 'NONE',  ( 0.000000000000000000, 0.000000000000000000, -1.000000000000000000 ) ) ;
#58034=EDGE_CURVE ( 'NONE', #253110, #200640, #77590, .T. ) ;
#58052=CARTESIAN_POINT ( 'NONE',  ( 21.06277459767431992, 8.872862438279399910, -45.70399919235632069 ) ) ;
#58111=ORIENTED_EDGE ( 'NONE', *, *, #164378, .F. ) ;
#58146=ORIENTED_EDGE ( 'NONE', *, *, #56660, .T. ) ;
#58154=CARTESIAN_POINT ( 'NONE',  ( -18.59999999999999787, 1.261786168576181755, -41.58649896354548048 ) ) ;
#58181=ORIENTED_EDGE ( 'NONE', *, *, #61408, .F. ) ;
#58224=EDGE_LOOP ( 'NONE', ( #57336, #210919, #155205, #69408 ) ) ;
#58225=VECTOR ( 'NONE', #234030, 1000.000000000000000 ) ;
#58267=ORIENTED_EDGE ( 'NONE', *, *, #41505, .T. ) ;
#58283=ORIENTED_EDGE ( 'NONE', *, *, #257107, .T. ) ;
#58310=CARTESIAN_POINT ( 'NONE',  ( -20.54999999999999716, -8.999999999988844479, -57.10603087734755690 ) ) ;
#58326=DIRECTION ( 'NONE',  ( 1.000000000000000000, -0.000000000000000000, -0.000000000000000000 ) ) ;
#58328=AXIS2_PLACEMENT_3D ( 'NONE', #119189, #494, #208986 ) ;
#58362=LINE ( 'NONE', #154958, #42987 ) ;
#58399=VERTEX_POINT ( 'NONE', #28782 ) ;
#58417=DIRECTION ( 'NONE',  ( 0.000000000000000000, 0.1350103645451876666, -0.9908441862701600211 ) ) ;
#58421=VECTOR ( 'NONE', #4067, 1000.000000000000000 ) ;
#58456=ORIENTED_EDGE ( 'NONE', *, *, #50521, .T. ) ;
#58483=CARTESIAN_POINT ( 'NONE',  ( -23.25000000000000000, -0.1008583690875562017, -21.75043287651061164 ) ) ;
#58492=ADVANCED_FACE ( 'NONE', ( #42510 ), #192629, .T. ) ;
#58521=CIRCLE ( 'NONE', #100016, 0.09999999999999939493 ) ;
#58574=CARTESIAN_POINT ( 'NONE',  ( -21.03922262424672951, 11.62390063401586460, -40.35920804289344233 ) ) ;
#58618=CYLINDRICAL_SURFACE ( 'NONE', #113679, 0.09999999999999781286 ) ;
#58620=CARTESIAN_POINT ( 'NONE',  ( 20.94999999999999929, 10.72371710471867701, -54.75000000000000000 ) ) ;
#58643=DIRECTION ( 'NONE',  ( -1.000000000000000000, 0.000000000000000000, 0.000000000000000000 ) ) ;
#58653=DIRECTION ( 'NONE',  ( 1.000000000000000000, -0.000000000000000000, -0.000000000000000000 ) ) ;
#58666=CARTESIAN_POINT ( 'NONE',  ( 23.24999999999999289, 11.65000000001116298, -45.65000000000000568 ) ) ;
#58670=ORIENTED_EDGE ( 'NONE', *, *, #53724, .F. ) ;
#58675=CARTESIAN_POINT ( 'NONE',  ( 21.04999999999999716, -0.08561306079281309767, -27.08624026618970859 ) ) ;
#58679=CARTESIAN_POINT ( 'NONE',  ( -21.65000000000000213, 7.708578643773852157, -45.75000000000000000 ) ) ;
#58689=ORIENTED_EDGE ( 'NONE', *, *, #37856, .F. ) ;
#58693=CARTESIAN_POINT ( 'NONE',  ( -23.15000000000000213, 2.000000000011154189, -46.22462192276210402 ) ) ;
#58701=ADVANCED_FACE ( 'NONE', ( #34534 ), #72372, .T. ) ;
#58704=DIRECTION ( 'NONE',  ( 0.000000000000000000, 0.000000000000000000, -1.000000000000000000 ) ) ;
#58717=CARTESIAN_POINT ( 'NONE',  ( -21.08884785362073089, 0.04978309507788075683, -27.14280663257438420 ) ) ;
#58732=ORIENTED_EDGE ( 'NONE', *, *, #14692, .T. ) ;
#58742=EDGE_CURVE ( 'NONE', #208213, #2508, #177526, .T. ) ;
#58758=EDGE_LOOP ( 'NONE', ( #55250, #132871, #186621, #74923 ) ) ;
#58762=AXIS2_PLACEMENT_3D ( 'NONE', #100413, #138259, #1318 ) ;
#58766=CIRCLE ( 'NONE', #175347, 0.1000000000000028644 ) ;
#58781=CARTESIAN_POINT ( 'NONE',  ( 18.59999999999997655, -1.164121893230052995, -74.91484808557160591 ) ) ;
#58783=AXIS2_PLACEMENT_3D ( 'NONE', #251502, #247663, #72911 ) ;
#58792=FACE_OUTER_BOUND ( 'NONE', #241326, .T. ) ;
#58798=ORIENTED_EDGE ( 'NONE', *, *, #188916, .F. ) ;
#58867=ORIENTED_EDGE ( 'NONE', *, *, #64439, .F. ) ;
#58900=CARTESIAN_POINT ( 'NONE',  ( 23.15000000000000213, -8.663551401858002876, -43.02410111806730697 ) ) ;
#58938=DIRECTION ( 'NONE',  ( 0.000000000000000000, 0.000000000000000000, 1.000000000000000000 ) ) ;
#58947=CARTESIAN_POINT ( 'NONE',  ( -20.54999999999999716, 1.940186915899009490, -46.32911921105333164 ) ) ;
#58954=LINE ( 'NONE', #138494, #138770 ) ;
#58984=AXIS2_PLACEMENT_3D ( 'NONE', #134550, #35511, #215388 ) ;
#58985=CARTESIAN_POINT ( 'NONE',  ( -20.94999999999999929, -11.64999999998884306, -63.89999999999999858 ) ) ;
#59055=EDGE_CURVE ( 'NONE', #232170, #7325, #72066, .T. ) ;
#59056=DIRECTION ( 'NONE',  ( 0.000000000000000000, 1.000000000000000000, 2.891205793294679805E-16 ) ) ;
#59067=ORIENTED_EDGE ( 'NONE', *, *, #203394, .T. ) ;
#59079=CYLINDRICAL_SURFACE ( 'NONE', #105624, 0.1000000000000028644 ) ;
#59144=DIRECTION ( 'NONE',  ( 1.000000000000000000, 0.000000000000000000, 0.000000000000000000 ) ) ;
#59206=FACE_OUTER_BOUND ( 'NONE', #205100, .T. ) ;
#59209=DIRECTION ( 'NONE',  ( 0.000000000000000000, 0.000000000000000000, 1.000000000000000000 ) ) ;
#59229=ORIENTED_EDGE ( 'NONE', *, *, #22375, .T. ) ;
#59234=ADVANCED_FACE ( 'NONE', ( #178898 ), #1492, .F. ) ;
#59285=ORIENTED_EDGE ( 'NONE', *, *, #141402, .F. ) ;
#59302=DIRECTION ( 'NONE',  ( 1.000000000000000000, 0.000000000000000000, 0.000000000000000000 ) ) ;
#59317=EDGE_CURVE ( 'NONE', #204714, #143764, #135857, .T. ) ;
#59340=DIRECTION ( 'NONE',  ( -0.000000000000000000, -0.000000000000000000, 1.000000000000000000 ) ) ;
#59355=CARTESIAN_POINT ( 'NONE',  ( 21.14999999999999858, 6.650000000011155876, -45.65000000000000568 ) ) ;
#59426=CARTESIAN_POINT ( 'NONE',  ( 23.24999999999999645, 1.115600667400684642E-11, -67.00000000000000000 ) ) ;
#59440=AXIS2_PLACEMENT_3D ( 'NONE', #131975, #214084, #36769 ) ;
#59442=EDGE_LOOP ( 'NONE', ( #169777, #217705, #255809, #246185 ) ) ;
#59468=ADVANCED_FACE ( 'NONE', ( #172185 ), #60860, .F. ) ;
#59472=DIRECTION ( 'NONE',  ( 1.000000000000000000, 2.952720810173289112E-16, -0.000000000000000000 ) ) ;
#59475=CARTESIAN_POINT ( 'NONE',  ( 21.02374657821572868, 11.60000000083170413, -60.07179677019824027 ) ) ;
#59478=CARTESIAN_POINT ( 'NONE',  ( 18.59999999999999076, -1.249999999988843369, -41.50000000000000000 ) ) ;
#59503=AXIS2_PLACEMENT_3D ( 'NONE', #7787, #6482, #49472 ) ;
#59524=ORIENTED_EDGE ( 'NONE', *, *, #99413, .F. ) ;
#59566=CIRCLE ( 'NONE', #134410, 0.1000000000000028644 ) ;
#59588=DIRECTION ( 'NONE',  ( 1.000000000000000000, 3.265361837132813093E-16, -0.000000000000000000 ) ) ;
#59617=CARTESIAN_POINT ( 'NONE',  ( 20.22483756094572271, 9.501904678882469923, -41.63953912871468788 ) ) ;
#59647=CARTESIAN_POINT ( 'NONE',  ( -18.48550754432022103, -9.463399778548794217, -40.54878975241538797 ) ) ;
#59739=AXIS2_PLACEMENT_3D ( 'NONE', #251952, #77163, #152892 ) ;
#59764=ORIENTED_EDGE ( 'NONE', *, *, #31496, .T. ) ;
#59765=CARTESIAN_POINT ( 'NONE',  ( 21.05000000000000071, 1.162701749949165642, -41.40000000000000568 ) ) ;
#59776=ORIENTED_EDGE ( 'NONE', *, *, #117730, .T. ) ;
#59783=DIRECTION ( 'NONE',  ( -1.000000000000000000, 0.000000000000000000, 0.000000000000000000 ) ) ;
#59794=AXIS2_PLACEMENT_3D ( 'NONE', #64782, #140463, #220012 ) ;
#59805=ORIENTED_EDGE ( 'NONE', *, *, #36691, .T. ) ;
#59824=AXIS2_PLACEMENT_3D ( 'NONE', #148518, #186366, #66409 ) ;
#59852=CARTESIAN_POINT ( 'NONE',  ( -20.95613430942416144, 11.75000000001115907, -40.35716264822026744 ) ) ;
#59874=CARTESIAN_POINT ( 'NONE',  ( 20.95539060131842746, 10.62386215766680131, -41.15373381365618854 ) ) ;
#59884=CARTESIAN_POINT ( 'NONE',  ( 22.45301702632625762, 0.01521087972134078925, -21.85020777573961226 ) ) ;
#59901=DIRECTION ( 'NONE',  ( 1.000000000000000000, 0.000000000000000000, 0.000000000000000000 ) ) ;
#59940=CARTESIAN_POINT ( 'NONE',  ( -23.15000000000000213, 2.000000000011154189, -53.77537807723790309 ) ) ;
#60023=DIRECTION ( 'NONE',  ( 1.000000000000000000, -0.000000000000000000, 0.000000000000000000 ) ) ;
#60045=ORIENTED_EDGE ( 'NONE', *, *, #153479, .F. ) ;
#60121=DIRECTION ( 'NONE',  ( -1.000000000000000000, -0.000000000000000000, -0.000000000000000000 ) ) ;
#60172=DIRECTION ( 'NONE',  ( 0.000000000000000000, -1.000000000000000000, 0.000000000000000000 ) ) ;
#60198=AXIS2_PLACEMENT_3D ( 'NONE', #97849, #118750, #103002 ) ;
#60221=EDGE_CURVE ( 'NONE', #73682, #184556, #46321, .T. ) ;
#60229=CARTESIAN_POINT ( 'NONE',  ( -18.59999999999999787, -1.835341550213255957, -45.05515129256298223 ) ) ;
#60287=DIRECTION ( 'NONE',  ( 0.000000000000000000, 0.000000000000000000, -1.000000000000000000 ) ) ;
#60301=FACE_OUTER_BOUND ( 'NONE', #222223, .T. ) ;
#60303=EDGE_CURVE ( 'NONE', #1348, #201739, #121214, .T. ) ;
#60304=CARTESIAN_POINT ( 'NONE',  ( -23.15000000000000213, 1.115649653272650466E-11, -71.00000000000001421 ) ) ;
#60312=AXIS2_PLACEMENT_3D ( 'NONE', #174113, #51516, #33312 ) ;
#60317=EDGE_CURVE ( 'NONE', #121164, #156961, #104743, .T. ) ;
#60323=AXIS2_PLACEMENT_3D ( 'NONE', #31005, #192613, #191356 ) ;
#60326=AXIS2_PLACEMENT_3D ( 'NONE', #161757, #23544, #83443 ) ;
#60327=ORIENTED_EDGE ( 'NONE', *, *, #4800, .T. ) ;
#60369=VERTEX_POINT ( 'NONE', #240852 ) ;
#60370=FACE_OUTER_BOUND ( 'NONE', #172383, .T. ) ;
#60409=DIRECTION ( 'NONE',  ( 0.000000000000000000, 0.000000000000000000, -1.000000000000000000 ) ) ;
#60419=ORIENTED_EDGE ( 'NONE', *, *, #122687, .T. ) ;
#60422=ORIENTED_EDGE ( 'NONE', *, *, #231976, .F. ) ;
#60453=CYLINDRICAL_SURFACE ( 'NONE', #223682, 0.1000000000000028644 ) ;
#60544=EDGE_CURVE ( 'NONE', #126699, #216204, #217190, .T. ) ;
#60552=FACE_BOUND ( 'NONE', #6866, .T. ) ;
#60574=AXIS2_PLACEMENT_3D ( 'NONE', #151302, #15656, #131718 ) ;
#60577=CYLINDRICAL_SURFACE ( 'NONE', #201493, 0.09999999999999939493 ) ;
#60584=DIRECTION ( 'NONE',  ( -1.000000000000000000, -0.000000000000000000, -0.000000000000000000 ) ) ;
#60592=CARTESIAN_POINT ( 'NONE',  ( -21.13422380239059706, 1.115527483754041871E-11, -27.00667348519442612 ) ) ;
#60595=AXIS2_PLACEMENT_3D ( 'NONE', #32556, #92480, #251554 ) ;
#60654=ORIENTED_EDGE ( 'NONE', *, *, #108537, .T. ) ;
#60690=AXIS2_PLACEMENT_3D ( 'NONE', #43021, #83387, #120016 ) ;
#60691=VECTOR ( 'NONE', #48461, 1000.000000000000000 ) ;
#60693=CARTESIAN_POINT ( 'NONE',  ( 23.24999999999999645, -2.099999999988846344, -67.00000000000000000 ) ) ;
#60700=ORIENTED_EDGE ( 'NONE', *, *, #208004, .T. ) ;
#60708=DIRECTION ( 'NONE',  ( -0.000000000000000000, -0.000000000000000000, -1.000000000000000000 ) ) ;
#60738=DIRECTION ( 'NONE',  ( -1.000000000000000000, 0.000000000000000000, 0.000000000000000000 ) ) ;
#60770=AXIS2_PLACEMENT_3D ( 'NONE', #181028, #81871, #20675 ) ;
#60790=DIRECTION ( 'NONE',  ( 0.000000000000000000, 1.897661533703519897E-16, -1.000000000000000000 ) ) ;
#60857=AXIS2_PLACEMENT_3D ( 'NONE', #61870, #100933, #141391 ) ;
#60859=ORIENTED_EDGE ( 'NONE', *, *, #113628, .T. ) ;
#60860=( BOUNDED_SURFACE ( )  B_SPLINE_SURFACE ( 3, 2, ( 
 ( #92580, #229553, #31382 ),
 ( #11806, #113442, #173479 ),
 ( #131723, #133021, #32671 ),
 ( #212561, #192992, #14374 ) ),
 .UNSPECIFIED., .F., .F., .F. ) 
 B_SPLINE_SURFACE_WITH_KNOTS ( ( 4, 4 ),
 ( 3, 3 ),
 ( 0.04058434257139457990, 0.04256401539001584966 ),
 ( 0.000000000000000000, 1.000000000000000000 ),
 .UNSPECIFIED. ) 
 GEOMETRIC_REPRESENTATION_ITEM ( )  RATIONAL_B_SPLINE_SURFACE ( (
 ( 1.000000000000000000, 0.7103081912008052390, 1.000000000000000000),
 ( 1.000000000000000000, 0.7104998333555472279, 1.000000000000000000),
 ( 1.000000000000000000, 0.7107238315755474156, 1.000000000000000000),
 ( 1.000000000000000000, 0.7110073749539291832, 1.000000000000000000) ) ) 
 REPRESENTATION_ITEM ( '' )  SURFACE ( )  );
#60890=AXIS2_PLACEMENT_3D ( 'NONE', #239623, #63529, #120980 ) ;
#60940=ORIENTED_EDGE ( 'NONE', *, *, #189861, .F. ) ;
#60953=CARTESIAN_POINT ( 'NONE',  ( -18.43473496883417084, -9.494952410988139135, -40.54587157222824345 ) ) ;
#60994=EDGE_CURVE ( 'NONE', #91127, #200635, #173896, .T. ) ;
#61003=VERTEX_POINT ( 'NONE', #113872 ) ;
#61027=FACE_OUTER_BOUND ( 'NONE', #158404, .T. ) ;
#61032=AXIS2_PLACEMENT_3D ( 'NONE', #161645, #142046, #44249 ) ;
#61068=ORIENTED_EDGE ( 'NONE', *, *, #152796, .F. ) ;
#61099=CARTESIAN_POINT ( 'NONE',  ( -20.54999999999999716, 4.350000000011156054, -45.85000000000000142 ) ) ;
#61105=CARTESIAN_POINT ( 'NONE',  ( -23.25000000000000000, 2.600000000011156054, -46.72462192276210402 ) ) ;
#61108=VERTEX_POINT ( 'NONE', #60304 ) ;
#61118=ORIENTED_EDGE ( 'NONE', *, *, #112693, .T. ) ;
#61131=CARTESIAN_POINT ( 'NONE',  ( -21.05000000000000071, -11.64999999998884483, -33.50000000000000000 ) ) ;
#61138=CARTESIAN_POINT ( 'NONE',  ( 22.32929514600007792, 7.578647565387638174, -33.40092432188608740 ) ) ;
#61157=DIRECTION ( 'NONE',  ( 6.938893903907030216E-14, 0.000000000000000000, 1.000000000000000000 ) ) ;
#61175=CARTESIAN_POINT ( 'NONE',  ( 20.85000000000000142, -1.835859311432481045, -78.50443916879852679 ) ) ;
#61185=CARTESIAN_POINT ( 'NONE',  ( 20.95420533658165141, 10.54586447477073285, -41.06750602069324430 ) ) ;
#61196=CARTESIAN_POINT ( 'NONE',  ( -18.50000000000000000, -1.362429037182155023, -74.88888124792120493 ) ) ;
#61202=CIRCLE ( 'NONE', #206949, 0.6000000000000015321 ) ;
#61206=VERTEX_POINT ( 'NONE', #230629 ) ;
#61216=EDGE_LOOP ( 'NONE', ( #154658, #168750, #111665 ) ) ;
#61239=ORIENTED_EDGE ( 'NONE', *, *, #112263, .F. ) ;
#61310=EDGE_CURVE ( 'NONE', #131237, #88007, #14163, .T. ) ;
#61351=ORIENTED_EDGE ( 'NONE', *, *, #175533, .F. ) ;
#61363=VERTEX_POINT ( 'NONE', #88509 ) ;
#61372=AXIS2_PLACEMENT_3D ( 'NONE', #245087, #134107, #190263 ) ;
#61378=CIRCLE ( 'NONE', #153007, 0.2000000000000000944 ) ;
#61408=EDGE_CURVE ( 'NONE', #253110, #118445, #58362, .T. ) ;
#61429=TOROIDAL_SURFACE ( 'NONE', #207194, 11.90000000000000213, 0.1000000000000000056 ) ;
#61440=CARTESIAN_POINT ( 'NONE',  ( -20.85000000000000142, 0.1610488207298751417, -66.71581015563977246 ) ) ;
#61447=ORIENTED_EDGE ( 'NONE', *, *, #114715, .F. ) ;
#61486=CARTESIAN_POINT ( 'NONE',  ( 20.95512820512820440, 10.62384868372303615, -45.70016201942441825 ) ) ;
#61498=ADVANCED_FACE ( 'NONE', ( #21842 ), #117803, .F. ) ;
#61522=EDGE_CURVE ( 'NONE', #231817, #253110, #192837, .T. ) ;
#61533=DIRECTION ( 'NONE',  ( 1.000000000000000000, 0.000000000000000000, 0.000000000000000000 ) ) ;
#61538=FACE_OUTER_BOUND ( 'NONE', #182205, .T. ) ;
#61544=AXIS2_PLACEMENT_3D ( 'NONE', #83911, #241748, #245611 ) ;
#61551=CARTESIAN_POINT ( 'NONE',  ( -21.05000000000000071, -11.48912529306490349, -36.60000000000000142 ) ) ;
#61569=AXIS2_PLACEMENT_3D ( 'NONE', #166162, #113854, #95571 ) ;
#61710=ORIENTED_EDGE ( 'NONE', *, *, #199134, .T. ) ;
#61711=EDGE_CURVE ( 'NONE', #126560, #107516, #109603, .T. ) ;
#61712=ORIENTED_EDGE ( 'NONE', *, *, #42667, .T. ) ;
#61722=ORIENTED_EDGE ( 'NONE', *, *, #153343, .T. ) ;
#61732=CYLINDRICAL_SURFACE ( 'NONE', #31100, 0.09999999999999939493 ) ;
#61739=CARTESIAN_POINT ( 'NONE',  ( 23.25000000000000000, -11.64999999998883595, -21.75000000000000355 ) ) ;
#61791=AXIS2_PLACEMENT_3D ( 'NONE', #18566, #199790, #236317 ) ;
#61799=CIRCLE ( 'NONE', #78545, 0.09999999999999892308 ) ;
#61821=VERTEX_POINT ( 'NONE', #38529 ) ;
#61825=DIRECTION ( 'NONE',  ( 0.000000000000000000, 0.000000000000000000, 1.000000000000000000 ) ) ;
#61852=DIRECTION ( 'NONE',  ( 1.000000000000000000, 0.000000000000000000, 0.000000000000000000 ) ) ;
#61856=DIRECTION ( 'NONE',  ( -1.000000000000000000, -2.952720810173289112E-16, 0.000000000000000000 ) ) ;
#61870=CARTESIAN_POINT ( 'NONE',  ( 18.59999999999999432, -1.162701749926853712, -41.60000000000000142 ) ) ;
#61973=SPHERICAL_SURFACE ( 'NONE', #255747, 0.1000000000000000056 ) ;
#61978=ORIENTED_EDGE ( 'NONE', *, *, #25227, .F. ) ;
#61994=ORIENTED_EDGE ( 'NONE', *, *, #92709, .F. ) ;
#62039=FACE_OUTER_BOUND ( 'NONE', #253387, .T. ) ;
#62063=CARTESIAN_POINT ( 'NONE',  ( -20.64999999999999858, 7.150000000011155876, -54.65000000000000568 ) ) ;
#62067=DIRECTION ( 'NONE',  ( 0.000000000000000000, 0.000000000000000000, -1.000000000000000000 ) ) ;
#62070=ORIENTED_EDGE ( 'NONE', *, *, #207683, .F. ) ;
#62087=CARTESIAN_POINT ( 'NONE',  ( 20.94999999999999929, 11.63687328911533392, -60.17824078667518961 ) ) ;
#62145=EDGE_LOOP ( 'NONE', ( #122694, #193879, #250915, #2779, #196969 ) ) ;
#62198=CARTESIAN_POINT ( 'NONE',  ( -20.00857864376270001, 9.250000000011157297, -54.75000000000000000 ) ) ;
#62201=DIRECTION ( 'NONE',  ( 0.000000000000000000, 0.000000000000000000, 1.000000000000000000 ) ) ;
#62203=DIRECTION ( 'NONE',  ( -1.000000000000000000, -0.000000000000000000, -0.000000000000000000 ) ) ;
#62214=ADVANCED_FACE ( 'NONE', ( #98159 ), #232604, .T. ) ;
#62241=LINE ( 'NONE', #144307, #158220 ) ;
#62249=CARTESIAN_POINT ( 'NONE',  ( -18.60000000000000142, -9.321008403350132809, -40.73593824907788274 ) ) ;
#62273=CARTESIAN_POINT ( 'NONE',  ( 21.05000000000000071, -0.08559286335111393473, -27.08633726513048856 ) ) ;
#62287=CIRCLE ( 'NONE', #170678, 0.09999999999999939493 ) ;
#62295=AXIS2_PLACEMENT_3D ( 'NONE', #118244, #238174, #211253 ) ;
#62353=ORIENTED_EDGE ( 'NONE', *, *, #167206, .F. ) ;
#62359=FACE_OUTER_BOUND ( 'NONE', #205625, .T. ) ;
#62364=VECTOR ( 'NONE', #58326, 1000.000000000000000 ) ;
#62408=ORIENTED_EDGE ( 'NONE', *, *, #56243, .F. ) ;
#62414=ORIENTED_EDGE ( 'NONE', *, *, #72962, .T. ) ;
#62442=DIRECTION ( 'NONE',  ( -1.000000000000000000, -0.000000000000000000, -0.000000000000000000 ) ) ;
#62453=CIRCLE ( 'NONE', #70846, 0.1000000000000028644 ) ;
#62459=ORIENTED_EDGE ( 'NONE', *, *, #190454, .T. ) ;
#62467=CYLINDRICAL_SURFACE ( 'NONE', #95823, 0.09999999999999939493 ) ;
#62480=CARTESIAN_POINT ( 'NONE',  ( 20.95132126680579887, 10.48994987015794322, -41.07032453843452657 ) ) ;
#62482=EDGE_CURVE ( 'NONE', #46223, #234522, #18396, .T. ) ;
#62486=CIRCLE ( 'NONE', #154102, 0.1000000000000000472 ) ;
#62505=CARTESIAN_POINT ( 'NONE',  ( 22.59999999999999432, 11.74956712350054566, -33.39914163090129762 ) ) ;
#62509=CARTESIAN_POINT ( 'NONE',  ( 20.94999999999999929, 1.835341550235569663, -45.05515129256298223 ) ) ;
#62520=LINE ( 'NONE', #122502, #220200 ) ;
#62521=CARTESIAN_POINT ( 'NONE',  ( -23.15000000000000213, 1.115600667400684642E-11, -33.50000000000000000 ) ) ;
#62541=AXIS2_PLACEMENT_3D ( 'NONE', #136628, #37562, #216167 ) ;
#62591=CYLINDRICAL_SURFACE ( 'NONE', #139583, 0.09999999999999939493 ) ;
#62619=DIRECTION ( 'NONE',  ( 1.000000000000000000, -0.000000000000000000, -0.000000000000000000 ) ) ;
#62622=DIRECTION ( 'NONE',  ( 1.000000000000000000, 0.000000000000000000, 0.000000000000000000 ) ) ;
#62629=EDGE_CURVE ( 'NONE', #138653, #60369, #38687, .T. ) ;
#62632=CIRCLE ( 'NONE', #183429, 0.1000000000000028644 ) ;
#62682=ORIENTED_EDGE ( 'NONE', *, *, #80160, .F. ) ;
#62690=DIRECTION ( 'NONE',  ( 0.000000000000000000, 0.000000000000000000, -1.000000000000000000 ) ) ;
#62692=ORIENTED_EDGE ( 'NONE', *, *, #182672, .F. ) ;
#62693=ORIENTED_EDGE ( 'NONE', *, *, #94707, .F. ) ;
#62745=CARTESIAN_POINT ( 'NONE',  ( 18.59999999999999432, 1.736257131608553550, -45.06865232901750318 ) ) ;
#62747=CYLINDRICAL_SURFACE ( 'NONE', #25701, 0.09999999999999939493 ) ;
#62800=ORIENTED_EDGE ( 'NONE', *, *, #15903, .F. ) ;
#62805=ORIENTED_EDGE ( 'NONE', *, *, #185052, .T. ) ;
#62815=CIRCLE ( 'NONE', #17051, 0.1000000000000028644 ) ;
#62825=ORIENTED_EDGE ( 'NONE', *, *, #228405, .T. ) ;
#62833=CARTESIAN_POINT ( 'NONE',  ( 18.59999999999999787, -1.835859311432481045, -78.50443916879852679 ) ) ;
#62875=PLANE ( 'NONE',  #180613 ) ;
#62878=TOROIDAL_SURFACE ( 'NONE', #141975, 0.4000000000000003553, 0.1000000000000000056 ) ;
#62892=ORIENTED_EDGE ( 'NONE', *, *, #10347, .F. ) ;
#62913=DIRECTION ( 'NONE',  ( 0.000000000000000000, 0.9654727137038715545, 0.2605042016806676242 ) ) ;
#62917=ORIENTED_EDGE ( 'NONE', *, *, #147508, .F. ) ;
#62921=CARTESIAN_POINT ( 'NONE',  ( 23.14999999999999858, 5.000000000011153745, -54.59473398108690390 ) ) ;
#62928=EDGE_CURVE ( 'NONE', #194903, #150427, #126350, .T. ) ;
#62932=EDGE_CURVE ( 'NONE', #58399, #32909, #84611, .T. ) ;
#62939=CARTESIAN_POINT ( 'NONE',  ( -23.15000000000000213, 11.75000000001115907, -60.15839931010294350 ) ) ;
#62944=CARTESIAN_POINT ( 'NONE',  ( 18.59999999999999076, 6.550000000011156231, -54.75000000000000000 ) ) ;
#62963=ADVANCED_FACE ( 'NONE', ( #183848 ), #34797, .F. ) ;
#62966=EDGE_LOOP ( 'NONE', ( #175074, #33248, #75268, #148567 ) ) ;
#62969=EDGE_CURVE ( 'NONE', #225825, #72318, #205439, .T. ) ;
#62988=EDGE_LOOP ( 'NONE', ( #7314, #197518, #35617, #115735 ) ) ;
#62991=LINE ( 'NONE', #142516, #79943 ) ;
#63013=CARTESIAN_POINT ( 'NONE',  ( -18.50000000000000000, 11.65000000001115232, -45.65000000000000568 ) ) ;
#63034=CIRCLE ( 'NONE', #125428, 0.09999999999999939493 ) ;
#63100=CARTESIAN_POINT ( 'NONE',  ( -22.39999999999999858, -0.1008583690875575894, -21.75043287651061164 ) ) ;
#63103=B_SPLINE_CURVE_WITH_KNOTS ( 'NONE', 3,
 ( #111688, #12616, #153431, #172991, #15170, #94683 ),
 .UNSPECIFIED., .F., .F.,
 ( 4, 2, 4 ),
 ( 0.000000000000000000, 0.0001891491689349583357, 0.0003782983378699166714 ),
 .UNSPECIFIED. ) ;
#63129=SPHERICAL_SURFACE ( 'NONE', #60857, 0.1000000000000000056 ) ;
#63161=ORIENTED_EDGE ( 'NONE', *, *, #127709, .T. ) ;
#63163=FACE_OUTER_BOUND ( 'NONE', #33477, .T. ) ;
#63185=ADVANCED_FACE ( 'NONE', ( #145356 ), #221989, .T. ) ;
#63212=ADVANCED_FACE ( 'NONE', ( #121956 ), #109593, .T. ) ;
#63230=CIRCLE ( 'NONE', #862, 0.09999999999999939493 ) ;
#63234=CYLINDRICAL_SURFACE ( 'NONE', #193508, 0.5000000000000004441 ) ;
#63238=AXIS2_PLACEMENT_3D ( 'NONE', #250102, #113153, #111885 ) ;
#63248=DIRECTION ( 'NONE',  ( 0.000000000000000000, 0.000000000000000000, 1.000000000000000000 ) ) ;
#63304=DIRECTION ( 'NONE',  ( 0.000000000000000000, -0.000000000000000000, 1.000000000000000000 ) ) ;
#63329=FACE_BOUND ( 'NONE', #95412, .T. ) ;
#63345=CARTESIAN_POINT ( 'NONE',  ( -18.58222699835055280, 10.33200063080771969, -72.59316749566430360 ) ) ;
#63355=CARTESIAN_POINT ( 'NONE',  ( 21.00000000000000000, 9.750000000011153745, -45.75000000000000711 ) ) ;
#63366=DIRECTION ( 'NONE',  ( -1.000000000000000000, 0.000000000000000000, -0.000000000000000000 ) ) ;
#63373=AXIS2_PLACEMENT_3D ( 'NONE', #198362, #216638, #180101 ) ;
#63390=ORIENTED_EDGE ( 'NONE', *, *, #213642, .T. ) ;
#63417=CARTESIAN_POINT ( 'NONE',  ( -21.05000000000000071, 1.115600667400684642E-11, -33.50000000000000000 ) ) ;
#63460=EDGE_CURVE ( 'NONE', #80050, #82729, #243043, .T. ) ;
#63462=AXIS2_PLACEMENT_3D ( 'NONE', #126572, #27515, #108296 ) ;
#63508=DIRECTION ( 'NONE',  ( 0.000000000000000000, -1.000000000000000000, 0.000000000000000000 ) ) ;
#63517=ORIENTED_EDGE ( 'NONE', *, *, #143026, .F. ) ;
#63522=EDGE_LOOP ( 'NONE', ( #58267, #89096, #111862, #147486 ) ) ;
#63529=DIRECTION ( 'NONE',  ( 1.000000000000000000, -0.000000000000000000, -0.000000000000000000 ) ) ;
#63544=CARTESIAN_POINT ( 'NONE',  ( 21.05000000000000071, -0.02138556592644368787, -27.19503888731533792 ) ) ;
#63549=CARTESIAN_POINT ( 'NONE',  ( 21.14999999999999503, -11.74999999998883560, -36.39999999999999858 ) ) ;
#63552=VERTEX_POINT ( 'NONE', #22562 ) ;
#63561=DIRECTION ( 'NONE',  ( 0.000000000000000000, 0.000000000000000000, 1.000000000000000000 ) ) ;
#63566=VECTOR ( 'NONE', #183938, 1000.000000000000227 ) ;
#63593=ORIENTED_EDGE ( 'NONE', *, *, #220077, .T. ) ;
#63637=ORIENTED_EDGE ( 'NONE', *, *, #247258, .T. ) ;
#63671=CARTESIAN_POINT ( 'NONE',  ( 21.09551895715218350, 10.62143732718005573, -45.73712466589949344 ) ) ;
#63749=ORIENTED_EDGE ( 'NONE', *, *, #166281, .T. ) ;
#63765=CARTESIAN_POINT ( 'NONE',  ( -23.25000000000000000, -8.999999999988846255, -43.39396912265245021 ) ) ;
#63770=CIRCLE ( 'NONE', #155385, 0.1000000000000004774 ) ;
#63773=ADVANCED_FACE ( 'NONE', ( #169806 ), #150219, .F. ) ;
#63777=VECTOR ( 'NONE', #157795, 1000.000000000000000 ) ;
#63791=ORIENTED_EDGE ( 'NONE', *, *, #83314, .T. ) ;
#63817=CIRCLE ( 'NONE', #130447, 0.1000000000000028644 ) ;
#63841=LINE ( 'NONE', #20891, #100096 ) ;
#63889=AXIS2_PLACEMENT_3D ( 'NONE', #125465, #41129, #161061 ) ;
#63913=DIRECTION ( 'NONE',  ( 1.000000000000000000, 3.469446951953704435E-14, -2.003086131649669752E-14 ) ) ;
#63921=DIRECTION ( 'NONE',  ( 0.000000000000000000, 1.000000000000000000, 0.000000000000000000 ) ) ;
#63930=DIRECTION ( 'NONE',  ( -1.000000000000000000, 7.304098846218135653E-16, -4.607487905232624742E-31 ) ) ;
#63963=CIRCLE ( 'NONE', #17588, 0.1000000000000002554 ) ;
#64003=DIRECTION ( 'NONE',  ( 0.000000000000000000, 0.000000000000000000, -1.000000000000000000 ) ) ;
#64032=AXIS2_PLACEMENT_3D ( 'NONE', #253374, #77300, #39506 ) ;
#64034=ORIENTED_EDGE ( 'NONE', *, *, #170118, .T. ) ;
#64050=EDGE_CURVE ( 'NONE', #66671, #162149, #255843, .T. ) ;
#64104=DIRECTION ( 'NONE',  ( 1.000000000000000000, -0.000000000000000000, -0.000000000000000000 ) ) ;
#64142=DIRECTION ( 'NONE',  ( 1.000000000000000000, 0.000000000000000000, 0.000000000000000000 ) ) ;
#64171=TOROIDAL_SURFACE ( 'NONE', #255653, 0.6000000000000009770, 0.1000000000000000056 ) ;
#64188=EDGE_CURVE ( 'NONE', #179315, #173321, #181082, .T. ) ;
#64194=CARTESIAN_POINT ( 'NONE',  ( 18.59999999999999432, -1.736257131586239844, -45.06865232901750318 ) ) ;
#64195=DIRECTION ( 'NONE',  ( 0.000000000000000000, 0.9875055080513743810, -0.1575844902526802316 ) ) ;
#64198=CARTESIAN_POINT ( 'NONE',  ( 20.94999027547553894, 10.29326151435327219, -72.45928225104148623 ) ) ;
#64202=VERTEX_POINT ( 'NONE', #11382 ) ;
#64204=CARTESIAN_POINT ( 'NONE',  ( 18.59999999999999432, 1.162701749949165642, -41.60000000000000142 ) ) ;
#64207=ORIENTED_EDGE ( 'NONE', *, *, #228048, .F. ) ;
#64228=CIRCLE ( 'NONE', #97510, 0.5000000000000004441 ) ;
#64238=ORIENTED_EDGE ( 'NONE', *, *, #247247, .T. ) ;
#64254=CIRCLE ( 'NONE', #193258, 0.1000000000000028644 ) ;
#64260=EDGE_CURVE ( 'NONE', #19031, #135854, #6076, .T. ) ;
#64287=CIRCLE ( 'NONE', #6007, 0.1000000000000028644 ) ;
#64291=EDGE_LOOP ( 'NONE', ( #157413, #25041, #167650, #173861 ) ) ;
#64314=VERTEX_POINT ( 'NONE', #34821 ) ;
#64330=FACE_OUTER_BOUND ( 'NONE', #7532, .T. ) ;
#64342=ORIENTED_EDGE ( 'NONE', *, *, #149604, .T. ) ;
#64344=AXIS2_PLACEMENT_3D ( 'NONE', #8318, #87807, #96788 ) ;
#64350=ORIENTED_EDGE ( 'NONE', *, *, #53567, .T. ) ;
#64392=ORIENTED_EDGE ( 'NONE', *, *, #143004, .T. ) ;
#64412=EDGE_CURVE ( 'NONE', #46326, #141829, #247880, .T. ) ;
#64423=VERTEX_POINT ( 'NONE', #81577 ) ;
#64439=EDGE_CURVE ( 'NONE', #109631, #79720, #243600, .T. ) ;
#64458=CARTESIAN_POINT ( 'NONE',  ( 20.94999999999999929, 1.835341550235569663, -45.05515129256298223 ) ) ;
#64465=DIRECTION ( 'NONE',  ( -1.000000000000000000, -2.952720810173289112E-16, 0.000000000000000000 ) ) ;
#64467=CIRCLE ( 'NONE', #81186, 0.09999999999999939493 ) ;
#64474=CARTESIAN_POINT ( 'NONE',  ( -20.64999999999999858, 7.150000000011155876, -45.85000000000000142 ) ) ;
#64497=EDGE_CURVE ( 'NONE', #163061, #183157, #131165, .T. ) ;
#64516=AXIS2_PLACEMENT_3D ( 'NONE', #86004, #63913, #6492 ) ;
#64519=DIRECTION ( 'NONE',  ( 0.000000000000000000, -1.000000000000000000, 0.000000000000000000 ) ) ;
#64523=ORIENTED_EDGE ( 'NONE', *, *, #67913, .F. ) ;
#64560=DIRECTION ( 'NONE',  ( -4.408576920032448588E-17, 0.1350103645451876944, -0.9908441862701601321 ) ) ;
#64586=VECTOR ( 'NONE', #168324, 1000.000000000000000 ) ;
#64602=CARTESIAN_POINT ( 'NONE',  ( -21.05000000000000071, -11.64999999998884483, -36.50000000000000711 ) ) ;
#64648=CARTESIAN_POINT ( 'NONE',  ( 23.24999999999999645, 5.000000000011153745, -54.59473398108690390 ) ) ;
#64688=ORIENTED_EDGE ( 'NONE', *, *, #229748, .T. ) ;
#64692=DIRECTION ( 'NONE',  ( -1.000000000000000000, 0.000000000000000000, 0.000000000000000000 ) ) ;
#64698=CARTESIAN_POINT ( 'NONE',  ( -21.29999999999995808, 1.115600667400684642E-11, -37.54999999999999716 ) ) ;
#64700=ORIENTED_EDGE ( 'NONE', *, *, #84104, .T. ) ;
#64716=ADVANCED_FACE ( 'NONE', ( #237510 ), #2159, .F. ) ;
#64722=CARTESIAN_POINT ( 'NONE',  ( -18.59999999999999787, 7.021664781911246322, -70.83356540189728889 ) ) ;
#64759=DIRECTION ( 'NONE',  ( 1.000000000000000000, 0.000000000000000000, 0.000000000000000000 ) ) ;
#64760=DIRECTION ( 'NONE',  ( -1.000000000000000000, 0.000000000000000000, 0.000000000000000000 ) ) ;
#64781=CARTESIAN_POINT ( 'NONE',  ( 20.94999999999999929, 1.115650877919449413E-11, -62.90000000000001279 ) ) ;
#64782=CARTESIAN_POINT ( 'NONE',  ( 18.59999999999999432, -1.162701749926855266, -41.60000000000000142 ) ) ;
#64791=DIRECTION ( 'NONE',  ( 1.000000000000000000, 0.000000000000000000, 0.000000000000000000 ) ) ;
#64796=CARTESIAN_POINT ( 'NONE',  ( 21.05000000000000071, 11.60000000001116227, -60.07179676972450011 ) ) ;
#64805=CARTESIAN_POINT ( 'NONE',  ( 18.49999999999999645, -1.135018845899022466, -74.71697688343232358 ) ) ;
#64816=CIRCLE ( 'NONE', #10668, 4.000000000000003553 ) ;
#64821=TOROIDAL_SURFACE ( 'NONE', #173217, 4.099999999999999645, 0.1000000000000000056 ) ;
#64843=DIRECTION ( 'NONE',  ( -1.000000000000000000, -0.000000000000000000, -0.000000000000000000 ) ) ;
#64887=EDGE_LOOP ( 'NONE', ( #122990, #189531, #152278, #1353 ) ) ;
#64906=EDGE_CURVE ( 'NONE', #90674, #61206, #131352, .T. ) ;
#64916=DIRECTION ( 'NONE',  ( 0.000000000000000000, -1.265107689135680095E-16, 1.000000000000000000 ) ) ;
#64940=DIRECTION ( 'NONE',  ( -1.000000000000000000, -0.000000000000000000, -0.000000000000000000 ) ) ;
#65004=DIRECTION ( 'NONE',  ( -1.000000000000000000, 0.000000000000000000, 0.000000000000000000 ) ) ;
#65007=CIRCLE ( 'NONE', #239813, 11.70000000000000284 ) ;
#65064=ORIENTED_EDGE ( 'NONE', *, *, #102347, .T. ) ;
#65071=DIRECTION ( 'NONE',  ( 0.000000000000000000, 0.000000000000000000, -1.000000000000000000 ) ) ;
#65082=CARTESIAN_POINT ( 'NONE',  ( -21.64999999999999858, 7.250000000011148416, -54.65000000000000568 ) ) ;
#65086=EDGE_LOOP ( 'NONE', ( #247745, #158545, #27902, #131335, #62070 ) ) ;
#65095=CARTESIAN_POINT ( 'NONE',  ( 21.05000000000000071, 1.115600667400684642E-11, -33.50000000000000000 ) ) ;
#65097=EDGE_CURVE ( 'NONE', #14219, #87677, #145780, .T. ) ;
#65104=CARTESIAN_POINT ( 'NONE',  ( -18.47140463609786920, -9.671474685209730637, -73.67276045827406961 ) ) ;
#65143=FACE_OUTER_BOUND ( 'NONE', #232765, .T. ) ;
#65156=CARTESIAN_POINT ( 'NONE',  ( -23.25000000000000000, 1.115651490242849210E-11, -29.35000000000000142 ) ) ;
#65169=EDGE_CURVE ( 'NONE', #192209, #241724, #123675, .T. ) ;
#65279=ORIENTED_EDGE ( 'NONE', *, *, #250258, .F. ) ;
#65333=TOROIDAL_SURFACE ( 'NONE', #11167, 11.65000000000000036, 0.1000000000000000056 ) ;
#65358=( BOUNDED_CURVE ( )  B_SPLINE_CURVE ( 3, ( #38118, #134607, #133358, #257095 ),
 .UNSPECIFIED., .F., .F. ) 
 B_SPLINE_CURVE_WITH_KNOTS ( ( 4, 4 ),
 ( 1.570796326794895448, 3.141592653589791784 ),
 .UNSPECIFIED. ) 
 CURVE ( )  GEOMETRIC_REPRESENTATION_ITEM ( )  RATIONAL_B_SPLINE_CURVE ( ( 1.000000000000000000, 0.8047378541243650485, 0.8047378541243650485, 1.000000000000000000 ) ) 
 REPRESENTATION_ITEM ( '' )  );
#65366=EDGE_CURVE ( 'NONE', #84702, #147965, #139889, .T. ) ;
#65401=FACE_OUTER_BOUND ( 'NONE', #74777, .T. ) ;
#65499=VERTEX_POINT ( 'NONE', #97339 ) ;
#65502=CARTESIAN_POINT ( 'NONE',  ( 18.59999999999999432, 1.261786168576181755, -41.58649896354548048 ) ) ;
#65507=CARTESIAN_POINT ( 'NONE',  ( -18.41817142474039315, -9.498703066590936217, -73.60396548763712588 ) ) ;
#65508=ORIENTED_EDGE ( 'NONE', *, *, #238660, .T. ) ;
#65565=EDGE_CURVE ( 'NONE', #117247, #90674, #69382, .T. ) ;
#65607=VECTOR ( 'NONE', #40779, 1000.000000000000000 ) ;
#65611=DIRECTION ( 'NONE',  ( -0.000000000000000000, 0.8660254037844411501, 0.4999999999999956701 ) ) ;
#65618=VERTEX_POINT ( 'NONE', #43826 ) ;
#65656=LINE ( 'NONE', #162223, #74430 ) ;
#65672=EDGE_CURVE ( 'NONE', #147965, #186298, #129770, .T. ) ;
#65676=FACE_OUTER_BOUND ( 'NONE', #236871, .T. ) ;
#65705=ORIENTED_EDGE ( 'NONE', *, *, #27861, .F. ) ;
#65731=ORIENTED_EDGE ( 'NONE', *, *, #181461, .T. ) ;
#65752=CARTESIAN_POINT ( 'NONE',  ( 20.53930447207976684, 8.977148687535432714, -41.94250714157757187 ) ) ;
#65758=CARTESIAN_POINT ( 'NONE',  ( 18.59999999999999076, 7.070967871809997973, -70.74656422186831151 ) ) ;
#65771=ADVANCED_FACE ( 'NONE', ( #247141 ), #228881, .T. ) ;
#65837=ADVANCED_FACE ( 'NONE', ( #77471 ), #37119, .T. ) ;
#65853=ORIENTED_EDGE ( 'NONE', *, *, #187721, .F. ) ;
#65855=ADVANCED_FACE ( 'NONE', ( #95760 ), #234002, .F. ) ;
#65867=CARTESIAN_POINT ( 'NONE',  ( -22.41119224318417125, 1.115600667400684642E-11, -21.85042919245520210 ) ) ;
#65885=ORIENTED_EDGE ( 'NONE', *, *, #222001, .F. ) ;
#65917=ORIENTED_EDGE ( 'NONE', *, *, #136797, .T. ) ;
#65925=VERTEX_POINT ( 'NONE', #46072 ) ;
#65952=ORIENTED_EDGE ( 'NONE', *, *, #192654, .T. ) ;
#65955=VECTOR ( 'NONE', #247067, 1000.000000000000000 ) ;
#65992=CARTESIAN_POINT ( 'NONE',  ( 18.59999999999999076, 11.65000000001115943, -58.35000000000000142 ) ) ;
#66004=CARTESIAN_POINT ( 'NONE',  ( -20.64999999999999858, 4.350000000011156054, -54.65000000000000568 ) ) ;
#66005=EDGE_CURVE ( 'NONE', #11718, #97145, #140256, .T. ) ;
#66008=CIRCLE ( 'NONE', #86832, 4.049999999999998934 ) ;
#66016=ORIENTED_EDGE ( 'NONE', *, *, #79162, .T. ) ;
#66057=ADVANCED_FACE ( 'NONE', ( #10815 ), #109891, .T. ) ;
#66069=EDGE_CURVE ( 'NONE', #110700, #204714, #244317, .T. ) ;
#66084=CARTESIAN_POINT ( 'NONE',  ( 22.40000000000020819, -0.1008583690885111045, -21.75043287651029900 ) ) ;
#66101=ORIENTED_EDGE ( 'NONE', *, *, #229858, .T. ) ;
#66122=CARTESIAN_POINT ( 'NONE',  ( 21.05000000000000071, -0.01454569055822367736, -27.00298221356814565 ) ) ;
#66131=ORIENTED_EDGE ( 'NONE', *, *, #138148, .T. ) ;
#66188=ORIENTED_EDGE ( 'NONE', *, *, #76872, .F. ) ;
#66201=DIRECTION ( 'NONE',  ( 0.000000000000000000, 0.000000000000000000, -1.000000000000000000 ) ) ;
#66227=CIRCLE ( 'NONE', #99516, 0.2000000000000005107 ) ;
#66271=CARTESIAN_POINT ( 'NONE',  ( 23.14999999999998437, 1.115600667400684642E-11, -33.50000000000000000 ) ) ;
#66299=CARTESIAN_POINT ( 'NONE',  ( 18.49999999999999289, 7.021664781911246322, -70.83356540189728889 ) ) ;
#66302=CARTESIAN_POINT ( 'NONE',  ( -18.59999999999999787, 1.835341550235567887, -45.05515129256298223 ) ) ;
#66304=EDGE_LOOP ( 'NONE', ( #34278, #109259, #257227, #37661 ) ) ;
#66319=AXIS2_PLACEMENT_3D ( 'NONE', #87270, #105531, #185108 ) ;
#66321=DIRECTION ( 'NONE',  ( -1.000000000000000000, 0.000000000000000000, 0.000000000000000000 ) ) ;
#66335=DIRECTION ( 'NONE',  ( 0.7071067811865474617, 0.7071067811865474617, 0.000000000000000000 ) ) ;
#66352=CARTESIAN_POINT ( 'NONE',  ( 22.48660254037844552, 11.65000000001115588, -33.45000000000000995 ) ) ;
#66363=DIRECTION ( 'NONE',  ( 0.000000000000000000, 0.000000000000000000, 1.000000000000000000 ) ) ;
#66409=DIRECTION ( 'NONE',  ( 2.952720810173289112E-16, -1.000000000000000000, 0.000000000000000000 ) ) ;
#66415=CARTESIAN_POINT ( 'NONE',  ( -20.54999999999999716, 4.250000000011156409, -45.85000000000000142 ) ) ;
#66436=FACE_OUTER_BOUND ( 'NONE', #252341, .T. ) ;
#66447=DIRECTION ( 'NONE',  ( 1.000000000000000000, -0.000000000000000000, -0.000000000000000000 ) ) ;
#66448=ORIENTED_EDGE ( 'NONE', *, *, #168746, .F. ) ;
#66460=ORIENTED_EDGE ( 'NONE', *, *, #6697, .F. ) ;
#66477=EDGE_CURVE ( 'NONE', #104053, #224583, #132709, .T. ) ;
#66478=DIRECTION ( 'NONE',  ( -1.000000000000000000, 0.000000000000000000, 0.000000000000000000 ) ) ;
#66488=CARTESIAN_POINT ( 'NONE',  ( 22.39999999999999858, 7.790779598384538041, -33.50000000000000711 ) ) ;
#66506=EDGE_LOOP ( 'NONE', ( #245260, #158703, #86546, #66756 ) ) ;
#66601=DIRECTION ( 'NONE',  ( 1.000000000000000000, 0.000000000000000000, -0.000000000000000000 ) ) ;
#66618=EDGE_LOOP ( 'NONE', ( #203748, #150394, #227773, #217796 ) ) ;
#66620=CARTESIAN_POINT ( 'NONE',  ( -21.05000000000000071, 1.736257131608553550, -45.06865232901750318 ) ) ;
#66626=CARTESIAN_POINT ( 'NONE',  ( -23.15000000000000213, 1.115600667400684642E-11, -67.00000000000000000 ) ) ;
#66633=AXIS2_PLACEMENT_3D ( 'NONE', #82633, #240462, #43556 ) ;
#66671=VERTEX_POINT ( 'NONE', #238201 ) ;
#66683=DIRECTION ( 'NONE',  ( 1.000000000000000000, 0.000000000000000000, 0.000000000000000000 ) ) ;
#66701=AXIS2_PLACEMENT_3D ( 'NONE', #130835, #245652, #207842 ) ;
#66711=CARTESIAN_POINT ( 'NONE',  ( -20.94999999999999929, 1.115600667400684642E-11, -67.00000000000000000 ) ) ;
#66736=CARTESIAN_POINT ( 'NONE',  ( 18.50000972452444969, 10.29326151435342851, -72.45928225104145781 ) ) ;
#66746=AXIS2_PLACEMENT_3D ( 'NONE', #216807, #215526, #38201 ) ;
#66756=ORIENTED_EDGE ( 'NONE', *, *, #80729, .F. ) ;
#66764=AXIS2_PLACEMENT_3D ( 'NONE', #167615, #11094, #165026 ) ;
#66766=CARTESIAN_POINT ( 'NONE',  ( 22.59999999999999432, 0.1000000000111554016, -21.85042919245520210 ) ) ;
#66777=EDGE_LOOP ( 'NONE', ( #214251, #43337, #84941, #67857 ) ) ;
#66803=CARTESIAN_POINT ( 'NONE',  ( -18.44232395689875759, -9.552282557039388777, -73.84225198480679353 ) ) ;
#66880=ORIENTED_EDGE ( 'NONE', *, *, #187479, .T. ) ;
#66885=ORIENTED_EDGE ( 'NONE', *, *, #140393, .F. ) ;
#66893=CARTESIAN_POINT ( 'NONE',  ( 18.49999999999998579, -9.321008403350155902, -40.73593824907785432 ) ) ;
#66966=CARTESIAN_POINT ( 'NONE',  ( -22.59999970745345976, -0.009356377315828669564, -21.74948679233078863 ) ) ;
#66991=CARTESIAN_POINT ( 'NONE',  ( -23.24999999999999645, -9.599999999988845900, -73.60018939122203108 ) ) ;
#67012=ADVANCED_FACE ( 'NONE', ( #65676 ), #86448, .F. ) ;
#67017=ADVANCED_FACE ( 'NONE', ( #163502 ), #49444, .T. ) ;
#67041=CARTESIAN_POINT ( 'NONE',  ( 20.74897398619109268, 10.59569302167756888, -41.17931145625621525 ) ) ;
#67068=EDGE_LOOP ( 'NONE', ( #217723, #225146, #139549, #152415 ) ) ;
#67087=VERTEX_POINT ( 'NONE', #51222 ) ;
#67092=ORIENTED_EDGE ( 'NONE', *, *, #218882, .T. ) ;
#67097=CIRCLE ( 'NONE', #212860, 11.80000000000000426 ) ;
#67111=CIRCLE ( 'NONE', #121138, 0.09999999999999939493 ) ;
#67117=CARTESIAN_POINT ( 'NONE',  ( 18.59999999999999432, -1.866714910046153308, -45.25267524628200988 ) ) ;
#67145=AXIS2_PLACEMENT_3D ( 'NONE', #56351, #233741, #216725 ) ;
#67156=CARTESIAN_POINT ( 'NONE',  ( -22.49917693094574389, 0.08522996423282767908, -21.85020421546933989 ) ) ;
#67158=DIRECTION ( 'NONE',  ( 0.000000000000000000, 0.8660254037844385966, -0.5000000000000003331 ) ) ;
#67162=DIRECTION ( 'NONE',  ( 0.000000000000000000, 1.000000000000000000, 2.891205793294679805E-16 ) ) ;
#67170=EDGE_CURVE ( 'NONE', #133244, #2313, #194462, .T. ) ;
#67193=DIRECTION ( 'NONE',  ( -1.000000000000000000, -0.000000000000000000, -0.000000000000000000 ) ) ;
#67210=AXIS2_PLACEMENT_3D ( 'NONE', #8772, #129976, #113006 ) ;
#67212=VERTEX_POINT ( 'NONE', #19851 ) ;
#67224=VERTEX_POINT ( 'NONE', #158107 ) ;
#67257=FACE_OUTER_BOUND ( 'NONE', #183977, .T. ) ;
#67293=DIRECTION ( 'NONE',  ( 0.000000000000000000, -0.9908441862701596881, 0.1350103645451904977 ) ) ;
#67314=ADVANCED_FACE ( 'NONE', ( #118949 ), #77224, .T. ) ;
#67319=DIRECTION ( 'NONE',  ( -0.000000000000000000, -1.000000000000000000, 6.308085367188393199E-16 ) ) ;
#67324=ORIENTED_EDGE ( 'NONE', *, *, #184264, .F. ) ;
#67327=ORIENTED_EDGE ( 'NONE', *, *, #49349, .F. ) ;
#67387=CARTESIAN_POINT ( 'NONE',  ( -23.15000000000000213, 1.115600667400684642E-11, -70.90000000000000568 ) ) ;
#67398=EDGE_CURVE ( 'NONE', #108495, #18666, #165800, .T. ) ;
#67401=FACE_BOUND ( 'NONE', #218272, .T. ) ;
#67419=ORIENTED_EDGE ( 'NONE', *, *, #20306, .F. ) ;
#67430=DIRECTION ( 'NONE',  ( 1.000000000000000000, -0.000000000000000000, -0.000000000000000000 ) ) ;
#67449=CARTESIAN_POINT ( 'NONE',  ( -21.05000000000000071, 1.115600667400684642E-11, -33.50000000000000000 ) ) ;
#67471=ORIENTED_EDGE ( 'NONE', *, *, #169441, .T. ) ;
#67477=DIRECTION ( 'NONE',  ( 1.000000000000000000, 0.000000000000000000, 0.000000000000000000 ) ) ;
#67482=CARTESIAN_POINT ( 'NONE',  ( -22.50000000000000000, 11.64976291804307884, -33.41119002361307366 ) ) ;
#67483=VERTEX_POINT ( 'NONE', #201394 ) ;
#67514=EDGE_LOOP ( 'NONE', ( #162475, #121910, #178810, #158543, #257012 ) ) ;
#67518=VECTOR ( 'NONE', #81949, 1000.000000000000000 ) ;
#67554=VERTEX_POINT ( 'NONE', #179298 ) ;
#67564=ORIENTED_EDGE ( 'NONE', *, *, #242321, .F. ) ;
#67579=EDGE_CURVE ( 'NONE', #206237, #213025, #161311, .T. ) ;
#67616=LINE ( 'NONE', #25939, #120751 ) ;
#67625=DIRECTION ( 'NONE',  ( 2.694716079187272946E-16, -1.000000000000000000, 0.000000000000000000 ) ) ;
#67649=DIRECTION ( 'NONE',  ( 0.000000000000000000, 1.000000000000000000, 0.000000000000000000 ) ) ;
#67664=CARTESIAN_POINT ( 'NONE',  ( 18.49999999999999289, 11.75000000001115552, -58.35000000000000142 ) ) ;
#67695=DIRECTION ( 'NONE',  ( 1.000000000000000000, -0.000000000000000000, 0.000000000000000000 ) ) ;
#67704=DIRECTION ( 'NONE',  ( -1.000000000000000000, 0.000000000000000000, 0.000000000000000000 ) ) ;
#67735=EDGE_CURVE ( 'NONE', #181648, #110818, #194649, .T. ) ;
#67741=EDGE_LOOP ( 'NONE', ( #204698, #70648, #111780, #50134 ) ) ;
#67756=LINE ( 'NONE', #29938, #43255 ) ;
#67766=CARTESIAN_POINT ( 'NONE',  ( 20.94999999999999929, 1.115600667400684642E-11, -33.50000000000000000 ) ) ;
#67769=DIRECTION ( 'NONE',  ( 0.000000000000000000, 1.000000000000000000, 0.000000000000000000 ) ) ;
#67784=ORIENTED_EDGE ( 'NONE', *, *, #145227, .F. ) ;
#67789=ORIENTED_EDGE ( 'NONE', *, *, #177754, .T. ) ;
#67800=CARTESIAN_POINT ( 'NONE',  ( 20.95000000000000284, 11.60000000001116227, -60.07179676972450011 ) ) ;
#67808=VECTOR ( 'NONE', #39645, 1000.000000000000000 ) ;
#67821=CARTESIAN_POINT ( 'NONE',  ( 20.94999999999999574, 1.851028230152016674, -45.15391326942249606 ) ) ;
#67840=EDGE_LOOP ( 'NONE', ( #184258, #245374, #225058, #48624, #181514, #238315, #158904, #48568, #148604, #232326, #27435, #104616 ) ) ;
#67857=ORIENTED_EDGE ( 'NONE', *, *, #77356, .T. ) ;
#67864=EDGE_CURVE ( 'NONE', #210604, #138871, #169531, .T. ) ;
#67865=DIRECTION ( 'NONE',  ( 1.000000000000000000, 3.265361837132813093E-16, -0.000000000000000000 ) ) ;
#67869=ORIENTED_EDGE ( 'NONE', *, *, #136119, .T. ) ;
#67870=CIRCLE ( 'NONE', #221963, 0.09999999999999939493 ) ;
#67894=DIRECTION ( 'NONE',  ( 1.000000000000000000, 0.000000000000000000, 0.000000000000000000 ) ) ;
#67913=EDGE_CURVE ( 'NONE', #30860, #24511, #201100, .T. ) ;
#67921=CARTESIAN_POINT ( 'NONE',  ( -23.25000000000000000, 1.115626384983466744E-11, -64.90000000000000568 ) ) ;
#67924=ORIENTED_EDGE ( 'NONE', *, *, #257468, .F. ) ;
#67926=CARTESIAN_POINT ( 'NONE',  ( -20.07928932188135107, 9.220710678129810489, -54.75000000000000000 ) ) ;
#67963=ORIENTED_EDGE ( 'NONE', *, *, #23116, .T. ) ;
#67965=EDGE_CURVE ( 'NONE', #25637, #79373, #160728, .T. ) ;
#67972=ADVANCED_FACE ( 'NONE', ( #42048 ), #22490, .T. ) ;
#68012=CARTESIAN_POINT ( 'NONE',  ( -20.64999999999999858, 2.000000000011154189, -46.72462192276210402 ) ) ;
#68031=EDGE_CURVE ( 'NONE', #226768, #77793, #127992, .T. ) ;
#68041=CARTESIAN_POINT ( 'NONE',  ( -21.56666275994539816, 1.115600667400684642E-11, -26.54263159310667675 ) ) ;
#68042=ORIENTED_EDGE ( 'NONE', *, *, #137577, .T. ) ;
#68057=DIRECTION ( 'NONE',  ( 0.000000000000000000, 0.000000000000000000, -1.000000000000000000 ) ) ;
#68059=ORIENTED_EDGE ( 'NONE', *, *, #102220, .T. ) ;
#68079=EDGE_LOOP ( 'NONE', ( #70848, #204287, #76907, #89130, #246456 ) ) ;
#68095=ORIENTED_EDGE ( 'NONE', *, *, #146925, .T. ) ;
#68104=ORIENTED_EDGE ( 'NONE', *, *, #169442, .F. ) ;
#68135=DIRECTION ( 'NONE',  ( -1.000000000000000000, -0.000000000000000000, -0.000000000000000000 ) ) ;
#68167=AXIS2_PLACEMENT_3D ( 'NONE', #245133, #209866, #108196 ) ;
#68181=EDGE_CURVE ( 'NONE', #159998, #32909, #174000, .T. ) ;
#68182=SPHERICAL_SURFACE ( 'NONE', #141700, 0.1000000000000000056 ) ;
#68200=CIRCLE ( 'NONE', #142999, 0.09999999999999749367 ) ;
#68216=FACE_OUTER_BOUND ( 'NONE', #156844, .T. ) ;
#68228=VERTEX_POINT ( 'NONE', #31485 ) ;
#68249=AXIS2_PLACEMENT_3D ( 'NONE', #14117, #32408, #213570 ) ;
#68312=CARTESIAN_POINT ( 'NONE',  ( -23.25000000000000000, 11.75000000001115552, -67.00000000000000000 ) ) ;
#68400=ADVANCED_FACE ( 'NONE', ( #176122 ), #255578, .T. ) ;
#68403=CIRCLE ( 'NONE', #243367, 0.2000000000000057288 ) ;
#68449=CARTESIAN_POINT ( 'NONE',  ( -22.47120815636973745, 0.02890382191504723558, -21.85006801124650266 ) ) ;
#68452=ORIENTED_EDGE ( 'NONE', *, *, #235951, .T. ) ;
#68474=DIRECTION ( 'NONE',  ( 0.000000000000000000, 1.000000000000000000, 0.000000000000000000 ) ) ;
#68475=AXIS2_PLACEMENT_3D ( 'NONE', #1739, #205073, #46011 ) ;
#68504=CARTESIAN_POINT ( 'NONE',  ( -18.57399277249657032, 10.33112638556969465, -72.59012289269747953 ) ) ;
#68513=AXIS2_PLACEMENT_3D ( 'NONE', #160168, #24499, #121044 ) ;
#68522=EDGE_CURVE ( 'NONE', #241304, #135375, #147234, .T. ) ;
#68523=FACE_OUTER_BOUND ( 'NONE', #69345, .T. ) ;
#68539=VECTOR ( 'NONE', #89278, 1000.000000000000000 ) ;
#68593=EDGE_LOOP ( 'NONE', ( #41165, #251651, #82809, #191334 ) ) ;
#68600=AXIS2_PLACEMENT_3D ( 'NONE', #170079, #35689, #192181 ) ;
#68603=ORIENTED_EDGE ( 'NONE', *, *, #95194, .T. ) ;
#68626=EDGE_CURVE ( 'NONE', #197038, #163061, #151098, .T. ) ;
#68641=AXIS2_PLACEMENT_3D ( 'NONE', #30974, #110470, #208312 ) ;
#68664=ORIENTED_EDGE ( 'NONE', *, *, #132080, .T. ) ;
#68721=CARTESIAN_POINT ( 'NONE',  ( 20.94999999999999929, 1.115600667400684642E-11, -67.00000000000000000 ) ) ;
#68744=AXIS2_PLACEMENT_3D ( 'NONE', #149464, #12521, #93312 ) ;
#68765=EDGE_LOOP ( 'NONE', ( #139972, #107261, #35082, #133701, #154398, #165311, #91476, #72896, #123292, #201563, #229495, #99746 ) ) ;
#68776=DIRECTION ( 'NONE',  ( 0.000000000000000000, 0.000000000000000000, -1.000000000000000000 ) ) ;
#68783=DIRECTION ( 'NONE',  ( 0.000000000000000000, 0.000000000000000000, -1.000000000000000000 ) ) ;
#68810=LINE ( 'NONE', #70109, #13709 ) ;
#68820=VERTEX_POINT ( 'NONE', #221306 ) ;
#68860=CARTESIAN_POINT ( 'NONE',  ( -20.85000000000000142, -1.362429037182151470, -74.88888124792120493 ) ) ;
#68869=DIRECTION ( 'NONE',  ( 0.000000000000000000, 0.000000000000000000, -1.000000000000000000 ) ) ;
#68926=ADVANCED_FACE ( 'NONE', ( #43973 ), #124805, .F. ) ;
#68954=CARTESIAN_POINT ( 'NONE',  ( 21.05000000000000071, -11.48912529306489994, -63.89999999999999858 ) ) ;
#68987=VECTOR ( 'NONE', #63930, 1000.000000000000000 ) ;
#69013=CIRCLE ( 'NONE', #214720, 0.1000000000000028644 ) ;
#69060=CYLINDRICAL_SURFACE ( 'NONE', #13350, 4.049999999999998046 ) ;
#69120=EDGE_CURVE ( 'NONE', #179511, #11734, #22462, .T. ) ;
#69139=CARTESIAN_POINT ( 'NONE',  ( -18.50000000000000000, 11.65000000001115588, -67.00000000000000000 ) ) ;
#69147=EDGE_LOOP ( 'NONE', ( #490, #242180, #33112, #192003 ) ) ;
#69164=DIRECTION ( 'NONE',  ( -1.000000000000000000, 0.000000000000000000, 0.000000000000000000 ) ) ;
#69169=DIRECTION ( 'NONE',  ( 0.000000000000000000, 0.000000000000000000, 1.000000000000000000 ) ) ;
#69205=CARTESIAN_POINT ( 'NONE',  ( 21.14999999999999858, 11.65000000001115943, -33.60000000000000142 ) ) ;
#69252=EDGE_CURVE ( 'NONE', #134939, #197038, #150173, .T. ) ;
#69284=ORIENTED_EDGE ( 'NONE', *, *, #121148, .F. ) ;
#69300=DIRECTION ( 'NONE',  ( -0.000000000000000000, 0.01283462868039629209, -0.9999176327611372095 ) ) ;
#69331=LINE ( 'NONE', #206265, #60691 ) ;
#69339=EDGE_CURVE ( 'NONE', #133079, #78967, #35124, .T. ) ;
#69344=DIRECTION ( 'NONE',  ( -1.000000000000000000, -2.952720810173289112E-16, 0.000000000000000000 ) ) ;
#69345=EDGE_LOOP ( 'NONE', ( #221096, #8222, #251877, #137791 ) ) ;
#69360=CARTESIAN_POINT ( 'NONE',  ( 23.14999999999999503, 11.65000000001116298, -45.65000000000000568 ) ) ;
#69364=ORIENTED_EDGE ( 'NONE', *, *, #67864, .F. ) ;
#69380=ORIENTED_EDGE ( 'NONE', *, *, #241422, .F. ) ;
#69382=CIRCLE ( 'NONE', #15213, 0.1000000000000028644 ) ;
#69385=AXIS2_PLACEMENT_3D ( 'NONE', #199055, #200334, #21706 ) ;
#69390=EDGE_LOOP ( 'NONE', ( #5374, #5213, #69284, #237855 ) ) ;
#69395=DIRECTION ( 'NONE',  ( 0.000000000000000000, 0.000000000000000000, -1.000000000000000000 ) ) ;
#69402=EDGE_CURVE ( 'NONE', #203889, #113415, #31026, .T. ) ;
#69408=ORIENTED_EDGE ( 'NONE', *, *, #218311, .F. ) ;
#69423=EDGE_CURVE ( 'NONE', #72990, #45011, #218403, .T. ) ;
#69429=ORIENTED_EDGE ( 'NONE', *, *, #164519, .T. ) ;
#69434=ORIENTED_EDGE ( 'NONE', *, *, #162566, .F. ) ;
#69440=LINE ( 'NONE', #212795, #193957 ) ;
#69443=TOROIDAL_SURFACE ( 'NONE', #61032, 6.258578643762712446, 0.1000000000000000056 ) ;
#69449=ADVANCED_FACE ( 'NONE', ( #17085 ), #97588, .T. ) ;
#69451=CARTESIAN_POINT ( 'NONE',  ( 18.59999999999998721, 6.846123162363745074, -70.73772626684986164 ) ) ;
#69453=EDGE_CURVE ( 'NONE', #128224, #200640, #83424, .T. ) ;
#69454=DIRECTION ( 'NONE',  ( 0.000000000000000000, 1.000000000000000000, 0.000000000000000000 ) ) ;
#69463=CARTESIAN_POINT ( 'NONE',  ( -21.05000000000000426, 6.270085863700296080, -33.46513199698689078 ) ) ;
#69470=EDGE_CURVE ( 'NONE', #81117, #216222, #68403, .T. ) ;
#69483=ORIENTED_EDGE ( 'NONE', *, *, #136797, .F. ) ;
#69484=ORIENTED_EDGE ( 'NONE', *, *, #20306, .T. ) ;
#69494=AXIS2_PLACEMENT_3D ( 'NONE', #4470, #64465, #200119 ) ;
#69497=CARTESIAN_POINT ( 'NONE',  ( -20.85000000000000142, -1.164121893230052995, -74.91484808557160591 ) ) ;
#69542=ORIENTED_EDGE ( 'NONE', *, *, #68522, .F. ) ;
#69547=AXIS2_PLACEMENT_3D ( 'NONE', #253001, #95218, #73125 ) ;
#69551=CARTESIAN_POINT ( 'NONE',  ( 23.14999999999999858, 1.115600667400684642E-11, -67.00000000000000000 ) ) ;
#69557=ADVANCED_FACE ( 'NONE', ( #138271 ), #251752, .T. ) ;
#69562=DIRECTION ( 'NONE',  ( 0.000000000000000000, 0.000000000000000000, 1.000000000000000000 ) ) ;
#69565=FACE_OUTER_BOUND ( 'NONE', #154198, .T. ) ;
#69572=ORIENTED_EDGE ( 'NONE', *, *, #62482, .F. ) ;
#69577=EDGE_CURVE ( 'NONE', #203988, #1139, #18521, .T. ) ;
#69607=CARTESIAN_POINT ( 'NONE',  ( 18.59999999999996945, 10.33248238083634440, -72.59484654391314962 ) ) ;
#69613=ORIENTED_EDGE ( 'NONE', *, *, #74716, .F. ) ;
#69637=EDGE_CURVE ( 'NONE', #26511, #235569, #161739, .T. ) ;
#69642=CIRCLE ( 'NONE', #215355, 0.09999999999999843736 ) ;
#69653=ORIENTED_EDGE ( 'NONE', *, *, #182951, .F. ) ;
#69658=VERTEX_POINT ( 'NONE', #186426 ) ;
#69669=EDGE_CURVE ( 'NONE', #42536, #213770, #7782, .T. ) ;
#69694=EDGE_CURVE ( 'NONE', #133079, #256777, #205968, .T. ) ;
#69708=LINE ( 'NONE', #244463, #184804 ) ;
#69735=ORIENTED_EDGE ( 'NONE', *, *, #15108, .T. ) ;
#69736=ORIENTED_EDGE ( 'NONE', *, *, #240800, .T. ) ;
#69746=EDGE_CURVE ( 'NONE', #216222, #188358, #235183, .T. ) ;
#69782=ORIENTED_EDGE ( 'NONE', *, *, #88190, .F. ) ;
#69837=CARTESIAN_POINT ( 'NONE',  ( 21.05000000000000071, 10.62950747927180295, -41.12797939999666141 ) ) ;
#69838=DIRECTION ( 'NONE',  ( 0.000000000000000000, 0.000000000000000000, -1.000000000000000000 ) ) ;
#69852=ORIENTED_EDGE ( 'NONE', *, *, #179428, .T. ) ;
#69873=ADVANCED_FACE ( 'NONE', ( #37621 ), #256592, .F. ) ;
#69919=AXIS2_PLACEMENT_3D ( 'NONE', #154324, #172605, #211700 ) ;
#69951=DIRECTION ( 'NONE',  ( 0.000000000000000000, -1.000000000000000000, 0.000000000000000000 ) ) ;
#69952=AXIS2_PLACEMENT_3D ( 'NONE', #171318, #142399, #60287 ) ;
#69956=LINE ( 'NONE', #149497, #193814 ) ;
#69961=( BOUNDED_SURFACE ( )  B_SPLINE_SURFACE ( 3, 2, ( 
 ( #105898, #169797, #249307 ),
 ( #228462, #8121, #109768 ),
 ( #184168, #66803, #49803 ),
 ( #5519, #146324, #85044 ),
 ( #143757, #244138, #246711 ),
 ( #225838, #47218, #126773 ),
 ( #87628, #147620, #227150 ),
 ( #65507, #48517, #155362 ),
 ( #17123, #34134, #150207 ),
 ( #211449, #171087, #212744 ) ),
 .UNSPECIFIED., .F., .F., .F. ) 
 B_SPLINE_SURFACE_WITH_KNOTS ( ( 4, 2, 2, 2, 4 ),
 ( 3, 3 ),
 ( 0.0001836757140119083063, 0.0004000170051583575893, 0.0005081876507315822309, 0.0005622729735181946058, 0.0006163582963048068724 ),
 ( 0.000000000000000000, 1.000000000000000000 ),
 .UNSPECIFIED. ) 
 GEOMETRIC_REPRESENTATION_ITEM ( )  RATIONAL_B_SPLINE_SURFACE ( (
 ( 1.000000000000000000, 0.7071067811865425767, 1.000000000000000000),
 ( 1.000000000000000000, 0.6461995200036771969, 1.000000000000000000),
 ( 1.000000000000000000, 0.5776453529540377385, 1.000000000000000000),
 ( 1.000000000000000000, 0.4585233068356288633, 1.000000000000000000),
 ( 1.000000000000000000, 0.4154092989930812663, 1.000000000000000000),
 ( 1.000000000000000000, 0.3550093145840674258, 1.000000000000000000),
 ( 1.000000000000000000, 0.3354498651685111632, 1.000000000000000000),
 ( 1.000000000000000000, 0.3060347992257030914, 1.000000000000000000),
 ( 1.000000000000000000, 0.2963555829626022819, 1.000000000000000000),
 ( 1.000000000000000000, 0.2966190024560417804, 1.000000000000000000) ) ) 
 REPRESENTATION_ITEM ( '' )  SURFACE ( )  );
#70048=CARTESIAN_POINT ( 'NONE',  ( 18.52928932188133970, 10.27928932189250411, -58.15000000000000568 ) ) ;
#70050=CARTESIAN_POINT ( 'NONE',  ( 18.59999999999999787, -1.835341550213255957, -45.05515129256298223 ) ) ;
#70059=CARTESIAN_POINT ( 'NONE',  ( -21.52071067811865746, 7.779289321892505882, -54.65000000000000568 ) ) ;
#70063=FACE_OUTER_BOUND ( 'NONE', #111814, .T. ) ;
#70065=AXIS2_PLACEMENT_3D ( 'NONE', #116293, #159273, #215366 ) ;
#70071=CARTESIAN_POINT ( 'NONE',  ( 21.05000000000000071, 1.162701749949165642, -41.60000000000000142 ) ) ;
#70080=DIRECTION ( 'NONE',  ( 0.000000000000000000, -0.5000000000000014433, 0.8660254037844378194 ) ) ;
#70109=CARTESIAN_POINT ( 'NONE',  ( -20.94999999999999929, 1.750000000011155743, -45.16951155790164307 ) ) ;
#70145=CARTESIAN_POINT ( 'NONE',  ( -20.85000000000000142, -1.135018845899022466, -74.71697688343232358 ) ) ;
#70146=CARTESIAN_POINT ( 'NONE',  ( 21.14999999999999858, 1.115600667400684642E-11, -45.65000000000000568 ) ) ;
#70191=DIRECTION ( 'NONE',  ( 0.000000000000000000, 0.000000000000000000, -1.000000000000000000 ) ) ;
#70252=EDGE_CURVE ( 'NONE', #149752, #237399, #63103, .T. ) ;
#70258=FACE_OUTER_BOUND ( 'NONE', #89301, .T. ) ;
#70265=AXIS2_PLACEMENT_3D ( 'NONE', #129759, #48932, #26840 ) ;
#70281=DIRECTION ( 'NONE',  ( 1.000000000000000000, -0.000000000000000000, -0.000000000000000000 ) ) ;
#70289=DIRECTION ( 'NONE',  ( 0.7071067811865475727, -0.7071067811865475727, 0.000000000000000000 ) ) ;
#70305=DIRECTION ( 'NONE',  ( 0.000000000000000000, -1.000000000000000000, 0.000000000000000000 ) ) ;
#70337=CARTESIAN_POINT ( 'NONE',  ( -18.59999999999999787, -1.835341550213255957, -45.15515129256298366 ) ) ;
#70344=EDGE_LOOP ( 'NONE', ( #82923, #180315, #92043, #224348 ) ) ;
#70355=DIRECTION ( 'NONE',  ( 1.000000000000000000, -0.000000000000000000, -0.000000000000000000 ) ) ;
#70363=CIRCLE ( 'NONE', #45190, 7.900000000000000355 ) ;
#70382=AXIS2_PLACEMENT_3D ( 'NONE', #239240, #60584, #33707 ) ;
#70399=CYLINDRICAL_SURFACE ( 'NONE', #57571, 0.09999999999999939493 ) ;
#70408=ORIENTED_EDGE ( 'NONE', *, *, #16209, .T. ) ;
#70451=AXIS2_PLACEMENT_3D ( 'NONE', #192311, #250975, #231448 ) ;
#70462=CARTESIAN_POINT ( 'NONE',  ( 20.94999999999999574, 1.835341550235567887, -45.05515129256298223 ) ) ;
#70482=DIRECTION ( 'NONE',  ( 1.000000000000000000, -0.000000000000000000, -0.000000000000000000 ) ) ;
#70486=FACE_OUTER_BOUND ( 'NONE', #191448, .T. ) ;
#70507=CARTESIAN_POINT ( 'NONE',  ( 23.14999999999999858, 1.115600667400684642E-11, -67.00000000000000000 ) ) ;
#70610=EDGE_LOOP ( 'NONE', ( #96326, #181103, #164513, #106128 ) ) ;
#70619=EDGE_CURVE ( 'NONE', #74897, #139488, #206513, .T. ) ;
#70641=AXIS2_PLACEMENT_3D ( 'NONE', #1388, #217861, #118803 ) ;
#70648=ORIENTED_EDGE ( 'NONE', *, *, #41232, .F. ) ;
#70650=CARTESIAN_POINT ( 'NONE',  ( -22.59999999999999787, 11.64957080755595520, -33.40000000000000568 ) ) ;
#70667=DIRECTION ( 'NONE',  ( 0.000000000000000000, 0.000000000000000000, 1.000000000000000000 ) ) ;
#70683=CIRCLE ( 'NONE', #153923, 6.329289321881367059 ) ;
#70705=CARTESIAN_POINT ( 'NONE',  ( 21.05995757104869526, 8.775389244732430427, -45.69490512299120866 ) ) ;
#70714=CARTESIAN_POINT ( 'NONE',  ( -21.65000000000000213, 7.708578643773852157, -54.65000000000000568 ) ) ;
#70729=DIRECTION ( 'NONE',  ( 0.000000000000000000, 0.000000000000000000, -1.000000000000000000 ) ) ;
#70752=EDGE_CURVE ( 'NONE', #168869, #72318, #105915, .T. ) ;
#70754=CIRCLE ( 'NONE', #237329, 0.09999999999999939493 ) ;
#70758=CARTESIAN_POINT ( 'NONE',  ( -21.05000000000000426, 6.477046381801002894, -33.60000000000000853 ) ) ;
#70776=DIRECTION ( 'NONE',  ( 0.000000000000000000, 0.000000000000000000, -1.000000000000000000 ) ) ;
#70800=DIRECTION ( 'NONE',  ( 1.000000000000000000, 7.304098846218133681E-16, -4.607487905232622991E-31 ) ) ;
#70826=CYLINDRICAL_SURFACE ( 'NONE', #242853, 0.8750000000000007772 ) ;
#70836=DIRECTION ( 'NONE',  ( 0.000000000000000000, 0.000000000000000000, -1.000000000000000000 ) ) ;
#70846=AXIS2_PLACEMENT_3D ( 'NONE', #86299, #87592, #6791 ) ;
#70848=ORIENTED_EDGE ( 'NONE', *, *, #186406, .T. ) ;
#70867=CARTESIAN_POINT ( 'NONE',  ( -23.15000000000000213, -8.999999999988846255, -43.39396912265245021 ) ) ;
#70893=CARTESIAN_POINT ( 'NONE',  ( 18.59999999999999787, -1.263275465206102233, -74.90186466674640542 ) ) ;
#70919=FACE_OUTER_BOUND ( 'NONE', #152514, .T. ) ;
#70930=DIRECTION ( 'NONE',  ( 0.000000000000000000, 1.000000000000000000, 0.000000000000000000 ) ) ;
#70934=EDGE_CURVE ( 'NONE', #46286, #230427, #222872, .T. ) ;
#70977=EDGE_LOOP ( 'NONE', ( #103379, #170510, #254737 ) ) ;
#70987=VERTEX_POINT ( 'NONE', #84605 ) ;
#71045=LINE ( 'NONE', #87988, #176046 ) ;
#71066=ORIENTED_EDGE ( 'NONE', *, *, #163402, .F. ) ;
#71115=CIRCLE ( 'NONE', #54526, 0.09999999999999911737 ) ;
#71121=CARTESIAN_POINT ( 'NONE',  ( 20.95512820512820085, 10.62384868372303615, -41.16491356908760935 ) ) ;
#71124=LINE ( 'NONE', #150641, #127442 ) ;
#71126=CARTESIAN_POINT ( 'NONE',  ( -20.94999999999999929, 1.115600667400684642E-11, -67.00000000000000000 ) ) ;
#71128=CARTESIAN_POINT ( 'NONE',  ( 18.50000000000010303, 10.37342005529087530, -58.26578812462643953 ) ) ;
#71133=CARTESIAN_POINT ( 'NONE',  ( -18.59999999999999787, 1.115600667400684642E-11, -33.50000000000000000 ) ) ;
#71136=DIRECTION ( 'NONE',  ( 0.000000000000000000, -1.000000000000000000, 0.000000000000000000 ) ) ;
#71158=B_SPLINE_CURVE_WITH_KNOTS ( 'NONE', 3,
 ( #252934, #234670, #133016, #36497, #79423, #159013, #14369, #53467 ),
 .UNSPECIFIED., .F., .F.,
 ( 4, 2, 2, 4 ),
 ( 0.000000000000000000, 0.0001049670497870003278, 0.0002099340995740006557, 0.0004198681991479968120 ),
 .UNSPECIFIED. ) ;
#71173=ORIENTED_EDGE ( 'NONE', *, *, #201513, .T. ) ;
#71204=CARTESIAN_POINT ( 'NONE',  ( -20.94999999999999929, -11.39257802169451317, -63.92605042016806749 ) ) ;
#71213=TOROIDAL_SURFACE ( 'NONE', #46059, 0.4000000000000009104, 0.1000000000000000056 ) ;
#71237=DIRECTION ( 'NONE',  ( 0.000000000000000000, 0.8660254037844411501, 0.4999999999999956701 ) ) ;
#71242=VECTOR ( 'NONE', #185668, 1000.000000000000000 ) ;
#71270=CARTESIAN_POINT ( 'NONE',  ( 19.86930884467575353, 11.68691006698223411, -58.23922263893884121 ) ) ;
#71289=CARTESIAN_POINT ( 'NONE',  ( 18.49999999999998934, 6.550000000011156231, -54.75000000000000000 ) ) ;
#71326=VERTEX_POINT ( 'NONE', #15187 ) ;
#71330=ORIENTED_EDGE ( 'NONE', *, *, #24165, .F. ) ;
#71360=DIRECTION ( 'NONE',  ( 1.000000000000000000, 0.000000000000000000, 0.000000000000000000 ) ) ;
#71446=AXIS2_PLACEMENT_3D ( 'NONE', #178897, #182728, #220554 ) ;
#71464=CARTESIAN_POINT ( 'NONE',  ( -21.05000000000000071, 11.60000000001115339, -60.07179676972449300 ) ) ;
#71473=DIRECTION ( 'NONE',  ( 0.000000000000000000, 0.7397360091702777085, -0.6728971962616808744 ) ) ;
#71484=PLANE ( 'NONE',  #141821 ) ;
#71522=CIRCLE ( 'NONE', #67210, 0.09999999999999949207 ) ;
#71533=DIRECTION ( 'NONE',  ( -1.000000000000000000, -3.265361837132813093E-16, 0.000000000000000000 ) ) ;
#71588=AXIS2_PLACEMENT_3D ( 'NONE', #73753, #152013, #112854 ) ;
#71673=ORIENTED_EDGE ( 'NONE', *, *, #254499, .F. ) ;
#71704=DIRECTION ( 'NONE',  ( 1.000000000000000000, -0.000000000000000000, -0.000000000000000000 ) ) ;
#71728=CYLINDRICAL_SURFACE ( 'NONE', #128121, 0.09999999999999939493 ) ;
#71731=DIRECTION ( 'NONE',  ( 0.000000000000000000, 8.673617379883787770E-15, -1.000000000000000000 ) ) ;
#71732=EDGE_LOOP ( 'NONE', ( #7562, #184806, #208867, #178696 ) ) ;
#71735=ORIENTED_EDGE ( 'NONE', *, *, #98158, .F. ) ;
#71760=ORIENTED_EDGE ( 'NONE', *, *, #200757, .T. ) ;
#71775=VECTOR ( 'NONE', #24776, 1000.000000000000000 ) ;
#71778=FACE_OUTER_BOUND ( 'NONE', #137731, .T. ) ;
#71797=DIRECTION ( 'NONE',  ( 1.000000000000000000, -7.304098846218134667E-16, 0.000000000000000000 ) ) ;
#71821=AXIS2_PLACEMENT_3D ( 'NONE', #26868, #106349, #4685 ) ;
#71905=CARTESIAN_POINT ( 'NONE',  ( -22.42357213249529124, 0.09908696401271366305, -25.82706761364006454 ) ) ;
#71914=DIRECTION ( 'NONE',  ( 0.000000000000000000, -0.000000000000000000, -1.000000000000000000 ) ) ;
#71915=VERTEX_POINT ( 'NONE', #105935 ) ;
#71944=EDGE_CURVE ( 'NONE', #115688, #41243, #177851, .T. ) ;
#71946=DIRECTION ( 'NONE',  ( 0.000000000000000000, 0.000000000000000000, -1.000000000000000000 ) ) ;
#71951=DIRECTION ( 'NONE',  ( -1.000000000000000000, -0.000000000000000000, 0.000000000000000000 ) ) ;
#71980=DIRECTION ( 'NONE',  ( 0.000000000000000000, 0.5000000000000078826, -0.8660254037844340447 ) ) ;
#71992=ORIENTED_EDGE ( 'NONE', *, *, #141183, .T. ) ;
#71998=CARTESIAN_POINT ( 'NONE',  ( 20.94999999999999929, -1.349153571964892606, -74.78749733558989021 ) ) ;
#72000=LINE ( 'NONE', #152844, #206471 ) ;
#72012=TOROIDAL_SURFACE ( 'NONE', #155617, 0.2000000000000000111, 0.1000000000000000056 ) ;
#72040=EDGE_CURVE ( 'NONE', #87677, #29148, #160902, .T. ) ;
#72045=CARTESIAN_POINT ( 'NONE',  ( 18.59999999999999787, -9.321008403350148797, -40.73593824907786143 ) ) ;
#72048=AXIS2_PLACEMENT_3D ( 'NONE', #40357, #100260, #19478 ) ;
#72066=LINE ( 'NONE', #92886, #136117 ) ;
#72075=CARTESIAN_POINT ( 'NONE',  ( 21.33487959338958362, 6.725558151922348848, -33.50000000000000000 ) ) ;
#72091=DIRECTION ( 'NONE',  ( -0.000000000000000000, -0.7397360091702755991, -0.6728971962616832059 ) ) ;
#72102=FACE_OUTER_BOUND ( 'NONE', #103652, .T. ) ;
#72121=ORIENTED_EDGE ( 'NONE', *, *, #79590, .T. ) ;
#72122=VERTEX_POINT ( 'NONE', #113658 ) ;
#72145=DIRECTION ( 'NONE',  ( 0.000000000000000000, -0.8777080977375132376, 0.4791956752371582251 ) ) ;
#72171=DIRECTION ( 'NONE',  ( 0.000000000000000000, 0.000000000000000000, -1.000000000000000000 ) ) ;
#72198=DIRECTION ( 'NONE',  ( 0.000000000000000000, 1.224646799142015331E-16, 1.000000000000000000 ) ) ;
#72211=EDGE_CURVE ( 'NONE', #176891, #168958, #144108, .T. ) ;
#72242=ORIENTED_EDGE ( 'NONE', *, *, #146552, .T. ) ;
#72250=VECTOR ( 'NONE', #34223, 1000.000000000000000 ) ;
#72300=ADVANCED_FACE ( 'NONE', ( #106588 ), #19232, .F. ) ;
#72303=ORIENTED_EDGE ( 'NONE', *, *, #204546, .T. ) ;
#72310=CARTESIAN_POINT ( 'NONE',  ( -21.05000000000000071, 1.115600667400684642E-11, -67.00000000000000000 ) ) ;
#72318=VERTEX_POINT ( 'NONE', #33543 ) ;
#72322=FACE_OUTER_BOUND ( 'NONE', #109707, .T. ) ;
#72343=ORIENTED_EDGE ( 'NONE', *, *, #30628, .F. ) ;
#72345=ADVANCED_FACE ( 'NONE', ( #190006 ), #51745, .F. ) ;
#72351=CARTESIAN_POINT ( 'NONE',  ( 18.52928932188133970, 10.27928932189250411, -58.15000000000000568 ) ) ;
#72354=CARTESIAN_POINT ( 'NONE',  ( -23.25000000000000000, 1.115600667400684642E-11, -67.00000000000000000 ) ) ;
#72361=VERTEX_POINT ( 'NONE', #53050 ) ;
#72365=ORIENTED_EDGE ( 'NONE', *, *, #3451, .F. ) ;
#72370=CARTESIAN_POINT ( 'NONE',  ( -18.52643265882458579, 10.31973158071402530, -72.55053347133545572 ) ) ;
#72372=CYLINDRICAL_SURFACE ( 'NONE', #56822, 0.09999999999999804878 ) ;
#72419=DIRECTION ( 'NONE',  ( -0.000000000000000000, -0.000000000000000000, 1.000000000000000000 ) ) ;
#72425=DIRECTION ( 'NONE',  ( 0.000000000000000000, 0.6728971962616792091, -0.7397360091702790408 ) ) ;
#72429=CIRCLE ( 'NONE', #10043, 0.09999999999999843736 ) ;
#72434=ORIENTED_EDGE ( 'NONE', *, *, #20963, .T. ) ;
#72444=CARTESIAN_POINT ( 'NONE',  ( -21.44999999999999929, 7.350000000011155166, -54.65000000000000568 ) ) ;
#72472=CARTESIAN_POINT ( 'NONE',  ( -21.14999999999999858, 11.75000000001115552, -33.60000000000000142 ) ) ;
#72482=AXIS2_PLACEMENT_3D ( 'NONE', #122631, #17109, #200860 ) ;
#72497=DIRECTION ( 'NONE',  ( 1.000000000000000000, 0.000000000000000000, -0.000000000000000000 ) ) ;
#72499=CARTESIAN_POINT ( 'NONE',  ( -20.94999999999999929, 1.115600667400684642E-11, -62.90000000000001279 ) ) ;
#72501=EDGE_LOOP ( 'NONE', ( #190436, #29049, #216500, #159421 ) ) ;
#72504=EDGE_CURVE ( 'NONE', #14704, #134939, #118167, .T. ) ;
#72521=ORIENTED_EDGE ( 'NONE', *, *, #152497, .T. ) ;
#72522=FACE_OUTER_BOUND ( 'NONE', #12700, .T. ) ;
#72536=CARTESIAN_POINT ( 'NONE',  ( 18.49999999999999289, 10.20857864377385127, -54.85000000000000142 ) ) ;
#72602=CARTESIAN_POINT ( 'NONE',  ( 21.08035267497491105, 6.331706839794169817, -33.41731137522386774 ) ) ;
#72616=EDGE_LOOP ( 'NONE', ( #240219, #120544, #209909, #176222 ) ) ;
#72620=ORIENTED_EDGE ( 'NONE', *, *, #42667, .F. ) ;
#72626=VERTEX_POINT ( 'NONE', #205384 ) ;
#72632=EDGE_CURVE ( 'NONE', #212292, #208213, #144281, .T. ) ;
#72650=EDGE_LOOP ( 'NONE', ( #122072, #185603, #23543, #192937 ) ) ;
#72663=CIRCLE ( 'NONE', #35274, 0.09999999999999913125 ) ;
#72679=EDGE_LOOP ( 'NONE', ( #10990, #49029, #17371, #210125 ) ) ;
#72733=LINE ( 'NONE', #231789, #6611 ) ;
#72757=ORIENTED_EDGE ( 'NONE', *, *, #206753, .F. ) ;
#72796=CARTESIAN_POINT ( 'NONE',  ( 22.57320508075687115, 11.75000000001115552, -33.50000000000000000 ) ) ;
#72808=EDGE_LOOP ( 'NONE', ( #48634, #252100, #130184, #158287 ) ) ;
#72858=LINE ( 'NONE', #28621, #240481 ) ;
#72870=ORIENTED_EDGE ( 'NONE', *, *, #190772, .F. ) ;
#72874=CIRCLE ( 'NONE', #202018, 0.09999999999999693856 ) ;
#72879=VECTOR ( 'NONE', #212756, 1000.000000000000000 ) ;
#72881=CIRCLE ( 'NONE', #102036, 7.791421356237317575 ) ;
#72894=DIRECTION ( 'NONE',  ( 1.000000000000000000, 0.000000000000000000, 0.000000000000000000 ) ) ;
#72896=ORIENTED_EDGE ( 'NONE', *, *, #204674, .T. ) ;
#72907=PLANE ( 'NONE',  #83294 ) ;
#72911=DIRECTION ( 'NONE',  ( 0.000000000000000000, 0.000000000000000000, -1.000000000000000000 ) ) ;
#72934=EDGE_LOOP ( 'NONE', ( #241309, #238129, #154777, #234126 ) ) ;
#72962=EDGE_CURVE ( 'NONE', #125125, #43174, #223581, .T. ) ;
#72965=CARTESIAN_POINT ( 'NONE',  ( -20.94999999999999929, 1.736257131608553550, -45.06865232901750318 ) ) ;
#72990=VERTEX_POINT ( 'NONE', #63013 ) ;
#73004=ORIENTED_EDGE ( 'NONE', *, *, #168746, .T. ) ;
#73026=ORIENTED_EDGE ( 'NONE', *, *, #48272, .F. ) ;
#73039=ADVANCED_FACE ( 'NONE', ( #100817 ), #44552, .F. ) ;
#73050=CARTESIAN_POINT ( 'NONE',  ( -23.15000000000000213, 1.115600667400684642E-11, -33.50000000000000000 ) ) ;
#73054=AXIS2_PLACEMENT_3D ( 'NONE', #119655, #199183, #64791 ) ;
#73070=CARTESIAN_POINT ( 'NONE',  ( -21.05000000000000071, 1.835341550235567887, -45.05515129256298223 ) ) ;
#73073=FACE_OUTER_BOUND ( 'NONE', #69147, .T. ) ;
#73080=DIRECTION ( 'NONE',  ( 0.000000000000000000, -0.000000000000000000, 1.000000000000000000 ) ) ;
#73084=DIRECTION ( 'NONE',  ( 2.952720810173288619E-16, -1.000000000000000000, 0.000000000000000000 ) ) ;
#73120=ORIENTED_EDGE ( 'NONE', *, *, #207460, .F. ) ;
#73124=DIRECTION ( 'NONE',  ( 0.000000000000000000, 0.000000000000000000, -1.000000000000000000 ) ) ;
#73125=DIRECTION ( 'NONE',  ( 0.000000000000000000, 0.000000000000000000, -1.000000000000000000 ) ) ;
#73138=DIRECTION ( 'NONE',  ( -7.304098846218134667E-16, -1.000000000000000000, 0.000000000000000000 ) ) ;
#73139=CARTESIAN_POINT ( 'NONE',  ( -18.50000000000000000, 7.021664781911246322, -70.63356540189728605 ) ) ;
#73159=ADVANCED_FACE ( 'NONE', ( #133274 ), #148608, .T. ) ;
#73165=DIRECTION ( 'NONE',  ( 1.000000000000000000, 0.000000000000000000, 0.000000000000000000 ) ) ;
#73189=DIRECTION ( 'NONE',  ( 1.000000000000000000, 0.000000000000000000, -0.000000000000000000 ) ) ;
#73197=AXIS2_PLACEMENT_3D ( 'NONE', #58781, #176210, #95371 ) ;
#73205=CARTESIAN_POINT ( 'NONE',  ( 18.44208962362722204, -9.552340496897459232, -73.84217305546387422 ) ) ;
#73208=EDGE_LOOP ( 'NONE', ( #20874, #254774, #29818, #252036 ) ) ;
#73225=CIRCLE ( 'NONE', #106462, 0.1000000000000028644 ) ;
#73283=DIRECTION ( 'NONE',  ( 1.000000000000000000, -0.000000000000000000, -0.000000000000000000 ) ) ;
#73327=DIRECTION ( 'NONE',  ( 0.000000000000000000, -1.000000000000000000, 0.000000000000000000 ) ) ;
#73336=ADVANCED_FACE ( 'NONE', ( #45726 ), #101814, .T. ) ;
#73370=FACE_OUTER_BOUND ( 'NONE', #217977, .T. ) ;
#73372=DIRECTION ( 'NONE',  ( 0.000000000000000000, 1.000000000000000000, 0.000000000000000000 ) ) ;
#73385=DIRECTION ( 'NONE',  ( -1.000000000000000000, 0.000000000000000000, 0.000000000000000000 ) ) ;
#73388=DIRECTION ( 'NONE',  ( 1.000000000000000000, 0.000000000000000000, 0.000000000000000000 ) ) ;
#73409=LINE ( 'NONE', #31717, #14744 ) ;
#73413=CARTESIAN_POINT ( 'NONE',  ( -23.15000000000000213, 4.350000000011156054, -45.85000000000000142 ) ) ;
#73472=CIRCLE ( 'NONE', #48490, 2.000000000000001776 ) ;
#73474=CIRCLE ( 'NONE', #173464, 0.1000000000000028644 ) ;
#73487=DIRECTION ( 'NONE',  ( 0.000000000000000000, 0.000000000000000000, -1.000000000000000000 ) ) ;
#73498=ADVANCED_FACE ( 'NONE', ( #186533 ), #71728, .T. ) ;
#73522=CARTESIAN_POINT ( 'NONE',  ( -20.94999999999999929, 11.65000000001115232, -60.21613433702190576 ) ) ;
#73531=CARTESIAN_POINT ( 'NONE',  ( 21.04999999999999716, 6.496686585779318790, -33.51465611851394755 ) ) ;
#73548=DIRECTION ( 'NONE',  ( 0.000000000000000000, 1.000000000000000000, -6.308085367188393199E-16 ) ) ;
#73560=CARTESIAN_POINT ( 'NONE',  ( 18.59999999999999076, 1.835341550235567887, -45.15515129256298366 ) ) ;
#73570=ORIENTED_EDGE ( 'NONE', *, *, #62932, .F. ) ;
#73576=ORIENTED_EDGE ( 'NONE', *, *, #190314, .T. ) ;
#73606=DIRECTION ( 'NONE',  ( -0.000000000000000000, 0.6132151058540549204, -0.7899159663865520375 ) ) ;
#73654=CIRCLE ( 'NONE', #52760, 11.65000000000000036 ) ;
#73660=CARTESIAN_POINT ( 'NONE',  ( -18.59999999999999787, -1.835859311432481045, -78.50443916879852679 ) ) ;
#73673=CIRCLE ( 'NONE', #102844, 0.09999999999999939493 ) ;
#73682=VERTEX_POINT ( 'NONE', #4975 ) ;
#73687=EDGE_CURVE ( 'NONE', #22291, #201039, #107452, .T. ) ;
#73700=ADVANCED_FACE ( 'NONE', ( #224038 ), #45415, .F. ) ;
#73702=CARTESIAN_POINT ( 'NONE',  ( 18.49999999999999289, 10.23906162413259402, -58.25439743459697439 ) ) ;
#73733=EDGE_LOOP ( 'NONE', ( #212463, #183220, #182239, #163729 ) ) ;
#73753=CARTESIAN_POINT ( 'NONE',  ( -20.85000000000000142, -1.164121893230052995, -74.91484808557160591 ) ) ;
#73760=CARTESIAN_POINT ( 'NONE',  ( 21.05000000000000071, 5.000000000011153745, -55.09473398108690390 ) ) ;
#73775=ORIENTED_EDGE ( 'NONE', *, *, #23580, .T. ) ;
#73781=EDGE_CURVE ( 'NONE', #125880, #136260, #24092, .T. ) ;
#73790=DIRECTION ( 'NONE',  ( -1.000000000000000000, -0.000000000000000000, -0.000000000000000000 ) ) ;
#73797=VERTEX_POINT ( 'NONE', #188772 ) ;
#73816=ORIENTED_EDGE ( 'NONE', *, *, #163374, .T. ) ;
#73820=ORIENTED_EDGE ( 'NONE', *, *, #118543, .F. ) ;
#73821=DIRECTION ( 'NONE',  ( -1.000000000000000000, -0.000000000000000000, -0.000000000000000000 ) ) ;
#73824=ADVANCED_FACE ( 'NONE', ( #47973 ), #109228, .T. ) ;
#73842=DIRECTION ( 'NONE',  ( -1.000000000000000000, 0.000000000000000000, 0.000000000000000000 ) ) ;
#73856=AXIS2_PLACEMENT_3D ( 'NONE', #36537, #116057, #71797 ) ;
#73862=DIRECTION ( 'NONE',  ( 0.000000000000000000, 0.000000000000000000, -1.000000000000000000 ) ) ;
#73879=EDGE_LOOP ( 'NONE', ( #103990, #181048, #198055, #151528 ) ) ;
#73898=CARTESIAN_POINT ( 'NONE',  ( -20.94999999999999929, -1.164121893230052995, -74.71484808557160306 ) ) ;
#73952=VERTEX_POINT ( 'NONE', #173118 ) ;
#73983=AXIS2_PLACEMENT_3D ( 'NONE', #61440, #220525, #199693 ) ;
#73987=AXIS2_PLACEMENT_3D ( 'NONE', #149114, #108684, #12177 ) ;
#73996=DIRECTION ( 'NONE',  ( 0.000000000000000000, 0.000000000000000000, -1.000000000000000000 ) ) ;
#74007=EDGE_CURVE ( 'NONE', #104053, #82065, #4490, .T. ) ;
#74008=CIRCLE ( 'NONE', #86971, 4.000000000000003553 ) ;
#74018=LINE ( 'NONE', #173132, #23754 ) ;
#74021=CARTESIAN_POINT ( 'NONE',  ( -23.25000000000000000, -9.599999999988845900, -57.10603087734755690 ) ) ;
#74037=PLANE ( 'NONE',  #257252 ) ;
#74043=CARTESIAN_POINT ( 'NONE',  ( -20.94999999999999929, 11.63687328911525753, -60.17824078667513987 ) ) ;
#74076=CARTESIAN_POINT ( 'NONE',  ( 20.85000000000000142, -1.736705739456431807, -78.51742258762372728 ) ) ;
#74086=ORIENTED_EDGE ( 'NONE', *, *, #108693, .T. ) ;
#74107=CARTESIAN_POINT ( 'NONE',  ( -23.25000000000000000, -1.851617760457748618, -78.60318971960367662 ) ) ;
#74108=DIRECTION ( 'NONE',  ( 1.000000000000000000, -0.000000000000000000, -0.000000000000000000 ) ) ;
#74111=AXIS2_PLACEMENT_3D ( 'NONE', #161194, #201585, #219868 ) ;
#74125=ORIENTED_EDGE ( 'NONE', *, *, #42026, .F. ) ;
#74168=DIRECTION ( 'NONE',  ( 0.000000000000000000, 0.000000000000000000, -1.000000000000000000 ) ) ;
#74235=AXIS2_PLACEMENT_3D ( 'NONE', #77520, #99650, #119260 ) ;
#74284=CARTESIAN_POINT ( 'NONE',  ( -21.29999999999995808, 1.115650265596050101E-11, -29.45000000000000284 ) ) ;
#74318=EDGE_CURVE ( 'NONE', #252850, #107953, #165919, .T. ) ;
#74360=CARTESIAN_POINT ( 'NONE',  ( 22.39999999999999503, 1.115600667400684642E-11, -25.70922040162662370 ) ) ;
#74369=AXIS2_PLACEMENT_3D ( 'NONE', #38678, #185877, #128481 ) ;
#74379=ADVANCED_FACE ( 'NONE', ( #229411 ), #35092, .T. ) ;
#74381=CARTESIAN_POINT ( 'NONE',  ( 22.42196299218230493, 0.002441673998456600492, -21.85038829735053056 ) ) ;
#74393=DIRECTION ( 'NONE',  ( -1.000000000000000000, -0.000000000000000000, 0.000000000000000000 ) ) ;
#74408=ORIENTED_EDGE ( 'NONE', *, *, #136881, .T. ) ;
#74409=ADVANCED_FACE ( 'NONE', ( #231989 ), #93738, .T. ) ;
#74414=CARTESIAN_POINT ( 'NONE',  ( -20.15000000000000568, 9.291421356248463326, -45.85000000000000142 ) ) ;
#74425=ORIENTED_EDGE ( 'NONE', *, *, #11499, .F. ) ;
#74430=VECTOR ( 'NONE', #125635, 1000.000000000000000 ) ;
#74441=LINE ( 'NONE', #234757, #30254 ) ;
#74451=CYLINDRICAL_SURFACE ( 'NONE', #253644, 0.09999999999999693856 ) ;
#74452=CARTESIAN_POINT ( 'NONE',  ( 21.05000000000000071, 0.09779029131994770863, -27.24218538952387547 ) ) ;
#74503=LINE ( 'NONE', #134405, #219572 ) ;
#74506=ORIENTED_EDGE ( 'NONE', *, *, #174275, .T. ) ;
#74515=DIRECTION ( 'NONE',  ( 7.304098846218134667E-16, 1.000000000000000000, -0.000000000000000000 ) ) ;
#74517=CIRCLE ( 'NONE', #53627, 3.999999999999999112 ) ;
#74550=CIRCLE ( 'NONE', #91263, 0.09999999999999939493 ) ;
#74610=EDGE_CURVE ( 'NONE', #32909, #252850, #224536, .T. ) ;
#74630=ORIENTED_EDGE ( 'NONE', *, *, #187479, .F. ) ;
#74632=EDGE_CURVE ( 'NONE', #215029, #224490, #53653, .T. ) ;
#74658=AXIS2_PLACEMENT_3D ( 'NONE', #208012, #231424, #168913 ) ;
#74661=DIRECTION ( 'NONE',  ( 2.715809747126116508E-16, -1.000000000000000000, -2.172647797700893206E-15 ) ) ;
#74702=EDGE_CURVE ( 'NONE', #88400, #190257, #144614, .T. ) ;
#74716=EDGE_CURVE ( 'NONE', #137338, #226022, #15798, .T. ) ;
#74721=CIRCLE ( 'NONE', #16435, 0.1000000000000002554 ) ;
#74746=CARTESIAN_POINT ( 'NONE',  ( -23.15000000000000213, 1.115600667400684642E-11, -67.00000000000000000 ) ) ;
#74775=DIRECTION ( 'NONE',  ( 0.000000000000000000, 1.000000000000000000, 0.000000000000000000 ) ) ;
#74777=EDGE_LOOP ( 'NONE', ( #163079, #90821, #210916, #200036, #124560 ) ) ;
#74811=EDGE_CURVE ( 'NONE', #154736, #127278, #101682, .T. ) ;
#74823=CARTESIAN_POINT ( 'NONE',  ( 21.13422380239050824, 6.493326514816692985, -33.50000000000000000 ) ) ;
#74829=EDGE_CURVE ( 'NONE', #61363, #11718, #74721, .T. ) ;
#74833=ADVANCED_FACE ( 'NONE', ( #40503 ), #132960, .F. ) ;
#74863=VERTEX_POINT ( 'NONE', #102984 ) ;
#74867=AXIS2_PLACEMENT_3D ( 'NONE', #256363, #238136, #36119 ) ;
#74872=FACE_OUTER_BOUND ( 'NONE', #40400, .T. ) ;
#74882=ORIENTED_EDGE ( 'NONE', *, *, #249290, .T. ) ;
#74894=DIRECTION ( 'NONE',  ( 1.000000000000000000, 0.000000000000000000, 0.000000000000000000 ) ) ;
#74897=VERTEX_POINT ( 'NONE', #123862 ) ;
#74899=VECTOR ( 'NONE', #174727, 1000.000000000000000 ) ;
#74918=AXIS2_PLACEMENT_3D ( 'NONE', #193571, #16238, #137423 ) ;
#74923=ORIENTED_EDGE ( 'NONE', *, *, #118543, .T. ) ;
#74924=EDGE_CURVE ( 'NONE', #255894, #87561, #178778, .T. ) ;
#74965=ORIENTED_EDGE ( 'NONE', *, *, #92317, .F. ) ;
#74976=EDGE_CURVE ( 'NONE', #11734, #129370, #116382, .T. ) ;
#74980=EDGE_CURVE ( 'NONE', #119332, #204996, #2607, .T. ) ;
#74994=CARTESIAN_POINT ( 'NONE',  ( -21.05000000000000071, 1.851028230152016674, -45.15391326942250316 ) ) ;
#75014=DIRECTION ( 'NONE',  ( 1.000000000000000000, 0.000000000000000000, 0.000000000000000000 ) ) ;
#75029=LINE ( 'NONE', #237915, #117889 ) ;
#75058=CARTESIAN_POINT ( 'NONE',  ( -20.54999999999999716, 1.115600667400684642E-11, -33.50000000000000000 ) ) ;
#75070=EDGE_LOOP ( 'NONE', ( #224321, #179529, #131580, #123651 ) ) ;
#75102=ADVANCED_FACE ( 'NONE', ( #197927 ), #75460, .T. ) ;
#75104=DIRECTION ( 'NONE',  ( -0.8660254037843878594, 0.000000000000000000, -0.5000000000000880407 ) ) ;
#75107=ORIENTED_EDGE ( 'NONE', *, *, #98223, .F. ) ;
#75112=DIRECTION ( 'NONE',  ( 0.000000000000000000, 0.000000000000000000, -1.000000000000000000 ) ) ;
#75119=CARTESIAN_POINT ( 'NONE',  ( -18.59999999999999787, 9.350000000011156942, -45.75000000000000000 ) ) ;
#75125=CARTESIAN_POINT ( 'NONE',  ( 23.14999999999999503, 11.65000000001116298, -60.08519422934606524 ) ) ;
#75130=DIRECTION ( 'NONE',  ( 0.000000000000000000, 0.000000000000000000, -1.000000000000000000 ) ) ;
#75150=EDGE_LOOP ( 'NONE', ( #166325, #177653, #107852, #105176, #248787 ) ) ;
#75153=DIRECTION ( 'NONE',  ( -0.7071067811865475727, -0.7071067811865475727, 0.000000000000000000 ) ) ;
#75255=ORIENTED_EDGE ( 'NONE', *, *, #147676, .F. ) ;
#75268=ORIENTED_EDGE ( 'NONE', *, *, #97825, .F. ) ;
#75308=DIRECTION ( 'NONE',  ( 0.000000000000000000, -0.9893560106964500722, 0.1455152366551550613 ) ) ;
#75326=AXIS2_PLACEMENT_3D ( 'NONE', #99744, #21533, #155918 ) ;
#75358=CARTESIAN_POINT ( 'NONE',  ( 21.05000000000000071, 11.65000000001115943, -33.60000000000000142 ) ) ;
#75378=LINE ( 'NONE', #227041, #205438 ) ;
#75382=LINE ( 'NONE', #74107, #62364 ) ;
#75386=FACE_OUTER_BOUND ( 'NONE', #181271, .T. ) ;
#75420=CARTESIAN_POINT ( 'NONE',  ( -20.54999999999999716, 1.115600667400684642E-11, -67.00000000000000000 ) ) ;
#75422=CARTESIAN_POINT ( 'NONE',  ( -23.15000000000000213, 4.150000000011156764, -54.64999999999999858 ) ) ;
#75427=ORIENTED_EDGE ( 'NONE', *, *, #224895, .F. ) ;
#75455=LINE ( 'NONE', #154987, #17785 ) ;
#75460=CYLINDRICAL_SURFACE ( 'NONE', #41571, 0.09999999999999811817 ) ;
#75480=DIRECTION ( 'NONE',  ( 2.952720810173289112E-16, -1.000000000000000000, 0.000000000000000000 ) ) ;
#75481=ADVANCED_FACE ( 'NONE', ( #79895 ), #240301, .T. ) ;
#75487=AXIS2_PLACEMENT_3D ( 'NONE', #229729, #71951, #151506 ) ;
#75517=EDGE_CURVE ( 'NONE', #42156, #117767, #162553, .T. ) ;
#75586=CIRCLE ( 'NONE', #221274, 0.1000000000000016431 ) ;
#75587=CARTESIAN_POINT ( 'NONE',  ( 21.14999999999999503, -11.64999999998883595, -36.39999999999999858 ) ) ;
#75621=DIRECTION ( 'NONE',  ( 1.000000000000000000, 3.265361837132813093E-16, -0.000000000000000000 ) ) ;
#75623=DIRECTION ( 'NONE',  ( 0.000000000000000000, 0.000000000000000000, 1.000000000000000000 ) ) ;
#75630=CARTESIAN_POINT ( 'NONE',  ( 20.12500000000000000, 9.750000000011153745, -41.61177128211428311 ) ) ;
#75670=CARTESIAN_POINT ( 'NONE',  ( -18.59999999999999787, 11.65000000001115232, -40.51480577065400013 ) ) ;
#75675=FACE_OUTER_BOUND ( 'NONE', #7126, .T. ) ;
#75737=DIRECTION ( 'NONE',  ( 0.000000000000000000, 1.000000000000000000, 0.000000000000000000 ) ) ;
#75741=CARTESIAN_POINT ( 'NONE',  ( -21.05000000000000071, -11.64999999998884483, -36.39999999999999858 ) ) ;
#75755=CARTESIAN_POINT ( 'NONE',  ( 18.52326479938714954, -9.642364444904220733, -73.71475741340583454 ) ) ;
#75818=CARTESIAN_POINT ( 'NONE',  ( -21.05000000000000071, 1.115600667400684642E-11, -33.50000000000000000 ) ) ;
#75871=VERTEX_POINT ( 'NONE', #214015 ) ;
#75876=DIRECTION ( 'NONE',  ( -0.000000000000000000, 0.000000000000000000, 1.000000000000000000 ) ) ;
#75877=DIRECTION ( 'NONE',  ( -0.8660254037844352659, 0.000000000000000000, 0.5000000000000059952 ) ) ;
#75923=ORIENTED_EDGE ( 'NONE', *, *, #64050, .T. ) ;
#75932=DIRECTION ( 'NONE',  ( 0.000000000000000000, 0.6728971962616697722, -0.7397360091702875895 ) ) ;
#75979=FACE_OUTER_BOUND ( 'NONE', #146030, .T. ) ;
#76011=CARTESIAN_POINT ( 'NONE',  ( -21.14999999999999858, -11.74999999998884448, -33.50000000000000000 ) ) ;
#76017=ORIENTED_EDGE ( 'NONE', *, *, #116423, .F. ) ;
#76035=ORIENTED_EDGE ( 'NONE', *, *, #138548, .F. ) ;
#76041=ADVANCED_FACE ( 'NONE', ( #46903 ), #246413, .T. ) ;
#76061=CARTESIAN_POINT ( 'NONE',  ( 21.07928932188134397, 6.328516656404468144, -33.40110485434561127 ) ) ;
#76083=AXIS2_PLACEMENT_3D ( 'NONE', #74746, #14760, #235070 ) ;
#76091=DIRECTION ( 'NONE',  ( 0.000000000000000000, 0.000000000000000000, 1.000000000000000000 ) ) ;
#76094=ORIENTED_EDGE ( 'NONE', *, *, #124465, .T. ) ;
#76097=ORIENTED_EDGE ( 'NONE', *, *, #116831, .T. ) ;
#76130=ORIENTED_EDGE ( 'NONE', *, *, #40277, .F. ) ;
#76147=CARTESIAN_POINT ( 'NONE',  ( 22.39999999999999503, 11.75000000001116263, -33.40000000000000568 ) ) ;
#76196=DIRECTION ( 'NONE',  ( 0.000000000000000000, 1.776356839400254803E-15, -1.000000000000000000 ) ) ;
#76200=ADVANCED_FACE ( 'NONE', ( #256613 ), #118464, .F. ) ;
#76229=LINE ( 'NONE', #145191, #6873 ) ;
#76240=ADVANCED_FACE ( 'NONE', ( #61027 ), #117172, .F. ) ;
#76249=DIRECTION ( 'NONE',  ( 0.000000000000000000, 1.734723475976757554E-14, -1.000000000000000000 ) ) ;
#76273=CARTESIAN_POINT ( 'NONE',  ( 20.94999999999999929, -11.29603075032412640, -63.95210084033612929 ) ) ;
#76275=CARTESIAN_POINT ( 'NONE',  ( -20.64999999999999858, -9.499999999988846255, -57.10603087734755690 ) ) ;
#76277=CARTESIAN_POINT ( 'NONE',  ( 23.14999999999999503, 11.65000000001116298, -59.98519422934606382 ) ) ;
#76335=EDGE_LOOP ( 'NONE', ( #251719, #114353, #216743, #154760 ) ) ;
#76354=CARTESIAN_POINT ( 'NONE',  ( 21.05000000000000071, -11.48912529306489994, -64.00000000000000000 ) ) ;
#76360=CARTESIAN_POINT ( 'NONE',  ( 18.49999999999999289, 6.450000000011156587, -21.75000000000000355 ) ) ;
#76369=CIRCLE ( 'NONE', #222104, 0.2000000000000000944 ) ;
#76375=DIRECTION ( 'NONE',  ( 0.000000000000000000, 0.000000000000000000, -1.000000000000000000 ) ) ;
#76394=( BOUNDED_SURFACE ( )  B_SPLINE_SURFACE ( 3, 2, ( 
 ( #62505, #142025, #6361 ),
 ( #165461, #128897, #89746 ),
 ( #227991, #187600, #109304 ),
 ( #8944, #208448, #66352 ) ),
 .UNSPECIFIED., .F., .F., .T. ) 
 B_SPLINE_SURFACE_WITH_KNOTS ( ( 4, 4 ),
 ( 3, 3 ),
 ( 0.0006461284895273985886, 0.0007503702773985944244 ),
 ( 0.000000000000000000, 1.000000000000000000 ),
 .UNSPECIFIED. ) 
 GEOMETRIC_REPRESENTATION_ITEM ( )  RATIONAL_B_SPLINE_SURFACE ( (
 ( 1.000000000000000000, 0.7071067811865475727, 1.000000000000000000),
 ( 1.000000000000000000, 0.7076476444648753805, 1.000000000000000000),
 ( 1.000000000000000000, 0.7075727925191906964, 1.000000000000000000),
 ( 1.000000000000000000, 0.7071067811865475727, 1.000000000000000000) ) ) 
 REPRESENTATION_ITEM ( '' )  SURFACE ( )  );
#76404=EDGE_CURVE ( 'NONE', #45390, #33354, #204577, .T. ) ;
#76405=DIRECTION ( 'NONE',  ( 1.000000000000000000, 0.000000000000000000, 0.000000000000000000 ) ) ;
#76421=ORIENTED_EDGE ( 'NONE', *, *, #255373, .F. ) ;
#76445=ADVANCED_FACE ( 'NONE', ( #110429 ), #108734, .T. ) ;
#76453=LINE ( 'NONE', #173045, #128366 ) ;
#76524=FILL_AREA_STYLE_COLOUR ( '', #6516 ) ;
#76572=EDGE_CURVE ( 'NONE', #53762, #53755, #71522, .T. ) ;
#76594=AXIS2_PLACEMENT_3D ( 'NONE', #98457, #195063, #178065 ) ;
#76597=ORIENTED_EDGE ( 'NONE', *, *, #104904, .F. ) ;
#76635=DIRECTION ( 'NONE',  ( 0.1538461538461510236, 0.9880948137434718559, 0.000000000000000000 ) ) ;
#76661=CARTESIAN_POINT ( 'NONE',  ( -20.85000000000000142, 7.070967871809997973, -70.74656422186831151 ) ) ;
#76743=DIRECTION ( 'NONE',  ( -1.000000000000000000, 0.000000000000000000, 0.000000000000000000 ) ) ;
#76770=DIRECTION ( 'NONE',  ( 1.000000000000000000, 0.000000000000000000, -0.000000000000000000 ) ) ;
#76776=CARTESIAN_POINT ( 'NONE',  ( 23.14999999999998437, 1.115600667400684642E-11, -37.54999999999999716 ) ) ;
#76779=AXIS2_PLACEMENT_3D ( 'NONE', #246376, #16446, #76375 ) ;
#76782=CIRCLE ( 'NONE', #147528, 3.999999999999999112 ) ;
#76783=DIRECTION ( 'NONE',  ( 0.000000000000000000, 1.000000000000000000, 0.000000000000000000 ) ) ;
#76854=VERTEX_POINT ( 'NONE', #168868 ) ;
#76872=EDGE_CURVE ( 'NONE', #14704, #194376, #162539, .T. ) ;
#76876=DIRECTION ( 'NONE',  ( 0.000000000000000000, -0.1455152366551522025, -0.9893560106964505163 ) ) ;
#76886=EDGE_CURVE ( 'NONE', #195525, #41986, #46348, .T. ) ;
#76887=DIRECTION ( 'NONE',  ( -1.000000000000000000, -0.000000000000000000, -0.000000000000000000 ) ) ;
#76899=FACE_OUTER_BOUND ( 'NONE', #218985, .T. ) ;
#76900=VECTOR ( 'NONE', #213688, 1000.000000000000000 ) ;
#76905=DIRECTION ( 'NONE',  ( 1.000000000000000000, 0.000000000000000000, 0.000000000000000000 ) ) ;
#76907=ORIENTED_EDGE ( 'NONE', *, *, #23809, .F. ) ;
#76909=EDGE_CURVE ( 'NONE', #2368, #102509, #221313, .T. ) ;
#76941=DIRECTION ( 'NONE',  ( 2.840903330521631775E-16, -0.8700118002898321601, 0.4930308989875230585 ) ) ;
#76962=CIRCLE ( 'NONE', #226803, 7.800000000000001599 ) ;
#76988=CARTESIAN_POINT ( 'NONE',  ( 20.85000000000000142, 11.65000000001115943, -67.00000000000000000 ) ) ;
#76991=CARTESIAN_POINT ( 'NONE',  ( 23.24999999999999645, 1.115600667400684642E-11, -67.00000000000000000 ) ) ;
#76999=ORIENTED_EDGE ( 'NONE', *, *, #85878, .T. ) ;
#77004=ORIENTED_EDGE ( 'NONE', *, *, #153159, .F. ) ;
#77027=CARTESIAN_POINT ( 'NONE',  ( -18.59999999999999787, 1.835341550235567887, -45.05515129256298223 ) ) ;
#77032=VECTOR ( 'NONE', #224457, 1000.000000000000000 ) ;
#77076=ADVANCED_FACE ( 'NONE', ( #106924 ), #10417, .F. ) ;
#77079=ORIENTED_EDGE ( 'NONE', *, *, #249252, .F. ) ;
#77149=CIRCLE ( 'NONE', #235361, 12.87499999999999822 ) ;
#77159=ORIENTED_EDGE ( 'NONE', *, *, #5328, .T. ) ;
#77163=DIRECTION ( 'NONE',  ( 0.000000000000000000, 0.4999999999999956701, -0.8660254037844411501 ) ) ;
#77164=DIRECTION ( 'NONE',  ( 0.000000000000000000, 0.000000000000000000, -1.000000000000000000 ) ) ;
#77175=CARTESIAN_POINT ( 'NONE',  ( 23.14999999999999503, 6.450000000011156587, -54.65000000000000568 ) ) ;
#77181=CARTESIAN_POINT ( 'NONE',  ( -18.59999999999999787, -1.835341550213255957, -45.05515129256298223 ) ) ;
#77185=CARTESIAN_POINT ( 'NONE',  ( 21.14999999999999858, 1.115600667400684642E-11, -26.95934304829875927 ) ) ;
#77212=CARTESIAN_POINT ( 'NONE',  ( 23.15000000000000213, -11.64999999998884483, -33.50000000000000000 ) ) ;
#77224=CYLINDRICAL_SURFACE ( 'NONE', #149226, 0.09999999999999939493 ) ;
#77255=CARTESIAN_POINT ( 'NONE',  ( 20.85000000000000142, 7.070967871809997973, -70.74656422186831151 ) ) ;
#77261=EDGE_CURVE ( 'NONE', #3690, #212292, #219489, .T. ) ;
#77300=DIRECTION ( 'NONE',  ( 0.000000000000000000, -0.1350103645451876666, -0.9908441862701600211 ) ) ;
#77308=ORIENTED_EDGE ( 'NONE', *, *, #10063, .F. ) ;
#77313=PLANE ( 'NONE',  #6364 ) ;
#77341=EDGE_CURVE ( 'NONE', #212737, #12445, #11706, .T. ) ;
#77348=DIRECTION ( 'NONE',  ( -1.000000000000000000, -0.000000000000000000, -0.000000000000000000 ) ) ;
#77356=EDGE_CURVE ( 'NONE', #136008, #202789, #158618, .T. ) ;
#77418=CARTESIAN_POINT ( 'NONE',  ( -20.64999999999999858, 1.115600667400684642E-11, -33.50000000000000000 ) ) ;
#77424=LINE ( 'NONE', #61739, #115653 ) ;
#77458=CARTESIAN_POINT ( 'NONE',  ( -18.59999999999999787, 9.350000000011156942, -54.85000000000000142 ) ) ;
#77462=AXIS2_PLACEMENT_3D ( 'NONE', #246741, #128098, #87664 ) ;
#77464=CARTESIAN_POINT ( 'NONE',  ( -20.94999999999999929, -11.41227409413852811, -64.10000000000000853 ) ) ;
#77471=FACE_OUTER_BOUND ( 'NONE', #91511, .T. ) ;
#77488=DIRECTION ( 'NONE',  ( 0.000000000000000000, 0.000000000000000000, -1.000000000000000000 ) ) ;
#77489=( BOUNDED_SURFACE ( )  B_SPLINE_SURFACE ( 3, 2, ( 
 ( #158455, #120606, #17610 ),
 ( #39796, #38482, #136261 ),
 ( #201396, #178007, #176721 ),
 ( #159719, #237951, #257462 ),
 ( #60592, #239253, #215805 ),
 ( #256169, #219671, #118010 ) ),
 .UNSPECIFIED., .F., .F., .F. ) 
 B_SPLINE_SURFACE_WITH_KNOTS ( ( 4, 2, 4 ),
 ( 3, 3 ),
 ( 0.0001792624049599548033, 0.0003686986002124707481, 0.0005581347954649866928 ),
 ( 0.000000000000000000, 1.000000000000000000 ),
 .UNSPECIFIED. ) 
 GEOMETRIC_REPRESENTATION_ITEM ( )  RATIONAL_B_SPLINE_SURFACE ( (
 ( 1.000000000000000000, 0.9238795325112840739, 1.000000000000000000),
 ( 1.000000000000000000, 0.9229318695237281878, 1.000000000000000000),
 ( 1.000000000000000000, 0.8926288119232251850, 1.000000000000000000),
 ( 1.000000000000000000, 0.8123777807269819684, 1.000000000000000000),
 ( 1.000000000000000000, 0.7629087100932636645, 1.000000000000000000),
 ( 1.000000000000000000, 0.7071067811865475727, 1.000000000000000000) ) ) 
 REPRESENTATION_ITEM ( '' )  SURFACE ( )  );
#77520=CARTESIAN_POINT ( 'NONE',  ( 20.94999999999999574, 6.350000000011161383, -43.34382208968312966 ) ) ;
#77530=CARTESIAN_POINT ( 'NONE',  ( -21.14999999999999858, -11.64999999998884483, -33.50000000000000000 ) ) ;
#77546=CIRCLE ( 'NONE', #139910, 11.75000000000000000 ) ;
#77558=DIRECTION ( 'NONE',  ( 0.000000000000000000, 1.000000000000000000, 0.000000000000000000 ) ) ;
#77578=CARTESIAN_POINT ( 'NONE',  ( -22.39999999999999858, 11.75000000001115552, -33.50000000000000000 ) ) ;
#77590=( BOUNDED_CURVE ( )  B_SPLINE_CURVE ( 3, ( #191985, #53726, #111136, #31633 ),
 .UNSPECIFIED., .F., .F. ) 
 B_SPLINE_CURVE_WITH_KNOTS ( ( 4, 4 ),
 ( 0.000000000000000000, 1.570796326794916320 ),
 .UNSPECIFIED. ) 
 CURVE ( )  GEOMETRIC_REPRESENTATION_ITEM ( )  RATIONAL_B_SPLINE_CURVE ( ( 1.000000000000000000, 0.8047378541243603856, 0.8047378541243603856, 1.000000000000000000 ) ) 
 REPRESENTATION_ITEM ( '' )  );
#77609=CARTESIAN_POINT ( 'NONE',  ( 21.11345278033270034, 8.882122073382243244, -45.74602217075484134 ) ) ;
#77669=DIRECTION ( 'NONE',  ( 0.000000000000000000, 0.000000000000000000, 1.000000000000000000 ) ) ;
#77689=AXIS2_PLACEMENT_3D ( 'NONE', #152659, #232184, #14429 ) ;
#77743=ORIENTED_EDGE ( 'NONE', *, *, #36139, .F. ) ;
#77752=ORIENTED_EDGE ( 'NONE', *, *, #98158, .T. ) ;
#77756=ORIENTED_EDGE ( 'NONE', *, *, #130486, .T. ) ;
#77774=CARTESIAN_POINT ( 'NONE',  ( 21.05000000000000071, 11.75000000001116085, -60.15839931010296482 ) ) ;
#77779=SPHERICAL_SURFACE ( 'NONE', #24462, 0.1000000000000000056 ) ;
#77793=VERTEX_POINT ( 'NONE', #135154 ) ;
#77817=DIRECTION ( 'NONE',  ( 0.000000000000000000, 0.000000000000000000, 1.000000000000000000 ) ) ;
#77835=VERTEX_POINT ( 'NONE', #253396 ) ;
#77836=TOROIDAL_SURFACE ( 'NONE', #69494, 0.6000000000000013101, 0.1000000000000000056 ) ;
#77850=AXIS2_PLACEMENT_3D ( 'NONE', #14927, #94439, #174030 ) ;
#77906=CARTESIAN_POINT ( 'NONE',  ( -20.94999999999999929, -1.835341550213255957, -45.05515129256298223 ) ) ;
#77913=AXIS2_PLACEMENT_3D ( 'NONE', #175354, #101870, #181454 ) ;
#77924=DIRECTION ( 'NONE',  ( 0.000000000000000000, 0.000000000000000000, 1.000000000000000000 ) ) ;
#77933=B_SPLINE_CURVE_WITH_KNOTS ( 'NONE', 3,
 ( #224512, #84972, #164558, #66736, #146251, #47136, #126703, #206242, #107130, #186693, #8051, #127994, #30191, #232244, #173588, #48439, #112289, #251781, #53587 ),
 .UNSPECIFIED., .F., .F.,
 ( 4, 3, 3, 3, 3, 3, 4 ),
 ( -2.000416914663624153E-06, 0.000000000000000000, 4.714008503746000344E-05, 9.979203887777331108E-05, 0.0001372215519229483770, 0.0001635031576220943145, 0.0001900083748504093127 ),
 .UNSPECIFIED. ) ;
#77936=ORIENTED_EDGE ( 'NONE', *, *, #256977, .T. ) ;
#77944=LINE ( 'NONE', #115806, #83053 ) ;
#77984=DIRECTION ( 'NONE',  ( 0.000000000000000000, 0.000000000000000000, 1.000000000000000000 ) ) ;
#77998=AXIS2_PLACEMENT_3D ( 'NONE', #161124, #198945, #81540 ) ;
#78036=ORIENTED_EDGE ( 'NONE', *, *, #164378, .T. ) ;
#78054=CIRCLE ( 'NONE', #198862, 0.1000000000000028644 ) ;
#78055=CARTESIAN_POINT ( 'NONE',  ( -20.94999999999999929, -11.48912529306490349, -36.60000000000000142 ) ) ;
#78076=ORIENTED_EDGE ( 'NONE', *, *, #204702, .T. ) ;
#78124=EDGE_CURVE ( 'NONE', #41986, #9191, #241685, .T. ) ;
#78143=CARTESIAN_POINT ( 'NONE',  ( -21.05000000000000071, 11.65000000001115232, -40.28386566297815108 ) ) ;
#78144=CARTESIAN_POINT ( 'NONE',  ( 18.59999999999999787, 1.115600667400684642E-11, -33.50000000000000000 ) ) ;
#78154=CARTESIAN_POINT ( 'NONE',  ( 20.12500000000000355, 9.258049272928479567, -41.86333883714243598 ) ) ;
#78163=AXIS2_PLACEMENT_3D ( 'NONE', #186039, #127347, #208186 ) ;
#78164=AXIS2_PLACEMENT_3D ( 'NONE', #56575, #138676, #236520 ) ;
#78194=LINE ( 'NONE', #114769, #63777 ) ;
#78212=CARTESIAN_POINT ( 'NONE',  ( 23.24999999999999289, 11.75000000001116263, -21.75000000000000355 ) ) ;
#78233=CARTESIAN_POINT ( 'NONE',  ( 21.05000000000000071, 1.115600667400684642E-11, -64.10000000000000853 ) ) ;
#78236=ORIENTED_EDGE ( 'NONE', *, *, #113065, .T. ) ;
#78262=VECTOR ( 'NONE', #226769, 1000.000000000000000 ) ;
#78265=CARTESIAN_POINT ( 'NONE',  ( -22.47007471830798409, 1.115783626517291733E-11, -25.77928934807352945 ) ) ;
#78267=DIRECTION ( 'NONE',  ( 0.000000000000000000, -1.000000000000000000, 0.000000000000000000 ) ) ;
#78274=SPHERICAL_SURFACE ( 'NONE', #155717, 0.1000000000000000056 ) ;
#78281=AXIS2_PLACEMENT_3D ( 'NONE', #47707, #167699, #166420 ) ;
#78294=DIRECTION ( 'NONE',  ( 1.000000000000000000, 0.000000000000000000, 0.000000000000000000 ) ) ;
#78309=DIRECTION ( 'NONE',  ( -0.000000000000000000, -0.000000000000000000, 1.000000000000000000 ) ) ;
#78350=ORIENTED_EDGE ( 'NONE', *, *, #39479, .T. ) ;
#78353=LINE ( 'NONE', #79627, #72879 ) ;
#78371=FACE_OUTER_BOUND ( 'NONE', #225007, .T. ) ;
#78374=ORIENTED_EDGE ( 'NONE', *, *, #38371, .T. ) ;
#78401=CIRCLE ( 'NONE', #194956, 12.97499999999999964 ) ;
#78402=ORIENTED_EDGE ( 'NONE', *, *, #67913, .T. ) ;
#78417=LINE ( 'NONE', #82245, #124740 ) ;
#78445=CARTESIAN_POINT ( 'NONE',  ( 18.50000000000000000, -9.419078080838366063, -73.82992535020829905 ) ) ;
#78451=EDGE_CURVE ( 'NONE', #140899, #154073, #113645, .T. ) ;
#78452=DIRECTION ( 'NONE',  ( 0.000000000000000000, 0.000000000000000000, -1.000000000000000000 ) ) ;
#78461=CARTESIAN_POINT ( 'NONE',  ( 20.97224591636398472, 10.62515341617478271, -45.74992590466358422 ) ) ;
#78519=AXIS2_PLACEMENT_3D ( 'NONE', #13373, #152909, #17236 ) ;
#78532=DIRECTION ( 'NONE',  ( 0.000000000000000000, 1.000000000000000000, 0.000000000000000000 ) ) ;
#78545=AXIS2_PLACEMENT_3D ( 'NONE', #74414, #35293, #56069 ) ;
#78591=CIRCLE ( 'NONE', #253383, 4.000000000000003553 ) ;
#78612=CARTESIAN_POINT ( 'NONE',  ( 18.39999999999999858, -9.599999999988845900, -73.60018939122203108 ) ) ;
#78616=DIRECTION ( 'NONE',  ( 1.000000000000000000, 0.000000000000000000, -0.000000000000000000 ) ) ;
#78618=AXIS2_PLACEMENT_3D ( 'NONE', #31169, #153703, #110664 ) ;
#78637=CARTESIAN_POINT ( 'NONE',  ( -18.50000000000000000, 11.75000000001115552, -45.65000000000000568 ) ) ;
#78651=DIRECTION ( 'NONE',  ( -1.000000000000000000, -0.000000000000000000, 0.000000000000000000 ) ) ;
#78677=DIRECTION ( 'NONE',  ( 0.000000000000000000, 0.9274965247785529332, -0.3738317757009255171 ) ) ;
#78714=AXIS2_PLACEMENT_3D ( 'NONE', #41415, #40141, #257815 ) ;
#78735=ORIENTED_EDGE ( 'NONE', *, *, #30628, .T. ) ;
#78744=EDGE_CURVE ( 'NONE', #32909, #68228, #151294, .T. ) ;
#78756=CARTESIAN_POINT ( 'NONE',  ( -21.05000000000000071, 11.62071067812980907, -40.36841665234103260 ) ) ;
#78761=ORIENTED_EDGE ( 'NONE', *, *, #255373, .T. ) ;
#78763=EDGE_LOOP ( 'NONE', ( #77936, #233626, #151297 ) ) ;
#78765=DIRECTION ( 'NONE',  ( 0.000000000000000000, -0.000000000000000000, 1.000000000000000000 ) ) ;
#78788=VERTEX_POINT ( 'NONE', #192980 ) ;
#78797=ORIENTED_EDGE ( 'NONE', *, *, #5328, .F. ) ;
#78799=DIRECTION ( 'NONE',  ( -1.000000000000000000, -3.265361837132813093E-16, 0.000000000000000000 ) ) ;
#78822=DIRECTION ( 'NONE',  ( -1.000000000000000000, 0.000000000000000000, -0.000000000000000000 ) ) ;
#78848=CARTESIAN_POINT ( 'NONE',  ( -18.50000000000000000, 11.65000000001115232, -33.60000000000000142 ) ) ;
#78859=EDGE_LOOP ( 'NONE', ( #54865, #96950, #61068, #235088 ) ) ;
#78880=CARTESIAN_POINT ( 'NONE',  ( 20.85000000000000142, 11.65000000001115943, -67.00000000000000000 ) ) ;
#78943=DIRECTION ( 'NONE',  ( -1.000000000000000000, 0.000000000000000000, 0.000000000000000000 ) ) ;
#78957=DIRECTION ( 'NONE',  ( 0.000000000000000000, 0.000000000000000000, -1.000000000000000000 ) ) ;
#78967=VERTEX_POINT ( 'NONE', #163798 ) ;
#78976=EDGE_CURVE ( 'NONE', #249646, #239047, #31618, .T. ) ;
#78978=DIRECTION ( 'NONE',  ( -1.000000000000000000, -2.952720810173289112E-16, 0.000000000000000000 ) ) ;
#78981=VECTOR ( 'NONE', #230250, 1000.000000000000000 ) ;
#78984=DIRECTION ( 'NONE',  ( -2.915501640297153790E-16, 1.000000000000000000, 0.000000000000000000 ) ) ;
#79027=ORIENTED_EDGE ( 'NONE', *, *, #251473, .F. ) ;
#79041=ORIENTED_EDGE ( 'NONE', *, *, #95765, .F. ) ;
#79051=DIRECTION ( 'NONE',  ( -0.000000000000000000, 1.000000000000000000, -0.000000000000000000 ) ) ;
#79054=DIRECTION ( 'NONE',  ( -0.7071067811865389130, 8.659560562355038861E-17, -0.7071067811865561215 ) ) ;
#79057=AXIS2_PLACEMENT_3D ( 'NONE', #138216, #39168, #20893 ) ;
#79063=ORIENTED_EDGE ( 'NONE', *, *, #85169, .F. ) ;
#79065=CARTESIAN_POINT ( 'NONE',  ( 23.14999999999999858, -11.74999999998883560, -21.75000000000000355 ) ) ;
#79067=EDGE_CURVE ( 'NONE', #173321, #64202, #148292, .T. ) ;
#79092=DIRECTION ( 'NONE',  ( -1.000000000000000000, 0.000000000000000000, 0.000000000000000000 ) ) ;
#79112=ORIENTED_EDGE ( 'NONE', *, *, #115188, .T. ) ;
#79120=EDGE_CURVE ( 'NONE', #102738, #137157, #71124, .T. ) ;
#79162=EDGE_CURVE ( 'NONE', #154736, #159251, #119262, .T. ) ;
#79197=CARTESIAN_POINT ( 'NONE',  ( 20.75572585718222385, 8.882316728409756834, -41.99725839870686883 ) ) ;
#79219=FACE_OUTER_BOUND ( 'NONE', #229979, .T. ) ;
#79244=ORIENTED_EDGE ( 'NONE', *, *, #32155, .F. ) ;
#79270=CIRCLE ( 'NONE', #116886, 0.1000000000000028644 ) ;
#79325=VECTOR ( 'NONE', #33943, 1000.000000000000000 ) ;
#79335=CARTESIAN_POINT ( 'NONE',  ( 21.14999999999999503, 1.115600667400684642E-11, -33.50000000000000000 ) ) ;
#79348=CARTESIAN_POINT ( 'NONE',  ( 21.00000000000000000, 9.750000000011153745, -54.65000000000000568 ) ) ;
#79373=VERTEX_POINT ( 'NONE', #257374 ) ;
#79403=DIRECTION ( 'NONE',  ( -0.000000000000000000, -0.000000000000000000, -1.000000000000000000 ) ) ;
#79423=CARTESIAN_POINT ( 'NONE',  ( -18.54118089899633048, -9.463537631836944186, -40.54857759786813176 ) ) ;
#79424=EDGE_CURVE ( 'NONE', #136260, #165708, #127635, .T. ) ;
#79435=DIRECTION ( 'NONE',  ( 0.000000000000000000, -0.9893560106964500722, 0.1455152366551550613 ) ) ;
#79457=EDGE_CURVE ( 'NONE', #147882, #101473, #165038, .T. ) ;
#79476=AXIS2_PLACEMENT_3D ( 'NONE', #211174, #232040, #200592 ) ;
#79479=DIRECTION ( 'NONE',  ( -1.000000000000000000, 0.000000000000000000, 0.000000000000000000 ) ) ;
#79488=DIRECTION ( 'NONE',  ( 0.000000000000000000, 0.000000000000000000, -1.000000000000000000 ) ) ;
#79496=DIRECTION ( 'NONE',  ( 0.000000000000000000, 0.000000000000000000, -1.000000000000000000 ) ) ;
#79497=DIRECTION ( 'NONE',  ( 1.000000000000000000, 0.000000000000000000, 0.000000000000000000 ) ) ;
#79506=LINE ( 'NONE', #198186, #120621 ) ;
#79549=CARTESIAN_POINT ( 'NONE',  ( -21.05000000000000071, 1.115649653272650466E-11, -71.00000000000001421 ) ) ;
#79565=CARTESIAN_POINT ( 'NONE',  ( 21.05000000000000071, -8.999999999988842703, -57.10603087734755690 ) ) ;
#79569=CARTESIAN_POINT ( 'NONE',  ( 21.05000000000000071, -1.162701749926853712, -41.40000000000000568 ) ) ;
#79590=EDGE_CURVE ( 'NONE', #15098, #171125, #244316, .T. ) ;
#79627=CARTESIAN_POINT ( 'NONE',  ( 23.14999999999999503, 11.75000000001116263, -21.75000000000000355 ) ) ;
#79630=EDGE_LOOP ( 'NONE', ( #22961, #226811, #143922, #120680 ) ) ;
#79645=CARTESIAN_POINT ( 'NONE',  ( -23.15000000000000213, -11.48912529306489994, -63.89999999999999858 ) ) ;
#79650=DIRECTION ( 'NONE',  ( -1.000000000000000000, 0.000000000000000000, 0.000000000000000000 ) ) ;
#79664=EDGE_CURVE ( 'NONE', #126429, #48124, #73673, .T. ) ;
#79698=CARTESIAN_POINT ( 'NONE',  ( -23.15000000000000213, 11.75000000001115552, -21.75000000000000355 ) ) ;
#79706=EDGE_LOOP ( 'NONE', ( #99219, #132146, #54256, #5140 ) ) ;
#79720=VERTEX_POINT ( 'NONE', #122784 ) ;
#79775=DIRECTION ( 'NONE',  ( 1.000000000000000000, 0.000000000000000000, 0.000000000000000000 ) ) ;
#79806=CARTESIAN_POINT ( 'NONE',  ( 21.05000000000000071, 5.900000000011162093, -56.78090023534362984 ) ) ;
#79813=ORIENTED_EDGE ( 'NONE', *, *, #79457, .T. ) ;
#79829=FACE_OUTER_BOUND ( 'NONE', #126300, .T. ) ;
#79848=ORIENTED_EDGE ( 'NONE', *, *, #255374, .T. ) ;
#79854=B_SPLINE_CURVE_WITH_KNOTS ( 'NONE', 3,
 ( #72796, #89741, #49346, #207149 ),
 .UNSPECIFIED., .F., .F.,
 ( 4, 4 ),
 ( 7.757919228897728493E-18, 0.0001058379652594581074 ),
 .UNSPECIFIED. ) ;
#79895=FACE_OUTER_BOUND ( 'NONE', #81535, .T. ) ;
#79906=LINE ( 'NONE', #139896, #227656 ) ;
#79916=ORIENTED_EDGE ( 'NONE', *, *, #76872, .T. ) ;
#79917=DIRECTION ( 'NONE',  ( 1.000000000000000000, -0.000000000000000000, -0.000000000000000000 ) ) ;
#79923=VERTEX_POINT ( 'NONE', #112212 ) ;
#79924=CARTESIAN_POINT ( 'NONE',  ( -21.44999999999999929, 7.150000000011155876, -45.85000000000000142 ) ) ;
#79943=VECTOR ( 'NONE', #222038, 1000.000000000000227 ) ;
#79958=ADVANCED_FACE ( 'NONE', ( #155201 ), #95192, .F. ) ;
#79978=DIRECTION ( 'NONE',  ( -0.000000000000000000, 0.000000000000000000, 1.000000000000000000 ) ) ;
#80000=ORIENTED_EDGE ( 'NONE', *, *, #107691, .F. ) ;
#80050=VERTEX_POINT ( 'NONE', #235972 ) ;
#80054=VERTEX_POINT ( 'NONE', #217676 ) ;
#80065=CARTESIAN_POINT ( 'NONE',  ( -18.59999999999999787, 11.75000000001115197, -40.51480577065400013 ) ) ;
#80076=CARTESIAN_POINT ( 'NONE',  ( -23.15000000000000213, 1.115600667400684642E-11, -33.50000000000000000 ) ) ;
#80084=DIRECTION ( 'NONE',  ( -0.000000000000000000, -0.9876197685951252359, -0.1568667991644863424 ) ) ;
#80110=DIRECTION ( 'NONE',  ( 1.000000000000000000, 0.000000000000000000, 0.000000000000000000 ) ) ;
#80146=ADVANCED_FACE ( 'NONE', ( #156488 ), #182447, .F. ) ;
#80160=EDGE_CURVE ( 'NONE', #226915, #240562, #199495, .T. ) ;
#80176=DIRECTION ( 'NONE',  ( -0.000000000000000000, 1.000000000000000000, 1.734723475976807292E-15 ) ) ;
#80185=ORIENTED_EDGE ( 'NONE', *, *, #78124, .T. ) ;
#80190=LINE ( 'NONE', #76360, #130052 ) ;
#80248=DIRECTION ( 'NONE',  ( 0.000000000000000000, 0.01562499999998609446, -0.9998779222360101304 ) ) ;
#80297=CARTESIAN_POINT ( 'NONE',  ( -20.64999999999999858, 4.350000000011156054, -45.85000000000000142 ) ) ;
#80323=DIRECTION ( 'NONE',  ( 0.000000000000000000, -1.000000000000000000, 0.000000000000000000 ) ) ;
#80329=CARTESIAN_POINT ( 'NONE',  ( -20.54999999999999716, 2.000000000011154189, -54.17537807723790166 ) ) ;
#80334=CYLINDRICAL_SURFACE ( 'NONE', #101640, 0.09999999999999939493 ) ;
#80340=ORIENTED_EDGE ( 'NONE', *, *, #207151, .T. ) ;
#80358=ORIENTED_EDGE ( 'NONE', *, *, #195758, .T. ) ;
#80382=EDGE_LOOP ( 'NONE', ( #61722, #20067, #73820, #28659 ) ) ;
#80441=CIRCLE ( 'NONE', #105398, 0.1000000000000028644 ) ;
#80462=ADVANCED_FACE ( 'NONE', ( #16647 ), #96145, .T. ) ;
#80482=VECTOR ( 'NONE', #182940, 1000.000000000000000 ) ;
#80498=VECTOR ( 'NONE', #242865, 1000.000000000000000 ) ;
#80513=CARTESIAN_POINT ( 'NONE',  ( 21.09107601085574402, 0.03930716472853410665, -27.13612202464005918 ) ) ;
#80518=AXIS2_PLACEMENT_3D ( 'NONE', #163651, #221038, #4555 ) ;
#80537=ORIENTED_EDGE ( 'NONE', *, *, #68626, .T. ) ;
#80542=AXIS2_PLACEMENT_3D ( 'NONE', #67117, #90520, #248321 ) ;
#80572=EDGE_CURVE ( 'NONE', #173321, #199184, #257118, .T. ) ;
#80608=ORIENTED_EDGE ( 'NONE', *, *, #218882, .F. ) ;
#80612=DIRECTION ( 'NONE',  ( 0.000000000000000000, 2.891205793294679805E-16, -1.000000000000000000 ) ) ;
#80627=ORIENTED_EDGE ( 'NONE', *, *, #246180, .T. ) ;
#80646=CIRCLE ( 'NONE', #230528, 0.1000000000000002554 ) ;
#80680=DIRECTION ( 'NONE',  ( 1.000000000000000000, -0.000000000000000000, -0.000000000000000000 ) ) ;
#80685=DIRECTION ( 'NONE',  ( 1.000000000000000000, 0.000000000000000000, 0.000000000000000000 ) ) ;
#80708=DIRECTION ( 'NONE',  ( 0.000000000000000000, 0.000000000000000000, -1.000000000000000000 ) ) ;
#80717=ADVANCED_FACE ( 'NONE', ( #175132 ), #211577, .F. ) ;
#80726=CARTESIAN_POINT ( 'NONE',  ( 20.95462737510932882, 10.55678195165489441, -41.06995005656229836 ) ) ;
#80729=EDGE_CURVE ( 'NONE', #109631, #28235, #155552, .T. ) ;
#80762=ORIENTED_EDGE ( 'NONE', *, *, #53567, .F. ) ;
#80773=CARTESIAN_POINT ( 'NONE',  ( -20.85000000000000142, -1.835859311432481045, -78.50443916879852679 ) ) ;
#80783=DIRECTION ( 'NONE',  ( 0.000000000000000000, -1.000000000000000000, 0.000000000000000000 ) ) ;
#80855=DIRECTION ( 'NONE',  ( 0.000000000000000000, 1.224646799142015331E-16, 1.000000000000000000 ) ) ;
#80865=ORIENTED_EDGE ( 'NONE', *, *, #145010, .F. ) ;
#80873=DIRECTION ( 'NONE',  ( -0.7071067811865474617, -0.7071067811865474617, -0.000000000000000000 ) ) ;
#80892=ADVANCED_FACE ( 'NONE', ( #161958 ), #161704, .F. ) ;
#80895=VERTEX_POINT ( 'NONE', #58947 ) ;
#80910=ORIENTED_EDGE ( 'NONE', *, *, #18426, .T. ) ;
#80923=CARTESIAN_POINT ( 'NONE',  ( -23.25000000000000000, 11.65000000001115588, -45.65000000000000568 ) ) ;
#80932=VERTEX_POINT ( 'NONE', #84926 ) ;
#80957=EDGE_CURVE ( 'NONE', #168958, #176891, #178278, .T. ) ;
#80964=CIRCLE ( 'NONE', #210002, 0.1999999999999987899 ) ;
#80969=CARTESIAN_POINT ( 'NONE',  ( -20.54999999999999716, 1.115600667400684642E-11, -46.47500000000000142 ) ) ;
#80984=CARTESIAN_POINT ( 'NONE',  ( -21.14999999999999858, 11.65000000001115588, -33.60000000000000142 ) ) ;
#80985=ORIENTED_EDGE ( 'NONE', *, *, #68522, .T. ) ;
#81018=CARTESIAN_POINT ( 'NONE',  ( 23.15000000000000213, -12.41227409413852811, -64.00000000000000000 ) ) ;
#81022=CARTESIAN_POINT ( 'NONE',  ( -20.94999999999999929, 7.021664781911246322, -70.83356540189728889 ) ) ;
#81033=CIRCLE ( 'NONE', #31217, 0.1000000000000028644 ) ;
#81117=VERTEX_POINT ( 'NONE', #215182 ) ;
#81145=ORIENTED_EDGE ( 'NONE', *, *, #178541, .T. ) ;
#81163=CARTESIAN_POINT ( 'NONE',  ( -23.25000000000000000, 1.115600667400684642E-11, -67.00000000000000000 ) ) ;
#81185=DIRECTION ( 'NONE',  ( -1.836970198721029934E-16, 1.000000000000000000, 0.000000000000000000 ) ) ;
#81186=AXIS2_PLACEMENT_3D ( 'NONE', #13892, #12625, #49156 ) ;
#81203=CARTESIAN_POINT ( 'NONE',  ( 21.00000000000000000, 9.750000000011153745, -45.85000000000000142 ) ) ;
#81247=EDGE_LOOP ( 'NONE', ( #244666, #166759, #47969, #6489 ) ) ;
#81258=EDGE_CURVE ( 'NONE', #195498, #96705, #246304, .T. ) ;
#81338=DIRECTION ( 'NONE',  ( 0.000000000000000000, 0.9908441862701596881, -0.1350103645451904977 ) ) ;
#81373=CARTESIAN_POINT ( 'NONE',  ( -21.13435531349800556, 6.493721063603304700, -33.50000000000000000 ) ) ;
#81410=EDGE_CURVE ( 'NONE', #227982, #19031, #57962, .T. ) ;
#81426=ORIENTED_EDGE ( 'NONE', *, *, #1096, .T. ) ;
#81475=CIRCLE ( 'NONE', #135665, 0.1000000000000028644 ) ;
#81476=CIRCLE ( 'NONE', #248099, 0.5000000000000004441 ) ;
#81516=ORIENTED_EDGE ( 'NONE', *, *, #226100, .T. ) ;
#81535=EDGE_LOOP ( 'NONE', ( #257102, #84204, #422, #195317 ) ) ;
#81538=CARTESIAN_POINT ( 'NONE',  ( -20.93302460841142931, 10.31565961587945424, -72.53641941191781939 ) ) ;
#81540=DIRECTION ( 'NONE',  ( -7.304098846218201720E-16, 1.000000000000000000, 0.000000000000000000 ) ) ;
#81547=CARTESIAN_POINT ( 'NONE',  ( -20.85000000000000142, 1.115600667400684642E-11, -67.00000000000000000 ) ) ;
#81551=ORIENTED_EDGE ( 'NONE', *, *, #210599, .T. ) ;
#81556=ORIENTED_EDGE ( 'NONE', *, *, #87797, .F. ) ;
#81577=CARTESIAN_POINT ( 'NONE',  ( 20.04142135623730070, 11.75000000001115907, -54.85000000000000142 ) ) ;
#81578=VERTEX_POINT ( 'NONE', #7368 ) ;
#81601=CARTESIAN_POINT ( 'NONE',  ( 21.97500000000000497, 9.750000000011153745, -45.75000000000000000 ) ) ;
#81611=VECTOR ( 'NONE', #226599, 1000.000000000000000 ) ;
#81641=CARTESIAN_POINT ( 'NONE',  ( -23.25000000000000000, -9.599999999988847676, -43.39396912265245021 ) ) ;
#81645=DIRECTION ( 'NONE',  ( -1.000000000000000000, 0.000000000000000000, 0.000000000000000000 ) ) ;
#81669=DIRECTION ( 'NONE',  ( 1.000000000000000000, -0.000000000000000000, -0.000000000000000000 ) ) ;
#81673=DIRECTION ( 'NONE',  ( -1.000000000000000000, 0.000000000000000000, 0.000000000000000000 ) ) ;
#81684=CARTESIAN_POINT ( 'NONE',  ( -18.50000000000000000, -1.135018845899022466, -74.71697688343232358 ) ) ;
#81720=DIRECTION ( 'NONE',  ( 0.000000000000000000, -7.105427357601027102E-15, -1.000000000000000000 ) ) ;
#81743=ORIENTED_EDGE ( 'NONE', *, *, #117730, .F. ) ;
#81754=VERTEX_POINT ( 'NONE', #127306 ) ;
#81798=FACE_OUTER_BOUND ( 'NONE', #208685, .T. ) ;
#81819=ORIENTED_EDGE ( 'NONE', *, *, #142843, .F. ) ;
#81836=CARTESIAN_POINT ( 'NONE',  ( -20.64999999999999858, 2.000000000011154189, -46.72462192276210402 ) ) ;
#81871=DIRECTION ( 'NONE',  ( 4.504528286903032433E-15, -0.1298341882520124002, -0.9915357197604841577 ) ) ;
#81902=ORIENTED_EDGE ( 'NONE', *, *, #159256, .F. ) ;
#81903=DIRECTION ( 'NONE',  ( 1.000000000000000000, 3.265361837132813093E-16, -0.000000000000000000 ) ) ;
#81916=EDGE_LOOP ( 'NONE', ( #108491, #255816, #177903, #175111 ) ) ;
#81930=EDGE_CURVE ( 'NONE', #100083, #194844, #9923, .T. ) ;
#81931=DIRECTION ( 'NONE',  ( -0.7071067811865474617, -0.7071067811865474617, -0.000000000000000000 ) ) ;
#81946=ORIENTED_EDGE ( 'NONE', *, *, #102220, .F. ) ;
#81949=DIRECTION ( 'NONE',  ( 1.000000000000000000, 7.304098846218134667E-16, -0.000000000000000000 ) ) ;
#81992=TOROIDAL_SURFACE ( 'NONE', #77913, 0.2000000000000000111, 0.1000000000000000056 ) ;
#81995=VERTEX_POINT ( 'NONE', #159721 ) ;
#81999=ORIENTED_EDGE ( 'NONE', *, *, #121340, .T. ) ;
#82011=VERTEX_POINT ( 'NONE', #200128 ) ;
#82049=ADVANCED_FACE ( 'NONE', ( #176723 ), #25363, .F. ) ;
#82065=VERTEX_POINT ( 'NONE', #184402 ) ;
#82081=LINE ( 'NONE', #241205, #257892 ) ;
#82097=EDGE_LOOP ( 'NONE', ( #210211, #208649, #3253, #232976 ) ) ;
#82101=AXIS2_PLACEMENT_3D ( 'NONE', #140703, #258038, #159020 ) ;
#82142=ORIENTED_EDGE ( 'NONE', *, *, #38426, .F. ) ;
#82167=EDGE_CURVE ( 'NONE', #127120, #135639, #53906, .T. ) ;
#82173=VERTEX_POINT ( 'NONE', #47448 ) ;
#82188=VECTOR ( 'NONE', #76941, 1000.000000000000227 ) ;
#82191=DIRECTION ( 'NONE',  ( 1.000000000000000000, 0.000000000000000000, 0.000000000000000000 ) ) ;
#82193=ORIENTED_EDGE ( 'NONE', *, *, #67398, .F. ) ;
#82201=ORIENTED_EDGE ( 'NONE', *, *, #171140, .F. ) ;
#82232=CIRCLE ( 'NONE', #2961, 0.09999999999999736877 ) ;
#82245=CARTESIAN_POINT ( 'NONE',  ( 23.24999999999999289, 11.65000000001116298, -21.75000000000000355 ) ) ;
#82276=AXIS2_PLACEMENT_3D ( 'NONE', #75587, #153867, #215065 ) ;
#82283=DIRECTION ( 'NONE',  ( 0.000000000000000000, 0.000000000000000000, -1.000000000000000000 ) ) ;
#82302=ORIENTED_EDGE ( 'NONE', *, *, #249707, .F. ) ;
#82312=AXIS2_PLACEMENT_3D ( 'NONE', #172940, #110346, #251123 ) ;
#82320=FACE_OUTER_BOUND ( 'NONE', #140472, .T. ) ;
#82336=CYLINDRICAL_SURFACE ( 'NONE', #88735, 0.09999999999999939493 ) ;
#82337=DIRECTION ( 'NONE',  ( -0.000000000000000000, 0.000000000000000000, -1.000000000000000000 ) ) ;
#82342=ADVANCED_FACE ( 'NONE', ( #198533 ), #98118, .T. ) ;
#82343=CARTESIAN_POINT ( 'NONE',  ( -23.25000000000000000, -0.09999999998884338825, -21.85042919245520210 ) ) ;
#82349=AXIS2_PLACEMENT_3D ( 'NONE', #171281, #250756, #72145 ) ;
#82351=CARTESIAN_POINT ( 'NONE',  ( -20.64999999999999858, 2.500000000011154633, -53.77537807723790309 ) ) ;
#82368=ADVANCED_FACE ( 'NONE', ( #117713 ), #237669, .F. ) ;
#82391=DIRECTION ( 'NONE',  ( -4.408576920032448588E-17, 0.1350103645451876666, -0.9908441862701600211 ) ) ;
#82534=CIRCLE ( 'NONE', #74235, 0.09999999999999693856 ) ;
#82541=DIRECTION ( 'NONE',  ( 1.000000000000000000, 0.000000000000000000, 0.000000000000000000 ) ) ;
#82543=CARTESIAN_POINT ( 'NONE',  ( 23.15000000000000213, -8.999999999988844479, -43.39396912265245021 ) ) ;
#82553=VERTEX_POINT ( 'NONE', #125431 ) ;
#82594=EDGE_CURVE ( 'NONE', #116043, #200421, #33655, .T. ) ;
#82606=EDGE_CURVE ( 'NONE', #244695, #18621, #129283, .T. ) ;
#82618=VECTOR ( 'NONE', #248629, 1000.000000000000000 ) ;
#82622=ORIENTED_EDGE ( 'NONE', *, *, #158862, .T. ) ;
#82625=VECTOR ( 'NONE', #90578, 1000.000000000000114 ) ;
#82629=PRESENTATION_STYLE_ASSIGNMENT (( #159643 ) ) ;
#82633=CARTESIAN_POINT ( 'NONE',  ( -23.15000000000000213, 1.115600667400684642E-11, -33.50000000000000000 ) ) ;
#82659=CARTESIAN_POINT ( 'NONE',  ( -21.05000000000000071, 6.413662734880689165, -33.58559286336213034 ) ) ;
#82678=EDGE_CURVE ( 'NONE', #86031, #227593, #54440, .T. ) ;
#82688=DIRECTION ( 'NONE',  ( 1.000000000000000000, 0.000000000000000000, 0.000000000000000000 ) ) ;
#82722=AXIS2_PLACEMENT_3D ( 'NONE', #201318, #181765, #81338 ) ;
#82729=VERTEX_POINT ( 'NONE', #58693 ) ;
#82742=CYLINDRICAL_SURFACE ( 'NONE', #246248, 0.1000000000000028644 ) ;
#82766=AXIS2_PLACEMENT_3D ( 'NONE', #67766, #163042, #45644 ) ;
#82771=VERTEX_POINT ( 'NONE', #143033 ) ;
#82787=AXIS2_PLACEMENT_3D ( 'NONE', #23423, #67649, #2525 ) ;
#82809=ORIENTED_EDGE ( 'NONE', *, *, #38468, .F. ) ;
#82813=CARTESIAN_POINT ( 'NONE',  ( -18.50000000000000000, 7.021664781911246322, -70.83356540189728889 ) ) ;
#82816=EDGE_CURVE ( 'NONE', #6368, #11590, #105161, .T. ) ;
#82818=CARTESIAN_POINT ( 'NONE',  ( -20.88420186297724257, 10.33025634372637391, -72.58709292826388548 ) ) ;
#82848=DIRECTION ( 'NONE',  ( 0.000000000000000000, 0.000000000000000000, -1.000000000000000000 ) ) ;
#82858=( BOUNDED_SURFACE ( )  B_SPLINE_SURFACE ( 3, 2, ( 
 ( #163946, #120992, #85643 ),
 ( #45276, #66122, #182230 ),
 ( #220065, #100084, #62273 ),
 ( #80513, #200501, #63544 ),
 ( #24459, #222600, #126078 ),
 ( #21870, #101340, #3570 ) ),
 .UNSPECIFIED., .F., .F., .F. ) 
 B_SPLINE_SURFACE_WITH_KNOTS ( ( 4, 2, 4 ),
 ( 3, 3 ),
 ( 0.0001300404313046605199, 0.0003183318589266607925, 0.0005066232865486610922 ),
 ( 0.000000000000000000, 1.000000000000000000 ),
 .UNSPECIFIED. ) 
 GEOMETRIC_REPRESENTATION_ITEM ( )  RATIONAL_B_SPLINE_SURFACE ( (
 ( 1.000000000000000000, 0.7071067811865475727, 1.000000000000000000),
 ( 1.000000000000000000, 0.7625113560538873125, 1.000000000000000000),
 ( 1.000000000000000000, 0.8126073484690201632, 1.000000000000000000),
 ( 1.000000000000000000, 0.8923049332730712546, 1.000000000000000000),
 ( 1.000000000000000000, 0.9231914937770823171, 1.000000000000000000),
 ( 1.000000000000000000, 0.9238795325112901802, 1.000000000000000000) ) ) 
 REPRESENTATION_ITEM ( '' )  SURFACE ( )  );
#82886=CARTESIAN_POINT ( 'NONE',  ( -18.59999999999999787, 10.33248238083634440, -72.59484654391314962 ) ) ;
#82895=VECTOR ( 'NONE', #67319, 1000.000000000000000 ) ;
#82900=CARTESIAN_POINT ( 'NONE',  ( -23.15000000000000213, -11.41227409413852811, -64.00000000000000000 ) ) ;
#82916=ORIENTED_EDGE ( 'NONE', *, *, #107954, .F. ) ;
#82923=ORIENTED_EDGE ( 'NONE', *, *, #21237, .T. ) ;
#82930=DIRECTION ( 'NONE',  ( -1.000000000000000000, -2.952720810173289112E-16, 0.000000000000000000 ) ) ;
#82932=CARTESIAN_POINT ( 'NONE',  ( 21.05000000000000071, 10.72371710471867701, -45.65000000000000568 ) ) ;
#82942=PLANE ( 'NONE',  #152437 ) ;
#82973=CYLINDRICAL_SURFACE ( 'NONE', #232122, 7.900000000000003908 ) ;
#82981=CIRCLE ( 'NONE', #49879, 0.09999999999999939493 ) ;
#83039=ORIENTED_EDGE ( 'NONE', *, *, #62928, .F. ) ;
#83044=CARTESIAN_POINT ( 'NONE',  ( 21.05000000000000071, 5.000000000011153745, -54.59473398108690390 ) ) ;
#83053=VECTOR ( 'NONE', #239609, 1000.000000000000000 ) ;
#83073=VERTEX_POINT ( 'NONE', #150761 ) ;
#83082=ORIENTED_EDGE ( 'NONE', *, *, #32918, .T. ) ;
#83160=AXIS2_PLACEMENT_3D ( 'NONE', #101276, #4768, #223825 ) ;
#83166=ADVANCED_FACE ( 'NONE', ( #138856 ), #203257, .F. ) ;
#83174=ORIENTED_EDGE ( 'NONE', *, *, #11962, .F. ) ;
#83176=EDGE_CURVE ( 'NONE', #96815, #80054, #141920, .T. ) ;
#83208=CARTESIAN_POINT ( 'NONE',  ( 21.17356465864818560, 0.09891124102502621418, -27.07719687375827533 ) ) ;
#83229=TOROIDAL_SURFACE ( 'NONE', #120695, 11.65000000000000036, 0.1000000000000000056 ) ;
#83236=EDGE_LOOP ( 'NONE', ( #44972, #237911, #141901, #152755 ) ) ;
#83285=CARTESIAN_POINT ( 'NONE',  ( -18.59999999999999787, 7.021664781911246322, -70.83356540189728889 ) ) ;
#83294=AXIS2_PLACEMENT_3D ( 'NONE', #152441, #251497, #212400 ) ;
#83301=DIRECTION ( 'NONE',  ( -2.952720810173289112E-16, 1.000000000000000000, 0.000000000000000000 ) ) ;
#83314=EDGE_CURVE ( 'NONE', #14771, #2240, #62815, .T. ) ;
#83316=ORIENTED_EDGE ( 'NONE', *, *, #225671, .F. ) ;
#83322=LINE ( 'NONE', #2520, #94743 ) ;
#83329=CARTESIAN_POINT ( 'NONE',  ( 21.05000000000000071, 11.65000000001116298, -59.98519422934605672 ) ) ;
#83334=VERTEX_POINT ( 'NONE', #50070 ) ;
#83387=DIRECTION ( 'NONE',  ( 2.342056488767301376E-15, -0.1350103645451904977, -0.9908441862701596881 ) ) ;
#83395=CARTESIAN_POINT ( 'NONE',  ( -23.25000000000000000, -1.835859311432481045, -78.60443916879853532 ) ) ;
#83418=ORIENTED_EDGE ( 'NONE', *, *, #54712, .F. ) ;
#83424=LINE ( 'NONE', #3922, #168419 ) ;
#83425=CARTESIAN_POINT ( 'NONE',  ( -23.15000000000000213, 11.65000000001115588, -54.85000000000000142 ) ) ;
#83436=TOROIDAL_SURFACE ( 'NONE', #95916, 0.2000000000000000111, 0.1000000000000000056 ) ;
#83437=CIRCLE ( 'NONE', #25222, 0.5000000000000004441 ) ;
#83443=DIRECTION ( 'NONE',  ( 0.000000000000000000, 1.000000000000000000, 0.000000000000000000 ) ) ;
#83450=EDGE_CURVE ( 'NONE', #82771, #251013, #140946, .T. ) ;
#83467=CIRCLE ( 'NONE', #141748, 11.65000000000000036 ) ;
#83489=ORIENTED_EDGE ( 'NONE', *, *, #171444, .F. ) ;
#83512=VECTOR ( 'NONE', #98735, 1000.000000000000000 ) ;
#83526=VECTOR ( 'NONE', #55070, 1000.000000000000000 ) ;
#83542=AXIS2_PLACEMENT_3D ( 'NONE', #63417, #81669, #120872 ) ;
#83553=EDGE_CURVE ( 'NONE', #1348, #153879, #242827, .T. ) ;
#83555=VERTEX_POINT ( 'NONE', #143728 ) ;
#83588=ADVANCED_FACE ( 'NONE', ( #145002 ), #142445, .T. ) ;
#83603=( BOUNDED_CURVE ( )  B_SPLINE_CURVE ( 3, ( #193450, #14826, #173918, #253402 ),
 .UNSPECIFIED., .F., .F. ) 
 B_SPLINE_CURVE_WITH_KNOTS ( ( 4, 4 ),
 ( 4.712388980384690562, 6.283185307179586232 ),
 .UNSPECIFIED. ) 
 CURVE ( )  GEOMETRIC_REPRESENTATION_ITEM ( )  RATIONAL_B_SPLINE_CURVE ( ( 1.000000000000000000, 0.8047378541243652705, 0.8047378541243652705, 1.000000000000000000 ) ) 
 REPRESENTATION_ITEM ( '' )  );
#83640=EDGE_CURVE ( 'NONE', #230716, #139488, #62453, .T. ) ;
#83657=FACE_OUTER_BOUND ( 'NONE', #182890, .T. ) ;
#83704=ADVANCED_FACE ( 'NONE', ( #202425 ), #44643, .F. ) ;
#83708=FACE_OUTER_BOUND ( 'NONE', #67068, .T. ) ;
#83717=ORIENTED_EDGE ( 'NONE', *, *, #99344, .T. ) ;
#83726=DIRECTION ( 'NONE',  ( -0.000000000000000000, -0.000000000000000000, 1.000000000000000000 ) ) ;
#83747=CARTESIAN_POINT ( 'NONE',  ( -21.05000000000000071, -11.64999999998884483, -36.50000000000000711 ) ) ;
#83771=AXIS2_PLACEMENT_3D ( 'NONE', #217517, #257891, #19338 ) ;
#83781=EDGE_CURVE ( 'NONE', #183680, #74897, #83437, .T. ) ;
#83788=DIRECTION ( 'NONE',  ( 1.000000000000000000, 0.000000000000000000, 0.000000000000000000 ) ) ;
#83808=EDGE_CURVE ( 'NONE', #140862, #191837, #194446, .T. ) ;
#83826=EDGE_CURVE ( 'NONE', #55121, #153815, #256910, .T. ) ;
#83890=TOROIDAL_SURFACE ( 'NONE', #54889, 1.900000000000002576, 0.1000000000000000056 ) ;
#83911=CARTESIAN_POINT ( 'NONE',  ( 21.05000000000000071, 1.115600667400684642E-11, -67.00000000000000000 ) ) ;
#83926=CARTESIAN_POINT ( 'NONE',  ( -21.05000000000000071, 6.478078221105890933, -33.59999993530665563 ) ) ;
#83932=DIRECTION ( 'NONE',  ( 1.000000000000000000, 0.000000000000000000, 0.000000000000000000 ) ) ;
#83951=AXIS2_PLACEMENT_3D ( 'NONE', #122516, #101611, #181209 ) ;
#83960=ADVANCED_FACE ( 'NONE', ( #143428 ), #183841, .F. ) ;
#83967=ORIENTED_EDGE ( 'NONE', *, *, #180447, .T. ) ;
#83987=AXIS2_PLACEMENT_3D ( 'NONE', #95822, #253616, #175415 ) ;
#84002=ORIENTED_EDGE ( 'NONE', *, *, #56877, .F. ) ;
#84005=VECTOR ( 'NONE', #52381, 1000.000000000000000 ) ;
#84007=VERTEX_POINT ( 'NONE', #43058 ) ;
#84019=ORIENTED_EDGE ( 'NONE', *, *, #95857, .T. ) ;
#84026=AXIS2_PLACEMENT_3D ( 'NONE', #211297, #234713, #54775 ) ;
#84054=EDGE_LOOP ( 'NONE', ( #202455, #252093, #174230, #19013 ) ) ;
#84074=DIRECTION ( 'NONE',  ( 0.000000000000000000, 0.9908441862701596881, 0.1350103645451904977 ) ) ;
#84084=CARTESIAN_POINT ( 'NONE',  ( -20.90851465518106167, 10.32532329027886320, -72.56993430183595706 ) ) ;
#84104=EDGE_CURVE ( 'NONE', #146761, #54754, #246389, .T. ) ;
#84149=DIRECTION ( 'NONE',  ( -0.000000000000000000, -0.1298341882519805091, -0.9915357197604881545 ) ) ;
#84161=ORIENTED_EDGE ( 'NONE', *, *, #123635, .T. ) ;
#84189=CARTESIAN_POINT ( 'NONE',  ( -21.00250684356851849, 11.75000000001115197, -40.51480576875963635 ) ) ;
#84204=ORIENTED_EDGE ( 'NONE', *, *, #186282, .T. ) ;
#84212=DIRECTION ( 'NONE',  ( 0.000000000000000000, 0.000000000000000000, 1.000000000000000000 ) ) ;
#84269=PLANE ( 'NONE',  #211805 ) ;
#84285=ORIENTED_EDGE ( 'NONE', *, *, #183240, .F. ) ;
#84317=CARTESIAN_POINT ( 'NONE',  ( -18.51555513499624439, -9.352657054493677791, -40.69516989569750365 ) ) ;
#84335=CIRCLE ( 'NONE', #34527, 4.150000000000001243 ) ;
#84345=ORIENTED_EDGE ( 'NONE', *, *, #127709, .F. ) ;
#84347=EDGE_CURVE ( 'NONE', #140862, #256921, #125352, .T. ) ;
#84377=AXIS2_PLACEMENT_3D ( 'NONE', #65992, #124695, #84212 ) ;
#84379=AXIS2_PLACEMENT_3D ( 'NONE', #204370, #25748, #105231 ) ;
#84381=AXIS2_PLACEMENT_3D ( 'NONE', #97594, #115920, #179748 ) ;
#84386=ORIENTED_EDGE ( 'NONE', *, *, #238929, .T. ) ;
#84436=VERTEX_POINT ( 'NONE', #239660 ) ;
#84446=ORIENTED_EDGE ( 'NONE', *, *, #2605, .T. ) ;
#84461=ORIENTED_EDGE ( 'NONE', *, *, #234307, .T. ) ;
#84474=ADVANCED_FACE ( 'NONE', ( #128704 ), #233885, .F. ) ;
#84475=CARTESIAN_POINT ( 'NONE',  ( 22.47071067811865319, 0.09909245471376171288, -25.77992525550195424 ) ) ;
#84487=CARTESIAN_POINT ( 'NONE',  ( -23.25000000000000000, -1.149570369564537842, -74.81591248450196474 ) ) ;
#84502=CARTESIAN_POINT ( 'NONE',  ( 21.53551880898956838, 6.784797761427480367, -33.40103026542833931 ) ) ;
#84537=TOROIDAL_SURFACE ( 'NONE', #167813, 0.2000000000000000111, 0.1000000000000000056 ) ;
#84578=DIRECTION ( 'NONE',  ( 0.000000000000000000, 0.000000000000000000, 1.000000000000000000 ) ) ;
#84590=VECTOR ( 'NONE', #14705, 1000.000000000000000 ) ;
#84605=CARTESIAN_POINT ( 'NONE',  ( -21.14999999999999858, 1.115600667400684642E-11, -26.95934304829875927 ) ) ;
#84611=CIRCLE ( 'NONE', #180518, 11.74999999999999645 ) ;
#84617=ORIENTED_EDGE ( 'NONE', *, *, #161599, .T. ) ;
#84629=ORIENTED_EDGE ( 'NONE', *, *, #31496, .F. ) ;
#84636=CARTESIAN_POINT ( 'NONE',  ( -23.15000000000000213, 1.115600667400684642E-11, -67.00000000000000000 ) ) ;
#84684=DIRECTION ( 'NONE',  ( 2.952720810173289112E-16, -1.000000000000000000, 0.000000000000000000 ) ) ;
#84702=VERTEX_POINT ( 'NONE', #181632 ) ;
#84720=AXIS2_PLACEMENT_3D ( 'NONE', #204154, #106327, #4665 ) ;
#84737=CARTESIAN_POINT ( 'NONE',  ( -20.64999999999999858, 2.000000000011154189, -54.17537807723790166 ) ) ;
#84738=ORIENTED_EDGE ( 'NONE', *, *, #220915, .F. ) ;
#84744=AXIS2_PLACEMENT_3D ( 'NONE', #225120, #144290, #128622 ) ;
#84758=LINE ( 'NONE', #67800, #145131 ) ;
#84768=ORIENTED_EDGE ( 'NONE', *, *, #127819, .F. ) ;
#84792=ORIENTED_EDGE ( 'NONE', *, *, #48179, .F. ) ;
#84926=CARTESIAN_POINT ( 'NONE',  ( -20.64999999999999858, 1.115600667400684642E-11, -65.00000000000000000 ) ) ;
#84941=ORIENTED_EDGE ( 'NONE', *, *, #149491, .F. ) ;
#84950=EDGE_CURVE ( 'NONE', #12445, #116181, #254493, .T. ) ;
#84972=CARTESIAN_POINT ( 'NONE',  ( 18.49999999999998934, 10.29288807859941457, -72.45800201601215917 ) ) ;
#84988=EDGE_CURVE ( 'NONE', #200797, #14640, #208463, .T. ) ;
#84995=DIRECTION ( 'NONE',  ( 0.000000000000000000, 0.008583690987124399305, -0.9999631594459055250 ) ) ;
#85044=CARTESIAN_POINT ( 'NONE',  ( -18.54260524012594047, -9.624219390062449975, -73.74077304577103575 ) ) ;
#85063=AXIS2_PLACEMENT_3D ( 'NONE', #115571, #54304, #232978 ) ;
#85065=ORIENTED_EDGE ( 'NONE', *, *, #206211, .T. ) ;
#85066=CARTESIAN_POINT ( 'NONE',  ( -21.05000000000000071, -1.261786168553869603, -41.58649896354548048 ) ) ;
#85105=DIRECTION ( 'NONE',  ( -1.000000000000000000, 0.000000000000000000, -0.000000000000000000 ) ) ;
#85122=CYLINDRICAL_SURFACE ( 'NONE', #57310, 0.1000000000000028644 ) ;
#85141=CARTESIAN_POINT ( 'NONE',  ( 20.94999999999999574, 6.550000000011159784, -43.34382208968312966 ) ) ;
#85169=EDGE_CURVE ( 'NONE', #72626, #54754, #221358, .T. ) ;
#85174=ORIENTED_EDGE ( 'NONE', *, *, #245933, .F. ) ;
#85207=CARTESIAN_POINT ( 'NONE',  ( -22.50000000000094147, 0.1008583691097610785, -21.75043287651059387 ) ) ;
#85214=CARTESIAN_POINT ( 'NONE',  ( 21.05000000000000426, 10.72371710471867878, -41.09441739161312057 ) ) ;
#85227=CARTESIAN_POINT ( 'NONE',  ( -21.05000000000000071, 6.497017786443051612, -33.51454569056947008 ) ) ;
#85240=LINE ( 'NONE', #9585, #96970 ) ;
#85260=SPHERICAL_SURFACE ( 'NONE', #192026, 0.1000000000000000056 ) ;
#85292=FACE_OUTER_BOUND ( 'NONE', #16483, .T. ) ;
#85308=EDGE_CURVE ( 'NONE', #228375, #2313, #208912, .T. ) ;
#85314=EDGE_LOOP ( 'NONE', ( #77752, #37433, #34257, #141770 ) ) ;
#85331=DIRECTION ( 'NONE',  ( -0.000000000000000000, -0.000000000000000000, -1.000000000000000000 ) ) ;
#85362=CIRCLE ( 'NONE', #118742, 0.1999999999999987899 ) ;
#85379=ORIENTED_EDGE ( 'NONE', *, *, #252188, .T. ) ;
#85421=CIRCLE ( 'NONE', #197881, 0.8750000000000007772 ) ;
#85453=EDGE_CURVE ( 'NONE', #113415, #213775, #239731, .T. ) ;
#85498=EDGE_LOOP ( 'NONE', ( #217762, #13337, #206993, #174178 ) ) ;
#85643=CARTESIAN_POINT ( 'NONE',  ( 21.05000000000000071, -0.09999999998884512298, -26.95934304829875927 ) ) ;
#85680=CARTESIAN_POINT ( 'NONE',  ( -18.59999999999999787, 11.65000000001115232, -54.85000000000000142 ) ) ;
#85717=CARTESIAN_POINT ( 'NONE',  ( -20.85000000000000142, 7.021664781911246322, -70.83356540189728889 ) ) ;
#85742=EDGE_CURVE ( 'NONE', #189515, #200872, #185843, .T. ) ;
#85749=CARTESIAN_POINT ( 'NONE',  ( 21.05000000000000071, 10.72371710471867701, -45.66119029412745078 ) ) ;
#85762=ORIENTED_EDGE ( 'NONE', *, *, #221357, .T. ) ;
#85770=AXIS2_PLACEMENT_3D ( 'NONE', #134746, #130921, #211753 ) ;
#85788=ORIENTED_EDGE ( 'NONE', *, *, #244147, .T. ) ;
#85801=EDGE_CURVE ( 'NONE', #137338, #31610, #254993, .T. ) ;
#85816=EDGE_CURVE ( 'NONE', #2443, #31458, #205165, .T. ) ;
#85843=EDGE_CURVE ( 'NONE', #133095, #191642, #124600, .T. ) ;
#85875=VERTEX_POINT ( 'NONE', #104979 ) ;
#85878=EDGE_CURVE ( 'NONE', #108455, #73797, #224951, .T. ) ;
#85913=LINE ( 'NONE', #67664, #160153 ) ;
#85987=EDGE_LOOP ( 'NONE', ( #170905, #125914, #1413, #15444 ) ) ;
#86002=ORIENTED_EDGE ( 'NONE', *, *, #13429, .T. ) ;
#86004=CARTESIAN_POINT ( 'NONE',  ( 23.14999999999999858, 11.65000000001116298, -59.98519422934606382 ) ) ;
#86013=CARTESIAN_POINT ( 'NONE',  ( -18.59999999999999787, -1.162701749926853712, -41.60000000000000142 ) ) ;
#86031=VERTEX_POINT ( 'NONE', #111444 ) ;
#86039=AXIS2_PLACEMENT_3D ( 'NONE', #174321, #153473, #78984 ) ;
#86046=ADVANCED_FACE ( 'NONE', ( #117853 ), #55125, .T. ) ;
#86048=CARTESIAN_POINT ( 'NONE',  ( 23.25000000000000000, -9.599999999988842347, -57.10603087734755690 ) ) ;
#86060=CARTESIAN_POINT ( 'NONE',  ( 21.05000000000000071, 1.115623935689868526E-11, -65.10000000000000853 ) ) ;
#86076=DIRECTION ( 'NONE',  ( 0.000000000000000000, 0.000000000000000000, -1.000000000000000000 ) ) ;
#86115=EDGE_CURVE ( 'NONE', #45034, #210604, #98255, .T. ) ;
#86170=AXIS2_PLACEMENT_3D ( 'NONE', #81203, #2962, #218146 ) ;
#86177=ORIENTED_EDGE ( 'NONE', *, *, #210467, .F. ) ;
#86235=DIRECTION ( 'NONE',  ( 1.000000000000000000, -0.000000000000000000, -0.000000000000000000 ) ) ;
#86260=AXIS2_PLACEMENT_3D ( 'NONE', #185698, #170033, #229955 ) ;
#86292=CARTESIAN_POINT ( 'NONE',  ( 20.94983749550516450, 10.29766095125292402, -72.47436639332755703 ) ) ;
#86299=CARTESIAN_POINT ( 'NONE',  ( -23.15000000000000213, 1.115600667400684642E-11, -46.27499999999999858 ) ) ;
#86311=CARTESIAN_POINT ( 'NONE',  ( -20.94999999999999929, 1.360870587203197646, -41.57299792709095954 ) ) ;
#86315=LINE ( 'NONE', #25116, #253309 ) ;
#86338=VERTEX_POINT ( 'NONE', #255411 ) ;
#86398=AXIS2_PLACEMENT_3D ( 'NONE', #88299, #225249, #160523 ) ;
#86409=AXIS2_PLACEMENT_3D ( 'NONE', #247415, #131325, #133890 ) ;
#86448=TOROIDAL_SURFACE ( 'NONE', #61544, 11.70000000000000107, 0.1000000000000000056 ) ;
#86478=CARTESIAN_POINT ( 'NONE',  ( -22.39999999999999858, 11.65000000001115588, -33.50000000000000000 ) ) ;
#86480=ORIENTED_EDGE ( 'NONE', *, *, #151385, .T. ) ;
#86546=ORIENTED_EDGE ( 'NONE', *, *, #163805, .F. ) ;
#86554=PLANE ( 'NONE',  #61569 ) ;
#86559=EDGE_LOOP ( 'NONE', ( #108221, #4693, #143970, #1049 ) ) ;
#86566=ORIENTED_EDGE ( 'NONE', *, *, #253778, .F. ) ;
#86569=CARTESIAN_POINT ( 'NONE',  ( 20.72390388899108515, 10.58996311843486993, -41.01134829574520779 ) ) ;
#86578=DIRECTION ( 'NONE',  ( 0.000000000000000000, -0.1350103645451904977, 0.9908441862701596881 ) ) ;
#86605=VERTEX_POINT ( 'NONE', #89648 ) ;
#86644=ORIENTED_EDGE ( 'NONE', *, *, #54155, .F. ) ;
#86664=DIRECTION ( 'NONE',  ( -0.000000000000000000, 0.000000000000000000, -1.000000000000000000 ) ) ;
#86684=VERTEX_POINT ( 'NONE', #196456 ) ;
#86704=VERTEX_POINT ( 'NONE', #154804 ) ;
#86711=CARTESIAN_POINT ( 'NONE',  ( 23.25000000000000355, -22.45632476061176774, -40.29389844773160689 ) ) ;
#86716=CARTESIAN_POINT ( 'NONE',  ( 23.15000000000000213, -11.64999999998883595, -63.89999999999999858 ) ) ;
#86723=VERTEX_POINT ( 'NONE', #195215 ) ;
#86735=CARTESIAN_POINT ( 'NONE',  ( -23.25000000000000000, 11.75000000001115552, -21.75000000000000355 ) ) ;
#86766=ORIENTED_EDGE ( 'NONE', *, *, #78976, .T. ) ;
#86832=AXIS2_PLACEMENT_3D ( 'NONE', #229878, #189472, #31706 ) ;
#86928=LINE ( 'NONE', #21855, #150736 ) ;
#86956=EDGE_CURVE ( 'NONE', #18621, #123416, #43241, .T. ) ;
#86971=AXIS2_PLACEMENT_3D ( 'NONE', #182198, #3539, #162635 ) ;
#86972=ADVANCED_FACE ( 'NONE', ( #20415 ), #80334, .F. ) ;
#87031=ORIENTED_EDGE ( 'NONE', *, *, #240229, .T. ) ;
#87032=ORIENTED_EDGE ( 'NONE', *, *, #73781, .F. ) ;
#87046=CARTESIAN_POINT ( 'NONE',  ( 21.12769345151713196, 10.71928767695172624, -45.74748034619748438 ) ) ;
#87142=DIRECTION ( 'NONE',  ( 1.000000000000000000, 0.000000000000000000, 0.000000000000000000 ) ) ;
#87174=CARTESIAN_POINT ( 'NONE',  ( -20.94999999999999929, -1.835859311432479268, -78.50443916879852679 ) ) ;
#87181=ORIENTED_EDGE ( 'NONE', *, *, #226906, .F. ) ;
#87188=EDGE_CURVE ( 'NONE', #201200, #38057, #192314, .T. ) ;
#87197=TOROIDAL_SURFACE ( 'NONE', #145462, 11.65000000000000036, 0.1000000000000000056 ) ;
#87198=TOROIDAL_SURFACE ( 'NONE', #237258, 4.149999999999999467, 0.1000000000000000056 ) ;
#87220=EDGE_CURVE ( 'NONE', #194844, #171093, #122346, .T. ) ;
#87238=ORIENTED_EDGE ( 'NONE', *, *, #8687, .T. ) ;
#87270=CARTESIAN_POINT ( 'NONE',  ( -20.94999999999999929, 1.115600667400684642E-11, -67.00000000000000000 ) ) ;
#87276=LINE ( 'NONE', #24789, #203011 ) ;
#87288=DIRECTION ( 'NONE',  ( -0.000000000000000000, 0.000000000000000000, 1.000000000000000000 ) ) ;
#87323=EDGE_LOOP ( 'NONE', ( #178373, #167262, #80358, #5050 ) ) ;
#87327=CARTESIAN_POINT ( 'NONE',  ( 18.49999999999998934, 19.85039924724470950, -35.78030305780136189 ) ) ;
#87345=EDGE_LOOP ( 'NONE', ( #230373, #10967, #246770, #254919 ) ) ;
#87355=ORIENTED_EDGE ( 'NONE', *, *, #235951, .F. ) ;
#87364=ORIENTED_EDGE ( 'NONE', *, *, #169896, .T. ) ;
#87389=CIRCLE ( 'NONE', #116626, 0.6000000000000033085 ) ;
#87442=CARTESIAN_POINT ( 'NONE',  ( -18.59999999999999787, 6.933893972137497030, -70.78564583437358237 ) ) ;
#87444=DIRECTION ( 'NONE',  ( 1.000000000000000000, 0.000000000000000000, 0.000000000000000000 ) ) ;
#87478=CIRCLE ( 'NONE', #53613, 12.77499999999999503 ) ;
#87488=CARTESIAN_POINT ( 'NONE',  ( -22.39999999999999858, 0.1000000000111554016, -33.50000000000000000 ) ) ;
#87531=DIRECTION ( 'NONE',  ( 0.000000000000000000, 0.000000000000000000, -1.000000000000000000 ) ) ;
#87550=DIRECTION ( 'NONE',  ( 0.000000000000000000, 0.000000000000000000, -1.000000000000000000 ) ) ;
#87554=EDGE_CURVE ( 'NONE', #179043, #78788, #183169, .T. ) ;
#87561=VERTEX_POINT ( 'NONE', #154216 ) ;
#87583=CARTESIAN_POINT ( 'NONE',  ( 20.91682497891422798, 10.32263460347359363, -72.56059579686719019 ) ) ;
#87592=DIRECTION ( 'NONE',  ( 0.000000000000000000, -1.000000000000000000, 0.000000000000000000 ) ) ;
#87628=CARTESIAN_POINT ( 'NONE',  ( -18.43459694179558284, -9.494210124986880217, -73.61700520266094827 ) ) ;
#87652=AXIS2_PLACEMENT_3D ( 'NONE', #250671, #255452, #61157 ) ;
#87664=DIRECTION ( 'NONE',  ( 0.000000000000000000, 4.163336342344333240E-14, -1.000000000000000000 ) ) ;
#87677=VERTEX_POINT ( 'NONE', #257064 ) ;
#87692=CARTESIAN_POINT ( 'NONE',  ( -18.59999999999999787, 11.65000000001115232, -45.65000000000000568 ) ) ;
#87695=CARTESIAN_POINT ( 'NONE',  ( -20.94999999999999929, -12.41227409413852811, -64.00000000000000000 ) ) ;
#87699=AXIS2_PLACEMENT_3D ( 'NONE', #49860, #9453, #214080 ) ;
#87721=DIRECTION ( 'NONE',  ( 0.000000000000000000, 1.000000000000000000, 0.000000000000000000 ) ) ;
#87734=EDGE_CURVE ( 'NONE', #217025, #149752, #219031, .T. ) ;
#87750=EDGE_CURVE ( 'NONE', #215192, #181648, #169183, .T. ) ;
#87758=DIRECTION ( 'NONE',  ( 1.000000000000000000, 0.000000000000000000, 0.000000000000000000 ) ) ;
#87784=DIRECTION ( 'NONE',  ( 1.000000000000000000, 0.000000000000000000, -0.000000000000000000 ) ) ;
#87795=CARTESIAN_POINT ( 'NONE',  ( 21.05000000000000071, 10.48443348965288990, -40.95680580149191030 ) ) ;
#87797=EDGE_CURVE ( 'NONE', #205018, #12615, #182736, .T. ) ;
#87798=CARTESIAN_POINT ( 'NONE',  ( -21.05000000000000071, 1.162701749949165642, -41.50000000000000000 ) ) ;
#87807=DIRECTION ( 'NONE',  ( 0.000000000000000000, 1.000000000000000000, 0.000000000000000000 ) ) ;
#87812=CARTESIAN_POINT ( 'NONE',  ( -23.25000000000000000, 4.350000000011156054, -54.84999999999999432 ) ) ;
#87879=ORIENTED_EDGE ( 'NONE', *, *, #146925, .F. ) ;
#87881=EDGE_CURVE ( 'NONE', #181648, #215192, #227410, .T. ) ;
#87887=ORIENTED_EDGE ( 'NONE', *, *, #67864, .T. ) ;
#87888=DIRECTION ( 'NONE',  ( 1.000000000000000000, 0.000000000000000000, 0.000000000000000000 ) ) ;
#87908=EDGE_CURVE ( 'NONE', #156407, #207108, #77546, .T. ) ;
#87944=AXIS2_PLACEMENT_3D ( 'NONE', #80773, #178651, #79497 ) ;
#87951=ORIENTED_EDGE ( 'NONE', *, *, #194452, .F. ) ;
#87972=CARTESIAN_POINT ( 'NONE',  ( -18.59999999999999787, 9.250000000011157297, -45.85000000000000142 ) ) ;
#87976=ADVANCED_FACE ( 'NONE', ( #254224 ), #82942, .T. ) ;
#87978=LINE ( 'NONE', #167573, #65955 ) ;
#87988=CARTESIAN_POINT ( 'NONE',  ( -23.25000000000000000, 4.150000000011156764, -54.75000000000000711 ) ) ;
#88007=VERTEX_POINT ( 'NONE', #64698 ) ;
#88053=EDGE_CURVE ( 'NONE', #9029, #222564, #44461, .T. ) ;
#88057=ORIENTED_EDGE ( 'NONE', *, *, #124046, .T. ) ;
#88092=DIRECTION ( 'NONE',  ( -0.000000000000000000, 1.000000000000000000, 0.000000000000000000 ) ) ;
#88190=EDGE_CURVE ( 'NONE', #200635, #187737, #196199, .T. ) ;
#88211=DIRECTION ( 'NONE',  ( 1.000000000000000000, -0.000000000000000000, -0.000000000000000000 ) ) ;
#88213=CARTESIAN_POINT ( 'NONE',  ( -23.25000000000000000, 11.65000000001115588, -54.75000000000000000 ) ) ;
#88227=EDGE_CURVE ( 'NONE', #14219, #81578, #219220, .T. ) ;
#88259=ORIENTED_EDGE ( 'NONE', *, *, #224691, .F. ) ;
#88264=DIRECTION ( 'NONE',  ( 0.000000000000000000, 1.000000000000000000, 1.224646799147353207E-16 ) ) ;
#88282=DIRECTION ( 'NONE',  ( 1.000000000000000000, 0.000000000000000000, 0.000000000000000000 ) ) ;
#88299=CARTESIAN_POINT ( 'NONE',  ( -20.64999999999999858, 1.115600667400684642E-11, -33.50000000000000000 ) ) ;
#88302=CARTESIAN_POINT ( 'NONE',  ( -22.49231231312463208, 11.64998490368843953, -33.43894711239862971 ) ) ;
#88305=CARTESIAN_POINT ( 'NONE',  ( 21.05000000000000071, -1.162701749926853712, -41.60000000000000142 ) ) ;
#88323=CARTESIAN_POINT ( 'NONE',  ( 21.07189867249812210, 10.72498027010430377, -45.71245144227673762 ) ) ;
#88385=CYLINDRICAL_SURFACE ( 'NONE', #93914, 0.09999999999999781286 ) ;
#88400=VERTEX_POINT ( 'NONE', #239179 ) ;
#88412=DIRECTION ( 'NONE',  ( 1.000000000000000000, 7.304098846218135653E-16, 0.000000000000000000 ) ) ;
#88509=CARTESIAN_POINT ( 'NONE',  ( 23.14999999999998437, 4.050000000011155343, -33.50000000000000000 ) ) ;
#88528=DIRECTION ( 'NONE',  ( 0.000000000000000000, 0.000000000000000000, -1.000000000000000000 ) ) ;
#88547=CARTESIAN_POINT ( 'NONE',  ( -20.94999999999999929, -1.162701749926853712, -41.60000000000000142 ) ) ;
#88596=EDGE_LOOP ( 'NONE', ( #46948, #95529, #177254, #63517 ) ) ;
#88614=DIRECTION ( 'NONE',  ( 0.000000000000000000, -3.447762908503805145E-13, 1.000000000000000000 ) ) ;
#88621=CIRCLE ( 'NONE', #176164, 0.09999999999999939493 ) ;
#88636=B_SPLINE_CURVE_WITH_KNOTS ( 'NONE', 3,
 ( #184343, #87795, #49971, #5686, #85214, #106069 ),
 .UNSPECIFIED., .F., .F.,
 ( 4, 2, 4 ),
 ( 0.000000000000000000, 0.0002113392456165986782, 0.0004226784912331973563 ),
 .UNSPECIFIED. ) ;
#88637=VERTEX_POINT ( 'NONE', #252011 ) ;
#88647=CARTESIAN_POINT ( 'NONE',  ( 20.94999999999999929, -1.835341550213257733, -45.05515129256298223 ) ) ;
#88648=DIRECTION ( 'NONE',  ( -1.000000000000000000, 3.469446951953635015E-14, 0.000000000000000000 ) ) ;
#88655=ORIENTED_EDGE ( 'NONE', *, *, #198879, .F. ) ;
#88661=VERTEX_POINT ( 'NONE', #180200 ) ;
#88666=VERTEX_POINT ( 'NONE', #141067 ) ;
#88691=CARTESIAN_POINT ( 'NONE',  ( -22.50000000000000000, 11.64957080755595520, -33.40000000000000568 ) ) ;
#88724=CARTESIAN_POINT ( 'NONE',  ( -20.54999999999999716, 4.250000000011156409, -45.75000000000000711 ) ) ;
#88730=EDGE_LOOP ( 'NONE', ( #248080, #167610, #245214, #154363 ) ) ;
#88733=AXIS2_PLACEMENT_3D ( 'NONE', #29936, #70355, #188988 ) ;
#88735=AXIS2_PLACEMENT_3D ( 'NONE', #103196, #142331, #79775 ) ;
#88742=AXIS2_PLACEMENT_3D ( 'NONE', #50355, #208191, #246023 ) ;
#88779=CARTESIAN_POINT ( 'NONE',  ( 21.05000000000000071, 6.257814610487280937, -33.40220970869120265 ) ) ;
#88792=EDGE_LOOP ( 'NONE', ( #127988, #28528, #58146, #159379, #14530 ) ) ;
#88816=CIRCLE ( 'NONE', #43066, 0.09999999999999749367 ) ;
#88818=CARTESIAN_POINT ( 'NONE',  ( -20.94999999999999929, 1.115600667400684642E-11, -67.00000000000000000 ) ) ;
#88848=EDGE_CURVE ( 'NONE', #244974, #100799, #254120, .T. ) ;
#88869=CARTESIAN_POINT ( 'NONE',  ( 21.05000000000000071, 10.72371710471867701, -33.50000000000000000 ) ) ;
#88889=AXIS2_PLACEMENT_3D ( 'NONE', #184236, #128127, #108559 ) ;
#88927=ORIENTED_EDGE ( 'NONE', *, *, #243235, .T. ) ;
#88961=ORIENTED_EDGE ( 'NONE', *, *, #142983, .T. ) ;
#88974=EDGE_CURVE ( 'NONE', #195545, #163442, #113850, .T. ) ;
#88977=ORIENTED_EDGE ( 'NONE', *, *, #184782, .F. ) ;
#88989=EDGE_CURVE ( 'NONE', #127486, #189010, #155588, .T. ) ;
#89022=CARTESIAN_POINT ( 'NONE',  ( -18.59999999999999787, 1.115600667400684642E-11, -67.00000000000000000 ) ) ;
#89049=DIRECTION ( 'NONE',  ( 0.000000000000000000, 0.000000000000000000, 1.000000000000000000 ) ) ;
#89078=CIRCLE ( 'NONE', #234846, 0.5000000000000004441 ) ;
#89096=ORIENTED_EDGE ( 'NONE', *, *, #35056, .F. ) ;
#89104=DIRECTION ( 'NONE',  ( 0.000000000000000000, 1.000000000000000000, 1.734723475976807292E-15 ) ) ;
#89130=ORIENTED_EDGE ( 'NONE', *, *, #168349, .F. ) ;
#89166=CIRCLE ( 'NONE', #51723, 0.1000000000000028644 ) ;
#89237=DIRECTION ( 'NONE',  ( 1.000000000000000000, 3.265361837132813093E-16, -0.000000000000000000 ) ) ;
#89278=DIRECTION ( 'NONE',  ( 0.000000000000000000, 0.000000000000000000, -1.000000000000000000 ) ) ;
#89301=EDGE_LOOP ( 'NONE', ( #174948, #43583, #171811, #183665 ) ) ;
#89311=DIRECTION ( 'NONE',  ( -0.000000000000000000, 0.000000000000000000, -1.000000000000000000 ) ) ;
#89326=CARTESIAN_POINT ( 'NONE',  ( -18.51697539158856998, 10.31565961587945779, -72.53641941191783360 ) ) ;
#89361=AXIS2_PLACEMENT_3D ( 'NONE', #65095, #51926, #211032 ) ;
#89382=EDGE_CURVE ( 'NONE', #190151, #149752, #126691, .T. ) ;
#89384=TOROIDAL_SURFACE ( 'NONE', #156061, 0.2000000000000000111, 0.1000000000000000056 ) ;
#89405=EDGE_CURVE ( 'NONE', #88007, #105461, #43310, .T. ) ;
#89414=FACE_OUTER_BOUND ( 'NONE', #165030, .T. ) ;
#89475=DIRECTION ( 'NONE',  ( 1.000000000000000000, 2.952720810173289112E-16, -0.000000000000000000 ) ) ;
#89601=CIRCLE ( 'NONE', #27109, 2.000000000000001776 ) ;
#89604=CARTESIAN_POINT ( 'NONE',  ( -22.49436431346200038, 11.64995094766461392, -33.43309647027773934 ) ) ;
#89617=AXIS2_PLACEMENT_3D ( 'NONE', #211561, #112468, #129449 ) ;
#89648=CARTESIAN_POINT ( 'NONE',  ( -20.94999999999999929, 1.115650877919449575E-11, -71.09999999999999432 ) ) ;
#89715=EDGE_CURVE ( 'NONE', #232170, #14704, #130965, .T. ) ;
#89741=CARTESIAN_POINT ( 'NONE',  ( 22.59080734064468032, 11.75000000001115552, -33.46925029190293088 ) ) ;
#89743=ADVANCED_FACE ( 'NONE', ( #191161 ), #239298, .F. ) ;
#89746=CARTESIAN_POINT ( 'NONE',  ( 22.49999999999999645, 11.64987090377453605, -33.41748010912699129 ) ) ;
#89802=FACE_OUTER_BOUND ( 'NONE', #208974, .T. ) ;
#89847=CARTESIAN_POINT ( 'NONE',  ( -21.59142135623730852, 7.850000000011158718, -45.75000000000000000 ) ) ;
#89851=LINE ( 'NONE', #172014, #182376 ) ;
#89870=DIRECTION ( 'NONE',  ( 1.000000000000000000, -0.000000000000000000, -0.000000000000000000 ) ) ;
#89891=CIRCLE ( 'NONE', #119139, 0.1000000000000028644 ) ;
#89917=ORIENTED_EDGE ( 'NONE', *, *, #27266, .T. ) ;
#89927=CARTESIAN_POINT ( 'NONE',  ( -20.54999999999999716, 2.500000000011154633, -53.77537807723790309 ) ) ;
#89935=VERTEX_POINT ( 'NONE', #8039 ) ;
#89947=DIRECTION ( 'NONE',  ( 1.000000000000000000, -0.000000000000000000, -0.000000000000000000 ) ) ;
#89955=ORIENTED_EDGE ( 'NONE', *, *, #81258, .F. ) ;
#89964=DIRECTION ( 'NONE',  ( -1.000000000000000000, 0.000000000000000000, 0.000000000000000000 ) ) ;
#90042=EDGE_CURVE ( 'NONE', #159998, #43292, #189418, .T. ) ;
#90044=ORIENTED_EDGE ( 'NONE', *, *, #59317, .T. ) ;
#90090=ORIENTED_EDGE ( 'NONE', *, *, #165318, .T. ) ;
#90092=CARTESIAN_POINT ( 'NONE',  ( 20.94999999999999929, 1.115600667400684642E-11, -74.80000000000001137 ) ) ;
#90122=CARTESIAN_POINT ( 'NONE',  ( 23.14999999999999858, 1.115600667400684642E-11, -71.00000000000001421 ) ) ;
#90135=ORIENTED_EDGE ( 'NONE', *, *, #69453, .T. ) ;
#90150=ORIENTED_EDGE ( 'NONE', *, *, #115188, .F. ) ;
#90154=CARTESIAN_POINT ( 'NONE',  ( -22.50000000000000000, 1.115600667400684642E-11, -27.25000000000000355 ) ) ;
#90175=DIRECTION ( 'NONE',  ( 0.000000000000000000, -1.000000000000000000, 0.000000000000000000 ) ) ;
#90184=ADVANCED_FACE ( 'NONE', ( #155273 ), #233510, .T. ) ;
#90202=ORIENTED_EDGE ( 'NONE', *, *, #139211, .T. ) ;
#90220=CARTESIAN_POINT ( 'NONE',  ( 23.14999999999999858, 1.115600667400684642E-11, -67.00000000000000000 ) ) ;
#90230=ORIENTED_EDGE ( 'NONE', *, *, #33406, .T. ) ;
#90233=EDGE_CURVE ( 'NONE', #15098, #40541, #51612, .T. ) ;
#90240=DIRECTION ( 'NONE',  ( -0.000000000000000000, 0.1298341882520022694, 0.9915357197604853789 ) ) ;
#90261=FACE_OUTER_BOUND ( 'NONE', #98666, .T. ) ;
#90290=CARTESIAN_POINT ( 'NONE',  ( 18.47073956224751257, -9.471729412460696551, -40.60868575281791237 ) ) ;
#90324=ADVANCED_FACE ( 'NONE', ( #43000 ), #218049, .T. ) ;
#90329=DIRECTION ( 'NONE',  ( 0.000000000000000000, 0.000000000000000000, -1.000000000000000000 ) ) ;
#90333=CIRCLE ( 'NONE', #102792, 11.75000000000000000 ) ;
#90385=DIRECTION ( 'NONE',  ( -1.000000000000000000, -0.000000000000000000, 0.000000000000000000 ) ) ;
#90391=LINE ( 'NONE', #249490, #142153 ) ;
#90419=DIRECTION ( 'NONE',  ( 1.000000000000000000, 0.000000000000000000, 0.000000000000000000 ) ) ;
#90427=FACE_OUTER_BOUND ( 'NONE', #71732, .T. ) ;
#90439=DIRECTION ( 'NONE',  ( 0.000000000000000000, 0.000000000000000000, -1.000000000000000000 ) ) ;
#90476=FACE_OUTER_BOUND ( 'NONE', #32715, .T. ) ;
#90489=AXIS2_PLACEMENT_3D ( 'NONE', #57675, #42004, #116396 ) ;
#90520=DIRECTION ( 'NONE',  ( 0.000000000000000000, 0.9876197685951252359, -0.1568667991644863424 ) ) ;
#90563=AXIS2_PLACEMENT_3D ( 'NONE', #19498, #216399, #119901 ) ;
#90568=EDGE_CURVE ( 'NONE', #238808, #187977, #135011, .T. ) ;
#90578=DIRECTION ( 'NONE',  ( -2.557131231893036985E-16, 0.8660254037844384856, -0.5000000000000002220 ) ) ;
#90622=DIRECTION ( 'NONE',  ( -1.000000000000000000, -0.000000000000000000, -0.000000000000000000 ) ) ;
#90630=DIRECTION ( 'NONE',  ( -1.000000000000000000, -2.952720810173289112E-16, 0.000000000000000000 ) ) ;
#90636=DIRECTION ( 'NONE',  ( -1.000000000000000000, 0.000000000000000000, 0.000000000000000000 ) ) ;
#90654=CARTESIAN_POINT ( 'NONE',  ( 18.52928932188133970, 10.27928932189250055, -58.15000000000000568 ) ) ;
#90656=ORIENTED_EDGE ( 'NONE', *, *, #95664, .F. ) ;
#90671=CARTESIAN_POINT ( 'NONE',  ( 18.59999999999999432, -1.162701749926853712, -41.60000000000000142 ) ) ;
#90674=VERTEX_POINT ( 'NONE', #243440 ) ;
#90705=ORIENTED_EDGE ( 'NONE', *, *, #207305, .T. ) ;
#90725=DIRECTION ( 'NONE',  ( 0.000000000000000000, 0.000000000000000000, 1.000000000000000000 ) ) ;
#90757=CARTESIAN_POINT ( 'NONE',  ( 23.15000000000000213, -8.999999999988842703, -57.10603087734755690 ) ) ;
#90779=ORIENTED_EDGE ( 'NONE', *, *, #213737, .F. ) ;
#90783=DIRECTION ( 'NONE',  ( 0.000000000000000000, 0.000000000000000000, -1.000000000000000000 ) ) ;
#90789=DIRECTION ( 'NONE',  ( -1.000000000000000000, -0.000000000000000000, 0.000000000000000000 ) ) ;
#90821=ORIENTED_EDGE ( 'NONE', *, *, #254212, .F. ) ;
#90862=ORIENTED_EDGE ( 'NONE', *, *, #119316, .T. ) ;
#90878=AXIS2_PLACEMENT_3D ( 'NONE', #137129, #236216, #40635 ) ;
#90918=FACE_OUTER_BOUND ( 'NONE', #50905, .T. ) ;
#90926=VERTEX_POINT ( 'NONE', #200171 ) ;
#90956=DIRECTION ( 'NONE',  ( 1.000000000000000000, 2.952720810173289112E-16, -0.000000000000000000 ) ) ;
#90974=ORIENTED_EDGE ( 'NONE', *, *, #74811, .T. ) ;
#90985=EDGE_CURVE ( 'NONE', #84702, #216494, #76962, .T. ) ;
#90996=TOROIDAL_SURFACE ( 'NONE', #124318, 11.70000000000000639, 0.1000000000000000056 ) ;
#91023=SPHERICAL_SURFACE ( 'NONE', #63238, 0.1000000000000000056 ) ;
#91035=VECTOR ( 'NONE', #189199, 1000.000000000000000 ) ;
#91042=FACE_OUTER_BOUND ( 'NONE', #26140, .T. ) ;
#91060=CYLINDRICAL_SURFACE ( 'NONE', #173915, 0.5000000000000004441 ) ;
#91076=DIRECTION ( 'NONE',  ( -1.000000000000000000, 0.000000000000000000, 0.000000000000000000 ) ) ;
#91127=VERTEX_POINT ( 'NONE', #167487 ) ;
#91129=AXIS2_PLACEMENT_3D ( 'NONE', #28779, #249079, #165697 ) ;
#91131=EDGE_LOOP ( 'NONE', ( #136527, #2348, #166122, #43698 ) ) ;
#91141=LINE ( 'NONE', #170740, #53602 ) ;
#91144=DIRECTION ( 'NONE',  ( 1.000000000000000000, 0.000000000000000000, 0.000000000000000000 ) ) ;
#91178=ORIENTED_EDGE ( 'NONE', *, *, #65097, .T. ) ;
#91189=EDGE_CURVE ( 'NONE', #2313, #83334, #6214, .T. ) ;
#91196=ADVANCED_FACE ( 'NONE', ( #112630 ), #141560, .T. ) ;
#91211=ORIENTED_EDGE ( 'NONE', *, *, #227413, .F. ) ;
#91242=CIRCLE ( 'NONE', #49541, 11.74999999999999645 ) ;
#91252=DIRECTION ( 'NONE',  ( 0.000000000000000000, -1.000000000000000000, 0.000000000000000000 ) ) ;
#91263=AXIS2_PLACEMENT_3D ( 'NONE', #31144, #8970, #91076 ) ;
#91264=ORIENTED_EDGE ( 'NONE', *, *, #127896, .F. ) ;
#91275=EDGE_LOOP ( 'NONE', ( #69735, #237432, #61978, #5998 ) ) ;
#91297=CARTESIAN_POINT ( 'NONE',  ( -22.50014994444008565, 11.74971973190325158, -33.41691984328069509 ) ) ;
#91300=FACE_OUTER_BOUND ( 'NONE', #205556, .T. ) ;
#91332=VECTOR ( 'NONE', #50307, 1000.000000000000000 ) ;
#91345=CARTESIAN_POINT ( 'NONE',  ( 23.24999999999999289, 11.65000000001116298, -45.65000000000000568 ) ) ;
#91348=CARTESIAN_POINT ( 'NONE',  ( 21.08489247129321242, 8.877675190881227252, -45.85000000000000853 ) ) ;
#91413=DIRECTION ( 'NONE',  ( 1.000000000000000000, -0.000000000000000000, -0.000000000000000000 ) ) ;
#91418=CARTESIAN_POINT ( 'NONE',  ( -20.64999999999999858, 1.940186915899004161, -54.17088078894667547 ) ) ;
#91427=AXIS2_PLACEMENT_3D ( 'NONE', #225614, #143531, #35192 ) ;
#91461=FACE_OUTER_BOUND ( 'NONE', #70977, .T. ) ;
#91462=CARTESIAN_POINT ( 'NONE',  ( 18.50000000000000355, -9.421074344976016590, -73.82447205943003610 ) ) ;
#91476=ORIENTED_EDGE ( 'NONE', *, *, #33406, .F. ) ;
#91479=EDGE_CURVE ( 'NONE', #80932, #9718, #89601, .T. ) ;
#91502=DIRECTION ( 'NONE',  ( 0.000000000000000000, 0.000000000000000000, 1.000000000000000000 ) ) ;
#91511=EDGE_LOOP ( 'NONE', ( #25260, #142855, #114963, #1836 ) ) ;
#91521=ORIENTED_EDGE ( 'NONE', *, *, #220734, .F. ) ;
#91531=CYLINDRICAL_SURFACE ( 'NONE', #167300, 11.80000000000000426 ) ;
#91566=CARTESIAN_POINT ( 'NONE',  ( -20.94999999999999929, 1.115600667400684642E-11, -55.30000000000000426 ) ) ;
#91582=CIRCLE ( 'NONE', #24967, 0.09999999999999939493 ) ;
#91590=AXIS2_PLACEMENT_3D ( 'NONE', #794, #79051, #94789 ) ;
#91613=DIRECTION ( 'NONE',  ( -0.000000000000000000, -0.000000000000000000, 1.000000000000000000 ) ) ;
#91618=CYLINDRICAL_SURFACE ( 'NONE', #95531, 0.09999999999999939493 ) ;
#91677=DIRECTION ( 'NONE',  ( 0.000000000000000000, -1.000000000000000000, 0.000000000000000000 ) ) ;
#91684=LINE ( 'NONE', #135927, #39731 ) ;
#91692=DIRECTION ( 'NONE',  ( 0.000000000000000000, 2.891205793294679805E-16, -1.000000000000000000 ) ) ;
#91711=ORIENTED_EDGE ( 'NONE', *, *, #107365, .F. ) ;
#91735=CARTESIAN_POINT ( 'NONE',  ( 22.00356870068866755, 5.513940439853673043E-12, -26.24575763824345387 ) ) ;
#91744=ORIENTED_EDGE ( 'NONE', *, *, #164723, .F. ) ;
#91809=FACE_OUTER_BOUND ( 'NONE', #101801, .T. ) ;
#91819=DIRECTION ( 'NONE',  ( 0.000000000000000000, 0.000000000000000000, -1.000000000000000000 ) ) ;
#91825=AXIS2_PLACEMENT_3D ( 'NONE', #101399, #141853, #179722 ) ;
#91858=AXIS2_PLACEMENT_3D ( 'NONE', #57603, #194594, #216691 ) ;
#91880=EDGE_LOOP ( 'NONE', ( #111379, #143650, #65885, #24496 ) ) ;
#91881=VECTOR ( 'NONE', #94559, 1000.000000000000000 ) ;
#91890=CARTESIAN_POINT ( 'NONE',  ( 21.14999999999999503, -0.09999999998884338825, -21.85042919245520210 ) ) ;
#91903=CARTESIAN_POINT ( 'NONE',  ( -18.50000972452446035, 10.29326151435326508, -72.45928225104148623 ) ) ;
#91907=CARTESIAN_POINT ( 'NONE',  ( -21.55000000000000071, 7.350000000011155166, -45.75000000000000000 ) ) ;
#91922=ADVANCED_FACE ( 'NONE', ( #92112 ), #189755, .F. ) ;
#91995=DIRECTION ( 'NONE',  ( 1.000000000000000000, 0.000000000000000000, 0.000000000000000000 ) ) ;
#92018=DIRECTION ( 'NONE',  ( -1.000000000000000000, 0.000000000000000000, 0.000000000000000000 ) ) ;
#92028=FACE_OUTER_BOUND ( 'NONE', #16994, .T. ) ;
#92043=ORIENTED_EDGE ( 'NONE', *, *, #92982, .F. ) ;
#92052=CARTESIAN_POINT ( 'NONE',  ( 21.04999999999999716, 8.871279686006802834, -42.05862899514095687 ) ) ;
#92054=ORIENTED_EDGE ( 'NONE', *, *, #209295, .F. ) ;
#92075=CARTESIAN_POINT ( 'NONE',  ( -18.59999999999999787, 11.60000000001115872, -40.42820323027555673 ) ) ;
#92079=CIRCLE ( 'NONE', #171250, 4.099999999999992539 ) ;
#92112=FACE_OUTER_BOUND ( 'NONE', #134932, .T. ) ;
#92141=CARTESIAN_POINT ( 'NONE',  ( 21.12757541349815682, 6.473380571262609351, -33.49483878419025018 ) ) ;
#92152=DIRECTION ( 'NONE',  ( -3.265361837132813093E-16, 1.000000000000000000, 0.000000000000000000 ) ) ;
#92232=DIRECTION ( 'NONE',  ( -1.000000000000000000, 0.000000000000000000, 0.000000000000000000 ) ) ;
#92286=AXIS2_PLACEMENT_3D ( 'NONE', #183802, #27340, #44306 ) ;
#92295=DIRECTION ( 'NONE',  ( 0.000000000000000000, -0.1298341882520022694, -0.9915357197604853789 ) ) ;
#92312=CARTESIAN_POINT ( 'NONE',  ( -20.54999999999999716, 4.350000000011156054, -54.65000000000000568 ) ) ;
#92317=EDGE_CURVE ( 'NONE', #36910, #14565, #26724, .T. ) ;
#92323=EDGE_CURVE ( 'NONE', #73682, #212264, #140029, .T. ) ;
#92331=DIRECTION ( 'NONE',  ( 0.000000000000000000, 2.602085213965226419E-14, -1.000000000000000000 ) ) ;
#92388=DIRECTION ( 'NONE',  ( 1.000000000000000000, -0.000000000000000000, -0.000000000000000000 ) ) ;
#92408=ADVANCED_FACE ( 'NONE', ( #52669 ), #23385, .T. ) ;
#92443=EDGE_CURVE ( 'NONE', #27329, #203889, #123489, .T. ) ;
#92456=VECTOR ( 'NONE', #140675, 1000.000000000000000 ) ;
#92480=DIRECTION ( 'NONE',  ( -0.000000000000000000, 0.000000000000000000, 1.000000000000000000 ) ) ;
#92501=ORIENTED_EDGE ( 'NONE', *, *, #37644, .F. ) ;
#92518=EDGE_LOOP ( 'NONE', ( #164328, #246462, #153172, #161027, #30462, #207478, #78236 ) ) ;
#92526=VECTOR ( 'NONE', #79479, 1000.000000000000000 ) ;
#92576=CARTESIAN_POINT ( 'NONE',  ( 20.94999999999999574, 6.400000000011158541, -43.43042463006157305 ) ) ;
#92580=CARTESIAN_POINT ( 'NONE',  ( -22.39999999999999858, 7.790779598384559357, -33.50000000000000711 ) ) ;
#92588=DIRECTION ( 'NONE',  ( 1.000000000000000000, 0.000000000000000000, 0.000000000000000000 ) ) ;
#92608=DIRECTION ( 'NONE',  ( 0.000000000000000000, -0.000000000000000000, 1.000000000000000000 ) ) ;
#92617=DIRECTION ( 'NONE',  ( -1.000000000000000000, 0.000000000000000000, 0.000000000000000000 ) ) ;
#92626=CARTESIAN_POINT ( 'NONE',  ( 23.14999999999999858, 5.600000000011153389, -45.90526601891310321 ) ) ;
#92651=VECTOR ( 'NONE', #252027, 1000.000000000000000 ) ;
#92699=CYLINDRICAL_SURFACE ( 'NONE', #47499, 0.1000000000000028644 ) ;
#92709=EDGE_CURVE ( 'NONE', #143764, #127078, #140207, .T. ) ;
#92716=EDGE_CURVE ( 'NONE', #6281, #84436, #15163, .T. ) ;
#92721=SPHERICAL_SURFACE ( 'NONE', #4601, 0.1000000000000000056 ) ;
#92723=CARTESIAN_POINT ( 'NONE',  ( 18.59999996954842771, -9.523204137847617545, -73.88304171191651903 ) ) ;
#92735=EDGE_CURVE ( 'NONE', #33939, #215029, #177696, .T. ) ;
#92760=ORIENTED_EDGE ( 'NONE', *, *, #57080, .F. ) ;
#92769=DIRECTION ( 'NONE',  ( -0.000000000000000000, -0.000000000000000000, 1.000000000000000000 ) ) ;
#92789=CARTESIAN_POINT ( 'NONE',  ( 21.09706851349341861, 8.775842513484549912, -45.73556621639964703 ) ) ;
#92839=ORIENTED_EDGE ( 'NONE', *, *, #171940, .T. ) ;
#92868=CARTESIAN_POINT ( 'NONE',  ( 19.97071067811864609, 11.72071067812981404, -58.25000000000000000 ) ) ;
#92886=CARTESIAN_POINT ( 'NONE',  ( -20.64999999999999858, 7.250000000011155521, -45.75000000000000000 ) ) ;
#92887=CARTESIAN_POINT ( 'NONE',  ( -20.54999999999999716, -9.499999999988846255, -57.10603087734755690 ) ) ;
#92912=DIRECTION ( 'NONE',  ( -2.978066053179067751E-16, 1.000000000000000000, 0.000000000000000000 ) ) ;
#92944=CIRCLE ( 'NONE', #97002, 0.1000000000000028644 ) ;
#92972=CARTESIAN_POINT ( 'NONE',  ( 18.49999999999999645, 1.736257131608553550, -45.06865232901750318 ) ) ;
#92982=EDGE_CURVE ( 'NONE', #127120, #188642, #74018, .T. ) ;
#92989=FACE_OUTER_BOUND ( 'NONE', #39701, .T. ) ;
#93035=CARTESIAN_POINT ( 'NONE',  ( -21.05000000000000071, 1.115600667400684642E-11, -63.00000000000000000 ) ) ;
#93041=TOROIDAL_SURFACE ( 'NONE', #1455, 7.800000000000000711, 0.1000000000000000056 ) ;
#93057=CARTESIAN_POINT ( 'NONE',  ( -23.15000000000000213, -8.999999999988846255, -43.39396912265245021 ) ) ;
#93069=DIRECTION ( 'NONE',  ( 0.000000000000000000, 0.000000000000000000, 1.000000000000000000 ) ) ;
#93080=LINE ( 'NONE', #249610, #150717 ) ;
#93096=ORIENTED_EDGE ( 'NONE', *, *, #36691, .F. ) ;
#93097=VECTOR ( 'NONE', #73842, 1000.000000000000000 ) ;
#93115=AXIS2_PLACEMENT_3D ( 'NONE', #202392, #4177, #40782 ) ;
#93136=ORIENTED_EDGE ( 'NONE', *, *, #18802, .T. ) ;
#93141=DIRECTION ( 'NONE',  ( 0.000000000000000000, 0.4930308989875230585, 0.8700118002898322711 ) ) ;
#93159=CIRCLE ( 'NONE', #47360, 0.1000000000000008799 ) ;
#93201=ORIENTED_EDGE ( 'NONE', *, *, #55452, .T. ) ;
#93235=LINE ( 'NONE', #74994, #58225 ) ;
#93312=DIRECTION ( 'NONE',  ( 0.000000000000000000, 0.000000000000000000, -1.000000000000000000 ) ) ;
#93334=CARTESIAN_POINT ( 'NONE',  ( 21.05000000000000071, 8.872080675389078408, -42.02104741883048433 ) ) ;
#93345=DIRECTION ( 'NONE',  ( 4.408576920032447355E-17, -0.1350103645451876666, 0.9908441862701600211 ) ) ;
#93368=CARTESIAN_POINT ( 'NONE',  ( 19.99999999738042789, 11.75000000001116440, -58.18717194963263495 ) ) ;
#93393=EDGE_LOOP ( 'NONE', ( #242023, #33322, #188515 ) ) ;
#93433=ORIENTED_EDGE ( 'NONE', *, *, #5027, .T. ) ;
#93445=DIRECTION ( 'NONE',  ( 2.915501640297155269E-16, -1.000000000000000000, 0.000000000000000000 ) ) ;
#93458=ORIENTED_EDGE ( 'NONE', *, *, #34965, .F. ) ;
#93480=EDGE_LOOP ( 'NONE', ( #108759, #133168, #49322, #117268, #139207, #238149, #204515, #170428, #66880, #232323, #124237, #55016, #69852, #136793 ) ) ;
#93513=DIRECTION ( 'NONE',  ( 1.000000000000000000, 0.000000000000000000, 0.000000000000000000 ) ) ;
#93517=ORIENTED_EDGE ( 'NONE', *, *, #201421, .F. ) ;
#93551=EDGE_CURVE ( 'NONE', #3656, #242144, #213150, .T. ) ;
#93576=DIRECTION ( 'NONE',  ( -0.7070776581709311559, 0.000000000000000000, 0.7071359030027479786 ) ) ;
#93634=CARTESIAN_POINT ( 'NONE',  ( -21.05000000000000071, 1.115600667400684642E-11, -67.00000000000000000 ) ) ;
#93685=CARTESIAN_POINT ( 'NONE',  ( 20.94999999999999929, 5.850000000011156942, -56.86750277572208034 ) ) ;
#93720=CARTESIAN_POINT ( 'NONE',  ( 22.60000000000000142, 1.115600667400684642E-11, -33.50000000000000000 ) ) ;
#93728=FACE_OUTER_BOUND ( 'NONE', #247619, .T. ) ;
#93738=CYLINDRICAL_SURFACE ( 'NONE', #95348, 0.09999999999999939493 ) ;
#93758=CARTESIAN_POINT ( 'NONE',  ( 18.49999999999999289, 7.120270961708750512, -70.65956304183931991 ) ) ;
#93799=DIRECTION ( 'NONE',  ( 1.000000000000000000, 0.000000000000000000, 0.000000000000000000 ) ) ;
#93813=VECTOR ( 'NONE', #247638, 1000.000000000000000 ) ;
#93839=AXIS2_PLACEMENT_3D ( 'NONE', #161440, #221367, #141844 ) ;
#93842=ORIENTED_EDGE ( 'NONE', *, *, #10989, .F. ) ;
#93849=CARTESIAN_POINT ( 'NONE',  ( -22.57320508075687115, 11.75000000001115552, -33.50000000000002842 ) ) ;
#93868=FACE_OUTER_BOUND ( 'NONE', #85314, .T. ) ;
#93905=CARTESIAN_POINT ( 'NONE',  ( -20.94999999999999929, -1.835341550213257733, -45.05515129256298223 ) ) ;
#93914=AXIS2_PLACEMENT_3D ( 'NONE', #10167, #11459, #208382 ) ;
#93921=CARTESIAN_POINT ( 'NONE',  ( 21.14999999999999858, 11.65000000001116298, -45.65000000000000568 ) ) ;
#93983=ORIENTED_EDGE ( 'NONE', *, *, #50924, .T. ) ;
#93989=DIRECTION ( 'NONE',  ( 1.000000000000000000, 0.000000000000000000, 0.000000000000000000 ) ) ;
#94006=CARTESIAN_POINT ( 'NONE',  ( 18.46932045258646937, -9.670685200254602876, -73.67386037299664281 ) ) ;
#94018=AXIS2_PLACEMENT_3D ( 'NONE', #207257, #108142, #72894 ) ;
#94025=ORIENTED_EDGE ( 'NONE', *, *, #45943, .F. ) ;
#94063=AXIS2_PLACEMENT_3D ( 'NONE', #117139, #196657, #135396 ) ;
#94075=CARTESIAN_POINT ( 'NONE',  ( 21.08832698747859169, 8.775364393428372267, -45.72871746646415403 ) ) ;
#94120=LINE ( 'NONE', #190692, #234075 ) ;
#94152=CARTESIAN_POINT ( 'NONE',  ( -23.15000000000000213, -8.999999999988844479, -57.70603087734755832 ) ) ;
#94154=CARTESIAN_POINT ( 'NONE',  ( 18.49505816908823874, -9.437872553199980530, -73.77765720167090535 ) ) ;
#94177=EDGE_CURVE ( 'NONE', #102509, #75871, #32699, .T. ) ;
#94178=CARTESIAN_POINT ( 'NONE',  ( 22.39999999999999503, 7.790779598384535376, -33.50000000000000000 ) ) ;
#94179=AXIS2_PLACEMENT_3D ( 'NONE', #171573, #153299, #91995 ) ;
#94184=EDGE_CURVE ( 'NONE', #19166, #125075, #190894, .T. ) ;
#94192=TOROIDAL_SURFACE ( 'NONE', #40074, 7.791421356237316687, 0.1000000000000000056 ) ;
#94220=AXIS2_PLACEMENT_3D ( 'NONE', #29375, #108865, #250926 ) ;
#94226=VERTEX_POINT ( 'NONE', #250404 ) ;
#94253=CARTESIAN_POINT ( 'NONE',  ( 22.39999999999999503, 0.1000000000111554016, -27.25000000000000355 ) ) ;
#94260=CIRCLE ( 'NONE', #240016, 0.1000000000000016431 ) ;
#94306=AXIS2_PLACEMENT_3D ( 'NONE', #41293, #19125, #119530 ) ;
#94321=AXIS2_PLACEMENT_3D ( 'NONE', #117095, #17976, #97489 ) ;
#94334=FACE_OUTER_BOUND ( 'NONE', #169371, .T. ) ;
#94368=ORIENTED_EDGE ( 'NONE', *, *, #76909, .F. ) ;
#94386=CIRCLE ( 'NONE', #131812, 0.1000000000000008937 ) ;
#94439=DIRECTION ( 'NONE',  ( 1.000000000000000000, 3.265361837132813093E-16, -0.000000000000000000 ) ) ;
#94454=VECTOR ( 'NONE', #149777, 1000.000000000000000 ) ;
#94462=ORIENTED_EDGE ( 'NONE', *, *, #181868, .T. ) ;
#94467=CARTESIAN_POINT ( 'NONE',  ( 18.59999999999997655, 11.75000000001115552, -67.00000000000000000 ) ) ;
#94488=DIRECTION ( 'NONE',  ( 0.000000000000000000, 0.000000000000000000, -1.000000000000000000 ) ) ;
#94491=ORIENTED_EDGE ( 'NONE', *, *, #121761, .F. ) ;
#94495=CIRCLE ( 'NONE', #48715, 2.100000000000004530 ) ;
#94498=ORIENTED_EDGE ( 'NONE', *, *, #88848, .T. ) ;
#94550=ORIENTED_EDGE ( 'NONE', *, *, #25256, .T. ) ;
#94559=DIRECTION ( 'NONE',  ( 0.000000000000000000, 0.000000000000000000, -1.000000000000000000 ) ) ;
#94563=CARTESIAN_POINT ( 'NONE',  ( 21.05000000000000071, 1.349084418638171412, -41.48649896354548616 ) ) ;
#94572=CARTESIAN_POINT ( 'NONE',  ( 22.60000000000000142, 1.115600667400684642E-11, -33.50000000000000000 ) ) ;
#94603=VECTOR ( 'NONE', #54324, 1000.000000000000000 ) ;
#94641=CARTESIAN_POINT ( 'NONE',  ( 20.85000000000000142, 1.115600667400684642E-11, -67.00000000000000000 ) ) ;
#94683=CARTESIAN_POINT ( 'NONE',  ( -21.05000000000000071, -0.09999999998884338825, -26.95934304829875927 ) ) ;
#94684=ORIENTED_EDGE ( 'NONE', *, *, #239023, .T. ) ;
#94707=EDGE_CURVE ( 'NONE', #84436, #48144, #141378, .T. ) ;
#94734=DIRECTION ( 'NONE',  ( 0.7071067811865388020, -0.7071067811865561215, 0.000000000000000000 ) ) ;
#94739=CARTESIAN_POINT ( 'NONE',  ( 21.05000000000000071, -11.74999999998883560, -63.89999999999999858 ) ) ;
#94743=VECTOR ( 'NONE', #79488, 1000.000000000000000 ) ;
#94744=CARTESIAN_POINT ( 'NONE',  ( 18.42555734704283665, -9.497158361925555070, -40.53983049773493974 ) ) ;
#94761=CARTESIAN_POINT ( 'NONE',  ( 22.60000000000000142, 0.1008583691098682150, -21.75043287651061164 ) ) ;
#94789=DIRECTION ( 'NONE',  ( 0.000000000000000000, 0.000000000000000000, -1.000000000000000000 ) ) ;
#94809=( NAMED_UNIT ( * ) SI_UNIT ( $, .STERADIAN. ) SOLID_ANGLE_UNIT ( ) );
#94847=CYLINDRICAL_SURFACE ( 'NONE', #171108, 0.09999999999999781286 ) ;
#94870=CARTESIAN_POINT ( 'NONE',  ( -21.14999999999999858, 11.65000000001115588, -40.28386566297815108 ) ) ;
#94892=ORIENTED_EDGE ( 'NONE', *, *, #154429, .T. ) ;
#94904=DIRECTION ( 'NONE',  ( 1.000000000000000000, 0.000000000000000000, 0.000000000000000000 ) ) ;
#94915=ORIENTED_EDGE ( 'NONE', *, *, #243718, .F. ) ;
#94931=EDGE_CURVE ( 'NONE', #43099, #153815, #119759, .T. ) ;
#94932=EDGE_LOOP ( 'NONE', ( #233902, #224193, #172161, #58181 ) ) ;
#94934=DIRECTION ( 'NONE',  ( -1.000000000000000000, -0.000000000000000000, -0.000000000000000000 ) ) ;
#95011=AXIS2_PLACEMENT_3D ( 'NONE', #20890, #3863, #139508 ) ;
#95015=DIRECTION ( 'NONE',  ( 1.000000000000000000, 0.000000000000000000, 0.000000000000000000 ) ) ;
#95016=LINE ( 'NONE', #252799, #199208 ) ;
#95019=DIRECTION ( 'NONE',  ( -3.440080580676165868E-14, -0.1298341882520124002, -0.9915357197604841577 ) ) ;
#95032=AXIS2_PLACEMENT_3D ( 'NONE', #172543, #252017, #226003 ) ;
#95041=EDGE_CURVE ( 'NONE', #194903, #86704, #7695, .T. ) ;
#95054=ADVANCED_FACE ( 'NONE', ( #75979 ), #39457, .T. ) ;
#95064=CARTESIAN_POINT ( 'NONE',  ( 23.24999999999999645, 4.775700934590584090, -45.34876810404598046 ) ) ;
#95081=ORIENTED_EDGE ( 'NONE', *, *, #14692, .F. ) ;
#95089=EDGE_LOOP ( 'NONE', ( #42778, #12995, #95203, #147593 ) ) ;
#95105=CIRCLE ( 'NONE', #115767, 0.1000000000000028644 ) ;
#95143=VERTEX_POINT ( 'NONE', #194676 ) ;
#95151=AXIS2_PLACEMENT_3D ( 'NONE', #234526, #231990, #196678 ) ;
#95192=PLANE ( 'NONE',  #73856 ) ;
#95194=EDGE_CURVE ( 'NONE', #86723, #239491, #44562, .T. ) ;
#95197=PLANE ( 'NONE',  #105259 ) ;
#95203=ORIENTED_EDGE ( 'NONE', *, *, #213092, .F. ) ;
#95218=DIRECTION ( 'NONE',  ( -1.000000000000000000, -0.000000000000000000, -0.000000000000000000 ) ) ;
#95226=FACE_OUTER_BOUND ( 'NONE', #194900, .T. ) ;
#95245=ORIENTED_EDGE ( 'NONE', *, *, #174964, .F. ) ;
#95274=DIRECTION ( 'NONE',  ( -1.000000000000000000, 0.000000000000000000, 0.000000000000000000 ) ) ;
#95290=TOROIDAL_SURFACE ( 'NONE', #157697, 0.2000000000000000111, 0.1000000000000000056 ) ;
#95299=EDGE_CURVE ( 'NONE', #115264, #81578, #78401, .T. ) ;
#95306=CARTESIAN_POINT ( 'NONE',  ( 18.40916198585730967, -9.499999999988844479, -73.60018963182341167 ) ) ;
#95317=CARTESIAN_POINT ( 'NONE',  ( -18.59999999999999787, 11.65000000001115232, -45.65000000000000568 ) ) ;
#95334=VECTOR ( 'NONE', #147963, 1000.000000000000000 ) ;
#95339=VERTEX_POINT ( 'NONE', #73139 ) ;
#95348=AXIS2_PLACEMENT_3D ( 'NONE', #151162, #251522, #95015 ) ;
#95351=CIRCLE ( 'NONE', #170416, 0.6000000000000015321 ) ;
#95361=EDGE_LOOP ( 'NONE', ( #147760, #57430, #229502 ) ) ;
#95368=ORIENTED_EDGE ( 'NONE', *, *, #124275, .T. ) ;
#95371=DIRECTION ( 'NONE',  ( 0.000000000000000000, 1.000000000000000000, 0.000000000000000000 ) ) ;
#95377=CARTESIAN_POINT ( 'NONE',  ( 23.15000000000000213, -11.74999999998883560, -45.65000000000000568 ) ) ;
#95396=ORIENTED_EDGE ( 'NONE', *, *, #155086, .F. ) ;
#95412=EDGE_LOOP ( 'NONE', ( #78076, #84617, #22082, #109064, #242212, #20108, #50506, #54662, #193037, #26433, #166500 ) ) ;
#95428=DIRECTION ( 'NONE',  ( 1.000000000000000000, 0.000000000000000000, 0.000000000000000000 ) ) ;
#95436=ORIENTED_EDGE ( 'NONE', *, *, #107954, .T. ) ;
#95454=FACE_OUTER_BOUND ( 'NONE', #187787, .T. ) ;
#95476=CARTESIAN_POINT ( 'NONE',  ( -20.64999999999999858, -9.399999999988846611, -57.10603087734755690 ) ) ;
#95484=DIRECTION ( 'NONE',  ( -1.000000000000000000, 0.000000000000000000, 0.000000000000000000 ) ) ;
#95509=AXIS2_PLACEMENT_3D ( 'NONE', #21486, #17595, #136245 ) ;
#95522=CARTESIAN_POINT ( 'NONE',  ( -23.15000000000000213, 1.115651490242849210E-11, -29.35000000000000142 ) ) ;
#95529=ORIENTED_EDGE ( 'NONE', *, *, #180165, .T. ) ;
#95531=AXIS2_PLACEMENT_3D ( 'NONE', #251972, #70800, #73372 ) ;
#95571=DIRECTION ( 'NONE',  ( -1.000000000000000000, 0.000000000000000000, 0.000000000000000000 ) ) ;
#95620=CARTESIAN_POINT ( 'NONE',  ( 21.11833042828137508, 6.445644693866518615, -33.49289949094065122 ) ) ;
#95664=EDGE_CURVE ( 'NONE', #19166, #225834, #78591, .T. ) ;
#95688=VERTEX_POINT ( 'NONE', #202041 ) ;
#95720=ORIENTED_EDGE ( 'NONE', *, *, #50581, .F. ) ;
#95721=CYLINDRICAL_SURFACE ( 'NONE', #78164, 0.1000000000000000472 ) ;
#95760=FACE_OUTER_BOUND ( 'NONE', #72808, .T. ) ;
#95765=EDGE_CURVE ( 'NONE', #136260, #97145, #74550, .T. ) ;
#95817=VECTOR ( 'NONE', #211612, 1000.000000000000000 ) ;
#95819=DIRECTION ( 'NONE',  ( 0.000000000000000000, 0.000000000000000000, 1.000000000000000000 ) ) ;
#95822=CARTESIAN_POINT ( 'NONE',  ( -22.50000000000000000, 11.75000000001115552, -33.50000000000000000 ) ) ;
#95823=AXIS2_PLACEMENT_3D ( 'NONE', #186269, #50573, #247517 ) ;
#95830=DIRECTION ( 'NONE',  ( -1.000000000000000000, 0.000000000000000000, 6.938893903907270030E-14 ) ) ;
#95833=AXIS2_PLACEMENT_3D ( 'NONE', #160319, #101562, #39081 ) ;
#95857=EDGE_CURVE ( 'NONE', #189424, #72122, #28766, .T. ) ;
#95869=FACE_OUTER_BOUND ( 'NONE', #722, .T. ) ;
#95881=EDGE_CURVE ( 'NONE', #80895, #46326, #112124, .T. ) ;
#95888=ORIENTED_EDGE ( 'NONE', *, *, #199134, .F. ) ;
#95889=CARTESIAN_POINT ( 'NONE',  ( -23.25000000000000000, 2.000000000011154189, -53.77537807723790309 ) ) ;
#95916=AXIS2_PLACEMENT_3D ( 'NONE', #47938, #126193, #167933 ) ;
#95918=CARTESIAN_POINT ( 'NONE',  ( 20.86777300164945004, 10.33200063080771969, -72.59316749566428939 ) ) ;
#95921=VERTEX_POINT ( 'NONE', #174524 ) ;
#95933=ORIENTED_EDGE ( 'NONE', *, *, #10347, .T. ) ;
#95963=ORIENTED_EDGE ( 'NONE', *, *, #87734, .T. ) ;
#95968=FACE_OUTER_BOUND ( 'NONE', #25469, .T. ) ;
#96003=CARTESIAN_POINT ( 'NONE',  ( -18.46907102845853998, -9.473727364752948077, -73.67603473873651865 ) ) ;
#96008=CIRCLE ( 'NONE', #25327, 11.80000000000000426 ) ;
#96019=CARTESIAN_POINT ( 'NONE',  ( 18.39999999999999858, -9.499999999988842703, -40.53206939669966857 ) ) ;
#96083=ORIENTED_EDGE ( 'NONE', *, *, #254215, .F. ) ;
#96094=CARTESIAN_POINT ( 'NONE',  ( -18.50000000000000000, 7.021664781911246322, -70.83356540189728889 ) ) ;
#96106=AXIS2_PLACEMENT_3D ( 'NONE', #21895, #161420, #183539 ) ;
#96110=DIRECTION ( 'NONE',  ( 0.000000000000000000, 0.4930308989875230585, 0.8700118002898322711 ) ) ;
#96119=DIRECTION ( 'NONE',  ( 0.000000000000000000, 0.000000000000000000, -1.000000000000000000 ) ) ;
#96136=CARTESIAN_POINT ( 'NONE',  ( -23.15000000000000213, -11.39257802169451139, -63.92605042016806749 ) ) ;
#96141=CARTESIAN_POINT ( 'NONE',  ( 23.14999999999999503, 11.65000000001116298, -54.85000000000000142 ) ) ;
#96145=CYLINDRICAL_SURFACE ( 'NONE', #40730, 0.09999999999999939493 ) ;
#96184=LINE ( 'NONE', #253979, #102207 ) ;
#96193=CIRCLE ( 'NONE', #137691, 0.1000000000000008799 ) ;
#96201=TOROIDAL_SURFACE ( 'NONE', #254403, 11.65000000000000036, 0.1000000000000000056 ) ;
#96219=CARTESIAN_POINT ( 'NONE',  ( 23.24999999999999289, 6.650000000011155876, -45.65000000000000568 ) ) ;
#96227=DIRECTION ( 'NONE',  ( -0.7071067811865474617, -0.7071067811865474617, -0.000000000000000000 ) ) ;
#96228=CARTESIAN_POINT ( 'NONE',  ( -18.42554971533677488, -9.497159669426592288, -40.53982691354863022 ) ) ;
#96288=CARTESIAN_POINT ( 'NONE',  ( 20.85000000000000142, -1.851617760457748618, -78.60318971960367662 ) ) ;
#96289=ORIENTED_EDGE ( 'NONE', *, *, #94177, .T. ) ;
#96300=EDGE_LOOP ( 'NONE', ( #124478, #47109, #59067, #131713 ) ) ;
#96322=CARTESIAN_POINT ( 'NONE',  ( -21.05000000000000071, -1.835341550213255957, -45.15515129256298366 ) ) ;
#96326=ORIENTED_EDGE ( 'NONE', *, *, #137173, .F. ) ;
#96341=DIRECTION ( 'NONE',  ( -2.602085213965226419E-14, -0.000000000000000000, -1.000000000000000000 ) ) ;
#96354=DIRECTION ( 'NONE',  ( -1.000000000000000000, -2.952720810173289112E-16, 0.000000000000000000 ) ) ;
#96364=CIRCLE ( 'NONE', #13198, 0.1999999999999987899 ) ;
#96368=EDGE_CURVE ( 'NONE', #82065, #19295, #195547, .T. ) ;
#96370=DIRECTION ( 'NONE',  ( 1.000000000000000000, -0.000000000000000000, -0.000000000000000000 ) ) ;
#96400=CARTESIAN_POINT ( 'NONE',  ( -23.25000000000000000, 11.75000000001115552, -59.98519422934606382 ) ) ;
#96405=ORIENTED_EDGE ( 'NONE', *, *, #225220, .F. ) ;
#96419=DIRECTION ( 'NONE',  ( 1.000000000000000000, 2.952720810173289112E-16, -0.000000000000000000 ) ) ;
#96439=DIRECTION ( 'NONE',  ( -1.000000000000000000, 0.000000000000000000, 0.000000000000000000 ) ) ;
#96465=AXIS2_PLACEMENT_3D ( 'NONE', #196566, #119621, #117045 ) ;
#96540=CARTESIAN_POINT ( 'NONE',  ( -23.15000000000000213, -11.48912529306489994, -64.00000000000000000 ) ) ;
#96546=AXIS2_PLACEMENT_3D ( 'NONE', #172958, #111653, #110363 ) ;
#96550=AXIS2_PLACEMENT_3D ( 'NONE', #158536, #75153, #16458 ) ;
#96552=CARTESIAN_POINT ( 'NONE',  ( 21.14999999999999858, 0.09779029131994770863, -27.24218538952387547 ) ) ;
#96557=CARTESIAN_POINT ( 'NONE',  ( -21.05000000000000071, -11.48912529306490349, -36.39999999999999858 ) ) ;
#96562=CARTESIAN_POINT ( 'NONE',  ( 18.37172112093854892, -9.570961652231936512, -73.81673445348330631 ) ) ;
#96595=CARTESIAN_POINT ( 'NONE',  ( 20.04142135623730070, 11.65000000001115943, -54.85000000000000142 ) ) ;
#96627=CARTESIAN_POINT ( 'NONE',  ( 23.14999999999999503, 6.450000000011156587, -21.75000000000000355 ) ) ;
#96628=VERTEX_POINT ( 'NONE', #243844 ) ;
#96659=ORIENTED_EDGE ( 'NONE', *, *, #131464, .F. ) ;
#96675=CARTESIAN_POINT ( 'NONE',  ( -20.54999999999999716, -8.999999999988844479, -57.10603087734755690 ) ) ;
#96699=CARTESIAN_POINT ( 'NONE',  ( 18.45139536634708222, -9.486081720270041373, -73.64051161781067378 ) ) ;
#96701=ORIENTED_EDGE ( 'NONE', *, *, #235673, .F. ) ;
#96705=VERTEX_POINT ( 'NONE', #26103 ) ;
#96715=EDGE_LOOP ( 'NONE', ( #126908, #9691, #191567, #224014 ) ) ;
#96718=DIRECTION ( 'NONE',  ( 0.7071067811865475727, 0.7071067811865475727, -0.000000000000000000 ) ) ;
#96720=DIRECTION ( 'NONE',  ( 0.000000000000000000, -1.265107689135680095E-16, 1.000000000000000000 ) ) ;
#96724=CARTESIAN_POINT ( 'NONE',  ( 21.13614978966381841, 1.115600741516067204E-11, -27.00089529816621337 ) ) ;
#96744=LINE ( 'NONE', #253269, #84590 ) ;
#96746=DIRECTION ( 'NONE',  ( -1.000000000000000000, -3.265361837132813093E-16, 0.000000000000000000 ) ) ;
#96755=LINE ( 'NONE', #135892, #95817 ) ;
#96775=LINE ( 'NONE', #16017, #99379 ) ;
#96780=CARTESIAN_POINT ( 'NONE',  ( -20.54999999999999716, 2.000000000011154189, -53.77537807723790309 ) ) ;
#96783=CARTESIAN_POINT ( 'NONE',  ( 20.94999999999999929, 1.115600667400684642E-11, -67.00000000000000000 ) ) ;
#96788=DIRECTION ( 'NONE',  ( 0.000000000000000000, 0.000000000000000000, -1.000000000000000000 ) ) ;
#96815=VERTEX_POINT ( 'NONE', #233298 ) ;
#96832=DIRECTION ( 'NONE',  ( -1.000000000000000000, -0.000000000000000000, -0.000000000000000000 ) ) ;
#96840=CIRCLE ( 'NONE', #105190, 0.1000000000000028644 ) ;
#96863=CARTESIAN_POINT ( 'NONE',  ( -22.57848426163147693, -0.004264329271961149644, -21.74994169310966541 ) ) ;
#96879=CIRCLE ( 'NONE', #17783, 11.74999999999999645 ) ;
#96881=FACE_OUTER_BOUND ( 'NONE', #221194, .T. ) ;
#96908=DIRECTION ( 'NONE',  ( 0.000000000000000000, -3.729655473350132098E-14, -1.000000000000000000 ) ) ;
#96913=ORIENTED_EDGE ( 'NONE', *, *, #133041, .F. ) ;
#96918=AXIS2_PLACEMENT_3D ( 'NONE', #180915, #2250, #947 ) ;
#96922=VERTEX_POINT ( 'NONE', #257912 ) ;
#96930=CARTESIAN_POINT ( 'NONE',  ( 23.14999999999999858, -1.999999999988846699, -67.00000000000000000 ) ) ;
#96950=ORIENTED_EDGE ( 'NONE', *, *, #216588, .T. ) ;
#96970=VECTOR ( 'NONE', #104802, 1000.000000000000000 ) ;
#96998=DIRECTION ( 'NONE',  ( 0.000000000000000000, 0.000000000000000000, -1.000000000000000000 ) ) ;
#97002=AXIS2_PLACEMENT_3D ( 'NONE', #246890, #223472, #224754 ) ;
#97004=CIRCLE ( 'NONE', #201110, 0.1999999999999987899 ) ;
#97068=TOROIDAL_SURFACE ( 'NONE', #151314, 0.2000000000000000111, 0.1000000000000000056 ) ;
#97082=DIRECTION ( 'NONE',  ( -0.000000000000000000, 0.000000000000000000, -1.000000000000000000 ) ) ;
#97124=LINE ( 'NONE', #77578, #223996 ) ;
#97145=VERTEX_POINT ( 'NONE', #133860 ) ;
#97147=ORIENTED_EDGE ( 'NONE', *, *, #15764, .F. ) ;
#97148=VECTOR ( 'NONE', #59340, 1000.000000000000000 ) ;
#97214=CIRCLE ( 'NONE', #172342, 0.1000000000000028644 ) ;
#97251=AXIS2_PLACEMENT_3D ( 'NONE', #109163, #71360, #230413 ) ;
#97300=EDGE_CURVE ( 'NONE', #143470, #147289, #62991, .T. ) ;
#97308=CARTESIAN_POINT ( 'NONE',  ( 20.94999999999999929, 1.115600667400684642E-11, -46.37500000000000000 ) ) ;
#97323=EDGE_CURVE ( 'NONE', #117767, #42156, #42564, .T. ) ;
#97339=CARTESIAN_POINT ( 'NONE',  ( -20.54999999999999716, -9.399999999988846611, -57.10603087734755690 ) ) ;
#97374=ORIENTED_EDGE ( 'NONE', *, *, #189177, .T. ) ;
#97391=EDGE_CURVE ( 'NONE', #24660, #149548, #10733, .T. ) ;
#97422=CARTESIAN_POINT ( 'NONE',  ( -18.50000000000000000, -9.399999999988850163, -73.88204184817267617 ) ) ;
#97426=DIRECTION ( 'NONE',  ( 0.000000000000000000, 0.000000000000000000, 1.000000000000000000 ) ) ;
#97489=DIRECTION ( 'NONE',  ( 0.000000000000000000, 0.000000000000000000, 1.000000000000000000 ) ) ;
#97498=DIRECTION ( 'NONE',  ( 0.000000000000000000, 0.9908441862701600211, -0.1350103645451876666 ) ) ;
#97510=AXIS2_PLACEMENT_3D ( 'NONE', #90757, #89475, #69951 ) ;
#97522=DIRECTION ( 'NONE',  ( -1.000000000000000000, -0.000000000000000000, -0.000000000000000000 ) ) ;
#97525=ADVANCED_FACE ( 'NONE', ( #237481 ), #35464, .T. ) ;
#97553=ORIENTED_EDGE ( 'NONE', *, *, #200758, .F. ) ;
#97574=CARTESIAN_POINT ( 'NONE',  ( -21.65000000000000213, 7.708578643773852157, -54.75000000000000000 ) ) ;
#97588=TOROIDAL_SURFACE ( 'NONE', #6031, 0.2000000000000000111, 0.1000000000000000056 ) ;
#97594=CARTESIAN_POINT ( 'NONE',  ( -20.54999999999999716, 7.250000000011155521, -45.75000000000000000 ) ) ;
#97603=CARTESIAN_POINT ( 'NONE',  ( -23.15000000000000213, -9.599999999988844124, -21.75000000000000711 ) ) ;
#97670=ORIENTED_EDGE ( 'NONE', *, *, #76886, .F. ) ;
#97671=CARTESIAN_POINT ( 'NONE',  ( 18.49999999999999289, 6.450000000011156587, -43.51702717044002355 ) ) ;
#97682=ORIENTED_EDGE ( 'NONE', *, *, #89715, .T. ) ;
#97687=CIRCLE ( 'NONE', #31683, 0.1000000000000001860 ) ;
#97692=FACE_OUTER_BOUND ( 'NONE', #29687, .T. ) ;
#97710=AXIS2_PLACEMENT_3D ( 'NONE', #191186, #231580, #193733 ) ;
#97720=CARTESIAN_POINT ( 'NONE',  ( 22.49436431346199683, 0.06690352973341695542, -21.85004905234654515 ) ) ;
#97735=CARTESIAN_POINT ( 'NONE',  ( -18.59999999999999787, 11.65000000001115232, -67.00000000000000000 ) ) ;
#97790=ORIENTED_EDGE ( 'NONE', *, *, #51428, .T. ) ;
#97825=EDGE_CURVE ( 'NONE', #189010, #137157, #142684, .T. ) ;
#97838=CARTESIAN_POINT ( 'NONE',  ( -21.08078803292166725, 0.07918598716886203481, -27.16698703556286176 ) ) ;
#97843=CARTESIAN_POINT ( 'NONE',  ( -21.70464131381649509, 7.095358018979010417, -33.50000000000000000 ) ) ;
#97849=CARTESIAN_POINT ( 'NONE',  ( -18.59999999999999787, 1.115600667400684642E-11, -67.00000000000000000 ) ) ;
#97862=ORIENTED_EDGE ( 'NONE', *, *, #166935, .F. ) ;
#97904=ORIENTED_EDGE ( 'NONE', *, *, #10738, .F. ) ;
#97916=AXIS2_PLACEMENT_3D ( 'NONE', #56545, #137386, #216922 ) ;
#98040=CARTESIAN_POINT ( 'NONE',  ( 21.14999999999999503, 1.115600667400684642E-11, -33.50000000000000000 ) ) ;
#98050=ORIENTED_EDGE ( 'NONE', *, *, #48403, .F. ) ;
#98054=DIRECTION ( 'NONE',  ( -0.000000000000000000, 1.000000000000000000, -1.224646799147352961E-16 ) ) ;
#98066=CIRCLE ( 'NONE', #44125, 0.1000000000000028644 ) ;
#98069=CARTESIAN_POINT ( 'NONE',  ( 20.94999999999999929, 1.115600667400684642E-11, -46.47500000000000142 ) ) ;
#98093=CIRCLE ( 'NONE', #94018, 0.09999999999999939493 ) ;
#98096=ORIENTED_EDGE ( 'NONE', *, *, #142096, .T. ) ;
#98115=AXIS2_PLACEMENT_3D ( 'NONE', #224459, #227029, #92331 ) ;
#98118=CYLINDRICAL_SURFACE ( 'NONE', #208211, 0.09999999999999939493 ) ;
#98136=EDGE_CURVE ( 'NONE', #200635, #43175, #213612, .T. ) ;
#98158=EDGE_CURVE ( 'NONE', #16250, #19295, #234455, .T. ) ;
#98159=FACE_OUTER_BOUND ( 'NONE', #122038, .T. ) ;
#98183=ORIENTED_EDGE ( 'NONE', *, *, #222469, .F. ) ;
#98212=ORIENTED_EDGE ( 'NONE', *, *, #67170, .T. ) ;
#98222=CARTESIAN_POINT ( 'NONE',  ( -21.64999999999999858, 7.350000000011155166, -45.75000000000000000 ) ) ;
#98223=EDGE_CURVE ( 'NONE', #143764, #101718, #68810, .T. ) ;
#98229=EDGE_LOOP ( 'NONE', ( #219412, #105593, #59524, #67784 ) ) ;
#98236=TOROIDAL_SURFACE ( 'NONE', #85770, 3.899999999999999467, 0.1000000000000000056 ) ;
#98246=DIRECTION ( 'NONE',  ( -1.000000000000000000, -0.000000000000000000, -0.000000000000000000 ) ) ;
#98255=LINE ( 'NONE', #20065, #67808 ) ;
#98292=ADVANCED_FACE ( 'NONE', ( #90918 ), #171784, .T. ) ;
#98339=ORIENTED_EDGE ( 'NONE', *, *, #18866, .T. ) ;
#98347=DIRECTION ( 'NONE',  ( 0.000000000000000000, 0.000000000000000000, -1.000000000000000000 ) ) ;
#98355=DIRECTION ( 'NONE',  ( 0.000000000000000000, 0.000000000000000000, 1.000000000000000000 ) ) ;
#98359=CYLINDRICAL_SURFACE ( 'NONE', #225298, 0.09999999999999939493 ) ;
#98378=ORIENTED_EDGE ( 'NONE', *, *, #170118, .F. ) ;
#98436=CARTESIAN_POINT ( 'NONE',  ( 21.04105312098505465, 8.875332623054768888, -45.82850674721203177 ) ) ;
#98454=CARTESIAN_POINT ( 'NONE',  ( 20.88420186297724257, 10.33025634372637391, -72.58709292826388548 ) ) ;
#98457=CARTESIAN_POINT ( 'NONE',  ( -20.85000000000000142, -1.835859311432481045, -78.50443916879852679 ) ) ;
#98526=DIRECTION ( 'NONE',  ( 2.952720810173289112E-16, -1.000000000000000000, 0.000000000000000000 ) ) ;
#98544=CARTESIAN_POINT ( 'NONE',  ( 18.59999999999999076, 10.20857864377385127, -54.85000000000000142 ) ) ;
#98550=CARTESIAN_POINT ( 'NONE',  ( 20.95483826173899899, 8.876166204781142710, -42.04627555289950891 ) ) ;
#98583=EDGE_CURVE ( 'NONE', #196889, #27581, #21306, .T. ) ;
#98587=CARTESIAN_POINT ( 'NONE',  ( -20.64999999999999858, -8.999999999988846255, -43.39396912265245021 ) ) ;
#98591=ORIENTED_EDGE ( 'NONE', *, *, #187753, .F. ) ;
#98596=ORIENTED_EDGE ( 'NONE', *, *, #212524, .F. ) ;
#98606=ORIENTED_EDGE ( 'NONE', *, *, #192494, .F. ) ;
#98619=LINE ( 'NONE', #135204, #215123 ) ;
#98620=AXIS2_PLACEMENT_3D ( 'NONE', #78212, #18252, #234731 ) ;
#98623=TOROIDAL_SURFACE ( 'NONE', #86170, 0.9750000000000019762, 0.1000000000000000056 ) ;
#98648=AXIS2_PLACEMENT_3D ( 'NONE', #22336, #100521, #121442 ) ;
#98666=EDGE_LOOP ( 'NONE', ( #189523, #177513, #236430, #4640 ) ) ;
#98687=DIRECTION ( 'NONE',  ( -1.000000000000000000, -3.265361837132813093E-16, 0.000000000000000000 ) ) ;
#98694=FACE_OUTER_BOUND ( 'NONE', #183198, .T. ) ;
#98704=ORIENTED_EDGE ( 'NONE', *, *, #166601, .T. ) ;
#98735=DIRECTION ( 'NONE',  ( 1.000000000000000000, 7.304098846218134667E-16, -0.000000000000000000 ) ) ;
#98750=FACE_OUTER_BOUND ( 'NONE', #61216, .T. ) ;
#98812=AXIS2_PLACEMENT_3D ( 'NONE', #68954, #209730, #225414 ) ;
#98863=AXIS2_PLACEMENT_3D ( 'NONE', #140941, #79650, #68776 ) ;
#98970=ORIENTED_EDGE ( 'NONE', *, *, #38472, .F. ) ;
#98976=CARTESIAN_POINT ( 'NONE',  ( 20.95512820512820440, 10.62384868372303615, -41.16491356908760935 ) ) ;
#98981=CARTESIAN_POINT ( 'NONE',  ( 20.46382478191414833, 8.901379558713770734, -42.04572809488309559 ) ) ;
#98993=CARTESIAN_POINT ( 'NONE',  ( 20.95545211741311320, 10.58641331155510024, -41.08614685958829682 ) ) ;
#98997=CARTESIAN_POINT ( 'NONE',  ( 22.39999999999999503, 11.75000000001115552, -33.50000000000000000 ) ) ;
#99005=CARTESIAN_POINT ( 'NONE',  ( 22.47110162079220785, 0.02879741281384913185, -21.85006406331566708 ) ) ;
#99013=LINE ( 'NONE', #258071, #183268 ) ;
#99014=CIRCLE ( 'NONE', #228239, 0.09999999999999939493 ) ;
#99024=SHAPE_DEFINITION_REPRESENTATION ( #230574, #45219 ) ;
#99039=CARTESIAN_POINT ( 'NONE',  ( 23.14999999999999503, 6.550000000011156231, -45.85000000000000142 ) ) ;
#99058=TOROIDAL_SURFACE ( 'NONE', #70065, 0.2000000000000000111, 0.1000000000000000056 ) ;
#99079=EDGE_CURVE ( 'NONE', #94226, #139128, #29864, .T. ) ;
#99112=AXIS2_PLACEMENT_3D ( 'NONE', #185351, #169684, #150099 ) ;
#99123=VERTEX_POINT ( 'NONE', #97671 ) ;
#99136=ORIENTED_EDGE ( 'NONE', *, *, #3805, .T. ) ;
#99153=CARTESIAN_POINT ( 'NONE',  ( 23.14999999999999503, 14.05000000001115623, -61.48630492923908974 ) ) ;
#99166=DIRECTION ( 'NONE',  ( 0.000000000000000000, -0.000000000000000000, 1.000000000000000000 ) ) ;
#99177=EDGE_LOOP ( 'NONE', ( #29658, #98212, #191996, #68042 ) ) ;
#99205=CARTESIAN_POINT ( 'NONE',  ( -23.15000000000000213, -8.999999999988846255, -42.89396912265245021 ) ) ;
#99213=EDGE_LOOP ( 'NONE', ( #174723, #43882, #122289, #18276 ) ) ;
#99216=EDGE_CURVE ( 'NONE', #105461, #88007, #100709, .T. ) ;
#99219=ORIENTED_EDGE ( 'NONE', *, *, #226906, .T. ) ;
#99233=EDGE_CURVE ( 'NONE', #200509, #208600, #235154, .T. ) ;
#99252=ORIENTED_EDGE ( 'NONE', *, *, #166485, .F. ) ;
#99270=ORIENTED_EDGE ( 'NONE', *, *, #244258, .T. ) ;
#99299=CARTESIAN_POINT ( 'NONE',  ( -23.25000000000000000, -1.736705739456431807, -78.51742258762372728 ) ) ;
#99314=DIRECTION ( 'NONE',  ( 0.000000000000000000, 0.000000000000000000, -1.000000000000000000 ) ) ;
#99319=DIRECTION ( 'NONE',  ( 1.000000000000000000, 0.000000000000000000, 0.000000000000000000 ) ) ;
#99344=EDGE_CURVE ( 'NONE', #81117, #46286, #229378, .T. ) ;
#99371=CARTESIAN_POINT ( 'NONE',  ( -18.59999999999999787, 11.75000000001115197, -45.65000000000000568 ) ) ;
#99379=VECTOR ( 'NONE', #35584, 1000.000000000000000 ) ;
#99413=EDGE_CURVE ( 'NONE', #55352, #17420, #241829, .T. ) ;
#99423=ORIENTED_EDGE ( 'NONE', *, *, #239190, .F. ) ;
#99434=EDGE_CURVE ( 'NONE', #19295, #40550, #56942, .T. ) ;
#99460=ORIENTED_EDGE ( 'NONE', *, *, #144972, .T. ) ;
#99478=AXIS2_PLACEMENT_3D ( 'NONE', #1518, #202305, #242701 ) ;
#99501=DIRECTION ( 'NONE',  ( 0.000000000000000000, 0.000000000000000000, -1.000000000000000000 ) ) ;
#99516=AXIS2_PLACEMENT_3D ( 'NONE', #255367, #80612, #76783 ) ;
#99524=CIRCLE ( 'NONE', #228749, 0.09999999999999939493 ) ;
#99539=DIRECTION ( 'NONE',  ( 1.000000000000000000, 0.000000000000000000, 0.000000000000000000 ) ) ;
#99559=DIRECTION ( 'NONE',  ( 0.000000000000000000, 0.000000000000000000, -1.000000000000000000 ) ) ;
#99580=AXIS2_PLACEMENT_3D ( 'NONE', #83285, #19505, #221517 ) ;
#99619=DIRECTION ( 'NONE',  ( 1.000000000000000000, -7.304098846218134667E-16, 0.000000000000000000 ) ) ;
#99622=ORIENTED_EDGE ( 'NONE', *, *, #92716, .T. ) ;
#99632=DIRECTION ( 'NONE',  ( 1.000000000000000000, 0.000000000000000000, 0.000000000000000000 ) ) ;
#99650=DIRECTION ( 'NONE',  ( -4.336808689941752679E-15, 0.8660254037844482555, 0.4999999999999837907 ) ) ;
#99673=DIRECTION ( 'NONE',  ( 0.000000000000000000, 0.000000000000000000, 1.000000000000000000 ) ) ;
#99718=CIRCLE ( 'NONE', #216450, 0.5000000000000004441 ) ;
#99744=CARTESIAN_POINT ( 'NONE',  ( 21.05000000000000071, -8.999999999988842703, -57.10603087734755690 ) ) ;
#99745=LINE ( 'NONE', #116763, #41675 ) ;
#99746=ORIENTED_EDGE ( 'NONE', *, *, #74716, .T. ) ;
#99785=DIRECTION ( 'NONE',  ( 0.000000000000000000, 1.000000000000000000, 0.000000000000000000 ) ) ;
#99791=CARTESIAN_POINT ( 'NONE',  ( 18.59999999999999787, -9.399999999988843058, -73.88204184817267617 ) ) ;
#99808=CIRCLE ( 'NONE', #208196, 0.1000000000000000472 ) ;
#99814=B_SPLINE_CURVE_WITH_KNOTS ( 'NONE', 3,
 ( #150281, #248076, #69463, #51134, #149001, #169877, #70758, #15922 ),
 .UNSPECIFIED., .F., .F.,
 ( 4, 2, 2, 4 ),
 ( 0.000000000000000000, 9.550056980124990193E-05, 0.0001910011396024998039, 0.0003820022792049996077 ),
 .UNSPECIFIED. ) ;
#99825=ORIENTED_EDGE ( 'NONE', *, *, #70934, .T. ) ;
#99832=VECTOR ( 'NONE', #8344, 1000.000000000000000 ) ;
#99836=ORIENTED_EDGE ( 'NONE', *, *, #257107, .F. ) ;
#99884=CARTESIAN_POINT ( 'NONE',  ( 23.14999999999999858, 5.000000000011153745, -54.59473398108690390 ) ) ;
#99889=CARTESIAN_POINT ( 'NONE',  ( 21.05000000000000071, 11.60000000001116049, -60.07179676972450011 ) ) ;
#99894=TOROIDAL_SURFACE ( 'NONE', #129174, 0.4000000000000012990, 0.1000000000000000056 ) ;
#99905=( GEOMETRIC_REPRESENTATION_CONTEXT ( 3 ) GLOBAL_UNCERTAINTY_ASSIGNED_CONTEXT ( ( #248576 ) ) GLOBAL_UNIT_ASSIGNED_CONTEXT ( ( #120538, #241739, #100897 ) ) REPRESENTATION_CONTEXT ( 'NONE', 'WORKASPACE' ) );
#100016=AXIS2_PLACEMENT_3D ( 'NONE', #77175, #112473, #32970 ) ;
#100020=DIRECTION ( 'NONE',  ( 0.000000000000000000, 0.000000000000000000, -1.000000000000000000 ) ) ;
#100038=CARTESIAN_POINT ( 'NONE',  ( -23.15000000000000213, 2.500000000011156409, -46.72462192276210402 ) ) ;
#100083=VERTEX_POINT ( 'NONE', #197454 ) ;
#100084=CARTESIAN_POINT ( 'NONE',  ( 21.05000000000011795, -0.01759718699745431436, -27.05922910633797684 ) ) ;
#100096=VECTOR ( 'NONE', #22165, 1000.000000000000000 ) ;
#100132=LINE ( 'NONE', #143119, #14383 ) ;
#100136=DIRECTION ( 'NONE',  ( 0.000000000000000000, 1.000000000000000000, -6.308085367188393199E-16 ) ) ;
#100163=DIRECTION ( 'NONE',  ( 0.000000000000000000, 0.000000000000000000, -1.000000000000000000 ) ) ;
#100164=DIRECTION ( 'NONE',  ( 0.000000000000000000, 8.673617379884087537E-15, -1.000000000000000000 ) ) ;
#100173=DIRECTION ( 'NONE',  ( 0.000000000000000000, 0.000000000000000000, -1.000000000000000000 ) ) ;
#100208=ORIENTED_EDGE ( 'NONE', *, *, #256977, .F. ) ;
#100218=EDGE_LOOP ( 'NONE', ( #131363, #208909, #127302, #173076 ) ) ;
#100233=ORIENTED_EDGE ( 'NONE', *, *, #160241, .T. ) ;
#100260=DIRECTION ( 'NONE',  ( 1.000000000000000000, 0.000000000000000000, 0.000000000000000000 ) ) ;
#100262=EDGE_LOOP ( 'NONE', ( #252881, #235194, #117222 ) ) ;
#100283=CARTESIAN_POINT ( 'NONE',  ( 20.95566103547454517, 10.61824765095822087, -41.13184019298059013 ) ) ;
#100324=AXIS2_PLACEMENT_3D ( 'NONE', #40223, #115888, #195445 ) ;
#100344=ADVANCED_FACE ( 'NONE', ( #52216 ), #131765, .F. ) ;
#100353=CARTESIAN_POINT ( 'NONE',  ( -20.94999999999999929, 1.261786168576181755, -41.58649896354548048 ) ) ;
#100378=CARTESIAN_POINT ( 'NONE',  ( -18.50000000000000000, 10.29270135741298375, -72.45736188715194714 ) ) ;
#100386=DIRECTION ( 'NONE',  ( 0.000000000000000000, 0.000000000000000000, -1.000000000000000000 ) ) ;
#100399=ORIENTED_EDGE ( 'NONE', *, *, #151668, .T. ) ;
#100405=CARTESIAN_POINT ( 'NONE',  ( -23.15000000000000213, 2.600000000011154278, -53.77537807723790309 ) ) ;
#100413=CARTESIAN_POINT ( 'NONE',  ( 22.39999999999999858, 0.1000000000111554016, -25.70922040162662014 ) ) ;
#100467=ORIENTED_EDGE ( 'NONE', *, *, #173309, .T. ) ;
#100505=VERTEX_POINT ( 'NONE', #133065 ) ;
#100512=EDGE_LOOP ( 'NONE', ( #109611, #229725, #40235, #154232 ) ) ;
#100521=DIRECTION ( 'NONE',  ( -1.000000000000000000, 0.000000000000000000, 0.000000000000000000 ) ) ;
#100565=SPHERICAL_SURFACE ( 'NONE', #71446, 0.1000000000000000056 ) ;
#100576=ADVANCED_FACE ( 'NONE', ( #182468 ), #138166, .F. ) ;
#100584=CIRCLE ( 'NONE', #154631, 0.1000000000000028644 ) ;
#100598=DIRECTION ( 'NONE',  ( -2.915501640297154283E-16, 1.000000000000000000, 0.000000000000000000 ) ) ;
#100607=CARTESIAN_POINT ( 'NONE',  ( -20.94999999999999929, -0.2561057920810652089, -33.46510355832771211 ) ) ;
#100637=DIRECTION ( 'NONE',  ( 1.000000000000000000, -0.000000000000000000, -0.000000000000000000 ) ) ;
#100641=EDGE_CURVE ( 'NONE', #165624, #138330, #183738, .T. ) ;
#100646=FACE_OUTER_BOUND ( 'NONE', #186540, .T. ) ;
#100665=DIRECTION ( 'NONE',  ( -1.836970198721029934E-16, 1.000000000000000000, 0.000000000000000000 ) ) ;
#100674=AXIS2_PLACEMENT_3D ( 'NONE', #50198, #56303, #36797 ) ;
#100709=CIRCLE ( 'NONE', #167417, 4.049999999999998046 ) ;
#100711=EDGE_LOOP ( 'NONE', ( #82622, #128790, #10845, #137373 ) ) ;
#100716=EDGE_CURVE ( 'NONE', #225961, #235379, #15057, .T. ) ;
#100728=B_SPLINE_CURVE_WITH_KNOTS ( 'NONE', 3,
 ( #51987, #209806, #31209, #54567, #111999, #114553, #50694 ),
 .UNSPECIFIED., .F., .F.,
 ( 4, 3, 4 ),
 ( 0.000000000000000000, 3.357501770814503222E-05, 5.199112466349739759E-05 ),
 .UNSPECIFIED. ) ;
#100731=ORIENTED_EDGE ( 'NONE', *, *, #233999, .T. ) ;
#100761=VERTEX_POINT ( 'NONE', #55410 ) ;
#100798=VECTOR ( 'NONE', #124065, 1000.000000000000000 ) ;
#100799=VERTEX_POINT ( 'NONE', #219644 ) ;
#100817=FACE_OUTER_BOUND ( 'NONE', #163644, .T. ) ;
#100824=CIRCLE ( 'NONE', #142384, 0.1000000000000028644 ) ;
#100844=DIRECTION ( 'NONE',  ( 1.000000000000000000, 0.000000000000000000, -0.000000000000000000 ) ) ;
#100869=CARTESIAN_POINT ( 'NONE',  ( -20.85000000000000142, -11.64999999998884483, -67.00000000000000000 ) ) ;
#100880=VECTOR ( 'NONE', #213941, 1000.000000000000000 ) ;
#100882=CARTESIAN_POINT ( 'NONE',  ( -20.64999999999999858, 1.925233644870972816, -46.23024353312612789 ) ) ;
#100897=( NAMED_UNIT ( * ) SI_UNIT ( $, .STERADIAN. ) SOLID_ANGLE_UNIT ( ) );
#100908=CARTESIAN_POINT ( 'NONE',  ( -22.50047199487802629, 0.04490605193094060477, -21.74995258108075902 ) ) ;
#100924=CARTESIAN_POINT ( 'NONE',  ( 20.94999999999999574, -11.39257802169451672, -36.57394957983193251 ) ) ;
#100933=DIRECTION ( 'NONE',  ( 0.000000000000000000, 1.000000000000000000, 0.000000000000000000 ) ) ;
#100962=VERTEX_POINT ( 'NONE', #70893 ) ;
#100986=DIRECTION ( 'NONE',  ( 0.000000000000000000, 2.664535259100343354E-15, -1.000000000000000000 ) ) ;
#100992=DIRECTION ( 'NONE',  ( 0.000000000000000000, -0.000000000000000000, 1.000000000000000000 ) ) ;
#101001=CARTESIAN_POINT ( 'NONE',  ( -22.57320508075687115, 11.65000000001115588, -33.50000000000002842 ) ) ;
#101002=CARTESIAN_POINT ( 'NONE',  ( 21.06086055315970285, 8.774707514967413857, -45.70232215515390806 ) ) ;
#101009=CARTESIAN_POINT ( 'NONE',  ( -20.94999999999999929, 1.115600667400684642E-11, -67.00000000000000000 ) ) ;
#101040=LINE ( 'NONE', #41154, #8891 ) ;
#101049=FACE_OUTER_BOUND ( 'NONE', #141137, .T. ) ;
#101104=DIRECTION ( 'NONE',  ( 1.000000000000000000, -0.000000000000000000, -0.000000000000000000 ) ) ;
#101210=ORIENTED_EDGE ( 'NONE', *, *, #146126, .F. ) ;
#101215=DIRECTION ( 'NONE',  ( -1.000000000000000000, 0.000000000000000000, 0.000000000000000000 ) ) ;
#101228=DIRECTION ( 'NONE',  ( 0.000000000000000000, 0.000000000000000000, -1.000000000000000000 ) ) ;
#101230=EDGE_LOOP ( 'NONE', ( #68059, #131968, #119575, #79244 ) ) ;
#101257=AXIS2_PLACEMENT_3D ( 'NONE', #22595, #83788, #60409 ) ;
#101276=CARTESIAN_POINT ( 'NONE',  ( -23.15000000000000213, 11.65000000001115588, -59.98519422934606382 ) ) ;
#101279=ADVANCED_FACE ( 'NONE', ( #184076 ), #213702, .F. ) ;
#101303=ORIENTED_EDGE ( 'NONE', *, *, #42824, .F. ) ;
#101317=CARTESIAN_POINT ( 'NONE',  ( -18.40000000000000568, -9.499999999988851584, -40.49936209718013203 ) ) ;
#101336=EDGE_LOOP ( 'NONE', ( #93842, #84629, #86177, #180458 ) ) ;
#101340=CARTESIAN_POINT ( 'NONE',  ( 21.05000000000000426, 0.09843750001147442974, -27.20076908990770903 ) ) ;
#101367=VECTOR ( 'NONE', #104915, 1000.000000000000000 ) ;
#101369=AXIS2_PLACEMENT_3D ( 'NONE', #70071, #32225, #50450 ) ;
#101378=ORIENTED_EDGE ( 'NONE', *, *, #20813, .T. ) ;
#101399=CARTESIAN_POINT ( 'NONE',  ( -18.59999999999999787, 1.115600667400684642E-11, -67.00000000000000000 ) ) ;
#101416=ORIENTED_EDGE ( 'NONE', *, *, #49365, .F. ) ;
#101427=DIRECTION ( 'NONE',  ( 0.000000000000000000, 0.000000000000000000, 1.000000000000000000 ) ) ;
#101433=DIRECTION ( 'NONE',  ( 0.000000000000000000, 0.000000000000000000, -1.000000000000000000 ) ) ;
#101436=ORIENTED_EDGE ( 'NONE', *, *, #94931, .T. ) ;
#101446=DIRECTION ( 'NONE',  ( 1.000000000000000000, 0.000000000000000000, 0.000000000000000000 ) ) ;
#101452=ORIENTED_EDGE ( 'NONE', *, *, #75517, .F. ) ;
#101473=VERTEX_POINT ( 'NONE', #228351 ) ;
#101474=CARTESIAN_POINT ( 'NONE',  ( 21.13461538461538325, 10.61458296203669427, -45.74999999999999289 ) ) ;
#101493=CARTESIAN_POINT ( 'NONE',  ( -20.94999999999999929, 1.115600667400684642E-11, -67.00000000000000000 ) ) ;
#101526=CARTESIAN_POINT ( 'NONE',  ( 18.59999999999997655, 1.115600667400684642E-11, -74.90000000000000568 ) ) ;
#101533=AXIS2_PLACEMENT_3D ( 'NONE', #252809, #195441, #14235 ) ;
#101539=EDGE_CURVE ( 'NONE', #138653, #100083, #217967, .T. ) ;
#101554=AXIS2_PLACEMENT_3D ( 'NONE', #173039, #36064, #252514 ) ;
#101562=DIRECTION ( 'NONE',  ( 0.000000000000000000, 0.000000000000000000, -1.000000000000000000 ) ) ;
#101590=ORIENTED_EDGE ( 'NONE', *, *, #208045, .T. ) ;
#101600=FACE_OUTER_BOUND ( 'NONE', #218769, .T. ) ;
#101611=DIRECTION ( 'NONE',  ( -1.000000000000000000, 0.000000000000000000, 0.000000000000000000 ) ) ;
#101632=EDGE_CURVE ( 'NONE', #109631, #147068, #193802, .T. ) ;
#101640=AXIS2_PLACEMENT_3D ( 'NONE', #159930, #60790, #41277 ) ;
#101667=CARTESIAN_POINT ( 'NONE',  ( 22.39999999999999503, 0.1000000000111554016, -25.70922040162662014 ) ) ;
#101671=ORIENTED_EDGE ( 'NONE', *, *, #170730, .F. ) ;
#101676=ORIENTED_EDGE ( 'NONE', *, *, #145352, .T. ) ;
#101682=LINE ( 'NONE', #157893, #195512 ) ;
#101694=CARTESIAN_POINT ( 'NONE',  ( -21.05000000000000071, 1.261786168576181755, -41.58649896354548048 ) ) ;
#101718=VERTEX_POINT ( 'NONE', #100353 ) ;
#101740=ORIENTED_EDGE ( 'NONE', *, *, #149164, .F. ) ;
#101743=ADVANCED_FACE ( 'NONE', ( #179936 ), #1502, .T. ) ;
#101801=EDGE_LOOP ( 'NONE', ( #220431, #197176, #150664 ) ) ;
#101814=CYLINDRICAL_SURFACE ( 'NONE', #73983, 0.09999999999999811817 ) ;
#101865=CARTESIAN_POINT ( 'NONE',  ( 21.03670563405601968, 10.62482368933940258, -45.82554688620915329 ) ) ;
#101866=DIRECTION ( 'NONE',  ( 0.000000000000000000, 0.1575844902526560010, 0.9875055080513781558 ) ) ;
#101868=DIRECTION ( 'NONE',  ( 1.000000000000000000, 0.000000000000000000, 0.000000000000000000 ) ) ;
#101870=DIRECTION ( 'NONE',  ( 0.000000000000000000, 2.891205793294679805E-16, -1.000000000000000000 ) ) ;
#101889=ORIENTED_EDGE ( 'NONE', *, *, #216023, .F. ) ;
#101893=( BOUNDED_SURFACE ( )  B_SPLINE_SURFACE ( 3, 2, ( 
 ( #6096, #203021, #103903 ),
 ( #25684, #146882, #183475 ),
 ( #4802, #243434, #165188 ),
 ( #126042, #244708, #66084 ) ),
 .UNSPECIFIED., .F., .F., .F. ) 
 B_SPLINE_SURFACE_WITH_KNOTS ( ( 4, 4 ),
 ( 3, 3 ),
 ( -2.710505431213761085E-20, 0.0003124336600439507920 ),
 ( 0.000000000000000000, 1.000000000000000000 ),
 .UNSPECIFIED. ) 
 GEOMETRIC_REPRESENTATION_ITEM ( )  RATIONAL_B_SPLINE_SURFACE ( (
 ( 1.000000000000000000, 0.7071067811865475727, 1.000000000000000000),
 ( 1.000000000000000000, 0.7089187706049818738, 1.000000000000000000),
 ( 1.000000000000000000, 0.7039288185052217095, 1.000000000000000000),
 ( 1.000000000000000000, 0.7040654476015687502, 1.000000000000000000) ) ) 
 REPRESENTATION_ITEM ( '' )  SURFACE ( )  );
#101957=DIRECTION ( 'NONE',  ( -3.265361837132813093E-16, 1.000000000000000000, 0.000000000000000000 ) ) ;
#101965=ORIENTED_EDGE ( 'NONE', *, *, #145546, .T. ) ;
#101980=DIRECTION ( 'NONE',  ( 0.000000000000000000, 0.000000000000000000, -1.000000000000000000 ) ) ;
#101995=CARTESIAN_POINT ( 'NONE',  ( 21.14999999999999858, -0.09999999998884338825, -33.50000000000000000 ) ) ;
#102036=AXIS2_PLACEMENT_3D ( 'NONE', #135370, #256557, #74168 ) ;
#102068=VECTOR ( 'NONE', #92769, 1000.000000000000000 ) ;
#102102=AXIS2_PLACEMENT_3D ( 'NONE', #161016, #145279, #224820 ) ;
#102131=FACE_OUTER_BOUND ( 'NONE', #166335, .T. ) ;
#102132=EDGE_CURVE ( 'NONE', #187737, #68820, #180762, .T. ) ;
#102138=CARTESIAN_POINT ( 'NONE',  ( -18.59999999999999787, 7.021664781911246322, -70.63356540189728605 ) ) ;
#102193=AXIS2_PLACEMENT_3D ( 'NONE', #212690, #112308, #13209 ) ;
#102195=VERTEX_POINT ( 'NONE', #107767 ) ;
#102207=VECTOR ( 'NONE', #19233, 1000.000000000000000 ) ;
#102216=CARTESIAN_POINT ( 'NONE',  ( -21.05000000000000071, 6.540656951712400691, -33.60000000000000142 ) ) ;
#102219=CARTESIAN_POINT ( 'NONE',  ( 18.49999999999999645, 1.835341550235567887, -45.05515129256298223 ) ) ;
#102220=EDGE_CURVE ( 'NONE', #9287, #213770, #247374, .T. ) ;
#102240=VECTOR ( 'NONE', #45650, 1000.000000000000000 ) ;
#102243=EDGE_CURVE ( 'NONE', #183810, #109070, #145601, .T. ) ;
#102246=ORIENTED_EDGE ( 'NONE', *, *, #98223, .T. ) ;
#102290=EDGE_CURVE ( 'NONE', #161272, #177338, #64228, .T. ) ;
#102305=CARTESIAN_POINT ( 'NONE',  ( -20.94999999999999929, 1.116121084443477685E-11, -36.39999999999999147 ) ) ;
#102310=CARTESIAN_POINT ( 'NONE',  ( 18.49999999999999645, -1.835341550213255957, -45.05515129256298223 ) ) ;
#102342=ORIENTED_EDGE ( 'NONE', *, *, #203339, .F. ) ;
#102347=EDGE_CURVE ( 'NONE', #142140, #51264, #210173, .T. ) ;
#102371=LINE ( 'NONE', #145378, #233481 ) ;
#102381=CIRCLE ( 'NONE', #114904, 0.09999999999999892308 ) ;
#102383=CARTESIAN_POINT ( 'NONE',  ( -20.94999027547553894, 10.29326151435327219, -72.45928225104148623 ) ) ;
#102385=CARTESIAN_POINT ( 'NONE',  ( -21.05000000000000071, -1.162701749926853712, -41.60000000000000142 ) ) ;
#102391=FACE_OUTER_BOUND ( 'NONE', #205615, .T. ) ;
#102399=ADVANCED_FACE ( 'NONE', ( #55459 ), #108084, .F. ) ;
#102428=CIRCLE ( 'NONE', #223271, 0.1000000000000028644 ) ;
#102431=ORIENTED_EDGE ( 'NONE', *, *, #184231, .T. ) ;
#102445=CARTESIAN_POINT ( 'NONE',  ( -21.05000000000000071, 1.115653327213047955E-11, -29.20000000000004547 ) ) ;
#102476=ORIENTED_EDGE ( 'NONE', *, *, #211398, .F. ) ;
#102484=ORIENTED_EDGE ( 'NONE', *, *, #158991, .T. ) ;
#102500=ORIENTED_EDGE ( 'NONE', *, *, #85816, .T. ) ;
#102505=AXIS2_PLACEMENT_3D ( 'NONE', #166971, #88648, #10434 ) ;
#102509=VERTEX_POINT ( 'NONE', #141155 ) ;
#102522=CIRCLE ( 'NONE', #244021, 0.1000000000000028644 ) ;
#102558=AXIS2_PLACEMENT_3D ( 'NONE', #124606, #67193, #183290 ) ;
#102665=CARTESIAN_POINT ( 'NONE',  ( 23.24999999999999289, 6.650000000011155876, -54.85000000000000142 ) ) ;
#102707=VECTOR ( 'NONE', #92018, 1000.000000000000000 ) ;
#102718=ORIENTED_EDGE ( 'NONE', *, *, #109380, .T. ) ;
#102738=VERTEX_POINT ( 'NONE', #75741 ) ;
#102758=AXIS2_PLACEMENT_3D ( 'NONE', #199419, #162863, #2465 ) ;
#102776=CARTESIAN_POINT ( 'NONE',  ( 21.22070241538126467, 0.09891903054618129965, -27.03005372713038312 ) ) ;
#102779=ORIENTED_EDGE ( 'NONE', *, *, #99434, .T. ) ;
#102792=AXIS2_PLACEMENT_3D ( 'NONE', #185779, #89237, #52675 ) ;
#102816=ORIENTED_EDGE ( 'NONE', *, *, #186063, .F. ) ;
#102820=AXIS2_PLACEMENT_3D ( 'NONE', #27471, #71704, #86076 ) ;
#102822=ORIENTED_EDGE ( 'NONE', *, *, #112424, .F. ) ;
#102826=DIRECTION ( 'NONE',  ( 0.000000000000000000, 1.000000000000000000, -6.938893903907240999E-14 ) ) ;
#102844=AXIS2_PLACEMENT_3D ( 'NONE', #23693, #19832, #99319 ) ;
#102847=TOROIDAL_SURFACE ( 'NONE', #48689, 4.099999999999999645, 0.1000000000000000056 ) ;
#102865=AXIS2_PLACEMENT_3D ( 'NONE', #109945, #150381, #108670 ) ;
#102890=EDGE_CURVE ( 'NONE', #86338, #118577, #121317, .T. ) ;
#102928=AXIS2_PLACEMENT_3D ( 'NONE', #255520, #251726, #73124 ) ;
#102966=ADVANCED_FACE ( 'NONE', ( #66436 ), #62591, .T. ) ;
#102976=CARTESIAN_POINT ( 'NONE',  ( 22.39999999999999503, 1.115600667400684642E-11, -25.74999999999999645 ) ) ;
#102984=CARTESIAN_POINT ( 'NONE',  ( 22.57320508075687115, 11.75000000001115552, -33.50000000000000000 ) ) ;
#102990=CARTESIAN_POINT ( 'NONE',  ( -21.08134388332232589, 0.07581891751813416014, -27.16531941948202444 ) ) ;
#102997=LINE ( 'NONE', #101694, #57329 ) ;
#103002=DIRECTION ( 'NONE',  ( 0.000000000000000000, 0.000000000000000000, 1.000000000000000000 ) ) ;
#103034=ORIENTED_EDGE ( 'NONE', *, *, #244451, .T. ) ;
#103038=EDGE_CURVE ( 'NONE', #127078, #95921, #46848, .T. ) ;
#103051=DIRECTION ( 'NONE',  ( -3.265361837132813093E-16, 1.000000000000000000, 0.000000000000000000 ) ) ;
#103113=AXIS2_PLACEMENT_3D ( 'NONE', #187613, #29835, #31129 ) ;
#103140=AXIS2_PLACEMENT_3D ( 'NONE', #132387, #30746, #253597 ) ;
#103170=DIRECTION ( 'NONE',  ( -1.000000000000000000, -3.265361837132813093E-16, 0.000000000000000000 ) ) ;
#103196=CARTESIAN_POINT ( 'NONE',  ( -20.64999999999999858, 7.150000000011155876, -45.75000000000000000 ) ) ;
#103210=SPHERICAL_SURFACE ( 'NONE', #106824, 0.1000000000000000056 ) ;
#103219=DIRECTION ( 'NONE',  ( 0.000000000000000000, 0.000000000000000000, -1.000000000000000000 ) ) ;
#103229=CARTESIAN_POINT ( 'NONE',  ( 20.94999999999999929, 1.115600667400684642E-11, -67.00000000000000000 ) ) ;
#103262=FACE_OUTER_BOUND ( 'NONE', #231035, .T. ) ;
#103275=ORIENTED_EDGE ( 'NONE', *, *, #72962, .F. ) ;
#103291=DIRECTION ( 'NONE',  ( 0.000000000000000000, 0.1575844902526835067, 0.9875055080513738259 ) ) ;
#103343=CARTESIAN_POINT ( 'NONE',  ( -21.55000000000000426, 7.750000000011159074, -54.75000000000000000 ) ) ;
#103357=ORIENTED_EDGE ( 'NONE', *, *, #178427, .T. ) ;
#103379=ORIENTED_EDGE ( 'NONE', *, *, #169525, .T. ) ;
#103389=CIRCLE ( 'NONE', #208051, 11.89999999999999858 ) ;
#103415=ORIENTED_EDGE ( 'NONE', *, *, #15006, .F. ) ;
#103472=EDGE_CURVE ( 'NONE', #138871, #35121, #145640, .T. ) ;
#103473=VECTOR ( 'NONE', #255078, 1000.000000000000000 ) ;
#103501=EDGE_CURVE ( 'NONE', #215192, #54944, #23107, .T. ) ;
#103512=DIRECTION ( 'NONE',  ( 0.000000000000000000, -0.5000000000000078826, -0.8660254037844340447 ) ) ;
#103516=DIRECTION ( 'NONE',  ( 0.000000000000000000, 0.000000000000000000, 1.000000000000000000 ) ) ;
#103522=CARTESIAN_POINT ( 'NONE',  ( -21.05000000000000071, 6.299230910103437608, -33.40156249999967741 ) ) ;
#103527=ADVANCED_FACE ( 'NONE', ( #67401, #29592 ), #128675, .T. ) ;
#103543=DIRECTION ( 'NONE',  ( 0.000000000000000000, 0.000000000000000000, -1.000000000000000000 ) ) ;
#103561=DIRECTION ( 'NONE',  ( -1.000000000000000000, 0.000000000000000000, 0.000000000000000000 ) ) ;
#103562=ORIENTED_EDGE ( 'NONE', *, *, #8493, .T. ) ;
#103619=CARTESIAN_POINT ( 'NONE',  ( -21.05000000000000071, 5.850000000011105428, -43.63249722427796939 ) ) ;
#103634=CIRCLE ( 'NONE', #70382, 11.80000000000000426 ) ;
#103644=EDGE_CURVE ( 'NONE', #201073, #87677, #181506, .T. ) ;
#103646=ORIENTED_EDGE ( 'NONE', *, *, #193982, .T. ) ;
#103652=EDGE_LOOP ( 'NONE', ( #26852, #40647, #6518, #145046 ) ) ;
#103653=AXIS2_PLACEMENT_3D ( 'NONE', #190410, #70482, #150004 ) ;
#103666=CARTESIAN_POINT ( 'NONE',  ( -21.05000000000000071, 1.851028230152016674, -45.15391326942250316 ) ) ;
#103682=AXIS2_PLACEMENT_3D ( 'NONE', #37796, #213841, #156472 ) ;
#103736=CARTESIAN_POINT ( 'NONE',  ( -23.15000000000000213, 1.115600667400684642E-11, -67.00000000000000000 ) ) ;
#103757=CYLINDRICAL_SURFACE ( 'NONE', #84720, 7.900000000000003908 ) ;
#103773=ORIENTED_EDGE ( 'NONE', *, *, #240097, .F. ) ;
#103779=EDGE_CURVE ( 'NONE', #182882, #45390, #97687, .T. ) ;
#103845=VERTEX_POINT ( 'NONE', #8416 ) ;
#103859=AXIS2_PLACEMENT_3D ( 'NONE', #126549, #64003, #69164 ) ;
#103878=ADVANCED_FACE ( 'NONE', ( #192199 ), #98236, .T. ) ;
#103903=CARTESIAN_POINT ( 'NONE',  ( 22.59999999999999432, 0.1008583691098678542, -21.75043287651060808 ) ) ;
#103927=EDGE_CURVE ( 'NONE', #13961, #9287, #214316, .T. ) ;
#103936=ORIENTED_EDGE ( 'NONE', *, *, #99434, .F. ) ;
#103962=AXIS2_PLACEMENT_3D ( 'NONE', #116963, #52162, #79092 ) ;
#103978=ORIENTED_EDGE ( 'NONE', *, *, #166206, .F. ) ;
#103990=ORIENTED_EDGE ( 'NONE', *, *, #230667, .F. ) ;
#103992=DIRECTION ( 'NONE',  ( 0.000000000000000000, 0.000000000000000000, -1.000000000000000000 ) ) ;
#103995=AXIS2_PLACEMENT_3D ( 'NONE', #173548, #253022, #148806 ) ;
#104016=DIRECTION ( 'NONE',  ( 0.000000000000000000, 0.000000000000000000, -1.000000000000000000 ) ) ;
#104017=AXIS2_PLACEMENT_3D ( 'NONE', #161231, #82930, #5976 ) ;
#104027=EDGE_LOOP ( 'NONE', ( #245983, #195268, #198937 ) ) ;
#104039=VERTEX_POINT ( 'NONE', #10051 ) ;
#104053=VERTEX_POINT ( 'NONE', #29652 ) ;
#104062=EDGE_CURVE ( 'NONE', #224583, #33354, #6306, .T. ) ;
#104073=DIRECTION ( 'NONE',  ( -0.000000000000000000, 1.000000000000000000, 0.000000000000000000 ) ) ;
#104075=CARTESIAN_POINT ( 'NONE',  ( -20.54999999999999716, -8.663551401858001100, -57.47589888193270014 ) ) ;
#104088=ORIENTED_EDGE ( 'NONE', *, *, #174037, .F. ) ;
#104092=CARTESIAN_POINT ( 'NONE',  ( 21.07928932188134397, 6.328516656404459262, -33.40110485434561127 ) ) ;
#104143=CARTESIAN_POINT ( 'NONE',  ( 20.95576188350343116, 10.60898054497455689, -41.11123372275429944 ) ) ;
#104159=CARTESIAN_POINT ( 'NONE',  ( 20.94999999999999574, 11.62071067812981795, -60.13158334765904556 ) ) ;
#104173=CARTESIAN_POINT ( 'NONE',  ( -18.39999999999999858, -9.499999999988849808, -40.49928567783884858 ) ) ;
#104208=CIRCLE ( 'NONE', #66633, 4.049999999999998046 ) ;
#104214=ADVANCED_FACE ( 'NONE', ( #11341 ), #147796, .T. ) ;
#104215=CARTESIAN_POINT ( 'NONE',  ( -18.43707690579160641, -9.682403433465239573, -73.65684337741278398 ) ) ;
#104231=VERTEX_POINT ( 'NONE', #170465 ) ;
#104241=CARTESIAN_POINT ( 'NONE',  ( 21.05000000000000071, -11.74999999998883560, -64.10000000000000853 ) ) ;
#104242=CARTESIAN_POINT ( 'NONE',  ( -20.54999999999999716, 2.000000000011154189, -53.77537807723790309 ) ) ;
#104257=ORIENTED_EDGE ( 'NONE', *, *, #243435, .F. ) ;
#104298=DIRECTION ( 'NONE',  ( -1.000000000000000000, 0.000000000000000000, 0.000000000000000000 ) ) ;
#104313=TOROIDAL_SURFACE ( 'NONE', #154280, 0.2000000000000000111, 0.1000000000000000056 ) ;
#104358=FACE_OUTER_BOUND ( 'NONE', #220133, .T. ) ;
#104369=DIRECTION ( 'NONE',  ( 0.000000000000000000, 0.000000000000000000, 1.000000000000000000 ) ) ;
#104390=DIRECTION ( 'NONE',  ( -1.000000000000000000, 0.000000000000000000, 0.000000000000000000 ) ) ;
#104394=AXIS2_PLACEMENT_3D ( 'NONE', #187569, #208413, #170604 ) ;
#104399=ADVANCED_FACE ( 'NONE', ( #166294 ), #8477, .T. ) ;
#104426=LINE ( 'NONE', #81018, #13167 ) ;
#104445=CARTESIAN_POINT ( 'NONE',  ( 18.49999999999999645, 1.115600667400684642E-11, -67.00000000000000000 ) ) ;
#104463=ORIENTED_EDGE ( 'NONE', *, *, #182724, .F. ) ;
#104487=DIRECTION ( 'NONE',  ( 1.000000000000000000, 0.000000000000000000, 0.000000000000000000 ) ) ;
#104537=DIRECTION ( 'NONE',  ( 1.000000000000000000, 0.000000000000000000, 0.000000000000000000 ) ) ;
#104561=AXIS2_PLACEMENT_3D ( 'NONE', #39833, #140166, #158497 ) ;
#104568=CIRCLE ( 'NONE', #46320, 11.80000000000000426 ) ;
#104578=CARTESIAN_POINT ( 'NONE',  ( -21.14999999999999858, -11.74999999998884448, -36.39999999999999858 ) ) ;
#104584=DIRECTION ( 'NONE',  ( 0.000000000000000000, -1.000000000000000000, 1.387778780781442047E-14 ) ) ;
#104600=DIRECTION ( 'NONE',  ( -0.000000000000000000, -2.891205793294679805E-16, 1.000000000000000000 ) ) ;
#104606=FACE_OUTER_BOUND ( 'NONE', #149910, .T. ) ;
#104616=ORIENTED_EDGE ( 'NONE', *, *, #107528, .T. ) ;
#104634=DIRECTION ( 'NONE',  ( 0.000000000000000000, 0.000000000000000000, -1.000000000000000000 ) ) ;
#104700=CIRCLE ( 'NONE', #8895, 0.1000000000000000472 ) ;
#104743=CIRCLE ( 'NONE', #250527, 0.5000000000000004441 ) ;
#104752=DIRECTION ( 'NONE',  ( 1.000000000000000000, -3.965082230804126670E-15, 0.000000000000000000 ) ) ;
#104759=EDGE_LOOP ( 'NONE', ( #212975, #36939, #210224, #242453 ) ) ;
#104782=DIRECTION ( 'NONE',  ( -1.000000000000000000, -0.000000000000000000, -0.000000000000000000 ) ) ;
#104789=CARTESIAN_POINT ( 'NONE',  ( -21.05000000000000071, 6.300179817925682713, -33.44851711811818262 ) ) ;
#104801=ORIENTED_EDGE ( 'NONE', *, *, #61711, .F. ) ;
#104802=DIRECTION ( 'NONE',  ( 1.000000000000000000, 0.000000000000000000, 0.000000000000000000 ) ) ;
#104820=CARTESIAN_POINT ( 'NONE',  ( 21.14999999999999858, 6.550000000011156231, -45.85000000000000142 ) ) ;
#104867=ORIENTED_EDGE ( 'NONE', *, *, #114509, .T. ) ;
#104904=EDGE_CURVE ( 'NONE', #136029, #139968, #69440, .T. ) ;
#104915=DIRECTION ( 'NONE',  ( -1.000000000000000000, -0.000000000000000000, -0.000000000000000000 ) ) ;
#104922=EDGE_CURVE ( 'NONE', #223187, #235258, #81475, .T. ) ;
#104927=( BOUNDED_CURVE ( )  B_SPLINE_CURVE ( 3, ( #19493, #98981, #78154, #75630 ),
 .UNSPECIFIED., .F., .F. ) 
 B_SPLINE_CURVE_WITH_KNOTS ( ( 4, 4 ),
 ( 3.192897208853993085, 4.712388980384689674 ),
 .UNSPECIFIED. ) 
 CURVE ( )  GEOMETRIC_REPRESENTATION_ITEM ( )  RATIONAL_B_SPLINE_CURVE ( ( 1.000000000000000000, 0.8166740347213228279, 0.8166740347213228279, 1.000000000000000000 ) ) 
 REPRESENTATION_ITEM ( '' )  );
#104940=ORIENTED_EDGE ( 'NONE', *, *, #69470, .F. ) ;
#104979=CARTESIAN_POINT ( 'NONE',  ( -18.59999999999999787, -1.736705739456431807, -78.51742258762372728 ) ) ;
#104989=CYLINDRICAL_SURFACE ( 'NONE', #57387, 0.1000000000000028644 ) ;
#105005=DIRECTION ( 'NONE',  ( 0.000000000000000000, 0.000000000000000000, 1.000000000000000000 ) ) ;
#105024=DIRECTION ( 'NONE',  ( 0.000000000000000000, 1.000000000000000000, 0.000000000000000000 ) ) ;
#105053=CARTESIAN_POINT ( 'NONE',  ( -20.94999999999999574, 11.75000000001115552, -40.34160068989711334 ) ) ;
#105059=CARTESIAN_POINT ( 'NONE',  ( 21.05000000000000071, -11.64999999998883595, -64.10000000000000853 ) ) ;
#105090=ORIENTED_EDGE ( 'NONE', *, *, #57873, .F. ) ;
#105099=CARTESIAN_POINT ( 'NONE',  ( 18.59999999999999432, 1.728086936805619311, -20.38443500516777007 ) ) ;
#105161=LINE ( 'NONE', #206881, #37723 ) ;
#105175=ORIENTED_EDGE ( 'NONE', *, *, #38472, .T. ) ;
#105176=ORIENTED_EDGE ( 'NONE', *, *, #183522, .T. ) ;
#105185=DIRECTION ( 'NONE',  ( -1.000000000000000000, 0.000000000000000000, 0.000000000000000000 ) ) ;
#105190=AXIS2_PLACEMENT_3D ( 'NONE', #746, #157319, #256318 ) ;
#105220=ORIENTED_EDGE ( 'NONE', *, *, #216132, .T. ) ;
#105231=DIRECTION ( 'NONE',  ( 0.000000000000000000, 0.000000000000000000, -1.000000000000000000 ) ) ;
#105244=EDGE_CURVE ( 'NONE', #204139, #101473, #50807, .T. ) ;
#105259=AXIS2_PLACEMENT_3D ( 'NONE', #254247, #148765, #49646 ) ;
#105260=EDGE_CURVE ( 'NONE', #203548, #213770, #214967, .T. ) ;
#105285=CARTESIAN_POINT ( 'NONE',  ( -23.15000000000000213, 11.65000000001115588, -54.84999999999999432 ) ) ;
#105290=DIRECTION ( 'NONE',  ( 1.000000000000000000, 0.000000000000000000, 0.000000000000000000 ) ) ;
#105315=AXIS2_PLACEMENT_3D ( 'NONE', #257467, #239258, #154611 ) ;
#105383=ORIENTED_EDGE ( 'NONE', *, *, #212524, .T. ) ;
#105398=AXIS2_PLACEMENT_3D ( 'NONE', #253027, #233495, #216468 ) ;
#105411=DIRECTION ( 'NONE',  ( -1.000000000000000000, 0.000000000000000000, 0.000000000000000000 ) ) ;
#105412=EDGE_LOOP ( 'NONE', ( #12883, #15322, #41748 ) ) ;
#105461=VERTEX_POINT ( 'NONE', #74284 ) ;
#105507=DIRECTION ( 'NONE',  ( -0.000000000000000000, 0.000000000000000000, -1.000000000000000000 ) ) ;
#105531=DIRECTION ( 'NONE',  ( -1.000000000000000000, 0.000000000000000000, 0.000000000000000000 ) ) ;
#105535=CARTESIAN_POINT ( 'NONE',  ( 21.14999999999999858, 11.65000000001116298, -21.75000000000000355 ) ) ;
#105576=CARTESIAN_POINT ( 'NONE',  ( 22.47071067811865319, 7.720074744509197728, -33.40090754529740025 ) ) ;
#105578=ORIENTED_EDGE ( 'NONE', *, *, #42026, .T. ) ;
#105585=CARTESIAN_POINT ( 'NONE',  ( -22.50000000000000000, 11.65000000001115588, -33.50000000000000000 ) ) ;
#105593=ORIENTED_EDGE ( 'NONE', *, *, #229562, .F. ) ;
#105601=AXIS2_PLACEMENT_3D ( 'NONE', #235403, #230270, #155906 ) ;
#105623=AXIS2_PLACEMENT_3D ( 'NONE', #168058, #207153, #67625 ) ;
#105624=AXIS2_PLACEMENT_3D ( 'NONE', #138622, #42145, #99501 ) ;
#105660=ORIENTED_EDGE ( 'NONE', *, *, #201216, .T. ) ;
#105664=ORIENTED_EDGE ( 'NONE', *, *, #43516, .T. ) ;
#105681=( BOUNDED_SURFACE ( )  B_SPLINE_SURFACE ( 3, 2, ( 
 ( #90654, #209321, #170259 ),
 ( #153248, #30727, #110222 ),
 ( #213173, #32003, #73702 ),
 ( #249745, #71128, #111519 ),
 ( #230174, #232763, #54100 ),
 ( #133644, #15001, #247161 ) ),
 .UNSPECIFIED., .F., .F., .F. ) 
 B_SPLINE_SURFACE_WITH_KNOTS ( ( 4, 2, 4 ),
 ( 3, 3 ),
 ( 3.141592653589793116, 3.926990816987241395, 4.712388980384689674 ),
 ( 0.000000000000000000, 1.000000000000000000 ),
 .UNSPECIFIED. ) 
 GEOMETRIC_REPRESENTATION_ITEM ( )  RATIONAL_B_SPLINE_SURFACE ( (
 ( 1.000000000000000000, 0.9238795325112820755, 1.000000000000000000),
 ( 1.000000000000000000, 0.9240297172244890112, 1.000000000000000000),
 ( 1.000000000000000000, 0.9038128468037535113, 1.000000000000000000),
 ( 1.000000000000000000, 0.8282379607651170206, 1.000000000000000000),
 ( 1.000000000000000000, 0.7727932973490044821, 1.000000000000000000),
 ( 1.000000000000000000, 0.7071067811865352493, 1.000000000000000000) ) ) 
 REPRESENTATION_ITEM ( '' )  SURFACE ( )  );
#105687=FACE_OUTER_BOUND ( 'NONE', #144046, .T. ) ;
#105710=DIRECTION ( 'NONE',  ( -1.000000000000000000, -0.000000000000000000, -0.000000000000000000 ) ) ;
#105732=CIRCLE ( 'NONE', #126611, 0.09999999999999843736 ) ;
#105735=AXIS2_PLACEMENT_3D ( 'NONE', #14245, #115894, #33834 ) ;
#105772=CARTESIAN_POINT ( 'NONE',  ( 18.59999999999999432, -1.835859311432481045, -78.50443916879852679 ) ) ;
#105791=ADVANCED_FACE ( 'NONE', ( #179164 ), #60453, .T. ) ;
#105810=DIRECTION ( 'NONE',  ( 0.000000000000000000, 0.000000000000000000, -1.000000000000000000 ) ) ;
#105828=ADVANCED_FACE ( 'NONE', ( #257323 ), #177868, .F. ) ;
#105857=AXIS2_PLACEMENT_3D ( 'NONE', #222053, #79978, #82541 ) ;
#105896=EDGE_LOOP ( 'NONE', ( #110907, #13880, #53665, #55249 ) ) ;
#105898=CARTESIAN_POINT ( 'NONE',  ( -18.50000000000000000, -9.399999999988850163, -73.88204184817267617 ) ) ;
#105915=LINE ( 'NONE', #164646, #35831 ) ;
#105919=CIRCLE ( 'NONE', #134958, 0.1000000000000028644 ) ;
#105922=LINE ( 'NONE', #85066, #149553 ) ;
#105935=CARTESIAN_POINT ( 'NONE',  ( 23.25000000000000000, -8.596261682231828516, -57.54987248284972168 ) ) ;
#105947=ORIENTED_EDGE ( 'NONE', *, *, #217995, .T. ) ;
#106032=ADVANCED_FACE ( 'NONE', ( #211545 ), #132136, .F. ) ;
#106037=ORIENTED_EDGE ( 'NONE', *, *, #102132, .T. ) ;
#106069=CARTESIAN_POINT ( 'NONE',  ( 21.05000000000000071, 10.72371710471867701, -41.16491356908760935 ) ) ;
#106118=DIRECTION ( 'NONE',  ( 0.000000000000000000, -0.1350103645451876666, -0.9908441862701600211 ) ) ;
#106123=CIRCLE ( 'NONE', #38958, 12.87499999999999822 ) ;
#106128=ORIENTED_EDGE ( 'NONE', *, *, #92323, .T. ) ;
#106168=CIRCLE ( 'NONE', #251939, 0.1000000000000002554 ) ;
#106174=DIRECTION ( 'NONE',  ( 0.000000000000000000, 0.000000000000000000, -1.000000000000000000 ) ) ;
#106179=DIRECTION ( 'NONE',  ( 0.000000000000000000, 0.000000000000000000, 1.000000000000000000 ) ) ;
#106245=ORIENTED_EDGE ( 'NONE', *, *, #99216, .F. ) ;
#106253=ORIENTED_EDGE ( 'NONE', *, *, #125002, .T. ) ;
#106289=ORIENTED_EDGE ( 'NONE', *, *, #141402, .T. ) ;
#106327=DIRECTION ( 'NONE',  ( 1.000000000000000000, -0.000000000000000000, -0.000000000000000000 ) ) ;
#106333=CARTESIAN_POINT ( 'NONE',  ( 18.60000000000000853, -9.364236010355613260, -40.68025440072462118 ) ) ;
#106335=TOROIDAL_SURFACE ( 'NONE', #198129, 11.65000000000000036, 0.1000000000000000056 ) ;
#106349=DIRECTION ( 'NONE',  ( 0.000000000000000000, 0.000000000000000000, 1.000000000000000000 ) ) ;
#106366=CARTESIAN_POINT ( 'NONE',  ( 23.14999999999999858, 5.900000000011162093, -56.78090023534362984 ) ) ;
#106392=ADVANCED_FACE ( 'NONE', ( #152582 ), #249719, .T. ) ;
#106410=EDGE_LOOP ( 'NONE', ( #110421, #229910, #177545, #216435 ) ) ;
#106421=LINE ( 'NONE', #4752, #228708 ) ;
#106462=AXIS2_PLACEMENT_3D ( 'NONE', #228374, #204932, #87550 ) ;
#106467=DIRECTION ( 'NONE',  ( 0.000000000000000000, 0.000000000000000000, -1.000000000000000000 ) ) ;
#106478=ORIENTED_EDGE ( 'NONE', *, *, #54762, .F. ) ;
#106492=CIRCLE ( 'NONE', #35810, 0.1000000000000001860 ) ;
#106548=ADVANCED_FACE ( 'NONE', ( #222770 ), #203233, .T. ) ;
#106572=AXIS2_PLACEMENT_3D ( 'NONE', #242798, #160739, #124160 ) ;
#106583=CARTESIAN_POINT ( 'NONE',  ( 20.94999999999999929, 4.850467289730772791, -45.53426740900168568 ) ) ;
#106588=FACE_OUTER_BOUND ( 'NONE', #228173, .T. ) ;
#106622=ORIENTED_EDGE ( 'NONE', *, *, #95194, .F. ) ;
#106639=CARTESIAN_POINT ( 'NONE',  ( -23.25000000000000000, 11.65000000001115588, -21.75000000000000355 ) ) ;
#106659=DIRECTION ( 'NONE',  ( 0.000000000000000000, 0.000000000000000000, 1.000000000000000000 ) ) ;
#106663=AXIS2_PLACEMENT_3D ( 'NONE', #136960, #202082, #138226 ) ;
#106824=AXIS2_PLACEMENT_3D ( 'NONE', #105772, #6695, #104487 ) ;
#106853=ORIENTED_EDGE ( 'NONE', *, *, #213737, .T. ) ;
#106854=DIRECTION ( 'NONE',  ( -6.938893903907224433E-15, 1.000000000000000000, 0.000000000000000000 ) ) ;
#106859=CARTESIAN_POINT ( 'NONE',  ( 21.05000000000000071, 5.400000000011154988, -57.10603087734755690 ) ) ;
#106891=LINE ( 'NONE', #147309, #102240 ) ;
#106898=ADVANCED_FACE ( 'NONE', ( #828 ), #57649, .T. ) ;
#106924=FACE_OUTER_BOUND ( 'NONE', #211666, .T. ) ;
#106951=AXIS2_PLACEMENT_3D ( 'NONE', #53801, #96746, #92912 ) ;
#106972=CARTESIAN_POINT ( 'NONE',  ( -20.00857864376270001, 9.150000000011157653, -54.75000000000000000 ) ) ;
#107000=LINE ( 'NONE', #164435, #64586 ) ;
#107065=ORIENTED_EDGE ( 'NONE', *, *, #69577, .F. ) ;
#107093=DIRECTION ( 'NONE',  ( 1.000000000000000000, 0.000000000000000000, 0.000000000000000000 ) ) ;
#107130=CARTESIAN_POINT ( 'NONE',  ( 18.51697539158856642, 10.31565961587946312, -72.53641941191783360 ) ) ;
#107132=DIRECTION ( 'NONE',  ( 0.000000000000000000, -0.8700118002898359348, 0.4930308989875165082 ) ) ;
#107146=AXIS2_PLACEMENT_3D ( 'NONE', #56013, #36514, #232135 ) ;
#107150=EDGE_CURVE ( 'NONE', #140260, #224599, #249215, .T. ) ;
#107245=CARTESIAN_POINT ( 'NONE',  ( 20.94999999999999929, 1.115600667400684642E-11, -68.90000000000000568 ) ) ;
#107261=ORIENTED_EDGE ( 'NONE', *, *, #34882, .T. ) ;
#107279=AXIS2_PLACEMENT_3D ( 'NONE', #195565, #96419, #18190 ) ;
#107298=FACE_OUTER_BOUND ( 'NONE', #46464, .T. ) ;
#107309=ORIENTED_EDGE ( 'NONE', *, *, #52184, .T. ) ;
#107327=CIRCLE ( 'NONE', #24144, 0.09999999999999939493 ) ;
#107339=EDGE_LOOP ( 'NONE', ( #205677, #98183, #186569, #33741 ) ) ;
#107346=DIRECTION ( 'NONE',  ( 1.000000000000000000, -0.000000000000000000, 0.000000000000000000 ) ) ;
#107354=CARTESIAN_POINT ( 'NONE',  ( -23.25000000000000000, 1.115600667400684642E-11, -67.00000000000000000 ) ) ;
#107365=EDGE_CURVE ( 'NONE', #82173, #235258, #41789, .T. ) ;
#107425=CARTESIAN_POINT ( 'NONE',  ( -23.25000000000000000, -8.596261682231832069, -57.54987248284972878 ) ) ;
#107447=CARTESIAN_POINT ( 'NONE',  ( 21.05000000000000071, -0.09999999998884338825, -33.50000000000000000 ) ) ;
#107452=CIRCLE ( 'NONE', #3370, 0.1000000000000028644 ) ;
#107490=EDGE_LOOP ( 'NONE', ( #229002, #64238, #177604, #132623 ) ) ;
#107516=VERTEX_POINT ( 'NONE', #201928 ) ;
#107528=EDGE_CURVE ( 'NONE', #23656, #139599, #199373, .T. ) ;
#107564=CIRCLE ( 'NONE', #61791, 7.900000000000003908 ) ;
#107598=CARTESIAN_POINT ( 'NONE',  ( 21.14999999999999503, -11.74999999998883560, -21.75000000000000355 ) ) ;
#107618=CARTESIAN_POINT ( 'NONE',  ( -18.55121869061588669, 10.32747123227773045, -72.57740328502492844 ) ) ;
#107627=DIRECTION ( 'NONE',  ( -0.000000000000000000, 1.000000000000000000, -0.000000000000000000 ) ) ;
#107636=ORIENTED_EDGE ( 'NONE', *, *, #33133, .T. ) ;
#107670=EDGE_LOOP ( 'NONE', ( #101965, #170460, #200206, #162514 ) ) ;
#107679=ORIENTED_EDGE ( 'NONE', *, *, #37021, .F. ) ;
#107691=EDGE_CURVE ( 'NONE', #216494, #1091, #171169, .T. ) ;
#107704=CARTESIAN_POINT ( 'NONE',  ( 20.94999999999999929, 6.550000000011156231, -43.51702717044002355 ) ) ;
#107725=EDGE_CURVE ( 'NONE', #141829, #248843, #130075, .T. ) ;
#107736=CARTESIAN_POINT ( 'NONE',  ( -20.64999999999999858, 4.250000000011156409, -45.75000000000000711 ) ) ;
#107738=AXIS2_PLACEMENT_3D ( 'NONE', #129239, #193072, #208782 ) ;
#107767=CARTESIAN_POINT ( 'NONE',  ( 23.14999999999999858, -3.999999999988843147, -67.00000000000000000 ) ) ;
#107810=DIRECTION ( 'NONE',  ( -1.000000000000000000, 0.000000000000000000, 0.000000000000000000 ) ) ;
#107845=FACE_OUTER_BOUND ( 'NONE', #36564, .T. ) ;
#107852=ORIENTED_EDGE ( 'NONE', *, *, #34970, .T. ) ;
#107866=DIRECTION ( 'NONE',  ( 0.000000000000000000, 0.000000000000000000, -1.000000000000000000 ) ) ;
#107953=VERTEX_POINT ( 'NONE', #7247 ) ;
#107954=EDGE_CURVE ( 'NONE', #8827, #173018, #182129, .T. ) ;
#107977=AXIS2_PLACEMENT_3D ( 'NONE', #6256, #166666, #198376 ) ;
#108084=( BOUNDED_SURFACE ( )  B_SPLINE_SURFACE ( 3, 2, ( 
 ( #213277, #34676, #131177 ),
 ( #135007, #12546, #175472 ),
 ( #235406, #93334, #15100 ),
 ( #56744, #92052, #152058 ) ),
 .UNSPECIFIED., .F., .F., .F. ) 
 B_SPLINE_SURFACE_WITH_KNOTS ( ( 4, 4 ),
 ( 3, 3 ),
 ( 0.0002700421466196717673, 0.0004789321604330915635 ),
 ( 0.000000000000000000, 1.000000000000000000 ),
 .UNSPECIFIED. ) 
 GEOMETRIC_REPRESENTATION_ITEM ( )  RATIONAL_B_SPLINE_SURFACE ( (
 ( 1.000000000000000000, 0.7071067811865475727, 1.000000000000000000),
 ( 1.000000000000000000, 0.7163411249511619783, 1.000000000000000000),
 ( 1.000000000000000000, 0.7221957104841967290, 1.000000000000000000),
 ( 1.000000000000000000, 0.7250110520819876836, 1.000000000000000000) ) ) 
 REPRESENTATION_ITEM ( '' )  SURFACE ( )  );
#108088=DIRECTION ( 'NONE',  ( 0.000000000000000000, 0.000000000000000000, -1.000000000000000000 ) ) ;
#108119=CARTESIAN_POINT ( 'NONE',  ( -18.59999999999999787, 9.250000000011157297, -54.65000000000000568 ) ) ;
#108126=DIRECTION ( 'NONE',  ( 0.000000000000000000, 0.000000000000000000, -1.000000000000000000 ) ) ;
#108142=DIRECTION ( 'NONE',  ( 0.000000000000000000, 0.000000000000000000, 1.000000000000000000 ) ) ;
#108156=ORIENTED_EDGE ( 'NONE', *, *, #101539, .T. ) ;
#108196=DIRECTION ( 'NONE',  ( 0.000000000000000000, 0.000000000000000000, -1.000000000000000000 ) ) ;
#108221=ORIENTED_EDGE ( 'NONE', *, *, #249707, .T. ) ;
#108226=ORIENTED_EDGE ( 'NONE', *, *, #20762, .T. ) ;
#108236=ADVANCED_FACE ( 'NONE', ( #200028 ), #21411, .T. ) ;
#108296=DIRECTION ( 'NONE',  ( 0.000000000000000000, 0.5000000000000078826, -0.8660254037844340447 ) ) ;
#108301=ORIENTED_EDGE ( 'NONE', *, *, #70252, .T. ) ;
#108310=DIRECTION ( 'NONE',  ( 1.000000000000000000, -0.000000000000000000, -0.000000000000000000 ) ) ;
#108331=STYLED_ITEM ( 'NONE', ( #82629 ), #193366 ) ;
#108393=FACE_OUTER_BOUND ( 'NONE', #205743, .T. ) ;
#108409=FACE_OUTER_BOUND ( 'NONE', #122750, .T. ) ;
#108455=VERTEX_POINT ( 'NONE', #32991 ) ;
#108459=PLANE ( 'NONE',  #42085 ) ;
#108486=ADVANCED_FACE ( 'NONE', ( #68216 ), #251984, .T. ) ;
#108491=ORIENTED_EDGE ( 'NONE', *, *, #58742, .F. ) ;
#108492=ORIENTED_EDGE ( 'NONE', *, *, #185338, .T. ) ;
#108495=VERTEX_POINT ( 'NONE', #167343 ) ;
#108537=EDGE_CURVE ( 'NONE', #122271, #14565, #132012, .T. ) ;
#108542=DIRECTION ( 'NONE',  ( 1.000000000000000000, 0.000000000000000000, 0.000000000000000000 ) ) ;
#108546=DIRECTION ( 'NONE',  ( 0.7071067811865487940, 0.000000000000000000, -0.7071067811865463515 ) ) ;
#108547=DIRECTION ( 'NONE',  ( -1.000000000000000000, 0.000000000000000000, 0.000000000000000000 ) ) ;
#108559=DIRECTION ( 'NONE',  ( 0.000000000000000000, 0.000000000000000000, -1.000000000000000000 ) ) ;
#108589=CARTESIAN_POINT ( 'NONE',  ( 18.43579564894474387, -9.519327535281304264, -40.47297664386042726 ) ) ;
#108636=EDGE_CURVE ( 'NONE', #161055, #203545, #27996, .T. ) ;
#108670=DIRECTION ( 'NONE',  ( 0.000000000000000000, 0.000000000000000000, -1.000000000000000000 ) ) ;
#108675=PLANE ( 'NONE',  #35752 ) ;
#108684=DIRECTION ( 'NONE',  ( 1.836970198721029934E-16, -1.000000000000000000, -0.000000000000000000 ) ) ;
#108693=EDGE_CURVE ( 'NONE', #100962, #119332, #222793, .T. ) ;
#108698=FACE_OUTER_BOUND ( 'NONE', #216692, .T. ) ;
#108705=AXIS2_PLACEMENT_3D ( 'NONE', #34096, #152754, #148881 ) ;
#108726=ORIENTED_EDGE ( 'NONE', *, *, #137615, .T. ) ;
#108733=CARTESIAN_POINT ( 'NONE',  ( -23.25000000000000000, -1.164121893230052995, -74.91484808557160591 ) ) ;
#108734=TOROIDAL_SURFACE ( 'NONE', #250385, 0.2000000000000000111, 0.1000000000000000056 ) ;
#108759=ORIENTED_EDGE ( 'NONE', *, *, #149604, .F. ) ;
#108819=DIRECTION ( 'NONE',  ( -0.000000000000000000, -0.000000000000000000, -1.000000000000000000 ) ) ;
#108865=DIRECTION ( 'NONE',  ( 1.713247197920696616E-14, 0.9876197685951252359, -0.1568667991644863424 ) ) ;
#108876=VECTOR ( 'NONE', #183736, 1000.000000000000000 ) ;
#108891=ORIENTED_EDGE ( 'NONE', *, *, #70934, .F. ) ;
#108919=DIRECTION ( 'NONE',  ( 0.000000000000000000, 1.000000000000000000, 0.000000000000000000 ) ) ;
#108929=TOROIDAL_SURFACE ( 'NONE', #83951, 11.65000000000000036, 0.1000000000000000056 ) ;
#108934=DIRECTION ( 'NONE',  ( 0.000000000000000000, 3.552713678800407449E-15, -1.000000000000000000 ) ) ;
#108935=DIRECTION ( 'NONE',  ( -1.000000000000000000, -0.000000000000000000, -0.000000000000000000 ) ) ;
#109021=DIRECTION ( 'NONE',  ( 1.000000000000000000, 0.000000000000000000, 0.000000000000000000 ) ) ;
#109043=AXIS2_PLACEMENT_3D ( 'NONE', #188281, #245693, #206566 ) ;
#109064=ORIENTED_EDGE ( 'NONE', *, *, #56844, .T. ) ;
#109070=VERTEX_POINT ( 'NONE', #162549 ) ;
#109105=CARTESIAN_POINT ( 'NONE',  ( -23.25000000000000000, -11.74999999998884448, -36.60000000000000853 ) ) ;
#109122=DIRECTION ( 'NONE',  ( 1.000000000000000000, 0.000000000000000000, 0.000000000000000000 ) ) ;
#109130=EDGE_CURVE ( 'NONE', #180750, #188642, #32466, .T. ) ;
#109163=CARTESIAN_POINT ( 'NONE',  ( 20.94999999999999929, -11.48912529306489994, -63.89999999999999858 ) ) ;
#109174=VERTEX_POINT ( 'NONE', #34588 ) ;
#109228=CYLINDRICAL_SURFACE ( 'NONE', #15900, 0.1000000000000028644 ) ;
#109259=ORIENTED_EDGE ( 'NONE', *, *, #46650, .T. ) ;
#109304=CARTESIAN_POINT ( 'NONE',  ( 22.49533356619861379, 11.65000000631534149, -33.43487741967727800 ) ) ;
#109338=CARTESIAN_POINT ( 'NONE',  ( 23.14999999999999503, 11.65000000001116298, -54.85000000000000142 ) ) ;
#109350=ORIENTED_EDGE ( 'NONE', *, *, #57069, .F. ) ;
#109380=EDGE_CURVE ( 'NONE', #212264, #61003, #120548, .T. ) ;
#109412=CARTESIAN_POINT ( 'NONE',  ( -21.13498764882296044, 0.001656394742485969677, -27.00438185652605938 ) ) ;
#109497=EDGE_LOOP ( 'NONE', ( #128602, #11852, #3943, #241907, #193414, #242574, #37709, #194133, #135034, #80185, #183073, #135329, #146840, #187089, #55990, #118127, #18739, #188019, #83082, #223916, #113322, #32244, #197752, #85174, #192878 ) ) ;
#109499=CARTESIAN_POINT ( 'NONE',  ( 21.05000000000000426, 6.258817194692626984, -33.46636726466636702 ) ) ;
#109533=CARTESIAN_POINT ( 'NONE',  ( -23.25000000000000000, 1.115600667400684642E-11, -69.10000000000000853 ) ) ;
#109559=AXIS2_PLACEMENT_3D ( 'NONE', #190992, #228822, #23259 ) ;
#109582=DIRECTION ( 'NONE',  ( 0.000000000000000000, 0.000000000000000000, -1.000000000000000000 ) ) ;
#109593=TOROIDAL_SURFACE ( 'NONE', #117965, 0.2000000000000000111, 0.1000000000000000056 ) ;
#109603=CIRCLE ( 'NONE', #88742, 0.5000000000000004441 ) ;
#109611=ORIENTED_EDGE ( 'NONE', *, *, #53433, .F. ) ;
#109622=CARTESIAN_POINT ( 'NONE',  ( -22.50000000000000000, 1.115600667400684642E-11, -33.39999999999999858 ) ) ;
#109626=DIRECTION ( 'NONE',  ( 1.000000000000000000, 0.000000000000000000, 0.000000000000000000 ) ) ;
#109631=VERTEX_POINT ( 'NONE', #253297 ) ;
#109662=ORIENTED_EDGE ( 'NONE', *, *, #87750, .T. ) ;
#109707=EDGE_LOOP ( 'NONE', ( #224351, #106853, #246113, #31802 ) ) ;
#109734=CIRCLE ( 'NONE', #30657, 0.1000000000000008937 ) ;
#109750=ORIENTED_EDGE ( 'NONE', *, *, #226100, .F. ) ;
#109768=CARTESIAN_POINT ( 'NONE',  ( -18.59999994787167310, -9.523637689750295010, -73.88244953477273214 ) ) ;
#109783=ORIENTED_EDGE ( 'NONE', *, *, #207836, .F. ) ;
#109820=EDGE_CURVE ( 'NONE', #232658, #113969, #153651, .T. ) ;
#109865=CIRCLE ( 'NONE', #72482, 0.1000000000000028644 ) ;
#109891=PLANE ( 'NONE',  #6998 ) ;
#109901=DIRECTION ( 'NONE',  ( 0.000000000000000000, -1.000000000000000000, -1.734723475976807292E-15 ) ) ;
#109904=CARTESIAN_POINT ( 'NONE',  ( 21.00000000000000000, 9.750000000011153745, -54.75000000000000000 ) ) ;
#109933=DIRECTION ( 'NONE',  ( 2.952720810173288619E-16, -1.000000000000000000, 0.000000000000000000 ) ) ;
#109945=CARTESIAN_POINT ( 'NONE',  ( 21.05000000000000071, 1.115600667400684642E-11, -67.00000000000000000 ) ) ;
#109964=DIRECTION ( 'NONE',  ( 0.000000000000000000, 0.000000000000000000, -1.000000000000000000 ) ) ;
#109976=AXIS2_PLACEMENT_3D ( 'NONE', #216937, #194849, #54022 ) ;
#109988=EDGE_CURVE ( 'NONE', #51264, #216196, #178572, .T. ) ;
#109989=CARTESIAN_POINT ( 'NONE',  ( -21.05000000000000071, 5.900000000011102586, -43.71909976465641989 ) ) ;
#110003=CARTESIAN_POINT ( 'NONE',  ( 22.39999999999999503, 1.115541036281197940E-11, -25.70922040162662370 ) ) ;
#110024=DIRECTION ( 'NONE',  ( 1.000000000000000000, 0.000000000000000000, 0.000000000000000000 ) ) ;
#110068=DIRECTION ( 'NONE',  ( 0.000000000000000000, -0.1568667991644863147, 0.9876197685951252359 ) ) ;
#110094=VERTEX_POINT ( 'NONE', #216434 ) ;
#110126=DIRECTION ( 'NONE',  ( 0.000000000000000000, 0.9908441862701596881, -0.1350103645451904977 ) ) ;
#110128=AXIS2_PLACEMENT_3D ( 'NONE', #190509, #206196, #27597 ) ;
#110138=VERTEX_POINT ( 'NONE', #239871 ) ;
#110187=DIRECTION ( 'NONE',  ( 0.000000000000000000, -0.000000000000000000, 1.000000000000000000 ) ) ;
#110211=EDGE_LOOP ( 'NONE', ( #223379, #73004, #176261 ) ) ;
#110220=CARTESIAN_POINT ( 'NONE',  ( -20.85000000000000142, -11.64999999998884306, -67.00000000000000000 ) ) ;
#110222=CARTESIAN_POINT ( 'NONE',  ( 18.49999999999999289, 10.20857864609425825, -58.20250686563007037 ) ) ;
#110251=LINE ( 'NONE', #50265, #192116 ) ;
#110257=DIRECTION ( 'NONE',  ( 1.000000000000000000, 0.000000000000000000, 0.000000000000000000 ) ) ;
#110328=EDGE_LOOP ( 'NONE', ( #224099, #141190, #229890, #75427 ) ) ;
#110331=EDGE_CURVE ( 'NONE', #7145, #143246, #91242, .T. ) ;
#110346=DIRECTION ( 'NONE',  ( 0.000000000000000000, -1.000000000000000000, 0.000000000000000000 ) ) ;
#110359=ORIENTED_EDGE ( 'NONE', *, *, #132167, .T. ) ;
#110363=DIRECTION ( 'NONE',  ( 0.7071359030027680737, 0.7070776581709111719, 0.000000000000000000 ) ) ;
#110388=DIRECTION ( 'NONE',  ( -4.391705002472929091E-16, 1.000000000000000000, 0.000000000000000000 ) ) ;
#110421=ORIENTED_EDGE ( 'NONE', *, *, #83553, .F. ) ;
#110427=CARTESIAN_POINT ( 'NONE',  ( 18.55857864376267941, 10.36715728753653565, -58.25000000000000711 ) ) ;
#110429=FACE_OUTER_BOUND ( 'NONE', #154000, .T. ) ;
#110446=EDGE_CURVE ( 'NONE', #18666, #108495, #141299, .T. ) ;
#110470=DIRECTION ( 'NONE',  ( 1.000000000000000000, 0.000000000000000000, 0.000000000000000000 ) ) ;
#110488=DIRECTION ( 'NONE',  ( -6.938893903907222856E-15, 1.000000000000000000, 2.891205793294679805E-16 ) ) ;
#110525=EDGE_LOOP ( 'NONE', ( #78374, #225188, #29681, #177298 ) ) ;
#110582=FACE_OUTER_BOUND ( 'NONE', #133575, .T. ) ;
#110594=ORIENTED_EDGE ( 'NONE', *, *, #56886, .T. ) ;
#110597=CYLINDRICAL_SURFACE ( 'NONE', #130907, 0.1000000000000000472 ) ;
#110614=ORIENTED_EDGE ( 'NONE', *, *, #62969, .F. ) ;
#110621=AXIS2_PLACEMENT_3D ( 'NONE', #167074, #207466, #210034 ) ;
#110628=EDGE_CURVE ( 'NONE', #40042, #166959, #78417, .T. ) ;
#110639=LINE ( 'NONE', #151061, #35256 ) ;
#110664=DIRECTION ( 'NONE',  ( 1.000000000000000000, 0.000000000000000000, 0.000000000000000000 ) ) ;
#110699=CARTESIAN_POINT ( 'NONE',  ( 21.05000000000000071, 1.115600667400684642E-11, -46.37500000000000000 ) ) ;
#110700=VERTEX_POINT ( 'NONE', #28781 ) ;
#110750=ORIENTED_EDGE ( 'NONE', *, *, #199970, .T. ) ;
#110757=ADVANCED_FACE ( 'NONE', ( #45721 ), #183950, .T. ) ;
#110793=EDGE_LOOP ( 'NONE', ( #21550, #222784 ) ) ;
#110799=FACE_OUTER_BOUND ( 'NONE', #194934, .T. ) ;
#110813=DIRECTION ( 'NONE',  ( -0.000000000000000000, -0.000000000000000000, -1.000000000000000000 ) ) ;
#110818=VERTEX_POINT ( 'NONE', #109533 ) ;
#110819=CARTESIAN_POINT ( 'NONE',  ( 20.94999999999999574, -1.162701749926853712, -41.60000000000000142 ) ) ;
#110827=AXIS2_PLACEMENT_3D ( 'NONE', #7440, #242202, #63561 ) ;
#110834=EDGE_CURVE ( 'NONE', #79923, #137338, #166461, .T. ) ;
#110853=TOROIDAL_SURFACE ( 'NONE', #181775, 0.2000000000000000111, 0.1000000000000000056 ) ;
#110881=CARTESIAN_POINT ( 'NONE',  ( 21.98333005346336577, 1.115600667400684642E-11, -26.12592467094333415 ) ) ;
#110896=VECTOR ( 'NONE', #7947, 1000.000000000000000 ) ;
#110899=ORIENTED_EDGE ( 'NONE', *, *, #138318, .T. ) ;
#110901=DIRECTION ( 'NONE',  ( 0.000000000000000000, 1.000000000000000000, -1.224646799147353207E-16 ) ) ;
#110907=ORIENTED_EDGE ( 'NONE', *, *, #250772, .T. ) ;
#110975=EDGE_CURVE ( 'NONE', #127685, #65499, #186731, .T. ) ;
#110999=AXIS2_PLACEMENT_3D ( 'NONE', #72310, #193537, #211816 ) ;
#111017=DIRECTION ( 'NONE',  ( 0.000000000000000000, 1.000000000000000000, 0.000000000000000000 ) ) ;
#111025=LINE ( 'NONE', #88869, #17141 ) ;
#111086=DIRECTION ( 'NONE',  ( 1.000000000000000000, 0.000000000000000000, 0.000000000000000000 ) ) ;
#111089=ORIENTED_EDGE ( 'NONE', *, *, #246995, .T. ) ;
#111093=DIRECTION ( 'NONE',  ( 0.000000000000000000, 0.000000000000000000, -1.000000000000000000 ) ) ;
#111114=EDGE_CURVE ( 'NONE', #159251, #12445, #140928, .T. ) ;
#111130=EDGE_LOOP ( 'NONE', ( #93096, #105578, #14719, #146230 ) ) ;
#111136=CARTESIAN_POINT ( 'NONE',  ( 19.88284271247461987, 11.69142135624847256, -58.25000000000000000 ) ) ;
#111142=AXIS2_PLACEMENT_3D ( 'NONE', #82343, #64104, #199784 ) ;
#111195=CARTESIAN_POINT ( 'NONE',  ( 20.94999999999999929, -8.999999999988842703, -57.10603087734755690 ) ) ;
#111196=CARTESIAN_POINT ( 'NONE',  ( -20.54999999999999716, 1.115600667400684642E-11, -67.00000000000000000 ) ) ;
#111198=ORIENTED_EDGE ( 'NONE', *, *, #147656, .T. ) ;
#111294=AXIS2_PLACEMENT_3D ( 'NONE', #52444, #210269, #70776 ) ;
#111317=VECTOR ( 'NONE', #191227, 1000.000000000000000 ) ;
#111374=ORIENTED_EDGE ( 'NONE', *, *, #146552, .F. ) ;
#111379=ORIENTED_EDGE ( 'NONE', *, *, #194000, .F. ) ;
#111434=VERTEX_POINT ( 'NONE', #132987 ) ;
#111444=CARTESIAN_POINT ( 'NONE',  ( 23.24999999999999645, 2.100000000011158274, -67.00000000000000000 ) ) ;
#111450=EDGE_CURVE ( 'NONE', #206017, #35453, #74517, .T. ) ;
#111455=EDGE_CURVE ( 'NONE', #254522, #215662, #211846, .T. ) ;
#111456=CARTESIAN_POINT ( 'NONE',  ( 20.94999999999999929, 7.120270961708750512, -70.65956304183931991 ) ) ;
#111462=ORIENTED_EDGE ( 'NONE', *, *, #159256, .T. ) ;
#111519=CARTESIAN_POINT ( 'NONE',  ( 18.49999999999999289, 10.34378108836433263, -58.32844527787764832 ) ) ;
#111531=CARTESIAN_POINT ( 'NONE',  ( 18.59999999999999076, 6.550000000011156231, -54.75000000000000000 ) ) ;
#111587=DIRECTION ( 'NONE',  ( 0.000000000000000000, 0.000000000000000000, -1.000000000000000000 ) ) ;
#111603=DIRECTION ( 'NONE',  ( 1.000000000000000000, 0.000000000000000000, 0.000000000000000000 ) ) ;
#111653=DIRECTION ( 'NONE',  ( 0.7070776581709139474, -0.7071359030027652981, -2.453168425935592377E-14 ) ) ;
#111654=CARTESIAN_POINT ( 'NONE',  ( 20.94999999999999929, 1.115600667400684642E-11, -67.00000000000000000 ) ) ;
#111657=CARTESIAN_POINT ( 'NONE',  ( -20.64999999999999858, 7.250000000011155521, -54.75000000000000000 ) ) ;
#111665=ORIENTED_EDGE ( 'NONE', *, *, #247536, .F. ) ;
#111688=CARTESIAN_POINT ( 'NONE',  ( -21.05000000000000071, 0.09779029131994770863, -27.24218538952388613 ) ) ;
#111707=CARTESIAN_POINT ( 'NONE',  ( 21.10320863425824811, 6.400277386470322405, -33.47497774877286503 ) ) ;
#111737=CARTESIAN_POINT ( 'NONE',  ( -18.50000000000000000, -9.399999999988850163, -73.88204184817267617 ) ) ;
#111749=DIRECTION ( 'NONE',  ( 1.000000000000000000, -7.304098846218134667E-16, -0.000000000000000000 ) ) ;
#111757=ORIENTED_EDGE ( 'NONE', *, *, #133862, .F. ) ;
#111761=DIRECTION ( 'NONE',  ( 0.000000000000000000, 0.000000000000000000, 1.000000000000000000 ) ) ;
#111774=ADVANCED_FACE ( 'NONE', ( #253548 ), #38373, .T. ) ;
#111776=EDGE_LOOP ( 'NONE', ( #197610, #108492, #99825, #16756 ) ) ;
#111777=ORIENTED_EDGE ( 'NONE', *, *, #25227, .T. ) ;
#111780=ORIENTED_EDGE ( 'NONE', *, *, #139903, .F. ) ;
#111814=EDGE_LOOP ( 'NONE', ( #190357, #109750, #32839, #131114 ) ) ;
#111829=DIRECTION ( 'NONE',  ( 4.026293107431335996E-15, -0.8700118002898359348, 0.4930308989875165082 ) ) ;
#111854=FACE_OUTER_BOUND ( 'NONE', #128765, .T. ) ;
#111862=ORIENTED_EDGE ( 'NONE', *, *, #232993, .F. ) ;
#111870=DIRECTION ( 'NONE',  ( 0.7071359030027419834, 0.000000000000000000, 0.7070776581709371511 ) ) ;
#111885=DIRECTION ( 'NONE',  ( 1.000000000000000000, 0.000000000000000000, 0.000000000000000000 ) ) ;
#111947=FACE_OUTER_BOUND ( 'NONE', #215287, .T. ) ;
#111948=CARTESIAN_POINT ( 'NONE',  ( 21.04999999999998650, 6.650000000011155876, -45.75000000000000711 ) ) ;
#111999=CARTESIAN_POINT ( 'NONE',  ( 22.49231231312462853, 11.64998490368843953, -33.43894711239862261 ) ) ;
#112012=CARTESIAN_POINT ( 'NONE',  ( -20.64999999999999858, 1.115600667400684642E-11, -67.00000000000000000 ) ) ;
#112065=ORIENTED_EDGE ( 'NONE', *, *, #150400, .T. ) ;
#112070=ORIENTED_EDGE ( 'NONE', *, *, #99079, .F. ) ;
#112124=CIRCLE ( 'NONE', #182864, 0.4000000000000045186 ) ;
#112126=EDGE_CURVE ( 'NONE', #226768, #67483, #249040, .T. ) ;
#112174=EDGE_LOOP ( 'NONE', ( #90656, #27136, #150635, #73120 ) ) ;
#112180=DIRECTION ( 'NONE',  ( 0.000000000000000000, 0.000000000000000000, -1.000000000000000000 ) ) ;
#112181=EDGE_LOOP ( 'NONE', ( #138674, #3987 ) ) ;
#112196=ORIENTED_EDGE ( 'NONE', *, *, #37502, .T. ) ;
#112211=DIRECTION ( 'NONE',  ( 0.000000000000000000, 1.224646799142015331E-16, 1.000000000000000000 ) ) ;
#112212=CARTESIAN_POINT ( 'NONE',  ( 23.15000000000000213, -11.64999999998883595, -64.00000000000000000 ) ) ;
#112220=CARTESIAN_POINT ( 'NONE',  ( 23.14999999999999503, 11.65000000001116298, -54.75000000000000000 ) ) ;
#112235=DIRECTION ( 'NONE',  ( -2.812466655313719426E-14, 0.1350103645451904977, 0.9908441862701596881 ) ) ;
#112253=ORIENTED_EDGE ( 'NONE', *, *, #196204, .F. ) ;
#112263=EDGE_CURVE ( 'NONE', #150811, #63552, #233071, .T. ) ;
#112289=CARTESIAN_POINT ( 'NONE',  ( 18.58222699835054570, 10.33200063080772324, -72.59316749566428939 ) ) ;
#112302=CIRCLE ( 'NONE', #241299, 0.2000000000000057288 ) ;
#112308=DIRECTION ( 'NONE',  ( -1.000000000000000000, 0.000000000000000000, 0.000000000000000000 ) ) ;
#112316=CARTESIAN_POINT ( 'NONE',  ( -22.37643362114956957, 0.09908137369253962323, -25.87421000604160426 ) ) ;
#112317=CARTESIAN_POINT ( 'NONE',  ( -20.54999999999999716, -8.999999999988844479, -57.50603087734755547 ) ) ;
#112390=ORIENTED_EDGE ( 'NONE', *, *, #252188, .F. ) ;
#112405=ORIENTED_EDGE ( 'NONE', *, *, #175980, .F. ) ;
#112410=DIRECTION ( 'NONE',  ( 0.000000000000000000, -0.8660254037844411501, -0.4999999999999956701 ) ) ;
#112424=EDGE_CURVE ( 'NONE', #73797, #85875, #179278, .T. ) ;
#112433=AXIS2_PLACEMENT_3D ( 'NONE', #204923, #26314, #105810 ) ;
#112450=EDGE_LOOP ( 'NONE', ( #58670, #232843, #37972, #133051 ) ) ;
#112463=EDGE_LOOP ( 'NONE', ( #57834, #216742, #238722, #209870 ) ) ;
#112468=DIRECTION ( 'NONE',  ( 1.000000000000000000, -0.000000000000000000, -0.000000000000000000 ) ) ;
#112473=DIRECTION ( 'NONE',  ( -0.000000000000000000, -0.000000000000000000, 1.000000000000000000 ) ) ;
#112517=CARTESIAN_POINT ( 'NONE',  ( -21.12230431290519661, 6.457566653304161797, -33.49479014831099022 ) ) ;
#112564=AXIS2_PLACEMENT_3D ( 'NONE', #189802, #50266, #75014 ) ;
#112575=ORIENTED_EDGE ( 'NONE', *, *, #164519, .F. ) ;
#112630=FACE_OUTER_BOUND ( 'NONE', #87345, .T. ) ;
#112642=EDGE_CURVE ( 'NONE', #134912, #173389, #159026, .T. ) ;
#112650=CARTESIAN_POINT ( 'NONE',  ( 20.94999999999999929, -9.499999999988844479, -57.10603087734755690 ) ) ;
#112683=CYLINDRICAL_SURFACE ( 'NONE', #32397, 0.09999999999999939493 ) ;
#112693=EDGE_CURVE ( 'NONE', #69658, #78788, #187647, .T. ) ;
#112843=DIRECTION ( 'NONE',  ( 0.000000000000000000, 0.000000000000000000, -1.000000000000000000 ) ) ;
#112850=DIRECTION ( 'NONE',  ( 0.000000000000000000, 0.008583690987128059571, -0.9999631594459056361 ) ) ;
#112853=LINE ( 'NONE', #197510, #91881 ) ;
#112854=DIRECTION ( 'NONE',  ( 0.000000000000000000, 0.000000000000000000, 1.000000000000000000 ) ) ;
#112860=EDGE_LOOP ( 'NONE', ( #162581, #233914, #139166, #163638 ) ) ;
#112871=ADVANCED_FACE ( 'NONE', ( #37469 ), #94847, .T. ) ;
#112873=LINE ( 'NONE', #55426, #91332 ) ;
#112931=ADVANCED_FACE ( 'NONE', ( #182104 ), #183535, .F. ) ;
#112948=CARTESIAN_POINT ( 'NONE',  ( 20.04142135391667168, 11.75000000001116263, -58.20250686563003484 ) ) ;
#112985=AXIS2_PLACEMENT_3D ( 'NONE', #93634, #74108, #212318 ) ;
#112990=CARTESIAN_POINT ( 'NONE',  ( 20.85000000000000142, 6.982009704867603972, -70.69615211825629331 ) ) ;
#113006=DIRECTION ( 'NONE',  ( -0.1538461538461510236, 0.9880948137434718559, 0.000000000000000000 ) ) ;
#113032=DIRECTION ( 'NONE',  ( 0.000000000000000000, 0.000000000000000000, -1.000000000000000000 ) ) ;
#113042=CARTESIAN_POINT ( 'NONE',  ( -22.59080734064477625, 11.75000000001115907, -33.46925029190298773 ) ) ;
#113065=EDGE_CURVE ( 'NONE', #231120, #53755, #110251, .T. ) ;
#113153=DIRECTION ( 'NONE',  ( 0.000000000000000000, 1.000000000000000000, 0.000000000000000000 ) ) ;
#113161=CIRCLE ( 'NONE', #8931, 0.6000000000000033085 ) ;
#113194=DIRECTION ( 'NONE',  ( 1.000000000000000000, -0.000000000000000000, -0.000000000000000000 ) ) ;
#113225=CARTESIAN_POINT ( 'NONE',  ( 23.14999999999999858, -2.099999999988846344, -67.00000000000000000 ) ) ;
#113231=CARTESIAN_POINT ( 'NONE',  ( -23.25000000000000000, 1.115600667400684642E-11, -37.54999999999999716 ) ) ;
#113259=EDGE_LOOP ( 'NONE', ( #250814, #188640, #54196, #2922 ) ) ;
#113271=LINE ( 'NONE', #55827, #164765 ) ;
#113309=CARTESIAN_POINT ( 'NONE',  ( -21.14999999999999858, -0.09999999998884338825, -21.85042919245520210 ) ) ;
#113322=ORIENTED_EDGE ( 'NONE', *, *, #55778, .T. ) ;
#113371=ORIENTED_EDGE ( 'NONE', *, *, #240800, .F. ) ;
#113375=FACE_OUTER_BOUND ( 'NONE', #235708, .T. ) ;
#113415=VERTEX_POINT ( 'NONE', #13115 ) ;
#113442=CARTESIAN_POINT ( 'NONE',  ( -22.00356870141260401, 7.254242362502188790, -33.49999999999084821 ) ) ;
#113447=CARTESIAN_POINT ( 'NONE',  ( 20.94999999999999574, -11.48912529306490349, -36.39999999999999858 ) ) ;
#113537=DIRECTION ( 'NONE',  ( 0.000000000000000000, -0.9915357197604792727, 0.1298341882520475943 ) ) ;
#113544=LINE ( 'NONE', #107447, #45787 ) ;
#113587=ORIENTED_EDGE ( 'NONE', *, *, #187380, .F. ) ;
#113611=EDGE_LOOP ( 'NONE', ( #59776, #23113, #61239 ) ) ;
#113622=AXIS2_PLACEMENT_3D ( 'NONE', #3130, #120559, #61852 ) ;
#113628=EDGE_CURVE ( 'NONE', #145358, #197707, #6366, .T. ) ;
#113637=EDGE_LOOP ( 'NONE', ( #85379, #202966, #148674, #142192 ) ) ;
#113645=CIRCLE ( 'NONE', #130567, 0.1999999999999996503 ) ;
#113650=DIRECTION ( 'NONE',  ( -2.952720810173289112E-16, 1.000000000000000000, 0.000000000000000000 ) ) ;
#113651=AXIS2_PLACEMENT_3D ( 'NONE', #126841, #124286, #188103 ) ;
#113656=AXIS2_PLACEMENT_3D ( 'NONE', #164479, #136199, #76249 ) ;
#113658=CARTESIAN_POINT ( 'NONE',  ( 21.14999999999999858, 10.71339244341104013, -45.75000000000000711 ) ) ;
#113662=EDGE_LOOP ( 'NONE', ( #177227, #207024, #26623, #73816 ) ) ;
#113679=AXIS2_PLACEMENT_3D ( 'NONE', #256779, #242397, #226686 ) ;
#113687=VECTOR ( 'NONE', #27417, 1000.000000000000114 ) ;
#113688=TOROIDAL_SURFACE ( 'NONE', #76083, 11.89999999999999858, 0.1000000000000000056 ) ;
#113714=VERTEX_POINT ( 'NONE', #131455 ) ;
#113731=DIRECTION ( 'NONE',  ( 1.000000000000000000, 2.952720810173289112E-16, -0.000000000000000000 ) ) ;
#113775=DIRECTION ( 'NONE',  ( -1.000000000000000000, -0.000000000000000000, -0.000000000000000000 ) ) ;
#113850=CIRCLE ( 'NONE', #213813, 0.1000000000000028644 ) ;
#113854=DIRECTION ( 'NONE',  ( -0.000000000000000000, 0.000000000000000000, -1.000000000000000000 ) ) ;
#113862=ADVANCED_FACE ( 'NONE', ( #19210 ), #236979, .F. ) ;
#113872=CARTESIAN_POINT ( 'NONE',  ( -20.94999999999999929, 11.65000000001115232, -60.21613433702190576 ) ) ;
#113880=VECTOR ( 'NONE', #40239, 1000.000000000000000 ) ;
#113909=DIRECTION ( 'NONE',  ( 1.000000000000000000, 0.000000000000000000, 0.000000000000000000 ) ) ;
#113926=VECTOR ( 'NONE', #5930, 1000.000000000000000 ) ;
#113931=CARTESIAN_POINT ( 'NONE',  ( -20.54999999999999716, 1.940186915899004161, -54.17088078894667547 ) ) ;
#113932=ORIENTED_EDGE ( 'NONE', *, *, #60221, .T. ) ;
#113969=VERTEX_POINT ( 'NONE', #231863 ) ;
#114001=ORIENTED_EDGE ( 'NONE', *, *, #25515, .T. ) ;
#114059=AXIS2_PLACEMENT_3D ( 'NONE', #76147, #16211, #38330 ) ;
#114062=DIRECTION ( 'NONE',  ( 0.000000000000000000, 0.000000000000000000, 1.000000000000000000 ) ) ;
#114136=DIRECTION ( 'NONE',  ( 1.000000000000000000, 0.000000000000000000, 0.000000000000000000 ) ) ;
#114139=VECTOR ( 'NONE', #90622, 1000.000000000000000 ) ;
#114282=ORIENTED_EDGE ( 'NONE', *, *, #1096, .F. ) ;
#114292=AXIS2_PLACEMENT_3D ( 'NONE', #113309, #76743, #57160 ) ;
#114343=CIRCLE ( 'NONE', #193472, 0.1000000000000028644 ) ;
#114353=ORIENTED_EDGE ( 'NONE', *, *, #242793, .F. ) ;
#114370=DIRECTION ( 'NONE',  ( -1.000000000000000000, -0.000000000000000000, -0.000000000000000000 ) ) ;
#114413=ADVANCED_FACE ( 'NONE', ( #34637 ), #137547, .T. ) ;
#114416=DIRECTION ( 'NONE',  ( 1.296989514748957922E-15, -0.9887567792719341719, 0.1495327102803664099 ) ) ;
#114454=CARTESIAN_POINT ( 'NONE',  ( 20.94999999999999929, 1.115600667400684642E-11, -67.00000000000000000 ) ) ;
#114458=CARTESIAN_POINT ( 'NONE',  ( -20.64999999999999858, 7.150000000011155876, -54.65000000000000568 ) ) ;
#114467=EDGE_CURVE ( 'NONE', #43703, #225394, #242520, .T. ) ;
#114480=ADVANCED_FACE ( 'NONE', ( #179290 ), #118000, .T. ) ;
#114507=EDGE_LOOP ( 'NONE', ( #190026, #104801, #69434, #88655 ) ) ;
#114509=EDGE_CURVE ( 'NONE', #195077, #163280, #194448, .T. ) ;
#114520=CIRCLE ( 'NONE', #214467, 0.09999999999999971412 ) ;
#114541=CIRCLE ( 'NONE', #156263, 0.1000000000000017958 ) ;
#114553=CARTESIAN_POINT ( 'NONE',  ( 22.48970261584622321, 11.65000000001115588, -33.44463051178259860 ) ) ;
#114557=CARTESIAN_POINT ( 'NONE',  ( -21.22070241538126112, 6.469946272880768845, -33.40108096946497795 ) ) ;
#114559=CARTESIAN_POINT ( 'NONE',  ( 20.85000000000000142, 0.1610488207298751417, -66.71581015563977246 ) ) ;
#114587=CIRCLE ( 'NONE', #131141, 4.149999999999999467 ) ;
#114590=CARTESIAN_POINT ( 'NONE',  ( -20.85000000000000142, -0.3238857010591806307, -66.95758958931398297 ) ) ;
#114616=CARTESIAN_POINT ( 'NONE',  ( 21.30000000000002558, 1.115600667400684642E-11, -37.54999999999999716 ) ) ;
#114619=DIRECTION ( 'NONE',  ( 1.000000000000000000, 0.000000000000000000, -0.000000000000000000 ) ) ;
#114697=DIRECTION ( 'NONE',  ( 0.000000000000000000, 0.000000000000000000, -1.000000000000000000 ) ) ;
#114699=CARTESIAN_POINT ( 'NONE',  ( -21.14999999999999858, 1.115600667400684642E-11, -33.50000000000000000 ) ) ;
#114702=FACE_OUTER_BOUND ( 'NONE', #7415, .T. ) ;
#114707=AXIS2_PLACEMENT_3D ( 'NONE', #131180, #17363, #52929 ) ;
#114714=DIRECTION ( 'NONE',  ( -1.000000000000000000, 0.000000000000000000, 0.000000000000000000 ) ) ;
#114715=EDGE_CURVE ( 'NONE', #217175, #22291, #63, .T. ) ;
#114724=DIRECTION ( 'NONE',  ( 0.000000000000000000, 0.000000000000000000, -1.000000000000000000 ) ) ;
#114728=CYLINDRICAL_SURFACE ( 'NONE', #131926, 0.1000000000000028644 ) ;
#114736=DIRECTION ( 'NONE',  ( 0.000000000000000000, 0.000000000000000000, -1.000000000000000000 ) ) ;
#114740=DIRECTION ( 'NONE',  ( 0.000000000000000000, -0.000000000000000000, -1.000000000000000000 ) ) ;
#114755=CARTESIAN_POINT ( 'NONE',  ( 22.39999999999999503, 1.115600667400684642E-11, -21.85042919245520210 ) ) ;
#114769=CARTESIAN_POINT ( 'NONE',  ( -21.14999999999999858, -11.74999999998884448, -33.50000000000000000 ) ) ;
#114770=AXIS2_PLACEMENT_3D ( 'NONE', #96094, #214770, #77817 ) ;
#114776=DIRECTION ( 'NONE',  ( 0.000000000000000000, -1.000000000000000000, 0.000000000000000000 ) ) ;
#114848=CARTESIAN_POINT ( 'NONE',  ( -2.995603634470884209E-16, -11.74999999998884448, -54.75000000000000000 ) ) ;
#114852=EDGE_LOOP ( 'NONE', ( #182573, #242578, #197804 ) ) ;
#114857=AXIS2_PLACEMENT_3D ( 'NONE', #144745, #82191, #224294 ) ;
#114861=CARTESIAN_POINT ( 'NONE',  ( -23.25000000000000000, 11.75000000001115552, -54.84999999999999432 ) ) ;
#114866=ADVANCED_FACE ( 'NONE', ( #125169 ), #169461, .T. ) ;
#114867=CARTESIAN_POINT ( 'NONE',  ( -21.53551880898957904, 0.09896973458281840830, -26.71520223858367160 ) ) ;
#114869=DIRECTION ( 'NONE',  ( 0.000000000000000000, 0.8660254037844352659, -0.5000000000000058842 ) ) ;
#114897=ORIENTED_EDGE ( 'NONE', *, *, #98136, .T. ) ;
#114899=CIRCLE ( 'NONE', #210568, 0.1000000000000028644 ) ;
#114904=AXIS2_PLACEMENT_3D ( 'NONE', #185343, #167101, #125376 ) ;
#114909=TOROIDAL_SURFACE ( 'NONE', #243890, 0.6000000000000009770, 0.1000000000000000056 ) ;
#114938=CIRCLE ( 'NONE', #214885, 0.1000000000000028644 ) ;
#114940=ORIENTED_EDGE ( 'NONE', *, *, #158991, .F. ) ;
#114963=ORIENTED_EDGE ( 'NONE', *, *, #246052, .T. ) ;
#114974=AXIS2_PLACEMENT_3D ( 'NONE', #169583, #213791, #71731 ) ;
#114989=DIRECTION ( 'NONE',  ( 1.000000000000000000, -7.304098846218135653E-16, 0.000000000000000000 ) ) ;
#115004=EDGE_CURVE ( 'NONE', #177537, #17741, #151331, .T. ) ;
#115015=ORIENTED_EDGE ( 'NONE', *, *, #179889, .F. ) ;
#115016=EDGE_CURVE ( 'NONE', #215662, #184556, #9832, .T. ) ;
#115020=ADVANCED_FACE ( 'NONE', ( #93728, #52016 ), #55853, .F. ) ;
#115045=AXIS2_PLACEMENT_3D ( 'NONE', #247390, #10076, #70080 ) ;
#115064=DIRECTION ( 'NONE',  ( -1.000000000000000000, -2.952720810173289112E-16, 0.000000000000000000 ) ) ;
#115098=DIRECTION ( 'NONE',  ( 0.000000000000000000, 0.000000000000000000, -1.000000000000000000 ) ) ;
#115188=EDGE_CURVE ( 'NONE', #64202, #250227, #30524, .T. ) ;
#115208=CARTESIAN_POINT ( 'NONE',  ( 23.14999999999999858, 5.500000000011153745, -54.59473398108690390 ) ) ;
#115240=ADVANCED_FACE ( 'NONE', ( #138603 ), #93041, .T. ) ;
#115249=LINE ( 'NONE', #215620, #210464 ) ;
#115264=VERTEX_POINT ( 'NONE', #113931 ) ;
#115276=DIRECTION ( 'NONE',  ( -0.7070776581708965169, -0.7071359030027827286, -0.000000000000000000 ) ) ;
#115299=EDGE_CURVE ( 'NONE', #45873, #121232, #55584, .T. ) ;
#115362=CARTESIAN_POINT ( 'NONE',  ( -23.15000000000000213, 11.75000000001115552, -33.50000000000000000 ) ) ;
#115366=ADVANCED_FACE ( 'NONE', ( #201178 ), #139900, .F. ) ;
#115395=DIRECTION ( 'NONE',  ( 0.000000000000000000, 0.1568667991644863147, -0.9876197685951252359 ) ) ;
#115399=DIRECTION ( 'NONE',  ( 1.000000000000000000, -0.000000000000000000, -0.000000000000000000 ) ) ;
#115434=ORIENTED_EDGE ( 'NONE', *, *, #17879, .F. ) ;
#115438=DIRECTION ( 'NONE',  ( 1.000000000000000000, 3.265361837132813093E-16, -0.000000000000000000 ) ) ;
#115441=CYLINDRICAL_SURFACE ( 'NONE', #105315, 0.1000000000000028644 ) ;
#115461=LINE ( 'NONE', #243118, #159744 ) ;
#115471=CIRCLE ( 'NONE', #215436, 0.09999999999999939493 ) ;
#115481=LINE ( 'NONE', #174225, #145 ) ;
#115487=ORIENTED_EDGE ( 'NONE', *, *, #102290, .F. ) ;
#115496=AXIS2_PLACEMENT_3D ( 'NONE', #239251, #24077, #103561 ) ;
#115503=ORIENTED_EDGE ( 'NONE', *, *, #54382, .F. ) ;
#115520=ORIENTED_EDGE ( 'NONE', *, *, #236251, .F. ) ;
#115535=ORIENTED_EDGE ( 'NONE', *, *, #212159, .F. ) ;
#115564=ORIENTED_EDGE ( 'NONE', *, *, #88989, .T. ) ;
#115571=CARTESIAN_POINT ( 'NONE',  ( -23.15000000000000213, -9.599999999988845900, -57.10603087734755690 ) ) ;
#115583=DIRECTION ( 'NONE',  ( -0.7071067811865475727, -0.7071067811865475727, 0.000000000000000000 ) ) ;
#115606=DIRECTION ( 'NONE',  ( 0.000000000000000000, -1.000000000000000000, 0.000000000000000000 ) ) ;
#115653=VECTOR ( 'NONE', #157010, 1000.000000000000000 ) ;
#115656=ORIENTED_EDGE ( 'NONE', *, *, #127896, .T. ) ;
#115688=VERTEX_POINT ( 'NONE', #193193 ) ;
#115703=ORIENTED_EDGE ( 'NONE', *, *, #17879, .T. ) ;
#115718=ORIENTED_EDGE ( 'NONE', *, *, #212079, .T. ) ;
#115735=ORIENTED_EDGE ( 'NONE', *, *, #63460, .T. ) ;
#115742=CARTESIAN_POINT ( 'NONE',  ( -20.94999999999999929, -11.64999999998884306, -36.60000000000000853 ) ) ;
#115767=AXIS2_PLACEMENT_3D ( 'NONE', #17391, #215576, #36983 ) ;
#115783=ORIENTED_EDGE ( 'NONE', *, *, #225532, .T. ) ;
#115789=TOROIDAL_SURFACE ( 'NONE', #7450, 12.77500000000000036, 0.1000000000000000056 ) ;
#115806=CARTESIAN_POINT ( 'NONE',  ( 21.30000000000002558, 1.115600667400684642E-11, -29.45000000000000284 ) ) ;
#115807=CARTESIAN_POINT ( 'NONE',  ( -18.41353343127310538, -9.499999999988848032, -40.53206939669965436 ) ) ;
#115833=AXIS2_PLACEMENT_3D ( 'NONE', #199692, #139664, #95428 ) ;
#115837=CARTESIAN_POINT ( 'NONE',  ( -21.78635804494510708, 7.035661485164336426, -33.40099493449231716 ) ) ;
#115859=EDGE_CURVE ( 'NONE', #107516, #159940, #38683, .T. ) ;
#115888=DIRECTION ( 'NONE',  ( 1.000000000000000000, -0.000000000000000000, -0.000000000000000000 ) ) ;
#115894=DIRECTION ( 'NONE',  ( 0.000000000000000000, 1.000000000000000000, 0.000000000000000000 ) ) ;
#115906=EDGE_CURVE ( 'NONE', #255180, #99123, #6519, .T. ) ;
#115919=CIRCLE ( 'NONE', #24354, 0.1999999999999987899 ) ;
#115920=DIRECTION ( 'NONE',  ( 0.000000000000000000, 2.891205793294679805E-16, -1.000000000000000000 ) ) ;
#115972=ADVANCED_FACE ( 'NONE', ( #151183 ), #238592, .F. ) ;
#115974=EDGE_LOOP ( 'NONE', ( #41033, #124566, #154081 ) ) ;
#115997=VECTOR ( 'NONE', #222624, 1000.000000000000000 ) ;
#116020=CARTESIAN_POINT ( 'NONE',  ( -21.00448002041600759, 11.75000000001115730, -40.34834086231045802 ) ) ;
#116043=VERTEX_POINT ( 'NONE', #93758 ) ;
#116053=CARTESIAN_POINT ( 'NONE',  ( 22.49066049874202022, 0.05634325154338428593, -21.84998776248290042 ) ) ;
#116057=DIRECTION ( 'NONE',  ( -7.304098846218134667E-16, -1.000000000000000000, 0.000000000000000000 ) ) ;
#116062=CARTESIAN_POINT ( 'NONE',  ( 18.60000000000000142, -9.321008403350125704, -40.73593824907789696 ) ) ;
#116064=ORIENTED_EDGE ( 'NONE', *, *, #115906, .T. ) ;
#116114=EDGE_CURVE ( 'NONE', #39510, #74897, #121065, .T. ) ;
#116132=ORIENTED_EDGE ( 'NONE', *, *, #185083, .T. ) ;
#116169=VECTOR ( 'NONE', #230623, 1000.000000000000000 ) ;
#116181=VERTEX_POINT ( 'NONE', #178466 ) ;
#116183=CIRCLE ( 'NONE', #37078, 12.87499999999999822 ) ;
#116259=ORIENTED_EDGE ( 'NONE', *, *, #202124, .F. ) ;
#116293=CARTESIAN_POINT ( 'NONE',  ( -20.85000000000000142, 7.021664781911246322, -70.83356540189728889 ) ) ;
#116319=AXIS2_PLACEMENT_3D ( 'NONE', #91418, #232225, #52258 ) ;
#116322=DIRECTION ( 'NONE',  ( 1.000000000000000000, 0.000000000000000000, 0.000000000000000000 ) ) ;
#116341=AXIS2_PLACEMENT_3D ( 'NONE', #171553, #48999, #208099 ) ;
#116363=CARTESIAN_POINT ( 'NONE',  ( 20.12500000000000000, 9.750000000011153745, -54.75000000000000000 ) ) ;
#116382=CIRCLE ( 'NONE', #66319, 11.65000000000000036 ) ;
#116394=DIRECTION ( 'NONE',  ( 1.000000000000000000, 0.000000000000000000, 0.000000000000000000 ) ) ;
#116396=DIRECTION ( 'NONE',  ( 0.000000000000000000, 0.000000000000000000, -1.000000000000000000 ) ) ;
#116407=CYLINDRICAL_SURFACE ( 'NONE', #176089, 0.1000000000000028644 ) ;
#116416=DIRECTION ( 'NONE',  ( 2.952720810173289112E-16, -1.000000000000000000, 0.000000000000000000 ) ) ;
#116423=EDGE_CURVE ( 'NONE', #145358, #9191, #150537, .T. ) ;
#116449=ORIENTED_EDGE ( 'NONE', *, *, #33516, .F. ) ;
#116469=AXIS2_PLACEMENT_3D ( 'NONE', #244598, #182077, #185916 ) ;
#116480=DIRECTION ( 'NONE',  ( 0.000000000000000000, 0.000000000000000000, -1.000000000000000000 ) ) ;
#116483=EDGE_CURVE ( 'NONE', #140969, #139968, #1621, .T. ) ;
#116494=CARTESIAN_POINT ( 'NONE',  ( 23.15000000000000213, -8.663551401857999323, -57.47589888193269303 ) ) ;
#116552=ORIENTED_EDGE ( 'NONE', *, *, #170019, .T. ) ;
#116556=VERTEX_POINT ( 'NONE', #58154 ) ;
#116626=AXIS2_PLACEMENT_3D ( 'NONE', #63765, #41662, #143301 ) ;
#116654=ORIENTED_EDGE ( 'NONE', *, *, #49365, .T. ) ;
#116696=DIRECTION ( 'NONE',  ( 1.000000000000000000, 0.000000000000000000, 0.000000000000000000 ) ) ;
#116734=ORIENTED_EDGE ( 'NONE', *, *, #15627, .F. ) ;
#116737=ORIENTED_EDGE ( 'NONE', *, *, #3981, .T. ) ;
#116763=CARTESIAN_POINT ( 'NONE',  ( 22.50000000000000000, 0.1000000000111554016, -21.75000000000000355 ) ) ;
#116824=FACE_OUTER_BOUND ( 'NONE', #100512, .T. ) ;
#116825=DIRECTION ( 'NONE',  ( 1.000000000000000000, 0.000000000000000000, 0.000000000000000000 ) ) ;
#116831=EDGE_CURVE ( 'NONE', #78788, #200509, #147564, .T. ) ;
#116871=CIRCLE ( 'NONE', #216828, 11.74999999999999645 ) ;
#116876=DIRECTION ( 'NONE',  ( 0.000000000000000000, -0.8660254037844383745, 0.5000000000000003331 ) ) ;
#116878=CARTESIAN_POINT ( 'NONE',  ( 20.95224633520496127, 8.900522166568386240, -41.99327644792126790 ) ) ;
#116886=AXIS2_PLACEMENT_3D ( 'NONE', #53839, #10866, #69562 ) ;
#116887=ORIENTED_EDGE ( 'NONE', *, *, #54084, .T. ) ;
#116914=EDGE_LOOP ( 'NONE', ( #233236, #105947, #174692, #128989 ) ) ;
#116920=DIRECTION ( 'NONE',  ( -1.000000000000000000, 0.000000000000000000, 0.000000000000000000 ) ) ;
#116923=FACE_OUTER_BOUND ( 'NONE', #212366, .T. ) ;
#116937=AXIS2_PLACEMENT_3D ( 'NONE', #68860, #10158, #166693 ) ;
#116963=CARTESIAN_POINT ( 'NONE',  ( 23.14999999999999858, -3.899999999988843502, -67.00000000000000000 ) ) ;
#116967=ORIENTED_EDGE ( 'NONE', *, *, #240472, .F. ) ;
#116989=DIRECTION ( 'NONE',  ( 0.000000000000000000, -0.8660254037844412611, -0.4999999999999956701 ) ) ;
#117012=ADVANCED_FACE ( 'NONE', ( #104358 ), #143504, .T. ) ;
#117034=CARTESIAN_POINT ( 'NONE',  ( 18.59999999999999076, 1.115600667400684642E-11, -67.00000000000000000 ) ) ;
#117035=AXIS2_PLACEMENT_3D ( 'NONE', #37607, #196649, #218771 ) ;
#117037=ORIENTED_EDGE ( 'NONE', *, *, #229178, .T. ) ;
#117045=DIRECTION ( 'NONE',  ( 0.000000000000000000, -0.3738317757009345654, 0.9274965247785492695 ) ) ;
#117053=DIRECTION ( 'NONE',  ( 0.000000000000000000, 0.000000000000000000, -1.000000000000000000 ) ) ;
#117055=CARTESIAN_POINT ( 'NONE',  ( -18.59999999999999787, 9.350000000011156942, -54.75000000000000000 ) ) ;
#117095=CARTESIAN_POINT ( 'NONE',  ( -18.59999999999999787, -1.835341550213255957, -45.05515129256298223 ) ) ;
#117120=EDGE_LOOP ( 'NONE', ( #138988, #136315, #133176, #201842, #161511, #218171, #156688, #220061, #145322, #178223, #3306, #68095, #137801, #63161, #22092, #110899, #240738, #32704, #68104, #253459, #207705, #94498, #169115, #47650, #250863, #101590, #116552 ) ) ;
#117139=CARTESIAN_POINT ( 'NONE',  ( 21.05000000000000071, 5.850000000011156942, -56.86750277572208034 ) ) ;
#117172=CYLINDRICAL_SURFACE ( 'NONE', #196209, 0.5000000000000004441 ) ;
#117174=VECTOR ( 'NONE', #133969, 1000.000000000000000 ) ;
#117203=LINE ( 'NONE', #58483, #195717 ) ;
#117204=FACE_OUTER_BOUND ( 'NONE', #185740, .T. ) ;
#117207=ORIENTED_EDGE ( 'NONE', *, *, #22072, .T. ) ;
#117222=ORIENTED_EDGE ( 'NONE', *, *, #127211, .F. ) ;
#117247=VERTEX_POINT ( 'NONE', #67821 ) ;
#117268=ORIENTED_EDGE ( 'NONE', *, *, #142983, .F. ) ;
#117326=B_SPLINE_CURVE_WITH_KNOTS ( 'NONE', 3,
 ( #142131, #122591, #202114, #23511, #97838, #102990, #177444, #256896, #157899, #58717, #138260, #126419, #204660, #186416, #205957, #188968, #109412, #222942, #10345 ),
 .UNSPECIFIED., .F., .F.,
 ( 4, 3, 3, 3, 3, 3, 4 ),
 ( 0.000000000000000000, 1.655171619026035414E-05, 2.773500582848518044E-05, 5.941817267378563579E-05, 0.0001114174635873545742, 0.0001914169455916377854, 0.0002627181070750677803 ),
 .UNSPECIFIED. ) ;
#117358=VECTOR ( 'NONE', #222504, 1000.000000000000000 ) ;
#117414=ORIENTED_EDGE ( 'NONE', *, *, #243758, .T. ) ;
#117428=AXIS2_PLACEMENT_3D ( 'NONE', #243484, #64843, #124837 ) ;
#117448=CARTESIAN_POINT ( 'NONE',  ( -21.93642651522410247, 7.327166239336959208, -33.50000000000000000 ) ) ;
#117464=DIRECTION ( 'NONE',  ( 0.000000000000000000, 0.000000000000000000, -1.000000000000000000 ) ) ;
#117465=DIRECTION ( 'NONE',  ( -1.000000000000000000, 0.000000000000000000, 0.000000000000000000 ) ) ;
#117504=DIRECTION ( 'NONE',  ( -1.000000000000000000, -0.000000000000000000, 0.000000000000000000 ) ) ;
#117553=DIRECTION ( 'NONE',  ( -0.000000000000000000, -0.000000000000000000, 1.000000000000000000 ) ) ;
#117565=ORIENTED_EDGE ( 'NONE', *, *, #134033, .T. ) ;
#117568=ADVANCED_FACE ( 'NONE', ( #6241 ), #83436, .T. ) ;
#117585=LINE ( 'NONE', #19785, #45580 ) ;
#117619=DIRECTION ( 'NONE',  ( -0.000000000000000000, 0.8660254037844502539, 0.4999999999999799050 ) ) ;
#117650=DIRECTION ( 'NONE',  ( -1.000000000000000000, 0.000000000000000000, 0.000000000000000000 ) ) ;
#117670=DIRECTION ( 'NONE',  ( 1.000000000000000000, 0.000000000000000000, 0.000000000000000000 ) ) ;
#117712=VECTOR ( 'NONE', #229679, 1000.000000000000000 ) ;
#117713=FACE_OUTER_BOUND ( 'NONE', #167833, .T. ) ;
#117730=EDGE_CURVE ( 'NONE', #150811, #73797, #62632, .T. ) ;
#117732=ORIENTED_EDGE ( 'NONE', *, *, #112693, .F. ) ;
#117759=DIRECTION ( 'NONE',  ( 0.000000000000000000, 0.000000000000000000, -1.000000000000000000 ) ) ;
#117767=VERTEX_POINT ( 'NONE', #39970 ) ;
#117773=DIRECTION ( 'NONE',  ( 0.000000000000000000, 6.308085367182471812E-16, 1.000000000000000000 ) ) ;
#117775=DIRECTION ( 'NONE',  ( 0.000000000000000000, -1.000000000000000000, 0.000000000000000000 ) ) ;
#117803=TOROIDAL_SURFACE ( 'NONE', #167906, 1.900000000000002576, 0.1000000000000000056 ) ;
#117848=CARTESIAN_POINT ( 'NONE',  ( 20.94999999999999929, 1.115600667400684642E-11, -71.00000000000001421 ) ) ;
#117853=FACE_OUTER_BOUND ( 'NONE', #251255, .T. ) ;
#117856=AXIS2_PLACEMENT_3D ( 'NONE', #28156, #55047, #212873 ) ;
#117868=CARTESIAN_POINT ( 'NONE',  ( 20.85000000000000142, -1.835859311432481045, -78.60443916879853532 ) ) ;
#117889=VECTOR ( 'NONE', #78822, 1000.000000000000000 ) ;
#117907=VECTOR ( 'NONE', #237834, 1000.000000000000000 ) ;
#117937=CARTESIAN_POINT ( 'NONE',  ( -20.64999999999999858, 1.115600667400684642E-11, -68.90000000000000568 ) ) ;
#117965=AXIS2_PLACEMENT_3D ( 'NONE', #223595, #41159, #63248 ) ;
#117984=CYLINDRICAL_SURFACE ( 'NONE', #148356, 4.000000000000003553 ) ;
#118000=CYLINDRICAL_SURFACE ( 'NONE', #238421, 0.1000000000000028644 ) ;
#118010=CARTESIAN_POINT ( 'NONE',  ( -21.05000000000000071, -0.09999999998884473440, -26.95934304829875927 ) ) ;
#118028=AXIS2_PLACEMENT_3D ( 'NONE', #205423, #4650, #105005 ) ;
#118064=ORIENTED_EDGE ( 'NONE', *, *, #203904, .F. ) ;
#118101=CARTESIAN_POINT ( 'NONE',  ( 20.85000000000000142, -11.64999999998883595, -67.00000000000000000 ) ) ;
#118103=VECTOR ( 'NONE', #191718, 1000.000000000000000 ) ;
#118119=CARTESIAN_POINT ( 'NONE',  ( -1.739115166359751801E-14, 11.65000000001114699, -58.35000000000000142 ) ) ;
#118127=ORIENTED_EDGE ( 'NONE', *, *, #3900, .F. ) ;
#118149=CARTESIAN_POINT ( 'NONE',  ( 23.14999999999999503, 11.75000000001116263, -54.85000000000000142 ) ) ;
#118167=LINE ( 'NONE', #119463, #248368 ) ;
#118207=CARTESIAN_POINT ( 'NONE',  ( 20.94999999999999929, 11.65000000001116121, -60.21613433702191287 ) ) ;
#118244=CARTESIAN_POINT ( 'NONE',  ( -21.05000000000000071, -1.162701749926853712, -41.60000000000000142 ) ) ;
#118247=DIRECTION ( 'NONE',  ( 0.000000000000000000, 0.000000000000000000, -1.000000000000000000 ) ) ;
#118248=ORIENTED_EDGE ( 'NONE', *, *, #60994, .F. ) ;
#118255=DIRECTION ( 'NONE',  ( 0.000000000000000000, 0.000000000000000000, -1.000000000000000000 ) ) ;
#118272=ORIENTED_EDGE ( 'NONE', *, *, #243309, .F. ) ;
#118289=DIRECTION ( 'NONE',  ( 1.000000000000000000, 0.000000000000000000, 0.000000000000000000 ) ) ;
#118329=DIRECTION ( 'NONE',  ( 0.000000000000000000, 0.000000000000000000, 1.000000000000000000 ) ) ;
#118358=CARTESIAN_POINT ( 'NONE',  ( 20.50589344625181809, 10.48318793148705019, -41.07299497867204252 ) ) ;
#118364=FACE_OUTER_BOUND ( 'NONE', #156252, .T. ) ;
#118382=CARTESIAN_POINT ( 'NONE',  ( -18.49999999999997868, -9.321008403350143467, -40.73593824907786853 ) ) ;
#118412=AXIS2_PLACEMENT_3D ( 'NONE', #122379, #217596, #235889 ) ;
#118415=PLANE ( 'NONE',  #134578 ) ;
#118445=VERTEX_POINT ( 'NONE', #72351 ) ;
#118457=DIRECTION ( 'NONE',  ( 0.000000000000000000, 0.9915357197604792727, -0.1298341882520475943 ) ) ;
#118464=CYLINDRICAL_SURFACE ( 'NONE', #100324, 0.1000000000000028644 ) ;
#118475=EDGE_CURVE ( 'NONE', #226447, #137736, #208011, .T. ) ;
#118496=PLANE ( 'NONE',  #84381 ) ;
#118525=EDGE_CURVE ( 'NONE', #179315, #143470, #124782, .T. ) ;
#118543=EDGE_CURVE ( 'NONE', #195498, #191837, #220650, .T. ) ;
#118577=VERTEX_POINT ( 'NONE', #117868 ) ;
#118581=ORIENTED_EDGE ( 'NONE', *, *, #146038, .F. ) ;
#118614=CARTESIAN_POINT ( 'NONE',  ( 20.95561247346651967, 10.59500736521470898, -41.09378276698163290 ) ) ;
#118640=CARTESIAN_POINT ( 'NONE',  ( 23.24999999999999289, 4.150000000011154988, -33.50000000000000000 ) ) ;
#118659=FACE_OUTER_BOUND ( 'NONE', #134241, .T. ) ;
#118706=ORIENTED_EDGE ( 'NONE', *, *, #60317, .F. ) ;
#118712=CARTESIAN_POINT ( 'NONE',  ( -21.07016717457011268, 1.115542391533913547E-11, -27.17905916189910442 ) ) ;
#118722=ADVANCED_FACE ( 'NONE', ( #64330 ), #3046, .F. ) ;
#118742=AXIS2_PLACEMENT_3D ( 'NONE', #40955, #39670, #154489 ) ;
#118744=CARTESIAN_POINT ( 'NONE',  ( 22.39999999999999503, 11.75000000001115552, -33.40000000000000568 ) ) ;
#118750=DIRECTION ( 'NONE',  ( -1.000000000000000000, 0.000000000000000000, 0.000000000000000000 ) ) ;
#118776=CIRCLE ( 'NONE', #6330, 0.1000000000000028644 ) ;
#118797=CIRCLE ( 'NONE', #93839, 11.80000000000000426 ) ;
#118803=DIRECTION ( 'NONE',  ( 0.000000000000000000, -0.9915357197604837136, 0.1298341882520134827 ) ) ;
#118804=ADVANCED_FACE ( 'NONE', ( #102131 ), #68182, .F. ) ;
#118812=ADVANCED_FACE ( 'NONE', ( #107298 ), #34974, .T. ) ;
#118832=ORIENTED_EDGE ( 'NONE', *, *, #242706, .F. ) ;
#118842=EDGE_LOOP ( 'NONE', ( #99252, #51144, #203454, #99460 ) ) ;
#118893=DIRECTION ( 'NONE',  ( 0.000000000000000000, 0.000000000000000000, -1.000000000000000000 ) ) ;
#118932=ORIENTED_EDGE ( 'NONE', *, *, #100641, .T. ) ;
#118936=EDGE_CURVE ( 'NONE', #29148, #113969, #41782, .T. ) ;
#118937=DIRECTION ( 'NONE',  ( 0.000000000000000000, -0.000000000000000000, -1.000000000000000000 ) ) ;
#118949=FACE_OUTER_BOUND ( 'NONE', #34333, .T. ) ;
#118964=ORIENTED_EDGE ( 'NONE', *, *, #72504, .T. ) ;
#119026=CYLINDRICAL_SURFACE ( 'NONE', #106572, 0.1000000000000028644 ) ;
#119048=ORIENTED_EDGE ( 'NONE', *, *, #14656, .F. ) ;
#119066=CIRCLE ( 'NONE', #60770, 0.1000000000000004496 ) ;
#119088=VERTEX_POINT ( 'NONE', #219237 ) ;
#119139=AXIS2_PLACEMENT_3D ( 'NONE', #197818, #141696, #161288 ) ;
#119147=SPHERICAL_SURFACE ( 'NONE', #51498, 0.1000000000000000056 ) ;
#119152=LINE ( 'NONE', #117848, #137018 ) ;
#119189=CARTESIAN_POINT ( 'NONE',  ( -18.59999999999999787, -9.499999999988842703, -45.65000000000001279 ) ) ;
#119260=DIRECTION ( 'NONE',  ( 0.000000000000000000, 0.4999999999999949485, -0.8660254037844415942 ) ) ;
#119262=CIRCLE ( 'NONE', #215118, 11.74999999999999645 ) ;
#119272=DIRECTION ( 'NONE',  ( 0.000000000000000000, -0.000000000000000000, 1.000000000000000000 ) ) ;
#119316=EDGE_CURVE ( 'NONE', #72318, #22952, #196801, .T. ) ;
#119332=VERTEX_POINT ( 'NONE', #53456 ) ;
#119348=AXIS2_PLACEMENT_3D ( 'NONE', #184461, #187062, #64519 ) ;
#119368=AXIS2_PLACEMENT_3D ( 'NONE', #34644, #16361, #193704 ) ;
#119394=AXIS2_PLACEMENT_3D ( 'NONE', #168526, #248004, #69395 ) ;
#119418=CARTESIAN_POINT ( 'NONE',  ( -21.05000000000000071, -11.48912529306490349, -36.60000000000000142 ) ) ;
#119421=ORIENTED_EDGE ( 'NONE', *, *, #90042, .F. ) ;
#119428=CARTESIAN_POINT ( 'NONE',  ( -20.94999675878240808, 10.29307482169070909, -72.45864214669403225 ) ) ;
#119439=ORIENTED_EDGE ( 'NONE', *, *, #76909, .T. ) ;
#119463=CARTESIAN_POINT ( 'NONE',  ( -21.55000000000000071, 7.250000000011155521, -45.85000000000000142 ) ) ;
#119468=ORIENTED_EDGE ( 'NONE', *, *, #257938, .T. ) ;
#119487=VERTEX_POINT ( 'NONE', #101526 ) ;
#119489=DIRECTION ( 'NONE',  ( 0.000000000000000000, 0.000000000000000000, -1.000000000000000000 ) ) ;
#119495=LINE ( 'NONE', #141608, #224931 ) ;
#119504=LINE ( 'NONE', #59478, #24023 ) ;
#119530=DIRECTION ( 'NONE',  ( 0.000000000000000000, 0.000000000000000000, -1.000000000000000000 ) ) ;
#119575=ORIENTED_EDGE ( 'NONE', *, *, #51195, .F. ) ;
#119592=DIRECTION ( 'NONE',  ( 0.000000000000000000, -0.000000000000000000, 1.000000000000000000 ) ) ;
#119602=DIRECTION ( 'NONE',  ( -1.000000000000000000, 0.000000000000000000, 0.000000000000000000 ) ) ;
#119621=DIRECTION ( 'NONE',  ( 0.000000000000000000, 0.9274965247785529332, 0.3738317757009255171 ) ) ;
#119642=CARTESIAN_POINT ( 'NONE',  ( 20.44999100639894962, 10.43971070322319683, -41.25907572597052564 ) ) ;
#119655=CARTESIAN_POINT ( 'NONE',  ( 23.14999999999999503, 11.65000000001116298, -45.65000000000000568 ) ) ;
#119667=CARTESIAN_POINT ( 'NONE',  ( -18.49346865148322294, -9.443073798513754724, -40.68519625531506989 ) ) ;
#119676=ORIENTED_EDGE ( 'NONE', *, *, #2245, .T. ) ;
#119717=VECTOR ( 'NONE', #60708, 1000.000000000000000 ) ;
#119759=CIRCLE ( 'NONE', #73987, 0.1999999999999987899 ) ;
#119794=DIRECTION ( 'NONE',  ( 0.000000000000000000, -1.000000000000000000, 0.000000000000000000 ) ) ;
#119806=EDGE_LOOP ( 'NONE', ( #160068, #48530, #141479, #241367 ) ) ;
#119833=ORIENTED_EDGE ( 'NONE', *, *, #17010, .T. ) ;
#119869=ORIENTED_EDGE ( 'NONE', *, *, #22072, .F. ) ;
#119881=VERTEX_POINT ( 'NONE', #162534 ) ;
#119901=DIRECTION ( 'NONE',  ( 1.000000000000000000, 0.000000000000000000, 0.000000000000000000 ) ) ;
#119908=AXIS2_PLACEMENT_3D ( 'NONE', #220878, #240455, #61825 ) ;
#119971=FACE_OUTER_BOUND ( 'NONE', #166565, .T. ) ;
#119995=CARTESIAN_POINT ( 'NONE',  ( 18.59999999999999432, -1.835859311432484375, -78.50443916879852679 ) ) ;
#120009=FACE_OUTER_BOUND ( 'NONE', #123373, .T. ) ;
#120016=DIRECTION ( 'NONE',  ( 0.000000000000000000, 0.9908441862701596881, -0.1350103645451904977 ) ) ;
#120027=EDGE_LOOP ( 'NONE', ( #183469, #6433, #81946 ) ) ;
#120066=EDGE_CURVE ( 'NONE', #201612, #100761, #230183, .T. ) ;
#120071=EDGE_LOOP ( 'NONE', ( #106037, #28567, #79027, #36040 ) ) ;
#120076=EDGE_CURVE ( 'NONE', #181631, #242144, #121451, .T. ) ;
#120106=CARTESIAN_POINT ( 'NONE',  ( -23.25000000000000000, 4.350000000011156054, -54.64999999999999858 ) ) ;
#120107=AXIS2_PLACEMENT_3D ( 'NONE', #229811, #154181, #55004 ) ;
#120117=DIRECTION ( 'NONE',  ( 1.000000000000000000, 0.000000000000000000, 0.000000000000000000 ) ) ;
#120118=ORIENTED_EDGE ( 'NONE', *, *, #136119, .F. ) ;
#120131=ORIENTED_EDGE ( 'NONE', *, *, #28530, .T. ) ;
#120190=FACE_OUTER_BOUND ( 'NONE', #13295, .T. ) ;
#120211=DIRECTION ( 'NONE',  ( 1.000000000000000000, -0.000000000000000000, -0.000000000000000000 ) ) ;
#120212=EDGE_CURVE ( 'NONE', #36652, #127250, #179684, .T. ) ;
#120230=ADVANCED_FACE ( 'NONE', ( #168351 ), #27549, .T. ) ;
#120261=ORIENTED_EDGE ( 'NONE', *, *, #77261, .T. ) ;
#120266=DIRECTION ( 'NONE',  ( 0.000000000000000000, -0.000000000000000000, 1.000000000000000000 ) ) ;
#120270=LINE ( 'NONE', #82351, #77032 ) ;
#120291=ORIENTED_EDGE ( 'NONE', *, *, #165227, .T. ) ;
#120316=CARTESIAN_POINT ( 'NONE',  ( -23.15000000000000213, 11.75000000001115552, -45.65000000000000568 ) ) ;
#120318=EDGE_LOOP ( 'NONE', ( #26185, #13995, #131608, #231021 ) ) ;
#120331=DIRECTION ( 'NONE',  ( 1.000000000000000000, 0.000000000000000000, 0.000000000000000000 ) ) ;
#120355=VERTEX_POINT ( 'NONE', #211284 ) ;
#120379=CARTESIAN_POINT ( 'NONE',  ( -18.59999999999999787, -1.249999999988843369, -74.80048075441509070 ) ) ;
#120415=VECTOR ( 'NONE', #65611, 999.9999999999998863 ) ;
#120436=CIRCLE ( 'NONE', #116319, 0.09999999999999843736 ) ;
#120495=CARTESIAN_POINT ( 'NONE',  ( -23.15000000000000213, 1.115600667400684642E-11, -37.54999999999999716 ) ) ;
#120523=ORIENTED_EDGE ( 'NONE', *, *, #138148, .F. ) ;
#120538=( LENGTH_UNIT ( ) NAMED_UNIT ( * ) SI_UNIT ( .MILLI., .METRE. ) );
#120539=ORIENTED_EDGE ( 'NONE', *, *, #55452, .F. ) ;
#120540=FACE_OUTER_BOUND ( 'NONE', #109497, .T. ) ;
#120544=ORIENTED_EDGE ( 'NONE', *, *, #52346, .T. ) ;
#120547=CARTESIAN_POINT ( 'NONE',  ( -22.60000000000094289, 0.1008583691096561485, -21.75043287651059387 ) ) ;
#120548=LINE ( 'NONE', #56658, #257396 ) ;
#120550=EDGE_CURVE ( 'NONE', #27581, #100505, #254808, .T. ) ;
#120557=CIRCLE ( 'NONE', #249716, 11.74999999999999645 ) ;
#120559=DIRECTION ( 'NONE',  ( 0.000000000000000000, 0.000000000000000000, 1.000000000000000000 ) ) ;
#120565=DIRECTION ( 'NONE',  ( -1.000000000000000000, 0.000000000000000000, 0.000000000000000000 ) ) ;
#120606=CARTESIAN_POINT ( 'NONE',  ( -21.05000000000000071, 0.09843750001115432469, -27.20076908991313047 ) ) ;
#120621=VECTOR ( 'NONE', #58653, 1000.000000000000000 ) ;
#120623=ORIENTED_EDGE ( 'NONE', *, *, #78124, .F. ) ;
#120630=ADVANCED_FACE ( 'NONE', ( #32375 ), #205838, .F. ) ;
#120646=CARTESIAN_POINT ( 'NONE',  ( 21.08804582317324616, 8.878166167103060502, -45.84999982940517071 ) ) ;
#120656=CARTESIAN_POINT ( 'NONE',  ( 23.25000000000000000, -8.999999999988844479, -43.39396912265245021 ) ) ;
#120680=ORIENTED_EDGE ( 'NONE', *, *, #186557, .F. ) ;
#120695=AXIS2_PLACEMENT_3D ( 'NONE', #79335, #57197, #101433 ) ;
#120712=CARTESIAN_POINT ( 'NONE',  ( -18.59999999999999787, -1.135018845899022466, -74.71697688343232358 ) ) ;
#120720=VECTOR ( 'NONE', #245416, 1000.000000000000000 ) ;
#120751=VECTOR ( 'NONE', #226685, 1000.000000000000000 ) ;
#120791=ORIENTED_EDGE ( 'NONE', *, *, #229568, .F. ) ;
#120806=CARTESIAN_POINT ( 'NONE',  ( 21.30000000000002558, 1.115650265596050101E-11, -37.54999999999999716 ) ) ;
#120821=CIRCLE ( 'NONE', #29262, 0.1000000000000028644 ) ;
#120826=ADVANCED_FACE ( 'NONE', ( #38762 ), #195290, .T. ) ;
#120860=ORIENTED_EDGE ( 'NONE', *, *, #134171, .F. ) ;
#120872=DIRECTION ( 'NONE',  ( 0.000000000000000000, 0.000000000000000000, -1.000000000000000000 ) ) ;
#120952=ORIENTED_EDGE ( 'NONE', *, *, #187380, .T. ) ;
#120965=CARTESIAN_POINT ( 'NONE',  ( 21.14999999999999858, 6.540656951712400691, -33.60000000000000142 ) ) ;
#120980=DIRECTION ( 'NONE',  ( 0.000000000000000000, -8.881784197001272834E-15, 1.000000000000000000 ) ) ;
#120992=CARTESIAN_POINT ( 'NONE',  ( 21.05000000000000071, 1.115486826172573664E-11, -26.95934304829875572 ) ) ;
#121034=EDGE_LOOP ( 'NONE', ( #247926, #32065, #31162, #84345 ) ) ;
#121044=DIRECTION ( 'NONE',  ( 0.000000000000000000, 0.000000000000000000, -1.000000000000000000 ) ) ;
#121047=DIRECTION ( 'NONE',  ( 1.000000000000000000, -0.000000000000000000, -0.000000000000000000 ) ) ;
#121058=AXIS2_PLACEMENT_3D ( 'NONE', #170602, #128866, #70191 ) ;
#121065=LINE ( 'NONE', #44062, #113880 ) ;
#121103=EDGE_LOOP ( 'NONE', ( #212017, #39104, #200868, #143505 ) ) ;
#121138=AXIS2_PLACEMENT_3D ( 'NONE', #92626, #213871, #57342 ) ;
#121142=ORIENTED_EDGE ( 'NONE', *, *, #82678, .T. ) ;
#121148=EDGE_CURVE ( 'NONE', #239047, #7145, #134404, .T. ) ;
#121154=CARTESIAN_POINT ( 'NONE',  ( -18.50000000000000000, -1.687074390080403941, -20.68542703345834965 ) ) ;
#121157=DIRECTION ( 'NONE',  ( 0.000000000000000000, 0.000000000000000000, -1.000000000000000000 ) ) ;
#121164=VERTEX_POINT ( 'NONE', #76275 ) ;
#121167=AXIS2_PLACEMENT_3D ( 'NONE', #123418, #118289, #101228 ) ;
#121177=VECTOR ( 'NONE', #109901, 1000.000000000000000 ) ;
#121188=ADVANCED_FACE ( 'NONE', ( #175420 ), #138670, .T. ) ;
#121196=CARTESIAN_POINT ( 'NONE',  ( 20.95496329884391784, 10.56743320610419445, -41.07430993228482663 ) ) ;
#121200=LINE ( 'NONE', #98997, #166623 ) ;
#121214=CIRCLE ( 'NONE', #187837, 0.1000000000000028644 ) ;
#121226=VERTEX_POINT ( 'NONE', #231525 ) ;
#121232=VERTEX_POINT ( 'NONE', #52861 ) ;
#121253=CYLINDRICAL_SURFACE ( 'NONE', #193737, 11.74999999999999645 ) ;
#121276=DIRECTION ( 'NONE',  ( -1.000000000000000000, 0.000000000000000000, 0.000000000000000000 ) ) ;
#121317=LINE ( 'NONE', #83395, #256067 ) ;
#121326=DIRECTION ( 'NONE',  ( 1.000000000000000000, -0.000000000000000000, -0.000000000000000000 ) ) ;
#121340=EDGE_CURVE ( 'NONE', #136008, #253318, #85240, .T. ) ;
#121355=ADVANCED_FACE ( 'NONE', ( #108698 ), #13807, .F. ) ;
#121368=DIRECTION ( 'NONE',  ( 0.000000000000000000, 0.000000000000000000, -1.000000000000000000 ) ) ;
#121442=DIRECTION ( 'NONE',  ( 0.000000000000000000, 0.000000000000000000, 1.000000000000000000 ) ) ;
#121450=DIRECTION ( 'NONE',  ( -0.000000000000000000, 0.000000000000000000, 1.000000000000000000 ) ) ;
#121451=CIRCLE ( 'NONE', #38222, 0.1000000000000029476 ) ;
#121481=ORIENTED_EDGE ( 'NONE', *, *, #146395, .T. ) ;
#121610=CARTESIAN_POINT ( 'NONE',  ( -21.05000000000000071, -11.64999999998884306, -64.10000000000000853 ) ) ;
#121625=CARTESIAN_POINT ( 'NONE',  ( 20.85000000000000142, -1.835859311432481045, -78.50443916879852679 ) ) ;
#121626=CIRCLE ( 'NONE', #175783, 0.1000000000000008937 ) ;
#121630=DIRECTION ( 'NONE',  ( 0.000000000000000000, 0.2605042016806672911, -0.9654727137038716656 ) ) ;
#121724=ADVANCED_FACE ( 'NONE', ( #1920 ), #56742, .T. ) ;
#121747=( BOUNDED_CURVE ( )  B_SPLINE_CURVE ( 3, ( #218412, #254929, #16405, #217122 ),
 .UNSPECIFIED., .F., .T. ) 
 B_SPLINE_CURVE_WITH_KNOTS ( ( 4, 4 ),
 ( 3.141592653589791784, 4.712388980384688786 ),
 .UNSPECIFIED. ) 
 CURVE ( )  GEOMETRIC_REPRESENTATION_ITEM ( )  RATIONAL_B_SPLINE_CURVE ( ( 1.000000000000000000, 0.8047378541243649375, 0.8047378541243649375, 1.000000000000000000 ) ) 
 REPRESENTATION_ITEM ( '' )  );
#121761=EDGE_CURVE ( 'NONE', #242144, #3656, #115461, .T. ) ;
#121822=AXIS2_PLACEMENT_3D ( 'NONE', #100405, #3899, #221638 ) ;
#121823=CARTESIAN_POINT ( 'NONE',  ( -22.45437739390953880, 1.115488181425289271E-11, -21.85042918840543535 ) ) ;
#121837=DIRECTION ( 'NONE',  ( 2.952720810173289112E-16, -1.000000000000000000, 0.000000000000000000 ) ) ;
#121862=DIRECTION ( 'NONE',  ( 0.000000000000000000, 1.000000000000000000, 0.000000000000000000 ) ) ;
#121889=CARTESIAN_POINT ( 'NONE',  ( 21.05000000000000071, 1.115600667400684642E-11, -46.47500000000000142 ) ) ;
#121910=ORIENTED_EDGE ( 'NONE', *, *, #95299, .F. ) ;
#121956=FACE_OUTER_BOUND ( 'NONE', #255790, .T. ) ;
#121966=ORIENTED_EDGE ( 'NONE', *, *, #83450, .F. ) ;
#121979=DIRECTION ( 'NONE',  ( 1.000000000000000000, 0.000000000000000000, 0.000000000000000000 ) ) ;
#121987=CARTESIAN_POINT ( 'NONE',  ( -20.94999999999999929, 10.29288807859936661, -72.45800201601217339 ) ) ;
#122038=EDGE_LOOP ( 'NONE', ( #238361, #189044, #156967, #256574 ) ) ;
#122072=ORIENTED_EDGE ( 'NONE', *, *, #187799, .T. ) ;
#122084=CARTESIAN_POINT ( 'NONE',  ( 18.52130828395271678, -9.481395502614633486, -40.52450672388363984 ) ) ;
#122093=CIRCLE ( 'NONE', #134540, 0.1000000000000028644 ) ;
#122101=CYLINDRICAL_SURFACE ( 'NONE', #253876, 0.1000000000000028644 ) ;
#122120=AXIS2_PLACEMENT_3D ( 'NONE', #121889, #205243, #146548 ) ;
#122208=DIRECTION ( 'NONE',  ( 0.000000000000000000, 5.204170427930272346E-14, 1.000000000000000000 ) ) ;
#122211=AXIS2_PLACEMENT_3D ( 'NONE', #213926, #35330, #194390 ) ;
#122216=AXIS2_PLACEMENT_3D ( 'NONE', #110819, #252900, #155128 ) ;
#122271=VERTEX_POINT ( 'NONE', #8074 ) ;
#122284=ADVANCED_FACE ( 'NONE', ( #171041 ), #51003, .F. ) ;
#122289=ORIENTED_EDGE ( 'NONE', *, *, #24106, .F. ) ;
#122306=CARTESIAN_POINT ( 'NONE',  ( -23.15000000000000213, 4.350000000011156054, -54.75000000000000000 ) ) ;
#122307=DIRECTION ( 'NONE',  ( -1.000000000000000000, 0.000000000000000000, 0.000000000000000000 ) ) ;
#122313=CIRCLE ( 'NONE', #51538, 3.899999999999999467 ) ;
#122338=DIRECTION ( 'NONE',  ( -1.000000000000000000, 0.000000000000000000, 0.000000000000000000 ) ) ;
#122346=CIRCLE ( 'NONE', #18288, 11.80000000000000426 ) ;
#122372=ORIENTED_EDGE ( 'NONE', *, *, #69252, .F. ) ;
#122379=CARTESIAN_POINT ( 'NONE',  ( -21.14999999999999858, -0.09999999998884338825, -21.85042919245519855 ) ) ;
#122393=DIRECTION ( 'NONE',  ( 1.000000000000000000, 3.265361837132813093E-16, -0.000000000000000000 ) ) ;
#122441=FACE_OUTER_BOUND ( 'NONE', #73208, .T. ) ;
#122444=VECTOR ( 'NONE', #158911, 1000.000000000000000 ) ;
#122502=CARTESIAN_POINT ( 'NONE',  ( 18.59999999999999076, 14.05000000001116689, -39.01369507076098841 ) ) ;
#122503=SPHERICAL_SURFACE ( 'NONE', #82787, 0.1000000000000000056 ) ;
#122506=FACE_OUTER_BOUND ( 'NONE', #96300, .T. ) ;
#122508=CIRCLE ( 'NONE', #5759, 0.1999999999999996503 ) ;
#122516=CARTESIAN_POINT ( 'NONE',  ( -18.59999999999999787, 1.115600667400684642E-11, -67.00000000000000000 ) ) ;
#122552=CARTESIAN_POINT ( 'NONE',  ( -21.05000000000000071, 6.540656951712397138, -33.60000000000000142 ) ) ;
#122581=CARTESIAN_POINT ( 'NONE',  ( 23.25000000000000000, -11.64999999998883595, -63.89999999999999858 ) ) ;
#122591=CARTESIAN_POINT ( 'NONE',  ( -21.07933241753356413, 0.09337959043042065588, -27.17135405162026274 ) ) ;
#122627=CYLINDRICAL_SURFACE ( 'NONE', #60326, 0.09999999999999939493 ) ;
#122631=CARTESIAN_POINT ( 'NONE',  ( -23.15000000000000213, -11.64999999998884483, -63.89999999999999858 ) ) ;
#122633=CARTESIAN_POINT ( 'NONE',  ( 21.46681500593265213, 6.857511159395769162, -33.50000000000000711 ) ) ;
#122648=DIRECTION ( 'NONE',  ( 0.000000000000000000, -1.000000000000000000, 0.000000000000000000 ) ) ;
#122662=CIRCLE ( 'NONE', #214784, 0.3999999999999975797 ) ;
#122672=EDGE_CURVE ( 'NONE', #175831, #163280, #47651, .T. ) ;
#122687=EDGE_CURVE ( 'NONE', #7520, #121164, #245078, .T. ) ;
#122689=DIRECTION ( 'NONE',  ( 1.000000000000000000, -0.000000000000000000, -0.000000000000000000 ) ) ;
#122694=ORIENTED_EDGE ( 'NONE', *, *, #197365, .T. ) ;
#122703=DIRECTION ( 'NONE',  ( 1.000000000000000000, 2.952720810173289112E-16, -0.000000000000000000 ) ) ;
#122739=DIRECTION ( 'NONE',  ( 1.000000000000000000, -7.304098846218133681E-16, 0.000000000000000000 ) ) ;
#122750=EDGE_LOOP ( 'NONE', ( #246197, #55766, #17613, #243204 ) ) ;
#122764=DIRECTION ( 'NONE',  ( -1.000000000000000000, 0.000000000000000000, 0.000000000000000000 ) ) ;
#122779=ORIENTED_EDGE ( 'NONE', *, *, #203827, .T. ) ;
#122784=CARTESIAN_POINT ( 'NONE',  ( -18.39999999999999858, -9.599999999988845900, -73.70018939122203960 ) ) ;
#122797=DIRECTION ( 'NONE',  ( -1.000000000000000000, 0.000000000000000000, 0.000000000000000000 ) ) ;
#122810=CARTESIAN_POINT ( 'NONE',  ( 23.24999999999999645, 5.600000000011153389, -21.75000000000000355 ) ) ;
#122860=EDGE_LOOP ( 'NONE', ( #215295, #152542, #102476 ) ) ;
#122885=ADVANCED_FACE ( 'NONE', ( #157574 ), #118415, .F. ) ;
#122891=CYLINDRICAL_SURFACE ( 'NONE', #224734, 11.74999999999999645 ) ;
#122895=ORIENTED_EDGE ( 'NONE', *, *, #124046, .F. ) ;
#122913=AXIS2_PLACEMENT_3D ( 'NONE', #52717, #13611, #74894 ) ;
#122914=DIRECTION ( 'NONE',  ( 0.000000000000000000, 0.000000000000000000, -1.000000000000000000 ) ) ;
#122939=DIRECTION ( 'NONE',  ( 1.000000000000000000, 6.938893903907222067E-15, 0.000000000000000000 ) ) ;
#122957=ORIENTED_EDGE ( 'NONE', *, *, #131679, .T. ) ;
#122982=ORIENTED_EDGE ( 'NONE', *, *, #150886, .T. ) ;
#122987=EDGE_LOOP ( 'NONE', ( #36802, #162000 ) ) ;
#122990=ORIENTED_EDGE ( 'NONE', *, *, #67170, .F. ) ;
#123003=DIRECTION ( 'NONE',  ( 1.000000000000000000, 0.000000000000000000, 0.000000000000000000 ) ) ;
#123038=ORIENTED_EDGE ( 'NONE', *, *, #110834, .T. ) ;
#123085=DIRECTION ( 'NONE',  ( -0.000000000000000000, -0.000000000000000000, -1.000000000000000000 ) ) ;
#123121=DIRECTION ( 'NONE',  ( 1.000000000000000000, 0.000000000000000000, 0.000000000000000000 ) ) ;
#123185=ORIENTED_EDGE ( 'NONE', *, *, #131449, .F. ) ;
#123189=AXIS2_PLACEMENT_3D ( 'NONE', #187308, #109021, #149470 ) ;
#123190=ORIENTED_EDGE ( 'NONE', *, *, #235438, .F. ) ;
#123282=CARTESIAN_POINT ( 'NONE',  ( -22.49510344025093644, 0.06712767820541534758, -21.85002989488574343 ) ) ;
#123292=ORIENTED_EDGE ( 'NONE', *, *, #8150, .T. ) ;
#123314=DIRECTION ( 'NONE',  ( 0.000000000000000000, 0.000000000000000000, 1.000000000000000000 ) ) ;
#123321=AXIS2_PLACEMENT_3D ( 'NONE', #233984, #253542, #30689 ) ;
#123347=ORIENTED_EDGE ( 'NONE', *, *, #53433, .T. ) ;
#123351=DIRECTION ( 'NONE',  ( 0.000000000000000000, 1.000000000000000000, 0.000000000000000000 ) ) ;
#123353=AXIS2_PLACEMENT_3D ( 'NONE', #201623, #25570, #243307 ) ;
#123373=EDGE_LOOP ( 'NONE', ( #182653, #95081, #84768, #60045 ) ) ;
#123377=TOROIDAL_SURFACE ( 'NONE', #231536, 3.899999999999999467, 0.1000000000000000056 ) ;
#123394=ORIENTED_EDGE ( 'NONE', *, *, #242385, .T. ) ;
#123416=VERTEX_POINT ( 'NONE', #32843 ) ;
#123418=CARTESIAN_POINT ( 'NONE',  ( 20.94999999999999574, 1.162701749949165642, -41.60000000000000142 ) ) ;
#123422=CYLINDRICAL_SURFACE ( 'NONE', #13053, 0.1000000000000000472 ) ;
#123483=EDGE_CURVE ( 'NONE', #64423, #55402, #134925, .T. ) ;
#123489=CIRCLE ( 'NONE', #48468, 0.1000000000000028644 ) ;
#123498=DIRECTION ( 'NONE',  ( -1.000000000000000000, -0.000000000000000000, -0.000000000000000000 ) ) ;
#123591=DIRECTION ( 'NONE',  ( 0.000000000000000000, 0.000000000000000000, 1.000000000000000000 ) ) ;
#123635=EDGE_CURVE ( 'NONE', #19295, #3179, #89166, .T. ) ;
#123643=CARTESIAN_POINT ( 'NONE',  ( 21.14999999999999858, 10.71339244341104013, -45.75000000000000711 ) ) ;
#123647=ORIENTED_EDGE ( 'NONE', *, *, #90042, .T. ) ;
#123651=ORIENTED_EDGE ( 'NONE', *, *, #102347, .F. ) ;
#123664=CARTESIAN_POINT ( 'NONE',  ( 21.59780538579342135, 0.09897866960914131207, -26.65290947005674482 ) ) ;
#123670=EDGE_CURVE ( 'NONE', #182341, #139599, #122508, .T. ) ;
#123675=LINE ( 'NONE', #84487, #81611 ) ;
#123686=ADVANCED_FACE ( 'NONE', ( #2648 ), #231432, .F. ) ;
#123724=DIRECTION ( 'NONE',  ( 0.000000000000000000, 0.000000000000000000, 1.000000000000000000 ) ) ;
#123736=CARTESIAN_POINT ( 'NONE',  ( 20.95520789717937404, 10.57693059939611224, -41.08023297387485684 ) ) ;
#123749=EDGE_CURVE ( 'NONE', #219135, #104039, #151562, .T. ) ;
#123751=CARTESIAN_POINT ( 'NONE',  ( 20.94999999999999929, 11.65000000001115943, -60.21613433702191287 ) ) ;
#123808=AXIS2_PLACEMENT_3D ( 'NONE', #149280, #8471, #249654 ) ;
#123862=CARTESIAN_POINT ( 'NONE',  ( -23.15000000000000213, -8.663551401858004652, -43.02410111806730697 ) ) ;
#123873=ORIENTED_EDGE ( 'NONE', *, *, #164723, .T. ) ;
#123875=DIRECTION ( 'NONE',  ( 3.469446951953646374E-14, -0.7899159663865635839, -0.6132151058540398214 ) ) ;
#123917=EDGE_CURVE ( 'NONE', #199100, #214956, #156015, .T. ) ;
#123937=EDGE_LOOP ( 'NONE', ( #120952, #227555, #106253, #153685 ) ) ;
#123970=EDGE_LOOP ( 'NONE', ( #151410, #134184, #87181 ) ) ;
#124026=DIRECTION ( 'NONE',  ( -0.000000000000000000, -2.891205793294679805E-16, 1.000000000000000000 ) ) ;
#124040=CARTESIAN_POINT ( 'NONE',  ( 21.05000000000000071, 1.115600667400684642E-11, -67.00000000000000000 ) ) ;
#124046=EDGE_CURVE ( 'NONE', #110094, #256921, #100132, .T. ) ;
#124062=ADVANCED_FACE ( 'NONE', ( #45323 ), #35235, .T. ) ;
#124064=CYLINDRICAL_SURFACE ( 'NONE', #99478, 0.5000000000000004441 ) ;
#124065=DIRECTION ( 'NONE',  ( -1.000000000000000000, 7.304098846218134667E-16, 2.111765289898285610E-31 ) ) ;
#124090=LINE ( 'NONE', #122810, #44700 ) ;
#124120=CARTESIAN_POINT ( 'NONE',  ( -23.25000000000000000, 1.115600667400684642E-11, -70.90000000000000568 ) ) ;
#124160=DIRECTION ( 'NONE',  ( 0.000000000000000000, 0.000000000000000000, -1.000000000000000000 ) ) ;
#124161=CARTESIAN_POINT ( 'NONE',  ( -18.59999999999999787, 11.65000000001115232, -21.75000000000000355 ) ) ;
#124164=VECTOR ( 'NONE', #171490, 1000.000000000000000 ) ;
#124184=DIRECTION ( 'NONE',  ( -3.890533409366484652E-14, -0.1298341882520124002, -0.9915357197604841577 ) ) ;
#124190=CARTESIAN_POINT ( 'NONE',  ( -20.54999999999999716, 2.000000000011154189, -53.77537807723790309 ) ) ;
#124196=CARTESIAN_POINT ( 'NONE',  ( 20.94999999999999929, 8.776282895303632259, -54.75000000000000000 ) ) ;
#124205=DIRECTION ( 'NONE',  ( 0.000000000000000000, 0.000000000000000000, -1.000000000000000000 ) ) ;
#124237=ORIENTED_EDGE ( 'NONE', *, *, #19953, .T. ) ;
#124253=CARTESIAN_POINT ( 'NONE',  ( 20.94999999999999929, 1.115600667400684642E-11, -67.00000000000000000 ) ) ;
#124275=EDGE_CURVE ( 'NONE', #200421, #204355, #35412, .T. ) ;
#124276=AXIS2_PLACEMENT_3D ( 'NONE', #138489, #218030, #228337 ) ;
#124286=DIRECTION ( 'NONE',  ( 0.000000000000000000, -1.000000000000000000, -2.891205793294679805E-16 ) ) ;
#124287=CARTESIAN_POINT ( 'NONE',  ( 23.15000000000000213, -12.41227409413852811, -63.89999999999999858 ) ) ;
#124300=CARTESIAN_POINT ( 'NONE',  ( 20.94999999999999929, -11.48912529306489994, -63.89999999999999858 ) ) ;
#124318=AXIS2_PLACEMENT_3D ( 'NONE', #6714, #107093, #244034 ) ;
#124340=ORIENTED_EDGE ( 'NONE', *, *, #67579, .T. ) ;
#124349=VECTOR ( 'NONE', #82391, 1000.000000000000114 ) ;
#124380=AXIS2_PLACEMENT_3D ( 'NONE', #119418, #121979, #21604 ) ;
#124395=DIRECTION ( 'NONE',  ( 0.000000000000000000, 0.000000000000000000, 1.000000000000000000 ) ) ;
#124401=CARTESIAN_POINT ( 'NONE',  ( -23.25000000000000000, 4.150000000011156764, -54.64999999999999858 ) ) ;
#124403=CARTESIAN_POINT ( 'NONE',  ( -21.05000000000000071, 6.257814610492678398, -33.40220970869076922 ) ) ;
#124443=ORIENTED_EDGE ( 'NONE', *, *, #185083, .F. ) ;
#124446=ORIENTED_EDGE ( 'NONE', *, *, #87881, .F. ) ;
#124450=CYLINDRICAL_SURFACE ( 'NONE', #1347, 0.1000000000000028644 ) ;
#124455=CARTESIAN_POINT ( 'NONE',  ( 20.97250901189795513, 10.62456803371303593, -41.16454571696699816 ) ) ;
#124465=EDGE_CURVE ( 'NONE', #43292, #58399, #13523, .T. ) ;
#124478=ORIENTED_EDGE ( 'NONE', *, *, #175901, .T. ) ;
#124490=CYLINDRICAL_SURFACE ( 'NONE', #253314, 0.1000000000000028644 ) ;
#124560=ORIENTED_EDGE ( 'NONE', *, *, #176371, .F. ) ;
#124566=ORIENTED_EDGE ( 'NONE', *, *, #254215, .T. ) ;
#124572=CARTESIAN_POINT ( 'NONE',  ( -22.44366136229477249, 0.009341569497225225491, -21.85028144252609295 ) ) ;
#124587=CARTESIAN_POINT ( 'NONE',  ( -2.995603634470884209E-16, -11.74999999998884448, -58.25000000000000000 ) ) ;
#124600=LINE ( 'NONE', #183281, #246689 ) ;
#124606=CARTESIAN_POINT ( 'NONE',  ( 22.47071067811865319, 1.115600667400684642E-11, -33.50000000000000000 ) ) ;
#124637=DIRECTION ( 'NONE',  ( 0.000000000000000000, -0.000000000000000000, 1.000000000000000000 ) ) ;
#124648=ADVANCED_FACE ( 'NONE', ( #31905 ), #46283, .T. ) ;
#124655=CIRCLE ( 'NONE', #3852, 11.74999999999999645 ) ;
#124668=ADVANCED_FACE ( 'NONE', ( #78371 ), #176221, .T. ) ;
#124695=DIRECTION ( 'NONE',  ( 0.000000000000000000, 1.000000000000000000, -0.000000000000000000 ) ) ;
#124740=VECTOR ( 'NONE', #117553, 1000.000000000000000 ) ;
#124750=DIRECTION ( 'NONE',  ( -4.801466763864313332E-15, -0.2605042016806672911, -0.9654727137038716656 ) ) ;
#124751=DIRECTION ( 'NONE',  ( 1.000000000000000000, -0.000000000000000000, -0.000000000000000000 ) ) ;
#124759=CARTESIAN_POINT ( 'NONE',  ( -20.54999999999999716, -8.999999999988846255, -43.39396912265245021 ) ) ;
#124782=CIRCLE ( 'NONE', #74918, 0.09999999999999761857 ) ;
#124787=DIRECTION ( 'NONE',  ( 1.000000000000000000, 0.000000000000000000, 0.000000000000000000 ) ) ;
#124805=PLANE ( 'NONE',  #45791 ) ;
#124837=DIRECTION ( 'NONE',  ( 0.000000000000000000, 0.000000000000000000, -1.000000000000000000 ) ) ;
#124838=CARTESIAN_POINT ( 'NONE',  ( 18.59999999999999076, 10.49142135624846439, -58.25000000000000000 ) ) ;
#124868=DIRECTION ( 'NONE',  ( 1.000000000000000000, 0.000000000000000000, 0.000000000000000000 ) ) ;
#124879=CIRCLE ( 'NONE', #103995, 0.09999999999999939493 ) ;
#124922=DIRECTION ( 'NONE',  ( -0.000000000000000000, -0.000000000000000000, 1.000000000000000000 ) ) ;
#124930=CARTESIAN_POINT ( 'NONE',  ( 18.52351027002947959, -9.642162904684028035, -73.71504695050977318 ) ) ;
#124936=ORIENTED_EDGE ( 'NONE', *, *, #243758, .F. ) ;
#124946=CARTESIAN_POINT ( 'NONE',  ( 21.13461538461538680, 10.61458296203669427, -45.85000000000000142 ) ) ;
#124971=ORIENTED_EDGE ( 'NONE', *, *, #194413, .T. ) ;
#125002=EDGE_CURVE ( 'NONE', #200872, #121232, #29996, .T. ) ;
#125023=CARTESIAN_POINT ( 'NONE',  ( 23.14999999999999858, 1.115600667400684642E-11, -69.00000000000000000 ) ) ;
#125061=CYLINDRICAL_SURFACE ( 'NONE', #222281, 0.1000000000000028644 ) ;
#125069=CARTESIAN_POINT ( 'NONE',  ( -21.05000000000000071, 1.115600667400684642E-11, -67.00000000000000000 ) ) ;
#125075=VERTEX_POINT ( 'NONE', #64781 ) ;
#125091=AXIS2_PLACEMENT_3D ( 'NONE', #248905, #70289, #186365 ) ;
#125092=ORIENTED_EDGE ( 'NONE', *, *, #70619, .T. ) ;
#125111=DIRECTION ( 'NONE',  ( 0.000000000000000000, 0.000000000000000000, -1.000000000000000000 ) ) ;
#125125=VERTEX_POINT ( 'NONE', #170359 ) ;
#125128=DIRECTION ( 'NONE',  ( 1.836970198721029934E-16, -1.000000000000000000, -0.000000000000000000 ) ) ;
#125133=FACE_OUTER_BOUND ( 'NONE', #130666, .T. ) ;
#125142=CYLINDRICAL_SURFACE ( 'NONE', #242419, 0.1000000000000000472 ) ;
#125169=FACE_OUTER_BOUND ( 'NONE', #207598, .T. ) ;
#125195=ORIENTED_EDGE ( 'NONE', *, *, #104062, .T. ) ;
#125224=AXIS2_PLACEMENT_3D ( 'NONE', #72444, #98355, #18860 ) ;
#125275=EDGE_LOOP ( 'NONE', ( #243089, #76999, #81743, #22348 ) ) ;
#125307=CARTESIAN_POINT ( 'NONE',  ( 20.94999999999999929, -8.999999999988842703, -57.10603087734755690 ) ) ;
#125333=AXIS2_PLACEMENT_3D ( 'NONE', #70145, #34869, #14003 ) ;
#125352=CIRCLE ( 'NONE', #96106, 0.1000000000000028644 ) ;
#125376=DIRECTION ( 'NONE',  ( -0.7071067811865388020, 0.7071067811865561215, 0.000000000000000000 ) ) ;
#125409=ADVANCED_FACE ( 'NONE', ( #186638 ), #103210, .T. ) ;
#125413=LINE ( 'NONE', #242768, #124349 ) ;
#125424=CARTESIAN_POINT ( 'NONE',  ( 18.59999999999999076, 6.450000000011156587, -43.51702717044002355 ) ) ;
#125428=AXIS2_PLACEMENT_3D ( 'NONE', #188190, #130771, #128215 ) ;
#125431=CARTESIAN_POINT ( 'NONE',  ( -18.50000000000000000, 9.150000000011157653, -45.85000000000000142 ) ) ;
#125441=CIRCLE ( 'NONE', #200255, 0.8750000000000007772 ) ;
#125453=CARTESIAN_POINT ( 'NONE',  ( -23.25000000000000000, 11.75000000001115552, -67.00000000000000000 ) ) ;
#125465=CARTESIAN_POINT ( 'NONE',  ( 20.94999999999999929, -9.499999999988844479, -57.10603087734755690 ) ) ;
#125502=ORIENTED_EDGE ( 'NONE', *, *, #198737, .F. ) ;
#125529=ORIENTED_EDGE ( 'NONE', *, *, #85308, .F. ) ;
#125533=ORIENTED_EDGE ( 'NONE', *, *, #140393, .T. ) ;
#125572=AXIS2_PLACEMENT_3D ( 'NONE', #90220, #232347, #133224 ) ;
#125594=CARTESIAN_POINT ( 'NONE',  ( -21.05000000000000071, 1.115653327213047955E-11, -29.20000000000004547 ) ) ;
#125608=ORIENTED_EDGE ( 'NONE', *, *, #175466, .T. ) ;
#125635=DIRECTION ( 'NONE',  ( 1.000000000000000000, -0.000000000000000000, -0.000000000000000000 ) ) ;
#125645=CARTESIAN_POINT ( 'NONE',  ( -21.10257677756356998, 6.398381742543890915, -33.47504925043203627 ) ) ;
#125655=ORIENTED_EDGE ( 'NONE', *, *, #245933, .T. ) ;
#125670=FACE_OUTER_BOUND ( 'NONE', #239329, .T. ) ;
#125717=ORIENTED_EDGE ( 'NONE', *, *, #71944, .F. ) ;
#125720=CARTESIAN_POINT ( 'NONE',  ( 20.74625933824090751, 8.882913521095439080, -42.05517102412104435 ) ) ;
#125724=ORIENTED_EDGE ( 'NONE', *, *, #3560, .T. ) ;
#125767=CIRCLE ( 'NONE', #133962, 11.80000000000000249 ) ;
#125835=EDGE_CURVE ( 'NONE', #135375, #240562, #48569, .T. ) ;
#125840=AXIS2_PLACEMENT_3D ( 'NONE', #62509, #200732, #22111 ) ;
#125852=DIRECTION ( 'NONE',  ( -1.000000000000000000, -0.000000000000000000, 0.000000000000000000 ) ) ;
#125854=CARTESIAN_POINT ( 'NONE',  ( -21.05000000000000071, -11.29603075032412995, -36.54789915966387071 ) ) ;
#125858=ADVANCED_FACE ( 'NONE', ( #249820 ), #69443, .T. ) ;
#125880=VERTEX_POINT ( 'NONE', #234092 ) ;
#125885=PLANE ( 'NONE',  #66764 ) ;
#125889=CARTESIAN_POINT ( 'NONE',  ( -18.50000000000000000, 10.29288807859935950, -72.45800201601217339 ) ) ;
#125906=DIRECTION ( 'NONE',  ( 1.000000000000000000, 0.000000000000000000, 0.000000000000000000 ) ) ;
#125914=ORIENTED_EDGE ( 'NONE', *, *, #108693, .F. ) ;
#125937=CARTESIAN_POINT ( 'NONE',  ( -21.44999999999999929, 7.150000000011155876, -54.65000000000000568 ) ) ;
#125944=DIRECTION ( 'NONE',  ( 0.000000000000000000, 2.891205793294679805E-16, -1.000000000000000000 ) ) ;
#125960=EDGE_CURVE ( 'NONE', #67554, #140862, #12512, .T. ) ;
#125969=DIRECTION ( 'NONE',  ( -0.000000000000000000, 0.000000000000000000, -1.000000000000000000 ) ) ;
#125983=ORIENTED_EDGE ( 'NONE', *, *, #124465, .F. ) ;
#126002=DIRECTION ( 'NONE',  ( -0.000000000000000000, 0.1350103645451876666, -0.9908441862701600211 ) ) ;
#126032=DIRECTION ( 'NONE',  ( 6.484947573744954877E-15, 0.9274965247785529332, -0.3738317757009255171 ) ) ;
#126036=DIRECTION ( 'NONE',  ( 5.603264701231745086E-32, -1.897661533703520636E-16, 1.000000000000000000 ) ) ;
#126037=AXIS2_PLACEMENT_3D ( 'NONE', #34618, #56686, #252342 ) ;
#126042=CARTESIAN_POINT ( 'NONE',  ( 22.40000000000010516, 1.020945751984553285E-11, -21.85042919245488946 ) ) ;
#126076=DIRECTION ( 'NONE',  ( -1.000000000000000000, 0.000000000000000000, 0.000000000000000000 ) ) ;
#126078=CARTESIAN_POINT ( 'NONE',  ( 21.05000000000000071, 0.03201369319893643955, -27.24115727646229601 ) ) ;
#126100=VERTEX_POINT ( 'NONE', #69607 ) ;
#126116=DIRECTION ( 'NONE',  ( 0.000000000000000000, 0.000000000000000000, -1.000000000000000000 ) ) ;
#126119=DIRECTION ( 'NONE',  ( 0.000000000000000000, 0.000000000000000000, -1.000000000000000000 ) ) ;
#126129=DIRECTION ( 'NONE',  ( 0.000000000000000000, 0.000000000000000000, -1.000000000000000000 ) ) ;
#126161=CARTESIAN_POINT ( 'NONE',  ( -22.49806830649814060, 11.64988965485023620, -33.42253568367449645 ) ) ;
#126165=EDGE_LOOP ( 'NONE', ( #126913, #254539, #65731, #234920 ) ) ;
#126179=CARTESIAN_POINT ( 'NONE',  ( 18.59999999999999076, 6.450000000011156587, -43.51702717044002355 ) ) ;
#126193=DIRECTION ( 'NONE',  ( 1.000000000000000000, 3.265361837132813093E-16, -0.000000000000000000 ) ) ;
#126208=FACE_OUTER_BOUND ( 'NONE', #201460, .T. ) ;
#126218=CARTESIAN_POINT ( 'NONE',  ( 21.05000000000000071, 1.835341550235569663, -45.05515129256298223 ) ) ;
#126239=CARTESIAN_POINT ( 'NONE',  ( 21.13461538461538325, 8.885417037985616773, -45.85000000000000142 ) ) ;
#126257=CARTESIAN_POINT ( 'NONE',  ( 21.05000000000000071, -9.499999999988844479, -57.10603087734755690 ) ) ;
#126285=VERTEX_POINT ( 'NONE', #76011 ) ;
#126300=EDGE_LOOP ( 'NONE', ( #196491, #15088, #83174, #34509 ) ) ;
#126322=VECTOR ( 'NONE', #9077, 1000.000000000000000 ) ;
#126330=CYLINDRICAL_SURFACE ( 'NONE', #103113, 4.049999999999998046 ) ;
#126350=CIRCLE ( 'NONE', #88733, 7.800000000000001599 ) ;
#126355=CARTESIAN_POINT ( 'NONE',  ( 18.59999999999999076, 11.75000000001115907, -58.35000000000000142 ) ) ;
#126367=CIRCLE ( 'NONE', #226292, 0.1000000000000028644 ) ;
#126376=PLANE ( 'NONE',  #125091 ) ;
#126384=CARTESIAN_POINT ( 'NONE',  ( -21.14999999999999858, 6.540656951712397138, -33.50000000000000000 ) ) ;
#126419=CARTESIAN_POINT ( 'NONE',  ( -21.09813707148783735, 0.03135149954058948085, -27.11493789426332413 ) ) ;
#126429=VERTEX_POINT ( 'NONE', #45868 ) ;
#126480=ORIENTED_EDGE ( 'NONE', *, *, #37329, .F. ) ;
#126508=FACE_OUTER_BOUND ( 'NONE', #72616, .T. ) ;
#126528=CIRCLE ( 'NONE', #97251, 0.2000000000000057288 ) ;
#126549=CARTESIAN_POINT ( 'NONE',  ( 23.14999999999999503, 11.65000000001116298, -21.75000000000000355 ) ) ;
#126560=VERTEX_POINT ( 'NONE', #32765 ) ;
#126567=CARTESIAN_POINT ( 'NONE',  ( -20.64999999999999858, 7.150000000011155876, -45.75000000000000000 ) ) ;
#126572=CARTESIAN_POINT ( 'NONE',  ( 20.94999999999999574, 14.00000000001115730, -38.92709253038254502 ) ) ;
#126611=AXIS2_PLACEMENT_3D ( 'NONE', #10003, #170415, #33462 ) ;
#126631=DIRECTION ( 'NONE',  ( 0.000000000000000000, 0.000000000000000000, -1.000000000000000000 ) ) ;
#126666=ORIENTED_EDGE ( 'NONE', *, *, #54762, .T. ) ;
#126677=DIRECTION ( 'NONE',  ( 0.000000000000000000, 0.000000000000000000, 1.000000000000000000 ) ) ;
#126691=CIRCLE ( 'NONE', #68249, 0.1000000000000010186 ) ;
#126693=VECTOR ( 'NONE', #79054, 1000.000000000000000 ) ;
#126695=ORIENTED_EDGE ( 'NONE', *, *, #123483, .F. ) ;
#126699=VERTEX_POINT ( 'NONE', #241212 ) ;
#126703=CARTESIAN_POINT ( 'NONE',  ( 18.50596464788227280, 10.30632246271648889, -72.50418367788958562 ) ) ;
#126707=CIRCLE ( 'NONE', #135047, 0.1000000000000001860 ) ;
#126773=CARTESIAN_POINT ( 'NONE',  ( -18.48408745364673322, -9.664322258651884212, -73.68307853332848367 ) ) ;
#126782=ORIENTED_EDGE ( 'NONE', *, *, #207151, .F. ) ;
#126800=DIRECTION ( 'NONE',  ( 0.000000000000000000, 0.000000000000000000, 1.000000000000000000 ) ) ;
#126803=ORIENTED_EDGE ( 'NONE', *, *, #104922, .F. ) ;
#126815=AXIS2_PLACEMENT_3D ( 'NONE', #114454, #216108, #134009 ) ;
#126827=AXIS2_PLACEMENT_3D ( 'NONE', #214639, #231667, #53000 ) ;
#126841=CARTESIAN_POINT ( 'NONE',  ( -20.64999999999999858, 7.250000000011155521, -45.85000000000000142 ) ) ;
#126873=CIRCLE ( 'NONE', #135036, 0.9750000000000036415 ) ;
#126874=CARTESIAN_POINT ( 'NONE',  ( -23.15000000000000213, 11.65000000001115588, -33.50000000000000000 ) ) ;
#126882=DIRECTION ( 'NONE',  ( -1.000000000000000000, 0.000000000000000000, 0.000000000000000000 ) ) ;
#126883=CARTESIAN_POINT ( 'NONE',  ( 23.24999999999999645, 1.115600667400684642E-11, -33.50000000000000000 ) ) ;
#126908=ORIENTED_EDGE ( 'NONE', *, *, #243718, .T. ) ;
#126913=ORIENTED_EDGE ( 'NONE', *, *, #118936, .F. ) ;
#126927=CARTESIAN_POINT ( 'NONE',  ( 23.24999999999999645, 5.000000000011153745, -45.90526601891310321 ) ) ;
#126943=LINE ( 'NONE', #143925, #37123 ) ;
#126965=DIRECTION ( 'NONE',  ( -1.000000000000000000, 0.000000000000000000, 0.000000000000000000 ) ) ;
#127006=AXIS2_PLACEMENT_3D ( 'NONE', #206848, #24381, #242113 ) ;
#127007=CARTESIAN_POINT ( 'NONE',  ( 21.00023020733503643, 1.115542391533913547E-11, -27.10913075473163403 ) ) ;
#127027=EDGE_LOOP ( 'NONE', ( #234697, #134170, #82201, #197355, #176539, #198861, #198219, #234301, #154623, #4182, #8, #11774, #90862, #124936, #164534, #13673 ) ) ;
#127063=CARTESIAN_POINT ( 'NONE',  ( -20.64999999999999858, 2.000000000011154189, -46.22462192276210402 ) ) ;
#127069=EDGE_CURVE ( 'NONE', #176891, #257458, #77944, .T. ) ;
#127077=CARTESIAN_POINT ( 'NONE',  ( 22.39999999999999503, -0.1008583690875579364, -21.75043287651061164 ) ) ;
#127078=VERTEX_POINT ( 'NONE', #217446 ) ;
#127084=ORIENTED_EDGE ( 'NONE', *, *, #121761, .T. ) ;
#127120=VERTEX_POINT ( 'NONE', #200478 ) ;
#127188=ORIENTED_EDGE ( 'NONE', *, *, #41246, .F. ) ;
#127189=FACE_OUTER_BOUND ( 'NONE', #6744, .T. ) ;
#127211=EDGE_CURVE ( 'NONE', #65925, #139968, #179004, .T. ) ;
#127234=ORIENTED_EDGE ( 'NONE', *, *, #74811, .F. ) ;
#127250=VERTEX_POINT ( 'NONE', #64805 ) ;
#127270=FACE_OUTER_BOUND ( 'NONE', #245511, .T. ) ;
#127278=VERTEX_POINT ( 'NONE', #150770 ) ;
#127284=EDGE_CURVE ( 'NONE', #154073, #6368, #37508, .T. ) ;
#127302=ORIENTED_EDGE ( 'NONE', *, *, #42333, .F. ) ;
#127306=CARTESIAN_POINT ( 'NONE',  ( -23.25000000000000000, 4.350000000011156054, -45.65000000000000568 ) ) ;
#127347=DIRECTION ( 'NONE',  ( 0.000000000000000000, 1.000000000000000000, -0.000000000000000000 ) ) ;
#127356=DIRECTION ( 'NONE',  ( 0.000000000000000000, 0.000000000000000000, 1.000000000000000000 ) ) ;
#127365=EDGE_CURVE ( 'NONE', #219135, #75871, #99808, .T. ) ;
#127386=ADVANCED_FACE ( 'NONE', ( #196303 ), #122891, .T. ) ;
#127442=VECTOR ( 'NONE', #230170, 1000.000000000000000 ) ;
#127479=DIRECTION ( 'NONE',  ( -1.000000000000000000, -1.040834085586090568E-13, 0.000000000000000000 ) ) ;
#127486=VERTEX_POINT ( 'NONE', #181589 ) ;
#127487=VERTEX_POINT ( 'NONE', #64194 ) ;
#127490=DIRECTION ( 'NONE',  ( 0.000000000000000000, 0.000000000000000000, -1.000000000000000000 ) ) ;
#127494=ADVANCED_FACE ( 'NONE', ( #201128 ), #214581, .T. ) ;
#127509=FACE_OUTER_BOUND ( 'NONE', #171844, .T. ) ;
#127517=FACE_OUTER_BOUND ( 'NONE', #31111, .T. ) ;
#127518=DIRECTION ( 'NONE',  ( 0.000000000000000000, 1.000000000000000000, 0.000000000000000000 ) ) ;
#127529=TOROIDAL_SURFACE ( 'NONE', #15103, 12.77499999999999858, 0.1000000000000000056 ) ;
#127545=CIRCLE ( 'NONE', #60890, 11.65000000000000036 ) ;
#127553=B_SPLINE_CURVE_WITH_KNOTS ( 'NONE', 3,
 ( #74360, #110881, #211268, #247824 ),
 .UNSPECIFIED., .F., .F.,
 ( 4, 4 ),
 ( 0.000000000000000000, 0.001767853679387111458 ),
 .UNSPECIFIED. ) ;
#127583=DIRECTION ( 'NONE',  ( 0.000000000000000000, 0.000000000000000000, -1.000000000000000000 ) ) ;
#127635=CIRCLE ( 'NONE', #44253, 4.049999999999998934 ) ;
#127636=ORIENTED_EDGE ( 'NONE', *, *, #221831, .F. ) ;
#127683=ADVANCED_FACE ( 'NONE', ( #211405 ), #168254, .T. ) ;
#127685=VERTEX_POINT ( 'NONE', #112317 ) ;
#127707=LINE ( 'NONE', #28652, #242596 ) ;
#127709=EDGE_CURVE ( 'NONE', #216121, #221539, #74503, .T. ) ;
#127717=DIRECTION ( 'NONE',  ( -1.000000000000000000, -2.952720810173289112E-16, 0.000000000000000000 ) ) ;
#127729=CARTESIAN_POINT ( 'NONE',  ( 21.14999999999999858, 11.75000000001116263, -21.75000000000000355 ) ) ;
#127734=VERTEX_POINT ( 'NONE', #178733 ) ;
#127748=LINE ( 'NONE', #6495, #22248 ) ;
#127770=ORIENTED_EDGE ( 'NONE', *, *, #223980, .F. ) ;
#127806=CARTESIAN_POINT ( 'NONE',  ( 21.05000000000000071, 6.540656951712400691, -33.60000000000000142 ) ) ;
#127819=EDGE_CURVE ( 'NONE', #190151, #70987, #117326, .T. ) ;
#127844=DIRECTION ( 'NONE',  ( 1.000000000000000000, 0.000000000000000000, 0.000000000000000000 ) ) ;
#127846=EDGE_CURVE ( 'NONE', #152028, #154736, #87276, .T. ) ;
#127860=CARTESIAN_POINT ( 'NONE',  ( -22.59066674512253670, 11.75000000001115552, -33.46949587636949275 ) ) ;
#127862=CARTESIAN_POINT ( 'NONE',  ( -23.15000000000000213, 1.115600667400684642E-11, -33.50000000000000000 ) ) ;
#127865=ORIENTED_EDGE ( 'NONE', *, *, #250932, .F. ) ;
#127896=EDGE_CURVE ( 'NONE', #186298, #150427, #244519, .T. ) ;
#127914=EDGE_CURVE ( 'NONE', #216222, #216494, #7183, .T. ) ;
#127916=AXIS2_PLACEMENT_3D ( 'NONE', #143840, #185553, #25215 ) ;
#127953=CARTESIAN_POINT ( 'NONE',  ( -23.15000000000000213, 1.115600667400684642E-11, -67.00000000000000000 ) ) ;
#127975=EDGE_CURVE ( 'NONE', #52785, #15098, #89851, .T. ) ;
#127983=EDGE_LOOP ( 'NONE', ( #67564, #53657, #223057, #105090 ) ) ;
#127988=ORIENTED_EDGE ( 'NONE', *, *, #213214, .T. ) ;
#127992=LINE ( 'NONE', #165847, #202978 ) ;
#127994=CARTESIAN_POINT ( 'NONE',  ( 18.54148534481893407, 10.32532329027886675, -72.56993430183595706 ) ) ;
#128001=ORIENTED_EDGE ( 'NONE', *, *, #210980, .T. ) ;
#128015=CARTESIAN_POINT ( 'NONE',  ( 21.14999999999999503, -0.09999999998884338825, -21.85042919245520210 ) ) ;
#128040=CYLINDRICAL_SURFACE ( 'NONE', #25667, 0.09999999999999939493 ) ;
#128047=DIRECTION ( 'NONE',  ( 0.000000000000000000, 0.1350103645451904977, -0.9908441862701596881 ) ) ;
#128086=ORIENTED_EDGE ( 'NONE', *, *, #213079, .F. ) ;
#128098=DIRECTION ( 'NONE',  ( -1.000000000000000000, -0.000000000000000000, 0.000000000000000000 ) ) ;
#128112=CARTESIAN_POINT ( 'NONE',  ( -21.05000000000000071, 1.115600667400684642E-11, -33.50000000000000000 ) ) ;
#128115=LINE ( 'NONE', #207663, #23141 ) ;
#128121=AXIS2_PLACEMENT_3D ( 'NONE', #106972, #69169, #127844 ) ;
#128127=DIRECTION ( 'NONE',  ( 0.000000000000000000, -1.000000000000000000, 0.000000000000000000 ) ) ;
#128135=TOROIDAL_SURFACE ( 'NONE', #182303, 0.4000000000000010214, 0.1000000000000000056 ) ;
#128139=CARTESIAN_POINT ( 'NONE',  ( 23.24999999999999645, 1.115600667400684642E-11, -33.50000000000000000 ) ) ;
#128215=DIRECTION ( 'NONE',  ( -1.000000000000000000, 0.000000000000000000, 0.000000000000000000 ) ) ;
#128224=VERTEX_POINT ( 'NONE', #124838 ) ;
#128225=CARTESIAN_POINT ( 'NONE',  ( -21.14999999999999858, 6.540656951712397138, -33.50000000000000000 ) ) ;
#128326=FACE_OUTER_BOUND ( 'NONE', #238335, .T. ) ;
#128339=EDGE_LOOP ( 'NONE', ( #233009, #257531, #214822, #7223 ) ) ;
#128366=VECTOR ( 'NONE', #257603, 1000.000000000000000 ) ;
#128377=CARTESIAN_POINT ( 'NONE',  ( 20.95512820512820440, 8.876151316299271343, -54.75000000000000000 ) ) ;
#128407=CIRCLE ( 'NONE', #207535, 0.09999999999999996392 ) ;
#128417=CARTESIAN_POINT ( 'NONE',  ( -22.42253884134832020, 0.001932351146464880492, -21.85039430265157634 ) ) ;
#128427=FACE_OUTER_BOUND ( 'NONE', #153922, .T. ) ;
#128449=ORIENTED_EDGE ( 'NONE', *, *, #99233, .F. ) ;
#128452=EDGE_CURVE ( 'NONE', #180952, #201418, #240479, .T. ) ;
#128479=LINE ( 'NONE', #91907, #124164 ) ;
#128481=DIRECTION ( 'NONE',  ( 0.000000000000000000, 0.000000000000000000, -1.000000000000000000 ) ) ;
#128491=ORIENTED_EDGE ( 'NONE', *, *, #116483, .F. ) ;
#128501=TOROIDAL_SURFACE ( 'NONE', #11827, 0.2000000000000000111, 0.1000000000000000056 ) ;
#128504=ADVANCED_FACE ( 'NONE', ( #69565 ), #48687, .T. ) ;
#128514=FACE_OUTER_BOUND ( 'NONE', #192067, .T. ) ;
#128602=ORIENTED_EDGE ( 'NONE', *, *, #244179, .T. ) ;
#128604=DIRECTION ( 'NONE',  ( 0.000000000000000000, 0.9908441862701596881, -0.1350103645451904977 ) ) ;
#128605=ADVANCED_FACE ( 'NONE', ( #154273 ), #134631, .F. ) ;
#128622=DIRECTION ( 'NONE',  ( 0.000000000000000000, 0.000000000000000000, -1.000000000000000000 ) ) ;
#128629=AXIS2_PLACEMENT_3D ( 'NONE', #940, #123498, #23135 ) ;
#128660=ORIENTED_EDGE ( 'NONE', *, *, #230553, .T. ) ;
#128663=CARTESIAN_POINT ( 'NONE',  ( -23.15000000000000213, 2.000000000011154189, -46.72462192276210402 ) ) ;
#128675=PLANE ( 'NONE',  #235448 ) ;
#128704=FACE_OUTER_BOUND ( 'NONE', #23577, .T. ) ;
#128744=EDGE_LOOP ( 'NONE', ( #90230, #67963, #257972, #177582 ) ) ;
#128759=ORIENTED_EDGE ( 'NONE', *, *, #108636, .T. ) ;
#128763=DIRECTION ( 'NONE',  ( 1.000000000000000000, 0.000000000000000000, 0.000000000000000000 ) ) ;
#128765=EDGE_LOOP ( 'NONE', ( #25892, #163872, #204470, #9977, #209602, #115718, #101676, #237119, #110750, #204999, #100731 ) ) ;
#128773=DIRECTION ( 'NONE',  ( 0.000000000000000000, 0.000000000000000000, 1.000000000000000000 ) ) ;
#128778=CARTESIAN_POINT ( 'NONE',  ( 21.05000000000000071, 10.72371710471867701, -45.65000000000000568 ) ) ;
#128790=ORIENTED_EDGE ( 'NONE', *, *, #115906, .F. ) ;
#128805=AXIS2_PLACEMENT_3D ( 'NONE', #215512, #101957, #197240 ) ;
#128821=TOROIDAL_SURFACE ( 'NONE', #212027, 11.70000000000000107, 0.1000000000000000056 ) ;
#128866=DIRECTION ( 'NONE',  ( 1.000000000000000000, 0.000000000000000000, -0.000000000000000000 ) ) ;
#128871=CARTESIAN_POINT ( 'NONE',  ( 20.94999999999999929, 1.115600667400684642E-11, -69.00000000000000000 ) ) ;
#128890=ORIENTED_EDGE ( 'NONE', *, *, #127284, .T. ) ;
#128897=CARTESIAN_POINT ( 'NONE',  ( 22.50014994444008209, 11.74971973190328534, -33.41691984328090825 ) ) ;
#128925=ORIENTED_EDGE ( 'NONE', *, *, #183919, .F. ) ;
#128949=EDGE_CURVE ( 'NONE', #77793, #141325, #49831, .T. ) ;
#128989=ORIENTED_EDGE ( 'NONE', *, *, #145227, .T. ) ;
#128993=DIRECTION ( 'NONE',  ( -0.000000000000000000, 1.000000000000000000, -0.000000000000000000 ) ) ;
#128999=CIRCLE ( 'NONE', #112433, 0.1000000000000028644 ) ;
#129014=AXIS2_PLACEMENT_3D ( 'NONE', #139715, #22379, #101866 ) ;
#129105=VERTEX_POINT ( 'NONE', #16821 ) ;
#129107=LINE ( 'NONE', #9155, #63566 ) ;
#129115=DIRECTION ( 'NONE',  ( -1.000000000000000000, 0.000000000000000000, -0.000000000000000000 ) ) ;
#129137=CARTESIAN_POINT ( 'NONE',  ( -22.59999999999999787, 11.74956712350054744, -33.39914163090129762 ) ) ;
#129154=CARTESIAN_POINT ( 'NONE',  ( -1.820710678118658388, -9.929289321870186313, -58.15000000000000568 ) ) ;
#129162=ORIENTED_EDGE ( 'NONE', *, *, #41246, .T. ) ;
#129174=AXIS2_PLACEMENT_3D ( 'NONE', #190195, #28598, #191496 ) ;
#129184=DIRECTION ( 'NONE',  ( -4.448008912761043807E-16, 1.000000000000000000, 0.000000000000000000 ) ) ;
#129239=CARTESIAN_POINT ( 'NONE',  ( -23.25000000000000000, 1.115600667400684642E-11, -33.50000000000000000 ) ) ;
#129254=DIRECTION ( 'NONE',  ( -1.000000000000000000, 0.000000000000000000, 0.000000000000000000 ) ) ;
#129263=AXIS2_PLACEMENT_3D ( 'NONE', #106859, #222956, #62622 ) ;
#129274=CARTESIAN_POINT ( 'NONE',  ( 23.14999999999998437, 11.75000000001115552, -33.50000000000000000 ) ) ;
#129283=CIRCLE ( 'NONE', #254158, 0.5000000000000004441 ) ;
#129308=ORIENTED_EDGE ( 'NONE', *, *, #123917, .T. ) ;
#129346=AXIS2_PLACEMENT_3D ( 'NONE', #227312, #249466, #33023 ) ;
#129356=DIRECTION ( 'NONE',  ( 0.000000000000000000, 0.000000000000000000, 1.000000000000000000 ) ) ;
#129370=VERTEX_POINT ( 'NONE', #12666 ) ;
#129396=ORIENTED_EDGE ( 'NONE', *, *, #1607, .F. ) ;
#129403=PLANE ( 'NONE',  #188671 ) ;
#129449=DIRECTION ( 'NONE',  ( 0.000000000000000000, 0.000000000000000000, -1.000000000000000000 ) ) ;
#129478=EDGE_CURVE ( 'NONE', #226022, #245137, #103389, .T. ) ;
#129530=CIRCLE ( 'NONE', #221086, 0.1000000000000028644 ) ;
#129540=AXIS2_PLACEMENT_3D ( 'NONE', #131755, #74393, #215148 ) ;
#129542=EDGE_CURVE ( 'NONE', #14799, #214929, #76453, .T. ) ;
#129679=CARTESIAN_POINT ( 'NONE',  ( -20.94999999999999929, -1.135018845899022466, -74.71697688343232358 ) ) ;
#129685=AXIS2_PLACEMENT_3D ( 'NONE', #33013, #156787, #231187 ) ;
#129700=VERTEX_POINT ( 'NONE', #219818 ) ;
#129750=AXIS2_PLACEMENT_3D ( 'NONE', #167565, #30619, #110126 ) ;
#129757=CARTESIAN_POINT ( 'NONE',  ( -21.05000000000000071, 1.835341550235567887, -45.05515129256298223 ) ) ;
#129759=CARTESIAN_POINT ( 'NONE',  ( -23.15000000000000213, -11.48912529306489994, -63.89999999999999858 ) ) ;
#129770=LINE ( 'NONE', #170242, #23618 ) ;
#129777=AXIS2_PLACEMENT_3D ( 'NONE', #14344, #33934, #114697 ) ;
#129785=CARTESIAN_POINT ( 'NONE',  ( 19.58285714285715073, 9.015001489659738354, -41.92065281608173422 ) ) ;
#129820=SPHERICAL_SURFACE ( 'NONE', #159433, 0.1000000000000000056 ) ;
#129830=VECTOR ( 'NONE', #170324, 1000.000000000000000 ) ;
#129894=DIRECTION ( 'NONE',  ( -1.000000000000000000, 0.000000000000000000, 0.000000000000000000 ) ) ;
#129896=DIRECTION ( 'NONE',  ( -1.000000000000000000, 0.000000000000000000, 0.000000000000000000 ) ) ;
#129956=CARTESIAN_POINT ( 'NONE',  ( 21.05000000000000071, -12.41227409413852811, -64.00000000000000000 ) ) ;
#129976=DIRECTION ( 'NONE',  ( 0.9880948137434723000, 0.1538461538461484146, -0.000000000000000000 ) ) ;
#130052=VECTOR ( 'NONE', #137612, 1000.000000000000000 ) ;
#130054=AXIS2_PLACEMENT_3D ( 'NONE', #11751, #172128, #156409 ) ;
#130075=LINE ( 'NONE', #135199, #179328 ) ;
#130080=AXIS2_PLACEMENT_3D ( 'NONE', #75058, #82688, #3169 ) ;
#130160=VECTOR ( 'NONE', #163723, 1000.000000000000000 ) ;
#130184=ORIENTED_EDGE ( 'NONE', *, *, #226947, .T. ) ;
#130208=SPHERICAL_SURFACE ( 'NONE', #78618, 0.1000000000000000056 ) ;
#130216=CIRCLE ( 'NONE', #200972, 0.09999999999999939493 ) ;
#130231=DIRECTION ( 'NONE',  ( 0.000000000000000000, -0.8660254037844383745, 0.5000000000000003331 ) ) ;
#130236=LINE ( 'NONE', #209796, #171170 ) ;
#130259=DIRECTION ( 'NONE',  ( 0.000000000000000000, 0.000000000000000000, -1.000000000000000000 ) ) ;
#130322=DIRECTION ( 'NONE',  ( 0.000000000000000000, 0.000000000000000000, -1.000000000000000000 ) ) ;
#130354=EDGE_CURVE ( 'NONE', #225394, #123416, #12043, .T. ) ;
#130366=CIRCLE ( 'NONE', #130556, 0.09999999999999939493 ) ;
#130367=FACE_OUTER_BOUND ( 'NONE', #193063, .T. ) ;
#130373=CARTESIAN_POINT ( 'NONE',  ( 21.05000000000000071, -9.399999999988844834, -57.10603087734755690 ) ) ;
#130379=CARTESIAN_POINT ( 'NONE',  ( 18.59999999999999076, 6.450000000011156587, -54.65000000000000568 ) ) ;
#130388=LINE ( 'NONE', #33920, #191053 ) ;
#130418=VERTEX_POINT ( 'NONE', #41896 ) ;
#130437=DIRECTION ( 'NONE',  ( 1.000000000000000000, 2.952720810173289112E-16, -0.000000000000000000 ) ) ;
#130447=AXIS2_PLACEMENT_3D ( 'NONE', #8016, #148807, #192742 ) ;
#130486=EDGE_CURVE ( 'NONE', #147965, #139128, #249551, .T. ) ;
#130517=VECTOR ( 'NONE', #39388, 1000.000000000000000 ) ;
#130556=AXIS2_PLACEMENT_3D ( 'NONE', #226028, #26601, #126965 ) ;
#130567=AXIS2_PLACEMENT_3D ( 'NONE', #34231, #113731, #135845 ) ;
#130568=CARTESIAN_POINT ( 'NONE',  ( 18.43630871534869797, -9.679800874791796517, -73.66063206798409624 ) ) ;
#130575=CARTESIAN_POINT ( 'NONE',  ( -20.54999999999999716, 2.400000000011155432, -53.77537807723790309 ) ) ;
#130580=AXIS2_PLACEMENT_3D ( 'NONE', #121625, #64195, #165878 ) ;
#130589=AXIS2_PLACEMENT_3D ( 'NONE', #114458, #51893, #251395 ) ;
#130616=ORIENTED_EDGE ( 'NONE', *, *, #180464, .F. ) ;
#130654=DIRECTION ( 'NONE',  ( 1.836970198721029934E-16, -1.000000000000000000, -0.000000000000000000 ) ) ;
#130666=EDGE_LOOP ( 'NONE', ( #121481, #188730, #133427, #135495 ) ) ;
#130676=ORIENTED_EDGE ( 'NONE', *, *, #68031, .F. ) ;
#130680=DIRECTION ( 'NONE',  ( 0.000000000000000000, -0.8777080977375132376, 0.4791956752371582251 ) ) ;
#130714=CARTESIAN_POINT ( 'NONE',  ( 18.40000000000000213, -9.499999999988840926, -40.49936209718013913 ) ) ;
#130736=CARTESIAN_POINT ( 'NONE',  ( -18.59999999999999787, 9.150000000011157653, -54.65000000000000568 ) ) ;
#130752=DIRECTION ( 'NONE',  ( 0.000000000000000000, 0.9908441862701596881, 0.1350103645451904977 ) ) ;
#130771=DIRECTION ( 'NONE',  ( -1.836970198721029934E-16, 1.000000000000000000, 0.000000000000000000 ) ) ;
#130780=DIRECTION ( 'NONE',  ( 0.000000000000000000, 0.000000000000000000, -1.000000000000000000 ) ) ;
#130813=EDGE_CURVE ( 'NONE', #223187, #86704, #37343, .T. ) ;
#130835=CARTESIAN_POINT ( 'NONE',  ( -23.15000000000000213, 11.65000000001115588, -21.75000000000000355 ) ) ;
#130842=LINE ( 'NONE', #173877, #170663 ) ;
#130854=CARTESIAN_POINT ( 'NONE',  ( 23.24999999999999645, 1.115600667400684642E-11, -67.00000000000000000 ) ) ;
#130864=CARTESIAN_POINT ( 'NONE',  ( 22.47071067811865319, 7.720074744509199505, -33.40090754529740025 ) ) ;
#130896=CARTESIAN_POINT ( 'NONE',  ( -18.59999999999999787, -9.399999999988851940, -73.88204184817267617 ) ) ;
#130902=CARTESIAN_POINT ( 'NONE',  ( 23.24999999999999289, 11.75000000001116263, -33.60000000000000142 ) ) ;
#130907=AXIS2_PLACEMENT_3D ( 'NONE', #51887, #11520, #131445 ) ;
#130921=DIRECTION ( 'NONE',  ( 1.000000000000000000, 0.000000000000000000, -0.000000000000000000 ) ) ;
#130941=ORIENTED_EDGE ( 'NONE', *, *, #37329, .T. ) ;
#130957=ORIENTED_EDGE ( 'NONE', *, *, #237116, .F. ) ;
#130961=CARTESIAN_POINT ( 'NONE',  ( -20.05000000000000426, 9.250000000011157297, -45.85000000000000142 ) ) ;
#130964=LINE ( 'NONE', #14890, #208531 ) ;
#130965=CIRCLE ( 'NONE', #18549, 0.1000000000000028644 ) ;
#130981=VERTEX_POINT ( 'NONE', #24592 ) ;
#130996=DIRECTION ( 'NONE',  ( -0.000000000000000000, 0.000000000000000000, -1.000000000000000000 ) ) ;
#131019=DIRECTION ( 'NONE',  ( 0.000000000000000000, 0.000000000000000000, -1.000000000000000000 ) ) ;
#131034=CARTESIAN_POINT ( 'NONE',  ( -18.50000324121759121, 10.29307482169070376, -72.45864214669403225 ) ) ;
#131039=DIRECTION ( 'NONE',  ( 1.000000000000000000, -0.000000000000000000, -0.000000000000000000 ) ) ;
#131047=VERTEX_POINT ( 'NONE', #94467 ) ;
#131066=CARTESIAN_POINT ( 'NONE',  ( 21.05000000000000071, 10.72371681401022592, -41.09439923588420385 ) ) ;
#131074=FACE_OUTER_BOUND ( 'NONE', #91131, .T. ) ;
#131114=ORIENTED_EDGE ( 'NONE', *, *, #64050, .F. ) ;
#131141=AXIS2_PLACEMENT_3D ( 'NONE', #126883, #185566, #244239 ) ;
#131153=VECTOR ( 'NONE', #153136, 1000.000000000000114 ) ;
#131165=CIRCLE ( 'NONE', #181270, 0.09999999999999939493 ) ;
#131177=CARTESIAN_POINT ( 'NONE',  ( 20.94999999999999929, 8.926614585098253229, -41.97168301922312850 ) ) ;
#131179=CIRCLE ( 'NONE', #22884, 0.5000000000000013323 ) ;
#131180=CARTESIAN_POINT ( 'NONE',  ( -23.15000000000000213, 2.000000000011154189, -53.77537807723790309 ) ) ;
#131182=EDGE_LOOP ( 'NONE', ( #207986, #211909, #220757, #52710 ) ) ;
#131213=CARTESIAN_POINT ( 'NONE',  ( 20.00000000000000355, 11.75000000001116263, -58.14999999999999858 ) ) ;
#131220=CARTESIAN_POINT ( 'NONE',  ( -23.15000000000000213, 1.115626384983466744E-11, -64.90000000000000568 ) ) ;
#131237=VERTEX_POINT ( 'NONE', #120495 ) ;
#131240=ADVANCED_FACE ( 'NONE', ( #244245 ), #39673, .T. ) ;
#131266=CARTESIAN_POINT ( 'NONE',  ( 21.14999999999999858, 6.540656951712400691, -33.50000000000000000 ) ) ;
#131311=ORIENTED_EDGE ( 'NONE', *, *, #84950, .T. ) ;
#131325=DIRECTION ( 'NONE',  ( -0.000000000000000000, 0.1350103645451649625, -0.9908441862701631297 ) ) ;
#131335=ORIENTED_EDGE ( 'NONE', *, *, #145404, .F. ) ;
#131343=EDGE_CURVE ( 'NONE', #105461, #42156, #150315, .T. ) ;
#131352=CIRCLE ( 'NONE', #214738, 0.1000000000000028644 ) ;
#131363=ORIENTED_EDGE ( 'NONE', *, *, #115016, .F. ) ;
#131377=CIRCLE ( 'NONE', #123189, 12.97499999999999964 ) ;
#131425=FACE_OUTER_BOUND ( 'NONE', #111776, .T. ) ;
#131445=DIRECTION ( 'NONE',  ( 0.000000000000000000, -0.9908441862701596881, -0.1350103645451904977 ) ) ;
#131449=EDGE_CURVE ( 'NONE', #140899, #91127, #58521, .T. ) ;
#131450=ORIENTED_EDGE ( 'NONE', *, *, #74924, .T. ) ;
#131455=CARTESIAN_POINT ( 'NONE',  ( 20.94999999999999929, -11.64999999998883595, -64.10000000000000853 ) ) ;
#131464=EDGE_CURVE ( 'NONE', #129700, #36910, #12783, .T. ) ;
#131507=EDGE_CURVE ( 'NONE', #88666, #71915, #220842, .T. ) ;
#131535=ORIENTED_EDGE ( 'NONE', *, *, #212079, .F. ) ;
#131540=ORIENTED_EDGE ( 'NONE', *, *, #105260, .F. ) ;
#131561=ORIENTED_EDGE ( 'NONE', *, *, #141209, .F. ) ;
#131576=DIRECTION ( 'NONE',  ( 0.000000000000000000, 0.000000000000000000, -1.000000000000000000 ) ) ;
#131580=ORIENTED_EDGE ( 'NONE', *, *, #109988, .F. ) ;
#131598=AXIS2_PLACEMENT_3D ( 'NONE', #147001, #33540, #226527 ) ;
#131607=DIRECTION ( 'NONE',  ( 0.000000000000000000, 0.000000000000000000, 1.000000000000000000 ) ) ;
#131608=ORIENTED_EDGE ( 'NONE', *, *, #65565, .F. ) ;
#131615=TOROIDAL_SURFACE ( 'NONE', #6723, 12.97499999999999787, 0.1000000000000000056 ) ;
#131679=EDGE_CURVE ( 'NONE', #17700, #257458, #41819, .T. ) ;
#131707=CIRCLE ( 'NONE', #69547, 11.70000000000000284 ) ;
#131713=ORIENTED_EDGE ( 'NONE', *, *, #15903, .T. ) ;
#131718=DIRECTION ( 'NONE',  ( 0.000000000000000000, 0.000000000000000000, 1.000000000000000000 ) ) ;
#131723=CARTESIAN_POINT ( 'NONE',  ( -21.46681500593267700, 6.857511159395789591, -33.50000000000000711 ) ) ;
#131730=CARTESIAN_POINT ( 'NONE',  ( -23.15000000000000213, 1.115600667400684642E-11, -67.00000000000000000 ) ) ;
#131744=AXIS2_PLACEMENT_3D ( 'NONE', #125307, #26214, #229548 ) ;
#131746=CARTESIAN_POINT ( 'NONE',  ( -18.59999999999999787, -1.249999999988843369, -41.50000000000000000 ) ) ;
#131755=CARTESIAN_POINT ( 'NONE',  ( -23.25000000000000000, 1.115600667400684642E-11, -67.00000000000000000 ) ) ;
#131765=CYLINDRICAL_SURFACE ( 'NONE', #737, 0.09999999999999939493 ) ;
#131767=ADVANCED_FACE ( 'NONE', ( #246523 ), #71213, .F. ) ;
#131812=AXIS2_PLACEMENT_3D ( 'NONE', #207908, #149216, #245731 ) ;
#131830=CARTESIAN_POINT ( 'NONE',  ( -20.85000000000000142, 11.65000000001115232, -67.00000000000000000 ) ) ;
#131863=CARTESIAN_POINT ( 'NONE',  ( 18.49999999999999645, -9.480686695267818820, -73.94111516875784673 ) ) ;
#131882=ORIENTED_EDGE ( 'NONE', *, *, #253283, .T. ) ;
#131885=DIRECTION ( 'NONE',  ( 0.000000000000000000, 0.000000000000000000, -1.000000000000000000 ) ) ;
#131911=ORIENTED_EDGE ( 'NONE', *, *, #166895, .F. ) ;
#131926=AXIS2_PLACEMENT_3D ( 'NONE', #134265, #213824, #80708 ) ;
#131927=CIRCLE ( 'NONE', #23639, 0.1000000000000028644 ) ;
#131966=DIRECTION ( 'NONE',  ( -0.000000000000000000, -0.000000000000000000, 1.000000000000000000 ) ) ;
#131968=ORIENTED_EDGE ( 'NONE', *, *, #69669, .F. ) ;
#131975=CARTESIAN_POINT ( 'NONE',  ( -23.25000000000000000, -1.164121893230052995, -74.91484808557160591 ) ) ;
#131987=VERTEX_POINT ( 'NONE', #98976 ) ;
#132004=CARTESIAN_POINT ( 'NONE',  ( 18.51565452909389009, -9.352859338825282975, -40.69490932123330396 ) ) ;
#132012=CIRCLE ( 'NONE', #102758, 0.09999999999999939493 ) ;
#132014=CYLINDRICAL_SURFACE ( 'NONE', #89617, 0.1000000000000028644 ) ;
#132020=ORIENTED_EDGE ( 'NONE', *, *, #185338, .F. ) ;
#132053=DIRECTION ( 'NONE',  ( 1.000000000000000000, 0.000000000000000000, 0.000000000000000000 ) ) ;
#132059=ORIENTED_EDGE ( 'NONE', *, *, #173309, .F. ) ;
#132072=FACE_OUTER_BOUND ( 'NONE', #58758, .T. ) ;
#132078=AXIS2_PLACEMENT_3D ( 'NONE', #182772, #82337, #61533 ) ;
#132080=EDGE_CURVE ( 'NONE', #84007, #51091, #17237, .T. ) ;
#132088=LINE ( 'NONE', #211637, #9270 ) ;
#132090=AXIS2_PLACEMENT_3D ( 'NONE', #48049, #204556, #7654 ) ;
#132102=CARTESIAN_POINT ( 'NONE',  ( 23.25000000000000000, 6.550000000011156231, -45.85000000000000142 ) ) ;
#132118=AXIS2_PLACEMENT_3D ( 'NONE', #242516, #183829, #143416 ) ;
#132136=TOROIDAL_SURFACE ( 'NONE', #111294, 1.900000000000002576, 0.1000000000000000056 ) ;
#132146=ORIENTED_EDGE ( 'NONE', *, *, #218457, .F. ) ;
#132151=CARTESIAN_POINT ( 'NONE',  ( 18.49999999999998934, 6.550000000011156231, -54.65000000000000568 ) ) ;
#132167=EDGE_CURVE ( 'NONE', #159251, #126285, #191421, .T. ) ;
#132193=ADVANCED_FACE ( 'NONE', ( #212252 ), #56231, .T. ) ;
#132207=DIRECTION ( 'NONE',  ( 1.000000000000000000, -0.000000000000000000, -0.000000000000000000 ) ) ;
#132208=EDGE_CURVE ( 'NONE', #231817, #64423, #252629, .T. ) ;
#132232=CARTESIAN_POINT ( 'NONE',  ( 21.05000000000000071, -11.48912529306489994, -63.89999999999999858 ) ) ;
#132240=DIRECTION ( 'NONE',  ( 0.000000000000000000, 0.000000000000000000, 1.000000000000000000 ) ) ;
#132247=CARTESIAN_POINT ( 'NONE',  ( -21.55000000000000426, 7.708578643773852157, -45.85000000000000142 ) ) ;
#132301=ORIENTED_EDGE ( 'NONE', *, *, #244179, .F. ) ;
#132326=AXIS2_PLACEMENT_3D ( 'NONE', #129757, #131039, #192309 ) ;
#132337=DIRECTION ( 'NONE',  ( 1.000000000000000000, 0.000000000000000000, 0.000000000000000000 ) ) ;
#132376=VECTOR ( 'NONE', #193589, 1000.000000000000000 ) ;
#132387=CARTESIAN_POINT ( 'NONE',  ( 20.94999999999999929, 5.850000000011105428, -43.63249722427796939 ) ) ;
#132393=AXIS2_PLACEMENT_3D ( 'NONE', #66271, #90956, #170559 ) ;
#132417=VERTEX_POINT ( 'NONE', #93035 ) ;
#132432=CARTESIAN_POINT ( 'NONE',  ( -23.25000000000000000, -1.835859311432481045, -78.50443916879852679 ) ) ;
#132507=CARTESIAN_POINT ( 'NONE',  ( 19.81427058490557158, 11.66856398039207932, -58.25000000000000000 ) ) ;
#132527=CARTESIAN_POINT ( 'NONE',  ( -20.85000000000000142, 6.933893972137497030, -70.78564583437358237 ) ) ;
#132560=CARTESIAN_POINT ( 'NONE',  ( 21.07971444708685738, 6.329792081637703127, -33.41217656368210243 ) ) ;
#132601=CARTESIAN_POINT ( 'NONE',  ( 18.59999999999999076, 10.20857864377385127, -54.85000000000000142 ) ) ;
#132623=ORIENTED_EDGE ( 'NONE', *, *, #138648, .F. ) ;
#132681=CYLINDRICAL_SURFACE ( 'NONE', #257748, 12.87499999999999822 ) ;
#132695=DIRECTION ( 'NONE',  ( 0.000000000000000000, -0.1455152366551522025, -0.9893560106964505163 ) ) ;
#132709=LINE ( 'NONE', #133968, #232070 ) ;
#132718=TOROIDAL_SURFACE ( 'NONE', #57666, 0.4000000000000015210, 0.1000000000000000056 ) ;
#132774=DIRECTION ( 'NONE',  ( -1.000000000000000000, -2.952720810173289112E-16, 0.000000000000000000 ) ) ;
#132819=DIRECTION ( 'NONE',  ( -1.000000000000000000, -2.952720810173289112E-16, 0.000000000000000000 ) ) ;
#132857=CARTESIAN_POINT ( 'NONE',  ( -21.05000000000000071, -11.74999999998884448, -63.89999999999999858 ) ) ;
#132871=ORIENTED_EDGE ( 'NONE', *, *, #202124, .T. ) ;
#132879=DIRECTION ( 'NONE',  ( 0.000000000000000000, 0.1298341882520022694, 0.9915357197604852679 ) ) ;
#132882=AXIS2_PLACEMENT_3D ( 'NONE', #183597, #166633, #6223 ) ;
#132947=ADVANCED_FACE ( 'NONE', ( #179981 ), #160436, .T. ) ;
#132952=DIRECTION ( 'NONE',  ( 0.000000000000000000, 0.000000000000000000, -1.000000000000000000 ) ) ;
#132960=TOROIDAL_SURFACE ( 'NONE', #241296, 0.4000000000000005773, 0.1000000000000000056 ) ;
#132967=CARTESIAN_POINT ( 'NONE',  ( -23.15000000000000213, 4.150000000011156764, -45.85000000000000142 ) ) ;
#132987=CARTESIAN_POINT ( 'NONE',  ( 21.05000000000000071, -0.09999999998884338825, -26.95934304829875927 ) ) ;
#132995=EDGE_CURVE ( 'NONE', #52403, #67483, #196630, .T. ) ;
#133016=CARTESIAN_POINT ( 'NONE',  ( -18.46902351632713035, -9.509470118669714367, -40.48645393425731953 ) ) ;
#133021=CARTESIAN_POINT ( 'NONE',  ( -21.53699400380027029, 6.787711793208516475, -33.50000000000000711 ) ) ;
#133041=EDGE_CURVE ( 'NONE', #141325, #96628, #202103, .T. ) ;
#133051=ORIENTED_EDGE ( 'NONE', *, *, #162388, .F. ) ;
#133065=CARTESIAN_POINT ( 'NONE',  ( -18.59999999999999787, 1.851028230152016674, -45.15391326942249606 ) ) ;
#133079=VERTEX_POINT ( 'NONE', #3896 ) ;
#133095=VERTEX_POINT ( 'NONE', #45593 ) ;
#133139=VECTOR ( 'NONE', #17240, 1000.000000000000000 ) ;
#133153=ADVANCED_FACE ( 'NONE', ( #65143 ), #125142, .F. ) ;
#133154=CARTESIAN_POINT ( 'NONE',  ( 18.33996824403467940, -9.569639859420588479, -73.81906563751665828 ) ) ;
#133161=DIRECTION ( 'NONE',  ( 0.000000000000000000, -0.000000000000000000, 1.000000000000000000 ) ) ;
#133168=ORIENTED_EDGE ( 'NONE', *, *, #54155, .T. ) ;
#133176=ORIENTED_EDGE ( 'NONE', *, *, #154139, .T. ) ;
#133201=EDGE_LOOP ( 'NONE', ( #20524, #228618, #27553, #231359 ) ) ;
#133224=DIRECTION ( 'NONE',  ( 0.000000000000000000, -1.000000000000000000, 0.000000000000000000 ) ) ;
#133244=VERTEX_POINT ( 'NONE', #110699 ) ;
#133264=DIRECTION ( 'NONE',  ( 0.000000000000000000, -0.9908441862701596881, 0.1350103645451899148 ) ) ;
#133274=FACE_OUTER_BOUND ( 'NONE', #187473, .T. ) ;
#133318=PLANE ( 'NONE',  #190816 ) ;
#133324=CARTESIAN_POINT ( 'NONE',  ( 21.70464131381650219, 7.095358018979006864, -33.50000000000000000 ) ) ;
#133358=CARTESIAN_POINT ( 'NONE',  ( -21.06715728752538652, 11.75000000001115197, -40.51480577065400013 ) ) ;
#133418=CARTESIAN_POINT ( 'NONE',  ( 23.15000000000000213, -11.48912529306489816, -63.89999999999999858 ) ) ;
#133423=ORIENTED_EDGE ( 'NONE', *, *, #56258, .T. ) ;
#133427=ORIENTED_EDGE ( 'NONE', *, *, #227507, .F. ) ;
#133474=CARTESIAN_POINT ( 'NONE',  ( 21.04999999999999716, 6.441084688482481724, -33.51771943330863479 ) ) ;
#133481=ADVANCED_FACE ( 'NONE', ( #81798 ), #82858, .T. ) ;
#133502=EDGE_LOOP ( 'NONE', ( #175037, #122957 ) ) ;
#133511=FACE_OUTER_BOUND ( 'NONE', #156689, .T. ) ;
#133568=LINE ( 'NONE', #34496, #190053 ) ;
#133575=EDGE_LOOP ( 'NONE', ( #175461, #104257, #63637 ) ) ;
#133602=DIRECTION ( 'NONE',  ( 0.000000000000000000, 0.000000000000000000, -1.000000000000000000 ) ) ;
#133604=CARTESIAN_POINT ( 'NONE',  ( 21.05000000000000071, 5.400000000011154988, -54.59473398108690390 ) ) ;
#133611=CONICAL_SURFACE ( 'NONE', #17119, 4.049999999999998046, 0.7853981633974604915 ) ;
#133644=CARTESIAN_POINT ( 'NONE',  ( 18.59999999999999432, 10.49142135624846617, -58.25000000000000000 ) ) ;
#133666=CARTESIAN_POINT ( 'NONE',  ( 23.15000000000000213, -8.999999999988842703, -57.10603087734755690 ) ) ;
#133673=EDGE_CURVE ( 'NONE', #194433, #168461, #97004, .T. ) ;
#133701=ORIENTED_EDGE ( 'NONE', *, *, #27449, .T. ) ;
#133748=ADVANCED_FACE ( 'NONE', ( #172969 ), #84537, .F. ) ;
#133777=CYLINDRICAL_SURFACE ( 'NONE', #155504, 0.09999999999999939493 ) ;
#133800=CARTESIAN_POINT ( 'NONE',  ( 18.59999999999997655, 1.115600667400684642E-11, -67.00000000000000000 ) ) ;
#133860=CARTESIAN_POINT ( 'NONE',  ( 23.24999999999999289, -4.149999999988843058, -33.50000000000000000 ) ) ;
#133862=EDGE_CURVE ( 'NONE', #101718, #41950, #226190, .T. ) ;
#133890=DIRECTION ( 'NONE',  ( 0.000000000000000000, -0.9908441862701596881, -0.1350103645451901924 ) ) ;
#133902=DIRECTION ( 'NONE',  ( 0.000000000000000000, 0.000000000000000000, -1.000000000000000000 ) ) ;
#133922=CARTESIAN_POINT ( 'NONE',  ( 21.05000000000000071, -8.999999999988844479, -43.39396912265245021 ) ) ;
#133933=ORIENTED_EDGE ( 'NONE', *, *, #217995, .F. ) ;
#133955=CARTESIAN_POINT ( 'NONE',  ( 20.85000000000000142, -1.135018845899022466, -74.71697688343232358 ) ) ;
#133962=AXIS2_PLACEMENT_3D ( 'NONE', #137838, #98687, #136553 ) ;
#133968=CARTESIAN_POINT ( 'NONE',  ( -20.94999999999999929, 14.05000000001115623, -39.01369507076099552 ) ) ;
#133969=DIRECTION ( 'NONE',  ( 0.000000000000000000, 0.000000000000000000, 1.000000000000000000 ) ) ;
#134009=DIRECTION ( 'NONE',  ( 0.000000000000000000, 0.000000000000000000, -1.000000000000000000 ) ) ;
#134033=EDGE_CURVE ( 'NONE', #91127, #6368, #80646, .T. ) ;
#134042=DIRECTION ( 'NONE',  ( 0.000000000000000000, -0.8660254037844383745, 0.5000000000000003331 ) ) ;
#134045=EDGE_CURVE ( 'NONE', #141916, #90926, #193114, .T. ) ;
#134081=LINE ( 'NONE', #93685, #38142 ) ;
#134107=DIRECTION ( 'NONE',  ( -1.000000000000000000, 0.000000000000000000, 0.000000000000000000 ) ) ;
#134113=DIRECTION ( 'NONE',  ( 0.000000000000000000, 0.000000000000000000, -1.000000000000000000 ) ) ;
#134120=DIRECTION ( 'NONE',  ( -1.000000000000000000, -2.952720810173289112E-16, 0.000000000000000000 ) ) ;
#134160=EDGE_LOOP ( 'NONE', ( #58689, #252450, #224244, #19928 ) ) ;
#134170=ORIENTED_EDGE ( 'NONE', *, *, #118475, .T. ) ;
#134171=EDGE_CURVE ( 'NONE', #67224, #78967, #127748, .T. ) ;
#134184=ORIENTED_EDGE ( 'NONE', *, *, #203332, .T. ) ;
#134195=ORIENTED_EDGE ( 'NONE', *, *, #37800, .F. ) ;
#134203=ORIENTED_EDGE ( 'NONE', *, *, #173317, .F. ) ;
#134235=DIRECTION ( 'NONE',  ( 0.000000000000000000, -1.000000000000000000, 0.000000000000000000 ) ) ;
#134241=EDGE_LOOP ( 'NONE', ( #60940, #79848, #198545, #63749, #173075, #197337, #247783, #11552, #220257, #80985 ) ) ;
#134265=CARTESIAN_POINT ( 'NONE',  ( -20.54999999999999716, 4.350000000011156054, -54.64999999999999858 ) ) ;
#134403=CARTESIAN_POINT ( 'NONE',  ( -22.47071067811865319, 0.09909245471376171288, -25.77992525550194003 ) ) ;
#134404=CIRCLE ( 'NONE', #138501, 0.09999999999999911737 ) ;
#134405=CARTESIAN_POINT ( 'NONE',  ( 21.05000000000000071, 6.650000000011155876, -43.34382208968312966 ) ) ;
#134409=CARTESIAN_POINT ( 'NONE',  ( 23.14999999999999147, 1.115600667400684642E-11, -33.50000000000000000 ) ) ;
#134410=AXIS2_PLACEMENT_3D ( 'NONE', #233222, #14175, #54552 ) ;
#134441=CIRCLE ( 'NONE', #217828, 0.5000000000000004441 ) ;
#134484=EDGE_LOOP ( 'NONE', ( #103936, #84161, #159640, #248279 ) ) ;
#134535=EDGE_CURVE ( 'NONE', #204996, #24660, #151033, .T. ) ;
#134540=AXIS2_PLACEMENT_3D ( 'NONE', #249012, #49514, #131607 ) ;
#134550=CARTESIAN_POINT ( 'NONE',  ( 23.14999999999999503, 11.65000000001116298, -21.75000000000000355 ) ) ;
#134552=LINE ( 'NONE', #92868, #72250 ) ;
#134553=DIRECTION ( 'NONE',  ( 0.000000000000000000, -1.000000000000000000, 0.000000000000000000 ) ) ;
#134561=DIRECTION ( 'NONE',  ( 0.000000000000000000, 0.000000000000000000, 1.000000000000000000 ) ) ;
#134578=AXIS2_PLACEMENT_3D ( 'NONE', #26707, #205299, #207911 ) ;
#134607=CARTESIAN_POINT ( 'NONE',  ( -21.14999999999999503, 11.75000000001115197, -40.41914724595876862 ) ) ;
#134631=CYLINDRICAL_SURFACE ( 'NONE', #195031, 0.5000000000000004441 ) ;
#134632=CYLINDRICAL_SURFACE ( 'NONE', #235086, 12.87499999999999822 ) ;
#134637=DIRECTION ( 'NONE',  ( 0.000000000000000000, -1.000000000000000000, -0.000000000000000000 ) ) ;
#134638=VERTEX_POINT ( 'NONE', #96288 ) ;
#134687=EDGE_LOOP ( 'NONE', ( #8021, #214989, #101889, #126480 ) ) ;
#134725=DIRECTION ( 'NONE',  ( 1.000000000000000000, -0.000000000000000000, -0.000000000000000000 ) ) ;
#134736=CARTESIAN_POINT ( 'NONE',  ( -20.94999999999999929, 1.162701749949165642, -41.50000000000000000 ) ) ;
#134740=EDGE_CURVE ( 'NONE', #141829, #244695, #42883, .T. ) ;
#134742=DIRECTION ( 'NONE',  ( -0.000000000000000000, 0.01283462868039629209, -0.9999176327611372095 ) ) ;
#134746=CARTESIAN_POINT ( 'NONE',  ( -23.15000000000000213, 1.115600667400684642E-11, -67.00000000000000000 ) ) ;
#134755=CARTESIAN_POINT ( 'NONE',  ( 21.14999999999999503, -0.1008583690875562017, -21.75043287651061164 ) ) ;
#134774=ORIENTED_EDGE ( 'NONE', *, *, #196590, .F. ) ;
#134806=ORIENTED_EDGE ( 'NONE', *, *, #55475, .F. ) ;
#134825=DIRECTION ( 'NONE',  ( 0.000000000000000000, 0.000000000000000000, -1.000000000000000000 ) ) ;
#134829=EDGE_CURVE ( 'NONE', #205763, #171197, #12633, .T. ) ;
#134834=CIRCLE ( 'NONE', #39227, 0.1000000000000028644 ) ;
#134844=DIRECTION ( 'NONE',  ( 0.000000000000000000, 0.000000000000000000, -1.000000000000000000 ) ) ;
#134860=EDGE_CURVE ( 'NONE', #28509, #86605, #205339, .T. ) ;
#134863=AXIS2_PLACEMENT_3D ( 'NONE', #10404, #229444, #251559 ) ;
#134903=DIRECTION ( 'NONE',  ( -1.000000000000000000, 0.000000000000000000, 0.000000000000000000 ) ) ;
#134904=EDGE_LOOP ( 'NONE', ( #246656, #63593, #13105, #43226 ) ) ;
#134909=FACE_OUTER_BOUND ( 'NONE', #53929, .T. ) ;
#134912=VERTEX_POINT ( 'NONE', #169151 ) ;
#134922=DIRECTION ( 'NONE',  ( 0.000000000000000000, -0.9908441862701596881, 0.1350103645451904977 ) ) ;
#134925=CIRCLE ( 'NONE', #218140, 0.09999999999999939493 ) ;
#134932=EDGE_LOOP ( 'NONE', ( #137484, #237699, #220143, #108156 ) ) ;
#134938=CARTESIAN_POINT ( 'NONE',  ( 21.05000000000000071, 1.115600667400684642E-11, -67.00000000000000000 ) ) ;
#134939=VERTEX_POINT ( 'NONE', #155995 ) ;
#134958=AXIS2_PLACEMENT_3D ( 'NONE', #227812, #46593, #107866 ) ;
#134991=CIRCLE ( 'NONE', #164070, 11.70000000000000284 ) ;
#135007=CARTESIAN_POINT ( 'NONE',  ( 21.05000000000000071, 8.815201804578244094, -41.92053749668480123 ) ) ;
#135011=CIRCLE ( 'NONE', #239102, 1.899999999999999023 ) ;
#135034=ORIENTED_EDGE ( 'NONE', *, *, #239528, .T. ) ;
#135036=AXIS2_PLACEMENT_3D ( 'NONE', #63355, #124637, #141620 ) ;
#135038=ORIENTED_EDGE ( 'NONE', *, *, #12022, .T. ) ;
#135047=AXIS2_PLACEMENT_3D ( 'NONE', #196216, #80084, #115395 ) ;
#135048=CARTESIAN_POINT ( 'NONE',  ( -23.25000000000000000, -0.09999999998884338825, -21.85042919245520210 ) ) ;
#135136=CARTESIAN_POINT ( 'NONE',  ( 20.95159278453404283, 8.907896337960204747, -41.98472018510925352 ) ) ;
#135153=VERTEX_POINT ( 'NONE', #209213 ) ;
#135154=CARTESIAN_POINT ( 'NONE',  ( 21.14999999999999858, 1.115600667400684642E-11, -21.85042919245520210 ) ) ;
#135160=DIRECTION ( 'NONE',  ( 0.000000000000000000, 0.000000000000000000, 1.000000000000000000 ) ) ;
#135166=VERTEX_POINT ( 'NONE', #31897 ) ;
#135199=CARTESIAN_POINT ( 'NONE',  ( -20.54999999999999716, 2.500000000011156409, -46.72462192276210402 ) ) ;
#135204=CARTESIAN_POINT ( 'NONE',  ( -20.54999999999999716, -9.499999999988848032, -43.39396912265245021 ) ) ;
#135212=DIRECTION ( 'NONE',  ( 0.000000000000000000, -0.4930308989875248349, -0.8700118002898312719 ) ) ;
#135250=EDGE_CURVE ( 'NONE', #77835, #214564, #88816, .T. ) ;
#135262=CARTESIAN_POINT ( 'NONE',  ( 18.49999999999999645, -1.637172712959225507, -45.08215336547201701 ) ) ;
#135301=DIRECTION ( 'NONE',  ( 0.000000000000000000, -0.1568667991644714932, 0.9876197685951274563 ) ) ;
#135317=CARTESIAN_POINT ( 'NONE',  ( 23.14999999999999858, 1.115600667400684642E-11, -67.00000000000000000 ) ) ;
#135326=ADVANCED_FACE ( 'NONE', ( #160830 ), #26499, .F. ) ;
#135329=ORIENTED_EDGE ( 'NONE', *, *, #239726, .T. ) ;
#135370=CARTESIAN_POINT ( 'NONE',  ( 22.50000000000000000, 1.115600667400684642E-11, -33.50000000000000000 ) ) ;
#135375=VERTEX_POINT ( 'NONE', #23892 ) ;
#135383=CARTESIAN_POINT ( 'NONE',  ( -21.12642695952773764, 6.375659922046319927, -33.40109671681064185 ) ) ;
#135396=DIRECTION ( 'NONE',  ( 0.000000000000000000, -0.5000000000000078826, -0.8660254037844340447 ) ) ;
#135407=DIRECTION ( 'NONE',  ( 0.000000000000000000, 0.000000000000000000, -1.000000000000000000 ) ) ;
#135429=AXIS2_PLACEMENT_3D ( 'NONE', #226567, #47937, #127490 ) ;
#135444=EDGE_LOOP ( 'NONE', ( #170831, #26611, #198189, #90779 ) ) ;
#135451=FACE_OUTER_BOUND ( 'NONE', #121034, .T. ) ;
#135495=ORIENTED_EDGE ( 'NONE', *, *, #181382, .F. ) ;
#135533=EDGE_LOOP ( 'NONE', ( #225884, #191388, #134806, #198192 ) ) ;
#135553=CARTESIAN_POINT ( 'NONE',  ( -22.47071067811865319, 7.720074744509219933, -33.40090754529740025 ) ) ;
#135555=AXIS2_PLACEMENT_3D ( 'NONE', #20539, #174521, #100020 ) ;
#135569=CARTESIAN_POINT ( 'NONE',  ( 20.95035502843362707, 10.47763832678762341, -41.07629970873637859 ) ) ;
#135596=DIRECTION ( 'NONE',  ( 0.000000000000000000, 0.000000000000000000, -1.000000000000000000 ) ) ;
#135639=VERTEX_POINT ( 'NONE', #18087 ) ;
#135665=AXIS2_PLACEMENT_3D ( 'NONE', #211502, #108547, #250612 ) ;
#135669=DIRECTION ( 'NONE',  ( 1.000000000000000000, -0.000000000000000000, -0.000000000000000000 ) ) ;
#135698=CARTESIAN_POINT ( 'NONE',  ( 18.41832399655378083, -9.682403266662738872, -73.65684362002765795 ) ) ;
#135719=ORIENTED_EDGE ( 'NONE', *, *, #176296, .T. ) ;
#135768=LINE ( 'NONE', #191941, #42563 ) ;
#135777=ORIENTED_EDGE ( 'NONE', *, *, #85801, .F. ) ;
#135785=ORIENTED_EDGE ( 'NONE', *, *, #107150, .F. ) ;
#135821=EDGE_CURVE ( 'NONE', #192117, #253488, #51571, .T. ) ;
#135825=AXIS2_PLACEMENT_3D ( 'NONE', #131730, #230856, #211272 ) ;
#135845=DIRECTION ( 'NONE',  ( 0.000000000000000000, -1.000000000000000000, 0.000000000000000000 ) ) ;
#135847=EDGE_CURVE ( 'NONE', #205356, #83334, #239055, .T. ) ;
#135854=VERTEX_POINT ( 'NONE', #141444 ) ;
#135857=LINE ( 'NONE', #66620, #58421 ) ;
#135858=DIRECTION ( 'NONE',  ( 0.000000000000000000, 0.000000000000000000, 1.000000000000000000 ) ) ;
#135888=CARTESIAN_POINT ( 'NONE',  ( 18.49999999999999645, 1.115600667400684642E-11, -33.50000000000000000 ) ) ;
#135892=CARTESIAN_POINT ( 'NONE',  ( -21.05000000000000071, 0.2561057921033771945, -33.46510355832771211 ) ) ;
#135927=CARTESIAN_POINT ( 'NONE',  ( -18.50000000000000000, -9.499999999988849808, -41.60000000000000142 ) ) ;
#135930=DIRECTION ( 'NONE',  ( 1.000000000000000000, 7.304098846218134667E-16, -0.000000000000000000 ) ) ;
#136005=LINE ( 'NONE', #39535, #172836 ) ;
#136008=VERTEX_POINT ( 'NONE', #223535 ) ;
#136013=CARTESIAN_POINT ( 'NONE',  ( 21.04999999999999716, 6.300183336278553980, -33.44867256765849106 ) ) ;
#136029=VERTEX_POINT ( 'NONE', #241830 ) ;
#136043=DIRECTION ( 'NONE',  ( 0.000000000000000000, 0.000000000000000000, -1.000000000000000000 ) ) ;
#136094=CARTESIAN_POINT ( 'NONE',  ( 21.05000000000000071, 14.05000000001115623, -61.48630492923908974 ) ) ;
#136117=VECTOR ( 'NONE', #210291, 1000.000000000000000 ) ;
#136119=EDGE_CURVE ( 'NONE', #200797, #45011, #47681, .T. ) ;
#136153=ORIENTED_EDGE ( 'NONE', *, *, #133862, .T. ) ;
#136155=ORIENTED_EDGE ( 'NONE', *, *, #122672, .F. ) ;
#136186=ORIENTED_EDGE ( 'NONE', *, *, #95765, .T. ) ;
#136199=DIRECTION ( 'NONE',  ( -1.000000000000000000, -0.000000000000000000, -0.000000000000000000 ) ) ;
#136236=DIRECTION ( 'NONE',  ( -0.000000000000000000, -0.1350103645451876666, 0.9908441862701600211 ) ) ;
#136245=DIRECTION ( 'NONE',  ( 1.000000000000000000, 0.000000000000000000, 0.000000000000000000 ) ) ;
#136255=CIRCLE ( 'NONE', #90489, 0.1000000000000028644 ) ;
#136260=VERTEX_POINT ( 'NONE', #165514 ) ;
#136261=CARTESIAN_POINT ( 'NONE',  ( -21.05000000000000071, 0.03175835306653384399, -27.24115287692075071 ) ) ;
#136280=CARTESIAN_POINT ( 'NONE',  ( 23.14999999999999503, 11.65000000001116298, -54.85000000000000142 ) ) ;
#136289=AXIS2_PLACEMENT_3D ( 'NONE', #78144, #75621, #255462 ) ;
#136315=ORIENTED_EDGE ( 'NONE', *, *, #240097, .T. ) ;
#136320=FACE_OUTER_BOUND ( 'NONE', #128339, .T. ) ;
#136407=CARTESIAN_POINT ( 'NONE',  ( 21.14999999999999858, -0.09999999998884338825, -26.95934304829875927 ) ) ;
#136440=ADVANCED_FACE ( 'NONE', ( #233200 ), #149810, .T. ) ;
#136455=ORIENTED_EDGE ( 'NONE', *, *, #29121, .T. ) ;
#136498=LINE ( 'NONE', #217320, #54091 ) ;
#136516=ORIENTED_EDGE ( 'NONE', *, *, #121340, .F. ) ;
#136527=ORIENTED_EDGE ( 'NONE', *, *, #210467, .T. ) ;
#136553=DIRECTION ( 'NONE',  ( -2.940209281316621509E-16, 1.000000000000000000, 0.000000000000000000 ) ) ;
#136569=ADVANCED_FACE ( 'NONE', ( #98750 ), #40137, .T. ) ;
#136590=EDGE_CURVE ( 'NONE', #235379, #14771, #206292, .T. ) ;
#136608=CARTESIAN_POINT ( 'NONE',  ( -18.50000000000000000, 1.115600667400684642E-11, -67.00000000000000000 ) ) ;
#136613=CIRCLE ( 'NONE', #232335, 11.90000000000000036 ) ;
#136628=CARTESIAN_POINT ( 'NONE',  ( 21.14999999999999858, 11.65000000001116298, -45.65000000000000568 ) ) ;
#136633=CARTESIAN_POINT ( 'NONE',  ( -18.50000000000000000, -9.419203418015493767, -40.74778581042865255 ) ) ;
#136647=CARTESIAN_POINT ( 'NONE',  ( -18.59999999999999787, 11.65000000001115232, -40.41480577065399871 ) ) ;
#136680=CYLINDRICAL_SURFACE ( 'NONE', #94063, 0.09999999999999781286 ) ;
#136726=ORIENTED_EDGE ( 'NONE', *, *, #42824, .T. ) ;
#136743=FACE_OUTER_BOUND ( 'NONE', #67840, .T. ) ;
#136759=DIRECTION ( 'NONE',  ( 0.000000000000000000, -0.000000000000000000, 1.000000000000000000 ) ) ;
#136761=AXIS2_PLACEMENT_3D ( 'NONE', #1507, #172819, #52809 ) ;
#136775=DIRECTION ( 'NONE',  ( 2.952720810173289112E-16, -1.000000000000000000, 0.000000000000000000 ) ) ;
#136793=ORIENTED_EDGE ( 'NONE', *, *, #97391, .T. ) ;
#136797=EDGE_CURVE ( 'NONE', #208213, #216334, #173007, .T. ) ;
#136828=CARTESIAN_POINT ( 'NONE',  ( 21.30000000000002558, 1.115650265596050101E-11, -29.45000000000000284 ) ) ;
#136840=ORIENTED_EDGE ( 'NONE', *, *, #39479, .F. ) ;
#136842=CARTESIAN_POINT ( 'NONE',  ( -21.14999999999999858, 11.75000000001115197, -40.28386566297815108 ) ) ;
#136849=DIRECTION ( 'NONE',  ( 0.000000000000000000, 1.897661533703519897E-16, -1.000000000000000000 ) ) ;
#136855=CARTESIAN_POINT ( 'NONE',  ( -22.50000000000000000, 1.115600667400684642E-11, -33.50000000000000000 ) ) ;
#136864=CIRCLE ( 'NONE', #74369, 0.4000000000000045186 ) ;
#136866=ADVANCED_FACE ( 'NONE', ( #32117 ), #77313, .F. ) ;
#136870=FACE_OUTER_BOUND ( 'NONE', #104759, .T. ) ;
#136877=CARTESIAN_POINT ( 'NONE',  ( -23.25000000000000000, 4.150000000011156764, -45.85000000000000142 ) ) ;
#136878=DIRECTION ( 'NONE',  ( -3.469446951953612296E-14, -0.9908441862701596881, -0.1350103645451904977 ) ) ;
#136881=EDGE_CURVE ( 'NONE', #121164, #9105, #69956, .T. ) ;
#136919=FACE_OUTER_BOUND ( 'NONE', #182206, .T. ) ;
#136941=DIRECTION ( 'NONE',  ( 0.000000000000000000, 1.734723475976757554E-14, 1.000000000000000000 ) ) ;
#136960=CARTESIAN_POINT ( 'NONE',  ( -23.15000000000000213, 2.600000000011156054, -46.72462192276210402 ) ) ;
#136965=CARTESIAN_POINT ( 'NONE',  ( -18.59999999999999787, 11.75000000001115197, -54.85000000000000142 ) ) ;
#136967=ORIENTED_EDGE ( 'NONE', *, *, #53749, .T. ) ;
#136975=DIRECTION ( 'NONE',  ( 1.000000000000000000, 0.000000000000000000, 0.000000000000000000 ) ) ;
#137018=VECTOR ( 'NONE', #13628, 1000.000000000000000 ) ;
#137019=LINE ( 'NONE', #217814, #194573 ) ;
#137085=EDGE_CURVE ( 'NONE', #239047, #69658, #69331, .T. ) ;
#137105=VECTOR ( 'NONE', #118329, 1000.000000000000000 ) ;
#137111=DIRECTION ( 'NONE',  ( 0.000000000000000000, -1.000000000000000000, 0.000000000000000000 ) ) ;
#137128=AXIS2_PLACEMENT_3D ( 'NONE', #61175, #40373, #181143 ) ;
#137129=CARTESIAN_POINT ( 'NONE',  ( 21.14999999999999858, 6.257814610487280937, -33.40220970869120265 ) ) ;
#137139=VERTEX_POINT ( 'NONE', #230983 ) ;
#137141=CARTESIAN_POINT ( 'NONE',  ( 21.14999999999999858, 11.65000000001115943, -33.60000000000000142 ) ) ;
#137157=VERTEX_POINT ( 'NONE', #96557 ) ;
#137158=DIRECTION ( 'NONE',  ( 0.000000000000000000, 0.000000000000000000, 1.000000000000000000 ) ) ;
#137165=CARTESIAN_POINT ( 'NONE',  ( 21.08479644141223019, 0.05855444257529528185, -27.15496134226810909 ) ) ;
#137173=EDGE_CURVE ( 'NONE', #215662, #212264, #218928, .T. ) ;
#137220=CARTESIAN_POINT ( 'NONE',  ( 20.94999999999999574, -1.736257131586239844, -45.06865232901750318 ) ) ;
#137258=FACE_OUTER_BOUND ( 'NONE', #127027, .T. ) ;
#137263=ORIENTED_EDGE ( 'NONE', *, *, #135847, .F. ) ;
#137267=DIRECTION ( 'NONE',  ( 1.000000000000000000, -0.000000000000000000, -0.000000000000000000 ) ) ;
#137326=CARTESIAN_POINT ( 'NONE',  ( -23.15000000000000213, 4.250000000011156409, -54.64999999999999858 ) ) ;
#137338=VERTEX_POINT ( 'NONE', #122581 ) ;
#137345=CARTESIAN_POINT ( 'NONE',  ( -23.15000000000000213, 1.115600667400684642E-11, -33.50000000000000000 ) ) ;
#137347=AXIS2_PLACEMENT_3D ( 'NONE', #71126, #108935, #188478 ) ;
#137373=ORIENTED_EDGE ( 'NONE', *, *, #151385, .F. ) ;
#137386=DIRECTION ( 'NONE',  ( 0.000000000000000000, 0.000000000000000000, -1.000000000000000000 ) ) ;
#137423=DIRECTION ( 'NONE',  ( 0.000000000000000000, -0.4930308989875248349, -0.8700118002898312719 ) ) ;
#137426=ORIENTED_EDGE ( 'NONE', *, *, #134535, .T. ) ;
#137433=EDGE_LOOP ( 'NONE', ( #257794, #9437, #9280, #97790 ) ) ;
#137466=AXIS2_PLACEMENT_3D ( 'NONE', #98587, #231743, #133902 ) ;
#137474=CARTESIAN_POINT ( 'NONE',  ( -18.50000000000000000, 11.75000000001115197, -21.75000000000000355 ) ) ;
#137484=ORIENTED_EDGE ( 'NONE', *, *, #42333, .T. ) ;
#137529=DIRECTION ( 'NONE',  ( 0.000000000000000000, 0.000000000000000000, -1.000000000000000000 ) ) ;
#137533=AXIS2_PLACEMENT_3D ( 'NONE', #137474, #17530, #99619 ) ;
#137547=CYLINDRICAL_SURFACE ( 'NONE', #142549, 0.1000000000000028644 ) ;
#137551=ORIENTED_EDGE ( 'NONE', *, *, #230667, .T. ) ;
#137576=DIRECTION ( 'NONE',  ( 0.000000000000000000, 0.000000000000000000, -1.000000000000000000 ) ) ;
#137577=EDGE_CURVE ( 'NONE', #224490, #72626, #34412, .T. ) ;
#137612=DIRECTION ( 'NONE',  ( -0.000000000000000000, -0.000000000000000000, -1.000000000000000000 ) ) ;
#137615=EDGE_CURVE ( 'NONE', #28056, #203988, #75455, .T. ) ;
#137653=VECTOR ( 'NONE', #16344, 1000.000000000000000 ) ;
#137681=ORIENTED_EDGE ( 'NONE', *, *, #66477, .F. ) ;
#137691=AXIS2_PLACEMENT_3D ( 'NONE', #128015, #208829, #84995 ) ;
#137700=ADVANCED_FACE ( 'NONE', ( #222605 ), #163564, .F. ) ;
#137702=CARTESIAN_POINT ( 'NONE',  ( 20.94999999999999574, 8.926614585098251453, -41.97168301922312850 ) ) ;
#137712=CIRCLE ( 'NONE', #21249, 0.1999999999999996503 ) ;
#137731=EDGE_LOOP ( 'NONE', ( #113371, #229235, #39144, #29555, #142187 ) ) ;
#137736=VERTEX_POINT ( 'NONE', #63549 ) ;
#137742=DIRECTION ( 'NONE',  ( 0.000000000000000000, 0.000000000000000000, 1.000000000000000000 ) ) ;
#137745=ORIENTED_EDGE ( 'NONE', *, *, #52346, .F. ) ;
#137756=DIRECTION ( 'NONE',  ( -1.000000000000000000, -0.000000000000000000, -0.000000000000000000 ) ) ;
#137769=CIRCLE ( 'NONE', #245950, 0.09999999999999939493 ) ;
#137791=ORIENTED_EDGE ( 'NONE', *, *, #79067, .T. ) ;
#137801=ORIENTED_EDGE ( 'NONE', *, *, #154477, .T. ) ;
#137824=FACE_OUTER_BOUND ( 'NONE', #164326, .T. ) ;
#137835=DIRECTION ( 'NONE',  ( 1.000000000000000000, 0.000000000000000000, 0.000000000000000000 ) ) ;
#137838=CARTESIAN_POINT ( 'NONE',  ( 18.60000000000000497, 1.115600667400684642E-11, -33.50000000000000000 ) ) ;
#137963=ORIENTED_EDGE ( 'NONE', *, *, #55721, .F. ) ;
#137996=FACE_OUTER_BOUND ( 'NONE', #4846, .T. ) ;
#138024=FACE_OUTER_BOUND ( 'NONE', #134160, .T. ) ;
#138080=AXIS2_PLACEMENT_3D ( 'NONE', #62921, #146301, #104584 ) ;
#138082=CARTESIAN_POINT ( 'NONE',  ( -21.64999999999999858, 7.250000000011148416, -45.75000000000000000 ) ) ;
#138096=DIRECTION ( 'NONE',  ( -1.000000000000000000, 0.000000000000000000, -0.000000000000000000 ) ) ;
#138108=AXIS2_PLACEMENT_3D ( 'NONE', #127862, #66601, #28802 ) ;
#138112=CARTESIAN_POINT ( 'NONE',  ( -21.12844524849339223, 11.75000000001115197, -40.40441347084259860 ) ) ;
#138122=CYLINDRICAL_SURFACE ( 'NONE', #228947, 0.09999999999999939493 ) ;
#138148=EDGE_CURVE ( 'NONE', #64314, #213025, #163643, .T. ) ;
#138166=SPHERICAL_SURFACE ( 'NONE', #125840, 0.1000000000000000056 ) ;
#138216=CARTESIAN_POINT ( 'NONE',  ( 21.05000000000000071, -11.64999999998883595, -63.89999999999999858 ) ) ;
#138221=AXIS2_PLACEMENT_3D ( 'NONE', #13301, #195809, #253178 ) ;
#138226=DIRECTION ( 'NONE',  ( 1.000000000000000000, 0.000000000000000000, 0.000000000000000000 ) ) ;
#138230=CARTESIAN_POINT ( 'NONE',  ( -21.46681500597819081, 1.115542391533913547E-11, -26.64248884057156630 ) ) ;
#138232=EDGE_CURVE ( 'NONE', #143246, #165624, #10770, .T. ) ;
#138259=DIRECTION ( 'NONE',  ( 0.000000000000000000, 1.000000000000000000, 0.000000000000000000 ) ) ;
#138260=CARTESIAN_POINT ( 'NONE',  ( -21.09316766718153247, 0.03926340232583150347, -27.12984668752529060 ) ) ;
#138261=DIRECTION ( 'NONE',  ( 0.000000000000000000, 0.000000000000000000, -1.000000000000000000 ) ) ;
#138271=FACE_OUTER_BOUND ( 'NONE', #121103, .T. ) ;
#138280=CARTESIAN_POINT ( 'NONE',  ( -20.85000000000000142, -1.149570369564537842, -74.81591248450196474 ) ) ;
#138318=EDGE_CURVE ( 'NONE', #76854, #180750, #16146, .T. ) ;
#138330=VERTEX_POINT ( 'NONE', #134755 ) ;
#138356=TOROIDAL_SURFACE ( 'NONE', #196825, 0.2000000000000000111, 0.1000000000000000056 ) ;
#138400=CARTESIAN_POINT ( 'NONE',  ( 18.42636655943171320, -9.496944315759476396, -73.60908057115553049 ) ) ;
#138479=DIRECTION ( 'NONE',  ( -1.000000000000000000, -0.000000000000000000, -0.000000000000000000 ) ) ;
#138489=CARTESIAN_POINT ( 'NONE',  ( 21.05000000000000071, 1.115600667400684642E-11, -33.50000000000000000 ) ) ;
#138494=CARTESIAN_POINT ( 'NONE',  ( -20.54999999999999716, -11.74999999998884448, -54.65000000000000568 ) ) ;
#138501=AXIS2_PLACEMENT_3D ( 'NONE', #13750, #112850, #194976 ) ;
#138524=DIRECTION ( 'NONE',  ( 1.000000000000000000, 1.836970198721029934E-16, 0.000000000000000000 ) ) ;
#138525=EDGE_CURVE ( 'NONE', #22291, #43175, #201168, .T. ) ;
#138540=AXIS2_PLACEMENT_3D ( 'NONE', #7310, #125969, #205504 ) ;
#138548=EDGE_CURVE ( 'NONE', #173035, #102738, #4236, .T. ) ;
#138598=AXIS2_PLACEMENT_3D ( 'NONE', #154255, #175106, #214185 ) ;
#138603=FACE_OUTER_BOUND ( 'NONE', #9537, .T. ) ;
#138606=ORIENTED_EDGE ( 'NONE', *, *, #111114, .T. ) ;
#138622=CARTESIAN_POINT ( 'NONE',  ( -21.05000000000000071, 1.835341550235567887, -45.05515129256298223 ) ) ;
#138631=CARTESIAN_POINT ( 'NONE',  ( 20.94999999999999929, 10.29270135741298731, -72.45736188715193293 ) ) ;
#138642=CIRCLE ( 'NONE', #122120, 0.1000000000000028644 ) ;
#138648=EDGE_CURVE ( 'NONE', #205763, #46223, #26574, .T. ) ;
#138653=VERTEX_POINT ( 'NONE', #16798 ) ;
#138670=TOROIDAL_SURFACE ( 'NONE', #126037, 4.149999999999999467, 0.1000000000000000056 ) ;
#138674=ORIENTED_EDGE ( 'NONE', *, *, #3451, .T. ) ;
#138676=DIRECTION ( 'NONE',  ( 0.000000000000000000, -0.1350103645451876944, 0.9908441862701601321 ) ) ;
#138681=ORIENTED_EDGE ( 'NONE', *, *, #249290, .F. ) ;
#138705=DIRECTION ( 'NONE',  ( -1.000000000000000000, -0.000000000000000000, 0.000000000000000000 ) ) ;
#138712=ORIENTED_EDGE ( 'NONE', *, *, #77356, .F. ) ;
#138716=DIRECTION ( 'NONE',  ( 1.000000000000000000, 0.000000000000000000, -0.000000000000000000 ) ) ;
#138742=VERTEX_POINT ( 'NONE', #20646 ) ;
#138750=DIRECTION ( 'NONE',  ( 0.000000000000000000, 0.000000000000000000, -1.000000000000000000 ) ) ;
#138765=DIRECTION ( 'NONE',  ( 1.000000000000000000, 0.000000000000000000, 0.000000000000000000 ) ) ;
#138770=VECTOR ( 'NONE', #219335, 1000.000000000000000 ) ;
#138807=EDGE_CURVE ( 'NONE', #138653, #242609, #220116, .T. ) ;
#138850=AXIS2_PLACEMENT_3D ( 'NONE', #6789, #146293, #219727 ) ;
#138856=FACE_OUTER_BOUND ( 'NONE', #234964, .T. ) ;
#138857=DIRECTION ( 'NONE',  ( -0.000000000000000000, 0.000000000000000000, 1.000000000000000000 ) ) ;
#138871=VERTEX_POINT ( 'NONE', #148275 ) ;
#138883=CARTESIAN_POINT ( 'NONE',  ( 21.87500000000000355, 9.750000000011153745, -45.85000000000000142 ) ) ;
#138888=DIRECTION ( 'NONE',  ( 0.000000000000000000, 0.000000000000000000, -1.000000000000000000 ) ) ;
#138892=CARTESIAN_POINT ( 'NONE',  ( 21.05000000000000071, -8.999999999988842703, -57.10603087734755690 ) ) ;
#138906=DIRECTION ( 'NONE',  ( 0.000000000000000000, 0.000000000000000000, 1.000000000000000000 ) ) ;
#138922=CIRCLE ( 'NONE', #26564, 0.1000000000000028644 ) ;
#138988=ORIENTED_EDGE ( 'NONE', *, *, #23555, .T. ) ;
#138999=CARTESIAN_POINT ( 'NONE',  ( 20.94999999999999574, 1.115600667400684642E-11, -33.50000000000000000 ) ) ;
#139008=CARTESIAN_POINT ( 'NONE',  ( 20.94999999999999929, 11.75000000001115730, -60.21613433702191287 ) ) ;
#139033=CARTESIAN_POINT ( 'NONE',  ( -22.39999999999999858, 1.115600667400684642E-11, -21.85042919245520210 ) ) ;
#139106=AXIS2_PLACEMENT_3D ( 'NONE', #176152, #78294, #138261 ) ;
#139113=ORIENTED_EDGE ( 'NONE', *, *, #25256, .F. ) ;
#139114=DIRECTION ( 'NONE',  ( 0.000000000000000000, 0.6728971962616697722, 0.7397360091702875895 ) ) ;
#139124=DIRECTION ( 'NONE',  ( -3.265361837132813093E-16, 1.000000000000000000, 0.000000000000000000 ) ) ;
#139128=VERTEX_POINT ( 'NONE', #209532 ) ;
#139166=ORIENTED_EDGE ( 'NONE', *, *, #14009, .F. ) ;
#139189=CARTESIAN_POINT ( 'NONE',  ( -18.47079683080346513, -9.471664105233731590, -40.60886054099234599 ) ) ;
#139207=ORIENTED_EDGE ( 'NONE', *, *, #97300, .T. ) ;
#139211=EDGE_CURVE ( 'NONE', #120355, #217025, #201134, .T. ) ;
#139343=AXIS2_PLACEMENT_3D ( 'NONE', #45366, #141893, #46627 ) ;
#139413=CIRCLE ( 'NONE', #197677, 0.1999999999999987899 ) ;
#139423=DIRECTION ( 'NONE',  ( 0.000000000000000000, 0.1568667991644863147, -0.9876197685951252359 ) ) ;
#139425=CARTESIAN_POINT ( 'NONE',  ( 22.49999999999999645, 0.08880997639808872746, -21.85023708196807846 ) ) ;
#139480=DIRECTION ( 'NONE',  ( 0.000000000000000000, 0.000000000000000000, -1.000000000000000000 ) ) ;
#139486=VERTEX_POINT ( 'NONE', #192248 ) ;
#139488=VERTEX_POINT ( 'NONE', #209219 ) ;
#139502=DIRECTION ( 'NONE',  ( 0.000000000000000000, 0.000000000000000000, -1.000000000000000000 ) ) ;
#139508=DIRECTION ( 'NONE',  ( 0.000000000000000000, 0.9654727137038715545, 0.2605042016806676242 ) ) ;
#139539=CARTESIAN_POINT ( 'NONE',  ( 20.85000000000000142, -0.3238857010591806307, -66.95758958931398297 ) ) ;
#139549=ORIENTED_EDGE ( 'NONE', *, *, #74610, .T. ) ;
#139574=ORIENTED_EDGE ( 'NONE', *, *, #256036, .F. ) ;
#139577=DIRECTION ( 'NONE',  ( 1.000000000000000000, 0.000000000000000000, 0.000000000000000000 ) ) ;
#139583=AXIS2_PLACEMENT_3D ( 'NONE', #145957, #142113, #225480 ) ;
#139599=VERTEX_POINT ( 'NONE', #98222 ) ;
#139642=ORIENTED_EDGE ( 'NONE', *, *, #168349, .T. ) ;
#139648=DIRECTION ( 'NONE',  ( 0.000000000000000000, 0.000000000000000000, 1.000000000000000000 ) ) ;
#139654=FACE_OUTER_BOUND ( 'NONE', #112860, .T. ) ;
#139656=DIRECTION ( 'NONE',  ( 1.000000000000000000, 0.000000000000000000, 0.000000000000000000 ) ) ;
#139664=DIRECTION ( 'NONE',  ( 0.000000000000000000, 0.000000000000000000, 1.000000000000000000 ) ) ;
#139714=DIRECTION ( 'NONE',  ( 0.000000000000000000, 0.000000000000000000, 1.000000000000000000 ) ) ;
#139715=CARTESIAN_POINT ( 'NONE',  ( -18.59999999999999787, -1.835859311432484375, -78.50443916879852679 ) ) ;
#139760=EDGE_CURVE ( 'NONE', #119332, #149548, #168228, .T. ) ;
#139836=EDGE_CURVE ( 'NONE', #15098, #43174, #247271, .T. ) ;
#139850=EDGE_CURVE ( 'NONE', #249646, #143246, #93159, .T. ) ;
#139858=ADVANCED_FACE ( 'NONE', ( #83708 ), #2915, .T. ) ;
#139864=CARTESIAN_POINT ( 'NONE',  ( -22.59999999999999787, 0.1008583691098682150, -21.75043287651061164 ) ) ;
#139889=CIRCLE ( 'NONE', #164869, 0.1000000000000002831 ) ;
#139896=CARTESIAN_POINT ( 'NONE',  ( -23.25000000000000000, 10.33248238083634440, -72.59484654391314962 ) ) ;
#139900=PLANE ( 'NONE',  #17630 ) ;
#139903=EDGE_CURVE ( 'NONE', #24660, #134638, #213988, .T. ) ;
#139910=AXIS2_PLACEMENT_3D ( 'NONE', #190445, #251675, #73084 ) ;
#139931=DIRECTION ( 'NONE',  ( 0.000000000000000000, -0.8660254037844412611, -0.4999999999999956701 ) ) ;
#139941=EDGE_LOOP ( 'NONE', ( #152081, #118706, #28681, #42106 ) ) ;
#139968=VERTEX_POINT ( 'NONE', #187994 ) ;
#139972=ORIENTED_EDGE ( 'NONE', *, *, #129478, .T. ) ;
#140022=ORIENTED_EDGE ( 'NONE', *, *, #240395, .F. ) ;
#140028=AXIS2_PLACEMENT_3D ( 'NONE', #246182, #127518, #247456 ) ;
#140029=CIRCLE ( 'NONE', #48297, 0.09999999999999824307 ) ;
#140074=AXIS2_PLACEMENT_3D ( 'NONE', #207237, #26029, #108126 ) ;
#140100=EDGE_CURVE ( 'NONE', #137139, #45034, #160020, .T. ) ;
#140103=ORIENTED_EDGE ( 'NONE', *, *, #20762, .F. ) ;
#140112=EDGE_CURVE ( 'NONE', #250227, #199184, #184934, .T. ) ;
#140136=CARTESIAN_POINT ( 'NONE',  ( -23.15000000000000213, 1.115600667400684642E-11, -67.00000000000000000 ) ) ;
#140155=ORIENTED_EDGE ( 'NONE', *, *, #127819, .T. ) ;
#140160=CARTESIAN_POINT ( 'NONE',  ( 21.14999999999999858, 8.786607556611267356, -45.75000000000000000 ) ) ;
#140166=DIRECTION ( 'NONE',  ( -1.000000000000000000, -2.952720810173289112E-16, 0.000000000000000000 ) ) ;
#140178=PLANE ( 'NONE',  #138850 ) ;
#140198=ORIENTED_EDGE ( 'NONE', *, *, #154312, .T. ) ;
#140207=CIRCLE ( 'NONE', #119394, 0.1000000000000028644 ) ;
#140224=AXIS2_PLACEMENT_3D ( 'NONE', #61099, #38990, #217584 ) ;
#140229=CYLINDRICAL_SURFACE ( 'NONE', #145200, 0.1000000000000000472 ) ;
#140243=ORIENTED_EDGE ( 'NONE', *, *, #3809, .T. ) ;
#140256=CIRCLE ( 'NONE', #219382, 4.149999999999999467 ) ;
#140260=VERTEX_POINT ( 'NONE', #65156 ) ;
#140263=ORIENTED_EDGE ( 'NONE', *, *, #131449, .T. ) ;
#140265=FACE_OUTER_BOUND ( 'NONE', #232235, .T. ) ;
#140346=CIRCLE ( 'NONE', #102928, 7.720710678118678061 ) ;
#140347=EDGE_LOOP ( 'NONE', ( #169897, #137963, #161253, #232043 ) ) ;
#140393=EDGE_CURVE ( 'NONE', #39510, #197787, #189229, .T. ) ;
#140433=CARTESIAN_POINT ( 'NONE',  ( -20.54999999999999716, 1.115600667400684642E-11, -68.90000000000000568 ) ) ;
#140463=DIRECTION ( 'NONE',  ( -0.000000000000000000, -0.1350103645451928291, -0.9908441862701594660 ) ) ;
#140472=EDGE_LOOP ( 'NONE', ( #106622, #81516, #64700, #117037 ) ) ;
#140547=ORIENTED_EDGE ( 'NONE', *, *, #123670, .T. ) ;
#140559=ADVANCED_FACE ( 'NONE', ( #241879 ), #63234, .F. ) ;
#140578=AXIS2_PLACEMENT_3D ( 'NONE', #233953, #55280, #134825 ) ;
#140596=DIRECTION ( 'NONE',  ( 0.000000000000000000, 1.000000000000000000, 0.000000000000000000 ) ) ;
#140627=ORIENTED_EDGE ( 'NONE', *, *, #98136, .F. ) ;
#140666=TOROIDAL_SURFACE ( 'NONE', #69952, 12.97499999999999609, 0.1000000000000000056 ) ;
#140673=CARTESIAN_POINT ( 'NONE',  ( 21.95218792049437795, 7.201507561257818324, -33.40097156020008384 ) ) ;
#140675=DIRECTION ( 'NONE',  ( -0.000000000000000000, -1.265107689135680095E-16, 1.000000000000000000 ) ) ;
#140703=CARTESIAN_POINT ( 'NONE',  ( 20.94999999999999929, 10.72371710471868056, -45.65000000000000568 ) ) ;
#140766=CIRCLE ( 'NONE', #249125, 0.1000000000000028644 ) ;
#140799=CARTESIAN_POINT ( 'NONE',  ( -18.59999999999999787, 9.350000000011156942, -54.65000000000000568 ) ) ;
#140858=CARTESIAN_POINT ( 'NONE',  ( -20.64999999999999858, 1.115623935689868526E-11, -65.10000000000000853 ) ) ;
#140859=VECTOR ( 'NONE', #164549, 1000.000000000000000 ) ;
#140862=VERTEX_POINT ( 'NONE', #137326 ) ;
#140878=EDGE_CURVE ( 'NONE', #4740, #72990, #40845, .T. ) ;
#140896=CARTESIAN_POINT ( 'NONE',  ( 21.00023020733438273, 6.390869245278871347, -33.50000000000000711 ) ) ;
#140899=VERTEX_POINT ( 'NONE', #179074 ) ;
#140928=CIRCLE ( 'NONE', #144999, 0.09999999999999939493 ) ;
#140941=CARTESIAN_POINT ( 'NONE',  ( 21.30000000000002558, 1.115600667400684642E-11, -33.50000000000000000 ) ) ;
#140946=B_SPLINE_CURVE_WITH_KNOTS ( 'NONE', 3,
 ( #159453, #158208, #56471, #96863, #237706, #139864 ),
 .UNSPECIFIED., .F., .F.,
 ( 4, 2, 4 ),
 ( 0.000000000000000000, 0.0001568709654583420778, 0.0003137419309166841557 ),
 .UNSPECIFIED. ) ;
#140966=CIRCLE ( 'NONE', #174315, 7.900000000000003908 ) ;
#140969=VERTEX_POINT ( 'NONE', #65502 ) ;
#140977=ORIENTED_EDGE ( 'NONE', *, *, #8150, .F. ) ;
#141008=EDGE_CURVE ( 'NONE', #135166, #147029, #160390, .T. ) ;
#141026=FACE_OUTER_BOUND ( 'NONE', #244764, .T. ) ;
#141063=FACE_OUTER_BOUND ( 'NONE', #107339, .T. ) ;
#141064=ORIENTED_EDGE ( 'NONE', *, *, #208045, .F. ) ;
#141067=CARTESIAN_POINT ( 'NONE',  ( 23.24999999999999645, 4.775700934590591196, -55.15123189595403375 ) ) ;
#141082=LINE ( 'NONE', #235050, #191011 ) ;
#141089=EDGE_LOOP ( 'NONE', ( #13956, #81551, #174911, #230160 ) ) ;
#141098=ADVANCED_FACE ( 'NONE', ( #169790 ), #249302, .T. ) ;
#141137=EDGE_LOOP ( 'NONE', ( #160212, #5916, #179513, #47995 ) ) ;
#141139=CARTESIAN_POINT ( 'NONE',  ( 20.94999999999999929, -11.48912529306489994, -64.00000000000000000 ) ) ;
#141155=CARTESIAN_POINT ( 'NONE',  ( -18.59999999999999787, -1.736257131586239844, -45.06865232901750318 ) ) ;
#141159=ORIENTED_EDGE ( 'NONE', *, *, #69423, .F. ) ;
#141167=CIRCLE ( 'NONE', #162027, 0.1000000000000028644 ) ;
#141183=EDGE_CURVE ( 'NONE', #73952, #126560, #77149, .T. ) ;
#141190=ORIENTED_EDGE ( 'NONE', *, *, #85453, .F. ) ;
#141209=EDGE_CURVE ( 'NONE', #57195, #252337, #168512, .T. ) ;
#141254=AXIS2_PLACEMENT_3D ( 'NONE', #72354, #253524, #50184 ) ;
#141260=ORIENTED_EDGE ( 'NONE', *, *, #158800, .F. ) ;
#141299=CIRCLE ( 'NONE', #95509, 0.9750000000000036415 ) ;
#141306=ORIENTED_EDGE ( 'NONE', *, *, #162734, .T. ) ;
#141325=VERTEX_POINT ( 'NONE', #27406 ) ;
#141334=ORIENTED_EDGE ( 'NONE', *, *, #207075, .F. ) ;
#141378=LINE ( 'NONE', #180524, #228086 ) ;
#141380=DIRECTION ( 'NONE',  ( 0.000000000000000000, 1.000000000000000000, 0.000000000000000000 ) ) ;
#141381=EDGE_CURVE ( 'NONE', #3179, #203889, #23558, .T. ) ;
#141391=DIRECTION ( 'NONE',  ( 1.000000000000000000, 0.000000000000000000, 0.000000000000000000 ) ) ;
#141399=CIRCLE ( 'NONE', #116469, 0.1000000000000028644 ) ;
#141402=EDGE_CURVE ( 'NONE', #237327, #81995, #106891, .T. ) ;
#141415=AXIS2_PLACEMENT_3D ( 'NONE', #228047, #49407, #10295 ) ;
#141431=ORIENTED_EDGE ( 'NONE', *, *, #136881, .F. ) ;
#141435=EDGE_LOOP ( 'NONE', ( #202015, #20986, #91521, #40600 ) ) ;
#141436=DIRECTION ( 'NONE',  ( 1.000000000000000000, 0.000000000000000000, -0.000000000000000000 ) ) ;
#141444=CARTESIAN_POINT ( 'NONE',  ( 23.14999999999999858, 2.000000000011158630, -67.00000000000000000 ) ) ;
#141479=ORIENTED_EDGE ( 'NONE', *, *, #60544, .F. ) ;
#141495=AXIS2_PLACEMENT_3D ( 'NONE', #88724, #13086, #73080 ) ;
#141528=AXIS2_PLACEMENT_3D ( 'NONE', #42681, #223865, #127356 ) ;
#141560=( BOUNDED_SURFACE ( )  B_SPLINE_SURFACE ( 3, 2, ( 
 ( #76061, #51331, #155641 ),
 ( #33136, #136013, #56480 ),
 ( #252126, #154367, #36974 ),
 ( #95620, #133474, #172653 ),
 ( #74823, #73531, #253412 ),
 ( #153082, #193462, #150482 ) ),
 .UNSPECIFIED., .F., .F., .F. ) 
 B_SPLINE_SURFACE_WITH_KNOTS ( ( 4, 2, 4 ),
 ( 3, 3 ),
 ( 0.0001792624049599544510, 0.0003686986002124726996, 0.0005581347954649909212 ),
 ( 0.000000000000000000, 1.000000000000000000 ),
 .UNSPECIFIED. ) 
 GEOMETRIC_REPRESENTATION_ITEM ( )  RATIONAL_B_SPLINE_SURFACE ( (
 ( 1.000000000000000000, 0.9238795325112832968, 1.000000000000000000),
 ( 1.000000000000000000, 0.9229318695238958314, 1.000000000000000000),
 ( 1.000000000000000000, 0.8926288119230034734, 1.000000000000000000),
 ( 1.000000000000000000, 0.8123777807272225537, 1.000000000000000000),
 ( 1.000000000000000000, 0.7629087100930789234, 1.000000000000000000),
 ( 1.000000000000000000, 0.7071067811865475727, 1.000000000000000000) ) ) 
 REPRESENTATION_ITEM ( '' )  SURFACE ( )  );
#141584=CARTESIAN_POINT ( 'NONE',  ( -20.64999999999999858, 2.400000000011155432, -46.72462192276210402 ) ) ;
#141608=CARTESIAN_POINT ( 'NONE',  ( 20.94999999999999929, -11.64999999998883595, -64.00000000000000000 ) ) ;
#141620=DIRECTION ( 'NONE',  ( 1.000000000000000000, 0.000000000000000000, 0.000000000000000000 ) ) ;
#141634=CARTESIAN_POINT ( 'NONE',  ( 18.46921299892754575, -9.509378177812612520, -40.48657870937042702 ) ) ;
#141635=CIRCLE ( 'NONE', #62541, 0.09999999999999939493 ) ;
#141690=CARTESIAN_POINT ( 'NONE',  ( 21.14999999999999858, -0.09999999998884338825, -21.85042919245520210 ) ) ;
#141696=DIRECTION ( 'NONE',  ( 0.000000000000000000, -1.000000000000000000, -0.000000000000000000 ) ) ;
#141700=AXIS2_PLACEMENT_3D ( 'NONE', #210273, #87721, #167305 ) ;
#141718=VECTOR ( 'NONE', #152448, 1000.000000000000000 ) ;
#141732=EDGE_CURVE ( 'NONE', #250000, #151911, #177516, .T. ) ;
#141748=AXIS2_PLACEMENT_3D ( 'NONE', #48372, #109626, #28867 ) ;
#141769=CARTESIAN_POINT ( 'NONE',  ( -18.54159361262942696, -9.463132135481966856, -40.54912221629287927 ) ) ;
#141770=ORIENTED_EDGE ( 'NONE', *, *, #147124, .F. ) ;
#141780=ADVANCED_FACE ( 'NONE', ( #7485 ), #182292, .T. ) ;
#141803=EDGE_CURVE ( 'NONE', #230427, #223187, #114938, .T. ) ;
#141821=AXIS2_PLACEMENT_3D ( 'NONE', #12794, #234369, #92295 ) ;
#141829=VERTEX_POINT ( 'NONE', #24510 ) ;
#141844=DIRECTION ( 'NONE',  ( 0.000000000000000000, 3.552713678800509607E-15, -1.000000000000000000 ) ) ;
#141853=DIRECTION ( 'NONE',  ( -1.000000000000000000, 0.000000000000000000, 0.000000000000000000 ) ) ;
#141893=DIRECTION ( 'NONE',  ( 1.000000000000000000, 0.000000000000000000, 0.000000000000000000 ) ) ;
#141901=ORIENTED_EDGE ( 'NONE', *, *, #124275, .F. ) ;
#141916=VERTEX_POINT ( 'NONE', #70059 ) ;
#141920=CIRCLE ( 'NONE', #75326, 0.5000000000000004441 ) ;
#141926=CARTESIAN_POINT ( 'NONE',  ( 21.12642695952774119, 0.09890328320052040045, -27.12434007796482760 ) ) ;
#141975=AXIS2_PLACEMENT_3D ( 'NONE', #158082, #237574, #99314 ) ;
#141977=ORIENTED_EDGE ( 'NONE', *, *, #125835, .F. ) ;
#141994=CIRCLE ( 'NONE', #129540, 3.900000000000000799 ) ;
#142017=DIRECTION ( 'NONE',  ( -0.000000000000000000, 0.9876197685951279004, -0.1568667991644694115 ) ) ;
#142020=DIRECTION ( 'NONE',  ( 1.000000000000000000, 0.000000000000000000, 0.000000000000000000 ) ) ;
#142021=EDGE_CURVE ( 'NONE', #118445, #88637, #50441, .T. ) ;
#142025=CARTESIAN_POINT ( 'NONE',  ( 22.49999999999999645, 11.74956712350054744, -33.39914163090129051 ) ) ;
#142037=LINE ( 'NONE', #165475, #153394 ) ;
#142046=DIRECTION ( 'NONE',  ( 1.000000000000000000, 0.000000000000000000, 0.000000000000000000 ) ) ;
#142051=ORIENTED_EDGE ( 'NONE', *, *, #216588, .F. ) ;
#142075=DIRECTION ( 'NONE',  ( -1.000000000000000000, -0.000000000000000000, -0.000000000000000000 ) ) ;
#142096=EDGE_CURVE ( 'NONE', #127734, #255180, #56816, .T. ) ;
#142113=DIRECTION ( 'NONE',  ( 2.952720810173289112E-16, -1.000000000000000000, -0.000000000000000000 ) ) ;
#142131=CARTESIAN_POINT ( 'NONE',  ( -21.07928932188134041, 0.09889514566555068775, -27.17148334360670958 ) ) ;
#142135=DIRECTION ( 'NONE',  ( 2.659396599871503635E-15, 0.6132151058540549204, -0.7899159663865520375 ) ) ;
#142140=VERTEX_POINT ( 'NONE', #107245 ) ;
#142142=DIRECTION ( 'NONE',  ( 1.000000000000000000, -0.000000000000000000, -0.000000000000000000 ) ) ;
#142153=VECTOR ( 'NONE', #134637, 1000.000000000000000 ) ;
#142154=ORIENTED_EDGE ( 'NONE', *, *, #251868, .T. ) ;
#142187=ORIENTED_EDGE ( 'NONE', *, *, #82678, .F. ) ;
#142192=ORIENTED_EDGE ( 'NONE', *, *, #128452, .T. ) ;
#142209=ORIENTED_EDGE ( 'NONE', *, *, #11778, .T. ) ;
#142231=ORIENTED_EDGE ( 'NONE', *, *, #145450, .F. ) ;
#142249=LINE ( 'NONE', #144803, #11393 ) ;
#142331=DIRECTION ( 'NONE',  ( 0.000000000000000000, 0.000000000000000000, 1.000000000000000000 ) ) ;
#142360=CARTESIAN_POINT ( 'NONE',  ( 20.94999999999999929, -9.499999999988848032, -43.39396912265245021 ) ) ;
#142384=AXIS2_PLACEMENT_3D ( 'NONE', #66302, #225346, #33639 ) ;
#142397=ORIENTED_EDGE ( 'NONE', *, *, #12022, .F. ) ;
#142399=DIRECTION ( 'NONE',  ( 1.000000000000000000, 0.000000000000000000, 0.000000000000000000 ) ) ;
#142401=VERTEX_POINT ( 'NONE', #236178 ) ;
#142413=LINE ( 'NONE', #221925, #235310 ) ;
#142428=EDGE_CURVE ( 'NONE', #141916, #135166, #161808, .T. ) ;
#142436=DIRECTION ( 'NONE',  ( 0.000000000000000000, -0.1350103645451904977, -0.9908441862701596881 ) ) ;
#142438=CARTESIAN_POINT ( 'NONE',  ( 20.94403535211772294, 10.30632246271647467, -72.50418367788957141 ) ) ;
#142441=DIRECTION ( 'NONE',  ( 0.000000000000000000, 0.9915357197604792727, -0.1298341882520475943 ) ) ;
#142445=SPHERICAL_SURFACE ( 'NONE', #258024, 0.1000000000000000056 ) ;
#142464=AXIS2_PLACEMENT_3D ( 'NONE', #96552, #176140, #222930 ) ;
#142516=CARTESIAN_POINT ( 'NONE',  ( 20.94999999999999929, 10.38178547073510316, -72.50784536388417223 ) ) ;
#142519=B_SPLINE_CURVE_WITH_KNOTS ( 'NONE', 3,
 ( #195058, #16421, #95918, #18953, #98454, #185424, #27676, #6783, #87583, #43356, #225803, #8083, #142438, #221947, #86292, #64198, #165880, #223250, #167181 ),
 .UNSPECIFIED., .F., .F.,
 ( 4, 3, 3, 3, 3, 3, 4 ),
 ( 1.387778780781445676E-17, 2.646747978908994698E-05, 5.271166642128863382E-05, 9.008788829885137981E-05, 0.0001426648776561022008, 0.0001897378458659801945, 0.0001917382627806380965 ),
 .UNSPECIFIED. ) ;
#142522=EDGE_CURVE ( 'NONE', #61821, #216196, #169511, .T. ) ;
#142549=AXIS2_PLACEMENT_3D ( 'NONE', #72472, #32074, #111587 ) ;
#142586=ADVANCED_FACE ( 'NONE', ( #126508 ), #240224, .F. ) ;
#142653=DIRECTION ( 'NONE',  ( 0.000000000000000000, 0.000000000000000000, -1.000000000000000000 ) ) ;
#142684=CIRCLE ( 'NONE', #34409, 0.1000000000000028644 ) ;
#142707=CIRCLE ( 'NONE', #192802, 0.1000000000000028644 ) ;
#142717=DIRECTION ( 'NONE',  ( 0.000000000000000000, 0.000000000000000000, -1.000000000000000000 ) ) ;
#142748=DIRECTION ( 'NONE',  ( -0.000000000000000000, -0.000000000000000000, -1.000000000000000000 ) ) ;
#142774=DIRECTION ( 'NONE',  ( 0.000000000000000000, 0.000000000000000000, 1.000000000000000000 ) ) ;
#142790=ORIENTED_EDGE ( 'NONE', *, *, #127365, .T. ) ;
#142818=CARTESIAN_POINT ( 'NONE',  ( -23.15000000000000213, 11.75000000001116263, -45.65000000000000568 ) ) ;
#142826=EDGE_LOOP ( 'NONE', ( #203645, #147400, #34188, #158960, #235680 ) ) ;
#142836=CARTESIAN_POINT ( 'NONE',  ( 18.59999999999999076, 11.65000000001115943, -58.35000000000000142 ) ) ;
#142843=EDGE_CURVE ( 'NONE', #205018, #67554, #115471, .T. ) ;
#142850=AXIS2_PLACEMENT_3D ( 'NONE', #37389, #13969, #235556 ) ;
#142855=ORIENTED_EDGE ( 'NONE', *, *, #102890, .T. ) ;
#142865=DIRECTION ( 'NONE',  ( 1.000000000000000000, 0.000000000000000000, -0.000000000000000000 ) ) ;
#142887=LINE ( 'NONE', #46363, #180620 ) ;
#142917=CARTESIAN_POINT ( 'NONE',  ( -21.05439746398122836, 11.75000000001115197, -40.48991648748479122 ) ) ;
#142983=EDGE_CURVE ( 'NONE', #143470, #199184, #11448, .T. ) ;
#142986=AXIS2_PLACEMENT_3D ( 'NONE', #146734, #105024, #125906 ) ;
#142999=AXIS2_PLACEMENT_3D ( 'NONE', #227701, #126032, #205564 ) ;
#143001=TOROIDAL_SURFACE ( 'NONE', #247063, 0.2000000000000000111, 0.1000000000000000056 ) ;
#143004=EDGE_CURVE ( 'NONE', #118445, #190257, #148823, .T. ) ;
#143026=EDGE_CURVE ( 'NONE', #143764, #45390, #190530, .T. ) ;
#143030=EDGE_CURVE ( 'NONE', #22210, #6281, #78054, .T. ) ;
#143033=CARTESIAN_POINT ( 'NONE',  ( -22.39999999999999858, -0.1008583690875579364, -21.75043287651061164 ) ) ;
#143053=VECTOR ( 'NONE', #188112, 1000.000000000000227 ) ;
#143118=CARTESIAN_POINT ( 'NONE',  ( -21.05000000000000071, -11.74999999998884448, -64.00000000000000000 ) ) ;
#143119=CARTESIAN_POINT ( 'NONE',  ( -23.15000000000000213, 4.250000000011156409, -54.75000000000000000 ) ) ;
#143177=ORIENTED_EDGE ( 'NONE', *, *, #72211, .T. ) ;
#143204=CARTESIAN_POINT ( 'NONE',  ( 21.06280952165568721, 10.62713230061198111, -45.70405388677878022 ) ) ;
#143209=CARTESIAN_POINT ( 'NONE',  ( 20.94999999999999929, -11.64999999998883595, -67.00000000000000000 ) ) ;
#143246=VERTEX_POINT ( 'NONE', #94761 ) ;
#143256=AXIS2_PLACEMENT_3D ( 'NONE', #80984, #121450, #241378 ) ;
#143272=DIRECTION ( 'NONE',  ( 1.000000000000000000, 0.000000000000000000, 0.000000000000000000 ) ) ;
#143273=CARTESIAN_POINT ( 'NONE',  ( 18.59999999999999076, 10.20857864377385127, -58.25000000000000000 ) ) ;
#143277=DIRECTION ( 'NONE',  ( 1.000000000000000000, -0.000000000000000000, -0.000000000000000000 ) ) ;
#143291=DIRECTION ( 'NONE',  ( 0.000000000000000000, -0.9876197685951252359, -0.1568667991644863424 ) ) ;
#143301=DIRECTION ( 'NONE',  ( 0.000000000000000000, 0.000000000000000000, -1.000000000000000000 ) ) ;
#143338=DIRECTION ( 'NONE',  ( 0.000000000000000000, 0.000000000000000000, -1.000000000000000000 ) ) ;
#143344=ADVANCED_FACE ( 'NONE', ( #25514 ), #104989, .F. ) ;
#143346=CARTESIAN_POINT ( 'NONE',  ( -21.05000000000000071, -11.64999999998884306, -64.00000000000000000 ) ) ;
#143416=DIRECTION ( 'NONE',  ( 0.000000000000000000, -0.8777080977375132376, 0.4791956752371582251 ) ) ;
#143428=FACE_OUTER_BOUND ( 'NONE', #31154, .T. ) ;
#143470=VERTEX_POINT ( 'NONE', #111456 ) ;
#143500=EDGE_CURVE ( 'NONE', #43099, #168869, #170202, .T. ) ;
#143504=CYLINDRICAL_SURFACE ( 'NONE', #201530, 12.87499999999999822 ) ;
#143505=ORIENTED_EDGE ( 'NONE', *, *, #156021, .F. ) ;
#143526=DIRECTION ( 'NONE',  ( 0.000000000000000000, 0.000000000000000000, 1.000000000000000000 ) ) ;
#143531=DIRECTION ( 'NONE',  ( 2.710505431213777355E-16, -1.000000000000000000, 0.000000000000000000 ) ) ;
#143545=AXIS2_PLACEMENT_3D ( 'NONE', #2540, #80783, #19564 ) ;
#143650=ORIENTED_EDGE ( 'NONE', *, *, #200475, .T. ) ;
#143663=ADVANCED_FACE ( 'NONE', ( #249021 ), #70399, .F. ) ;
#143674=CARTESIAN_POINT ( 'NONE',  ( 21.05000000000000071, -9.399999999988846611, -43.39396912265245021 ) ) ;
#143679=ADVANCED_FACE ( 'NONE', ( #6529 ), #182514, .F. ) ;
#143705=AXIS2_PLACEMENT_3D ( 'NONE', #179531, #38726, #118255 ) ;
#143728=CARTESIAN_POINT ( 'NONE',  ( -20.85000000000000142, 1.115600667400684642E-11, -74.90000000000000568 ) ) ;
#143738=CIRCLE ( 'NONE', #110999, 11.79999999999999716 ) ;
#143752=ORIENTED_EDGE ( 'NONE', *, *, #142522, .F. ) ;
#143757=CARTESIAN_POINT ( 'NONE',  ( -18.46154800491015990, -9.480206274230827290, -73.65745083838122298 ) ) ;
#143764=VERTEX_POINT ( 'NONE', #72965 ) ;
#143769=ORIENTED_EDGE ( 'NONE', *, *, #142021, .T. ) ;
#143811=ORIENTED_EDGE ( 'NONE', *, *, #65672, .T. ) ;
#143840=CARTESIAN_POINT ( 'NONE',  ( -20.64999999999999858, 7.150000000011155876, -54.65000000000000568 ) ) ;
#143846=CARTESIAN_POINT ( 'NONE',  ( -20.12071067811865888, 9.320710678129810134, -45.85000000000000142 ) ) ;
#143861=CARTESIAN_POINT ( 'NONE',  ( 23.14999999999999503, 6.650000000011155876, -45.75000000000000711 ) ) ;
#143922=ORIENTED_EDGE ( 'NONE', *, *, #217386, .F. ) ;
#143925=CARTESIAN_POINT ( 'NONE',  ( 20.94999999999999929, -8.999999999988842703, -57.60603087734755690 ) ) ;
#143929=ORIENTED_EDGE ( 'NONE', *, *, #79424, .F. ) ;
#143943=FACE_OUTER_BOUND ( 'NONE', #141435, .T. ) ;
#143947=EDGE_CURVE ( 'NONE', #83073, #105461, #206999, .T. ) ;
#143970=ORIENTED_EDGE ( 'NONE', *, *, #192964, .F. ) ;
#143984=CARTESIAN_POINT ( 'NONE',  ( -23.15000000000000213, -8.596261682231835621, -42.95012751715027832 ) ) ;
#144033=ORIENTED_EDGE ( 'NONE', *, *, #88974, .F. ) ;
#144046=EDGE_LOOP ( 'NONE', ( #176103, #62800, #141334, #213646 ) ) ;
#144061=EDGE_CURVE ( 'NONE', #147029, #90926, #7508, .T. ) ;
#144091=VECTOR ( 'NONE', #101104, 1000.000000000000000 ) ;
#144104=CARTESIAN_POINT ( 'NONE',  ( -22.49072729836729678, 0.05648193274477467801, -21.84999175084506007 ) ) ;
#144108=CIRCLE ( 'NONE', #98863, 4.049999999999998046 ) ;
#144124=VECTOR ( 'NONE', #186211, 1000.000000000000000 ) ;
#144145=EDGE_LOOP ( 'NONE', ( #227360, #222003, #230268, #206209 ) ) ;
#144266=AXIS2_PLACEMENT_3D ( 'NONE', #21797, #240839, #62201 ) ;
#144271=DIRECTION ( 'NONE',  ( 0.000000000000000000, 0.000000000000000000, -1.000000000000000000 ) ) ;
#144281=CIRCLE ( 'NONE', #215051, 0.5000000000000004441 ) ;
#144282=DIRECTION ( 'NONE',  ( -1.000000000000000000, 0.000000000000000000, 0.000000000000000000 ) ) ;
#144288=EDGE_CURVE ( 'NONE', #226768, #111434, #244445, .T. ) ;
#144290=DIRECTION ( 'NONE',  ( 1.000000000000000000, -0.000000000000000000, -0.000000000000000000 ) ) ;
#144307=CARTESIAN_POINT ( 'NONE',  ( -21.05000000000000071, 1.261786168576181755, -41.58649896354548048 ) ) ;
#144325=ORIENTED_EDGE ( 'NONE', *, *, #67579, .F. ) ;
#144337=ORIENTED_EDGE ( 'NONE', *, *, #100716, .F. ) ;
#144361=AXIS2_PLACEMENT_3D ( 'NONE', #153906, #172181, #75623 ) ;
#144446=CARTESIAN_POINT ( 'NONE',  ( 20.94999999999999929, 7.021664781911246322, -70.83356540189728889 ) ) ;
#144452=CARTESIAN_POINT ( 'NONE',  ( 21.13507111622890022, 10.71768338700954537, -45.74916858636079553 ) ) ;
#144473=AXIS2_PLACEMENT_3D ( 'NONE', #44756, #184249, #205080 ) ;
#144475=CARTESIAN_POINT ( 'NONE',  ( 21.06089410995825872, 10.72529553213474429, -45.70238073104311383 ) ) ;
#144480=ADVANCED_FACE ( 'NONE', ( #154458 ), #228833, .F. ) ;
#144492=DIRECTION ( 'NONE',  ( -0.000000000000000000, -1.000000000000000000, 0.000000000000000000 ) ) ;
#144550=EDGE_CURVE ( 'NONE', #21983, #137338, #77424, .T. ) ;
#144595=CARTESIAN_POINT ( 'NONE',  ( 22.50000000000000000, 11.64957080755595520, -33.40000000000000568 ) ) ;
#144614=( BOUNDED_CURVE ( )  B_SPLINE_CURVE ( 3, ( #14511, #52300, #34085, #32801 ),
 .UNSPECIFIED., .F., .F. ) 
 B_SPLINE_CURVE_WITH_KNOTS ( ( 4, 4 ),
 ( 1.570796326794896558, 3.141592653589793116 ),
 .UNSPECIFIED. ) 
 CURVE ( )  GEOMETRIC_REPRESENTATION_ITEM ( )  RATIONAL_B_SPLINE_CURVE ( ( 1.000000000000000000, 0.8047378541243649375, 0.8047378541243649375, 1.000000000000000000 ) ) 
 REPRESENTATION_ITEM ( '' )  );
#144626=ORIENTED_EDGE ( 'NONE', *, *, #188022, .F. ) ;
#144642=DIRECTION ( 'NONE',  ( 1.000000000000000000, 0.000000000000000000, -0.000000000000000000 ) ) ;
#144672=ORIENTED_EDGE ( 'NONE', *, *, #183522, .F. ) ;
#144702=ORIENTED_EDGE ( 'NONE', *, *, #142021, .F. ) ;
#144745=CARTESIAN_POINT ( 'NONE',  ( 20.94999999999999574, 1.115600667400684642E-11, -33.50000000000000000 ) ) ;
#144781=EDGE_LOOP ( 'NONE', ( #81145, #123190, #202186 ) ) ;
#144803=CARTESIAN_POINT ( 'NONE',  ( -18.50000000000000000, -26.43935341558978891, -51.64150860750746119 ) ) ;
#144820=AXIS2_PLACEMENT_3D ( 'NONE', #93720, #172020, #173314 ) ;
#144862=DIRECTION ( 'NONE',  ( -1.000000000000000000, -0.000000000000000000, 0.000000000000000000 ) ) ;
#144869=VECTOR ( 'NONE', #45141, 1000.000000000000000 ) ;
#144896=CARTESIAN_POINT ( 'NONE',  ( -23.25000000000000000, -8.999999999988844479, -57.10603087734755690 ) ) ;
#144918=DIRECTION ( 'NONE',  ( 6.938893903907030216E-14, 0.000000000000000000, 1.000000000000000000 ) ) ;
#144922=DIRECTION ( 'NONE',  ( 0.000000000000000000, 0.000000000000000000, -1.000000000000000000 ) ) ;
#144939=EDGE_CURVE ( 'NONE', #217025, #40550, #99814, .T. ) ;
#144972=EDGE_CURVE ( 'NONE', #24103, #3690, #57549, .T. ) ;
#144996=AXIS2_PLACEMENT_3D ( 'NONE', #34216, #195854, #75877 ) ;
#144998=ADVANCED_FACE ( 'NONE', ( #234946 ), #99058, .T. ) ;
#144999=AXIS2_PLACEMENT_3D ( 'NONE', #5284, #163127, #104390 ) ;
#145002=FACE_OUTER_BOUND ( 'NONE', #100262, .T. ) ;
#145010=EDGE_CURVE ( 'NONE', #22426, #208600, #249135, .T. ) ;
#145028=ORIENTED_EDGE ( 'NONE', *, *, #5033, .T. ) ;
#145046=ORIENTED_EDGE ( 'NONE', *, *, #178012, .T. ) ;
#145106=DIRECTION ( 'NONE',  ( 0.000000000000000000, -1.000000000000000000, 0.000000000000000000 ) ) ;
#145131=VECTOR ( 'NONE', #147337, 1000.000000000000000 ) ;
#145165=ORIENTED_EDGE ( 'NONE', *, *, #214462, .F. ) ;
#145190=VECTOR ( 'NONE', #214388, 1000.000000000000000 ) ;
#145191=CARTESIAN_POINT ( 'NONE',  ( -18.50000000000000000, 9.250000000011157297, -54.65000000000000568 ) ) ;
#145200=AXIS2_PLACEMENT_3D ( 'NONE', #39900, #64560, #84074 ) ;
#145218=CARTESIAN_POINT ( 'NONE',  ( -20.54999999999999716, 7.250000000011155521, -54.75000000000000000 ) ) ;
#145227=EDGE_CURVE ( 'NONE', #107953, #55352, #130388, .T. ) ;
#145241=CYLINDRICAL_SURFACE ( 'NONE', #187773, 0.1000000000000028644 ) ;
#145254=DIRECTION ( 'NONE',  ( 0.000000000000000000, 1.000000000000000000, 0.000000000000000000 ) ) ;
#145255=LINE ( 'NONE', #27926, #99832 ) ;
#145273=FACE_OUTER_BOUND ( 'NONE', #40358, .T. ) ;
#145279=DIRECTION ( 'NONE',  ( 1.000000000000000000, 0.000000000000000000, 0.000000000000000000 ) ) ;
#145281=VECTOR ( 'NONE', #48092, 1000.000000000000000 ) ;
#145319=ORIENTED_EDGE ( 'NONE', *, *, #127914, .F. ) ;
#145322=ORIENTED_EDGE ( 'NONE', *, *, #220077, .F. ) ;
#145346=ADVANCED_FACE ( 'NONE', ( #2095 ), #77779, .F. ) ;
#145352=EDGE_CURVE ( 'NONE', #17436, #43703, #136864, .T. ) ;
#145356=FACE_OUTER_BOUND ( 'NONE', #212553, .T. ) ;
#145358=VERTEX_POINT ( 'NONE', #183322 ) ;
#145363=ORIENTED_EDGE ( 'NONE', *, *, #69637, .T. ) ;
#145378=CARTESIAN_POINT ( 'NONE',  ( 21.05000000000000071, 8.776282895303632259, -33.50000000000000000 ) ) ;
#145395=ORIENTED_EDGE ( 'NONE', *, *, #22910, .T. ) ;
#145404=EDGE_CURVE ( 'NONE', #160723, #194844, #32852, .T. ) ;
#145406=CIRCLE ( 'NONE', #216143, 0.09999999999999939493 ) ;
#145428=DIRECTION ( 'NONE',  ( 0.000000000000000000, 3.469446951953515108E-14, 1.000000000000000000 ) ) ;
#145440=ORIENTED_EDGE ( 'NONE', *, *, #216926, .F. ) ;
#145450=EDGE_CURVE ( 'NONE', #206237, #88666, #95351, .T. ) ;
#145462=AXIS2_PLACEMENT_3D ( 'NONE', #117034, #59588, #139124 ) ;
#145497=DIRECTION ( 'NONE',  ( 1.000000000000000000, 0.000000000000000000, 0.000000000000000000 ) ) ;
#145512=DIRECTION ( 'NONE',  ( -1.000000000000000000, -0.000000000000000000, -0.000000000000000000 ) ) ;
#145522=ORIENTED_EDGE ( 'NONE', *, *, #203848, .T. ) ;
#145524=CARTESIAN_POINT ( 'NONE',  ( 18.59999999999999432, 1.637172712981537659, -45.08215336547201701 ) ) ;
#145531=CARTESIAN_POINT ( 'NONE',  ( -23.25000000000000000, 1.115600667400684642E-11, -33.50000000000000000 ) ) ;
#145542=CIRCLE ( 'NONE', #33163, 0.09999999999999939493 ) ;
#145546=EDGE_CURVE ( 'NONE', #12767, #180952, #53656, .T. ) ;
#145552=AXIS2_PLACEMENT_3D ( 'NONE', #159608, #215697, #233989 ) ;
#145600=DIRECTION ( 'NONE',  ( 1.000000000000000000, 0.000000000000000000, 0.000000000000000000 ) ) ;
#145601=LINE ( 'NONE', #206874, #26843 ) ;
#145604=DIRECTION ( 'NONE',  ( 0.000000000000000000, 0.9908441862701596881, 0.1350103645451904977 ) ) ;
#145605=EDGE_CURVE ( 'NONE', #64314, #3674, #145406, .T. ) ;
#145637=ORIENTED_EDGE ( 'NONE', *, *, #66005, .F. ) ;
#145640=LINE ( 'NONE', #186070, #214606 ) ;
#145645=EDGE_LOOP ( 'NONE', ( #192985, #33757, #26880, #208487 ) ) ;
#145674=CARTESIAN_POINT ( 'NONE',  ( 20.85000000000000142, 1.115600667400684642E-11, -74.80000000000001137 ) ) ;
#145730=VERTEX_POINT ( 'NONE', #220844 ) ;
#145737=AXIS2_PLACEMENT_3D ( 'NONE', #248427, #168936, #33267 ) ;
#145751=CARTESIAN_POINT ( 'NONE',  ( 18.54286124688534088, -9.623917578786652882, -73.74120233186270923 ) ) ;
#145766=ORIENTED_EDGE ( 'NONE', *, *, #127069, .T. ) ;
#145780=LINE ( 'NONE', #104075, #35881 ) ;
#145799=CARTESIAN_POINT ( 'NONE',  ( 21.14999999999999858, 8.786607556611267356, -45.75000000000000711 ) ) ;
#145805=DIRECTION ( 'NONE',  ( 1.000000000000000000, -0.000000000000000000, -0.000000000000000000 ) ) ;
#145826=DIRECTION ( 'NONE',  ( 0.000000000000000000, -0.8700118002898359348, 0.4930308989875165082 ) ) ;
#145885=DIRECTION ( 'NONE',  ( -1.000000000000000000, 0.000000000000000000, 0.000000000000000000 ) ) ;
#145957=CARTESIAN_POINT ( 'NONE',  ( 23.15000000000000213, -11.74999999998883737, -54.85000000000000142 ) ) ;
#145963=ADVANCED_FACE ( 'NONE', ( #192027 ), #91618, .T. ) ;
#145978=EDGE_LOOP ( 'NONE', ( #6300, #140155, #256732, #250613 ) ) ;
#145997=CARTESIAN_POINT ( 'NONE',  ( -20.85000000000000142, 1.115600667400684642E-11, -67.00000000000000000 ) ) ;
#146030=EDGE_LOOP ( 'NONE', ( #37033, #250218, #96405 ) ) ;
#146038=EDGE_CURVE ( 'NONE', #84702, #94226, #112302, .T. ) ;
#146117=FACE_OUTER_BOUND ( 'NONE', #91275, .T. ) ;
#146126=EDGE_CURVE ( 'NONE', #216196, #35027, #40679, .T. ) ;
#146163=EDGE_CURVE ( 'NONE', #189424, #161055, #239309, .T. ) ;
#146181=EDGE_CURVE ( 'NONE', #57243, #31610, #234993, .T. ) ;
#146230=ORIENTED_EDGE ( 'NONE', *, *, #198737, .T. ) ;
#146251=CARTESIAN_POINT ( 'NONE',  ( 18.50016250449482413, 10.29766095125186176, -72.47436639332788388 ) ) ;
#146293=DIRECTION ( 'NONE',  ( 0.000000000000000000, 0.9908441862701600211, -0.1350103645451876666 ) ) ;
#146295=EDGE_CURVE ( 'NONE', #163061, #67224, #204035, .T. ) ;
#146301=DIRECTION ( 'NONE',  ( 1.000000000000000000, 2.952720810173289112E-16, -0.000000000000000000 ) ) ;
#146302=EDGE_CURVE ( 'NONE', #96628, #226768, #127553, .T. ) ;
#146320=DIRECTION ( 'NONE',  ( -3.469446951953605354E-14, 1.000000000000000000, 0.000000000000000000 ) ) ;
#146324=CARTESIAN_POINT ( 'NONE',  ( -18.37151313414709008, -9.571014125767069558, -73.81666290923895701 ) ) ;
#146327=ADVANCED_FACE ( 'NONE', ( #252943 ), #33962, .T. ) ;
#146337=DIRECTION ( 'NONE',  ( 1.000000000000000000, 0.000000000000000000, 0.000000000000000000 ) ) ;
#146346=DIRECTION ( 'NONE',  ( 1.000000000000000000, -0.000000000000000000, -0.000000000000000000 ) ) ;
#146349=ORIENTED_EDGE ( 'NONE', *, *, #204511, .F. ) ;
#146369=EDGE_CURVE ( 'NONE', #184107, #153506, #152608, .T. ) ;
#146376=DIRECTION ( 'NONE',  ( 1.000000000000000000, 0.000000000000000000, 0.000000000000000000 ) ) ;
#146395=EDGE_CURVE ( 'NONE', #88661, #121232, #154036, .T. ) ;
#146408=DIRECTION ( 'NONE',  ( -1.000000000000000000, 0.000000000000000000, 0.000000000000000000 ) ) ;
#146453=( BOUNDED_SURFACE ( )  B_SPLINE_SURFACE ( 3, 2, ( 
 ( #51502, #249739, #71121 ),
 ( #131066, #69837, #149379 ),
 ( #172813, #153239, #189762 ),
 ( #50233, #151947, #150638 ),
 ( #213169, #230167, #232756 ),
 ( #210608, #256085, #197455 ) ),
 .UNSPECIFIED., .F., .F., .T. ) 
 B_SPLINE_SURFACE_WITH_KNOTS ( ( 4, 2, 4 ),
 ( 3, 3 ),
 ( 6.719893378901017553E-05, 0.0002757154632485577309, 0.0004842319927081052862 ),
 ( 0.000000000000000000, 1.000000000000000000 ),
 .UNSPECIFIED. ) 
 GEOMETRIC_REPRESENTATION_ITEM ( )  RATIONAL_B_SPLINE_SURFACE ( (
 ( 1.000000000000000000, 0.7250110520819756932, 1.000000000000000000),
 ( 1.000000000000000000, 0.7277932058359009027, 1.000000000000000000),
 ( 1.000000000000000000, 0.7278452872617788838, 1.000000000000000000),
 ( 1.000000000000000000, 0.7221445671549024947, 1.000000000000000000),
 ( 1.000000000000000000, 0.7163662143779696567, 1.000000000000000000),
 ( 1.000000000000000000, 0.7071067811865475727, 1.000000000000000000) ) ) 
 REPRESENTATION_ITEM ( '' )  SURFACE ( )  );
#146455=ADVANCED_FACE ( 'NONE', ( #71778 ), #49924, .T. ) ;
#146484=ADVANCED_FACE ( 'NONE', ( #234680 ), #245744, .T. ) ;
#146510=EDGE_CURVE ( 'NONE', #14565, #119881, #104927, .T. ) ;
#146544=DIRECTION ( 'NONE',  ( -2.940209281316621016E-16, 1.000000000000000000, 0.000000000000000000 ) ) ;
#146548=DIRECTION ( 'NONE',  ( 0.000000000000000000, 0.000000000000000000, -1.000000000000000000 ) ) ;
#146549=CARTESIAN_POINT ( 'NONE',  ( 20.97565083910961548, 10.47461740128996510, -41.07794317658855476 ) ) ;
#146550=ORIENTED_EDGE ( 'NONE', *, *, #120076, .F. ) ;
#146552=EDGE_CURVE ( 'NONE', #127250, #241724, #20920, .T. ) ;
#146620=ADVANCED_FACE ( 'NONE', ( #162869 ), #201977, .T. ) ;
#146624=DIRECTION ( 'NONE',  ( -0.000000000000000000, -0.000000000000000000, 1.000000000000000000 ) ) ;
#146640=DIRECTION ( 'NONE',  ( 0.000000000000000000, 0.000000000000000000, 1.000000000000000000 ) ) ;
#146650=VERTEX_POINT ( 'NONE', #184975 ) ;
#146668=DIRECTION ( 'NONE',  ( 0.000000000000000000, 0.000000000000000000, 1.000000000000000000 ) ) ;
#146689=AXIS2_PLACEMENT_3D ( 'NONE', #15775, #135669, #36623 ) ;
#146719=LINE ( 'NONE', #204140, #113926 ) ;
#146734=CARTESIAN_POINT ( 'NONE',  ( 20.94999999999999929, -1.835341550213257733, -45.05515129256298223 ) ) ;
#146735=ORIENTED_EDGE ( 'NONE', *, *, #521, .F. ) ;
#146757=DIRECTION ( 'NONE',  ( 0.000000000000000000, 0.000000000000000000, -1.000000000000000000 ) ) ;
#146761=VERTEX_POINT ( 'NONE', #205818 ) ;
#146775=CIRCLE ( 'NONE', #51087, 0.1000000000000028644 ) ;
#146782=EDGE_CURVE ( 'NONE', #191642, #43027, #250022, .T. ) ;
#146798=DIRECTION ( 'NONE',  ( 0.000000000000000000, 0.9908441862701596881, 0.1350103645451904977 ) ) ;
#146840=ORIENTED_EDGE ( 'NONE', *, *, #177754, .F. ) ;
#146875=AXIS2_PLACEMENT_3D ( 'NONE', #216181, #97498, #254028 ) ;
#146882=CARTESIAN_POINT ( 'NONE',  ( 22.50046968638084621, 0.04516984715173071041, -21.74995484552572833 ) ) ;
#146899=DIRECTION ( 'NONE',  ( 0.000000000000000000, -1.000000000000000000, 0.000000000000000000 ) ) ;
#146925=EDGE_CURVE ( 'NONE', #122271, #129700, #102371, .T. ) ;
#146927=CARTESIAN_POINT ( 'NONE',  ( -20.94999999999999929, 1.115600667400684642E-11, -33.50000000000000000 ) ) ;
#146928=CARTESIAN_POINT ( 'NONE',  ( 18.39999999999999858, -9.599999999988845900, -73.70018939122203960 ) ) ;
#146944=FACE_OUTER_BOUND ( 'NONE', #114852, .T. ) ;
#146989=AXIS2_PLACEMENT_3D ( 'NONE', #69551, #49962, #109933 ) ;
#147001=CARTESIAN_POINT ( 'NONE',  ( 22.39999999999999503, 11.65000000001116298, -33.60000000000000142 ) ) ;
#147005=VECTOR ( 'NONE', #80873, 1000.000000000000114 ) ;
#147014=DIRECTION ( 'NONE',  ( 0.000000000000000000, -1.000000000000000000, 0.000000000000000000 ) ) ;
#147029=VERTEX_POINT ( 'NONE', #132247 ) ;
#147068=VERTEX_POINT ( 'NONE', #211795 ) ;
#147124=EDGE_CURVE ( 'NONE', #16250, #172639, #130964, .T. ) ;
#147176=DIRECTION ( 'NONE',  ( -0.000000000000000000, 1.265107689135680095E-16, -1.000000000000000000 ) ) ;
#147234=LINE ( 'NONE', #183799, #78262 ) ;
#147264=FACE_OUTER_BOUND ( 'NONE', #6299, .T. ) ;
#147269=ORIENTED_EDGE ( 'NONE', *, *, #179889, .T. ) ;
#147271=CARTESIAN_POINT ( 'NONE',  ( 18.49999999999999645, -1.835859311432484375, -78.50443916879852679 ) ) ;
#147281=CARTESIAN_POINT ( 'NONE',  ( 20.94999999999999929, -8.663551401858002876, -43.02410111806730697 ) ) ;
#147289=VERTEX_POINT ( 'NONE', #138631 ) ;
#147309=CARTESIAN_POINT ( 'NONE',  ( -22.50000000000000000, 0.1000000000111554016, -33.50000000000000000 ) ) ;
#147337=DIRECTION ( 'NONE',  ( 1.000000000000000000, 7.304098846218133681E-16, -4.217023435051677501E-16 ) ) ;
#147360=EDGE_CURVE ( 'NONE', #27579, #86605, #31528, .T. ) ;
#147380=AXIS2_PLACEMENT_3D ( 'NONE', #167728, #12501, #247225 ) ;
#147400=ORIENTED_EDGE ( 'NONE', *, *, #45882, .T. ) ;
#147427=VERTEX_POINT ( 'NONE', #168158 ) ;
#147438=DIRECTION ( 'NONE',  ( 0.000000000000000000, -1.000000000000000000, 0.000000000000000000 ) ) ;
#147486=ORIENTED_EDGE ( 'NONE', *, *, #143500, .F. ) ;
#147508=EDGE_CURVE ( 'NONE', #178023, #226447, #98093, .T. ) ;
#147528=AXIS2_PLACEMENT_3D ( 'NONE', #222420, #90630, #9823 ) ;
#147545=DIRECTION ( 'NONE',  ( 8.673617379884087537E-15, -0.000000000000000000, 1.000000000000000000 ) ) ;
#147564=CIRCLE ( 'NONE', #239142, 0.09999999999999967248 ) ;
#147586=LINE ( 'NONE', #240587, #97148 ) ;
#147588=DIRECTION ( 'NONE',  ( -1.000000000000000000, 0.000000000000000000, 0.000000000000000000 ) ) ;
#147593=ORIENTED_EDGE ( 'NONE', *, *, #129542, .F. ) ;
#147620=CARTESIAN_POINT ( 'NONE',  ( -18.31331870001056572, -9.536294719169660539, -73.86857869098540164 ) ) ;
#147621=ORIENTED_EDGE ( 'NONE', *, *, #157000, .F. ) ;
#147626=ORIENTED_EDGE ( 'NONE', *, *, #64188, .F. ) ;
#147637=EDGE_CURVE ( 'NONE', #33354, #82065, #113271, .T. ) ;
#147646=CARTESIAN_POINT ( 'NONE',  ( -18.50000000000000000, -1.637172712959223952, -45.08215336547201701 ) ) ;
#147656=EDGE_CURVE ( 'NONE', #120355, #186437, #2321, .T. ) ;
#147676=EDGE_CURVE ( 'NONE', #83555, #147965, #52315, .T. ) ;
#147722=CARTESIAN_POINT ( 'NONE',  ( 18.51997666896865624, -9.392332131507705739, -40.64340618748368428 ) ) ;
#147760=ORIENTED_EDGE ( 'NONE', *, *, #102132, .F. ) ;
#147785=DIRECTION ( 'NONE',  ( -1.000000000000000000, -0.000000000000000000, -0.000000000000000000 ) ) ;
#147796=TOROIDAL_SURFACE ( 'NONE', #39662, 2.100000000000002309, 0.1000000000000000056 ) ;
#147804=ORIENTED_EDGE ( 'NONE', *, *, #159946, .T. ) ;
#147811=DIRECTION ( 'NONE',  ( 1.000000000000000000, 0.000000000000000000, -0.000000000000000000 ) ) ;
#147855=DIRECTION ( 'NONE',  ( 1.000000000000000000, -0.000000000000000000, -0.000000000000000000 ) ) ;
#147860=FACE_OUTER_BOUND ( 'NONE', #83236, .T. ) ;
#147861=ORIENTED_EDGE ( 'NONE', *, *, #94707, .T. ) ;
#147881=DIRECTION ( 'NONE',  ( 0.000000000000000000, -0.9908441862701596881, -0.1350103645451904977 ) ) ;
#147882=VERTEX_POINT ( 'NONE', #146928 ) ;
#147909=ADVANCED_FACE ( 'NONE', ( #188639 ), #27035, .F. ) ;
#147937=DIRECTION ( 'NONE',  ( 1.000000000000000000, 0.000000000000000000, 0.000000000000000000 ) ) ;
#147941=ORIENTED_EDGE ( 'NONE', *, *, #195750, .F. ) ;
#147945=ORIENTED_EDGE ( 'NONE', *, *, #24420, .T. ) ;
#147961=EDGE_CURVE ( 'NONE', #184556, #171093, #212075, .T. ) ;
#147963=DIRECTION ( 'NONE',  ( 1.000000000000000000, -0.000000000000000000, -0.000000000000000000 ) ) ;
#147965=VERTEX_POINT ( 'NONE', #132527 ) ;
#147970=EDGE_LOOP ( 'NONE', ( #128660, #69380, #92501, #158383 ) ) ;
#148110=CARTESIAN_POINT ( 'NONE',  ( 20.94999999999999929, 5.000000000011153745, -54.59473398108690390 ) ) ;
#148133=EDGE_LOOP ( 'NONE', ( #171506, #121142 ) ) ;
#148178=CIRCLE ( 'NONE', #35785, 0.2000000000000057288 ) ;
#148229=DIRECTION ( 'NONE',  ( 0.000000000000000000, -1.000000000000000000, 0.000000000000000000 ) ) ;
#148265=CARTESIAN_POINT ( 'NONE',  ( 21.08078803292165659, 6.333012964448271553, -33.42081401284222153 ) ) ;
#148274=VERTEX_POINT ( 'NONE', #73560 ) ;
#148275=CARTESIAN_POINT ( 'NONE',  ( 23.15000000000000213, -11.39257802169451139, -63.92605042016806749 ) ) ;
#148292=CIRCLE ( 'NONE', #52412, 7.900000000000003908 ) ;
#148294=AXIS2_PLACEMENT_3D ( 'NONE', #114848, #216512, #73189 ) ;
#148314=CARTESIAN_POINT ( 'NONE',  ( -22.48970261584618058, 11.65000000001115588, -33.44463051178259150 ) ) ;
#148331=CARTESIAN_POINT ( 'NONE',  ( 21.06490991615909536, 10.72489134759826790, -45.70371135353313008 ) ) ;
#148333=ORIENTED_EDGE ( 'NONE', *, *, #43516, .F. ) ;
#148339=LINE ( 'NONE', #97308, #103473 ) ;
#148356=AXIS2_PLACEMENT_3D ( 'NONE', #162268, #240500, #99673 ) ;
#148357=AXIS2_PLACEMENT_3D ( 'NONE', #132601, #49200, #67477 ) ;
#148361=ORIENTED_EDGE ( 'NONE', *, *, #22648, .F. ) ;
#148377=AXIS2_PLACEMENT_3D ( 'NONE', #224745, #201345, #103512 ) ;
#148433=EDGE_CURVE ( 'NONE', #107953, #58399, #79906, .T. ) ;
#148445=ORIENTED_EDGE ( 'NONE', *, *, #165318, .F. ) ;
#148449=VECTOR ( 'NONE', #172481, 1000.000000000000000 ) ;
#148513=FACE_OUTER_BOUND ( 'NONE', #182047, .T. ) ;
#148518=CARTESIAN_POINT ( 'NONE',  ( 23.14999999999999503, 6.650000000011155876, -54.65000000000000568 ) ) ;
#148535=ADVANCED_FACE ( 'NONE', ( #60370 ), #98623, .F. ) ;
#148567=ORIENTED_EDGE ( 'NONE', *, *, #88989, .F. ) ;
#148568=DIRECTION ( 'NONE',  ( 1.000000000000000000, 0.000000000000000000, -0.000000000000000000 ) ) ;
#148603=ADVANCED_FACE ( 'NONE', ( #104606 ), #69961, .T. ) ;
#148604=ORIENTED_EDGE ( 'NONE', *, *, #88053, .F. ) ;
#148605=DIRECTION ( 'NONE',  ( 1.000000000000000000, 0.000000000000000000, 0.000000000000000000 ) ) ;
#148608=TOROIDAL_SURFACE ( 'NONE', #181915, 0.2000000000000000111, 0.1000000000000000056 ) ;
#148674=ORIENTED_EDGE ( 'NONE', *, *, #223238, .T. ) ;
#148728=DIRECTION ( 'NONE',  ( -3.469446951953515108E-14, 0.000000000000000000, 1.000000000000000000 ) ) ;
#148762=EDGE_LOOP ( 'NONE', ( #13556, #133423, #106289, #19557 ) ) ;
#148765=DIRECTION ( 'NONE',  ( 0.000000000000000000, -1.000000000000000000, 0.000000000000000000 ) ) ;
#148768=EDGE_CURVE ( 'NONE', #118445, #128224, #221479, .T. ) ;
#148796=B_SPLINE_CURVE_WITH_KNOTS ( 'NONE', 3,
 ( #177397, #237345, #58675, #238622, #34043, #253040, #194388, #74452 ),
 .UNSPECIFIED., .F., .F.,
 ( 4, 2, 2, 4 ),
 ( 0.000000000000000000, 0.0001881495939909227498, 0.0002822243909863841383, 0.0003762991879818454997 ),
 .UNSPECIFIED. ) ;
#148806=DIRECTION ( 'NONE',  ( -1.000000000000000000, 0.000000000000000000, 0.000000000000000000 ) ) ;
#148807=DIRECTION ( 'NONE',  ( -0.000000000000000000, 1.000000000000000000, 0.000000000000000000 ) ) ;
#148814=AXIS2_PLACEMENT_3D ( 'NONE', #239057, #139931, #71980 ) ;
#148823=CIRCLE ( 'NONE', #178042, 0.09999999999999939493 ) ;
#148830=CARTESIAN_POINT ( 'NONE',  ( -22.39999999999999858, 7.790779598384560245, -33.50000000000000000 ) ) ;
#148836=CARTESIAN_POINT ( 'NONE',  ( -21.14999999999999858, -0.09999999998884338825, -26.95934304829875927 ) ) ;
#148861=ORIENTED_EDGE ( 'NONE', *, *, #141209, .T. ) ;
#148881=DIRECTION ( 'NONE',  ( 1.000000000000000000, 0.000000000000000000, 0.000000000000000000 ) ) ;
#148930=CARTESIAN_POINT ( 'NONE',  ( 20.94999999999999574, -1.835341550213255957, -45.05515129256298223 ) ) ;
#149001=CARTESIAN_POINT ( 'NONE',  ( -21.05000000000000426, 6.332272273946811580, -33.53753606328567116 ) ) ;
#149007=ADVANCED_FACE ( 'NONE', ( #20340 ), #163689, .T. ) ;
#149032=DIRECTION ( 'NONE',  ( -1.000000000000000000, 0.000000000000000000, 0.000000000000000000 ) ) ;
#149078=EDGE_CURVE ( 'NONE', #248843, #212292, #721, .T. ) ;
#149114=CARTESIAN_POINT ( 'NONE',  ( -21.05000000000000071, -11.74999999998884448, -64.10000000000000853 ) ) ;
#149125=ORIENTED_EDGE ( 'NONE', *, *, #158826, .T. ) ;
#149142=CARTESIAN_POINT ( 'NONE',  ( -18.50000000000000000, 1.162701749949165642, -41.60000000000000142 ) ) ;
#149160=CARTESIAN_POINT ( 'NONE',  ( 21.07094088545369104, 0.09889370256337753906, -27.17983277808285791 ) ) ;
#149164=EDGE_CURVE ( 'NONE', #163442, #216204, #177980, .T. ) ;
#149196=ORIENTED_EDGE ( 'NONE', *, *, #230159, .T. ) ;
#149206=EDGE_CURVE ( 'NONE', #81995, #26532, #19768, .T. ) ;
#149216=DIRECTION ( 'NONE',  ( 0.000000000000000000, 0.7397360091702755991, -0.6728971962616832059 ) ) ;
#149226=AXIS2_PLACEMENT_3D ( 'NONE', #236307, #216740, #117650 ) ;
#149239=ORIENTED_EDGE ( 'NONE', *, *, #248273, .F. ) ;
#149280=CARTESIAN_POINT ( 'NONE',  ( -22.50000000000000000, 1.115600667400684642E-11, -33.50000000000000000 ) ) ;
#149294=EDGE_LOOP ( 'NONE', ( #97904, #115783, #87951 ) ) ;
#149321=CARTESIAN_POINT ( 'NONE',  ( -20.94999999999999929, -11.29603075032412640, -63.95210084033612929 ) ) ;
#149330=AXIS2_PLACEMENT_3D ( 'NONE', #167082, #191779, #189187 ) ;
#149331=EDGE_LOOP ( 'NONE', ( #59764, #94684, #22053, #78350, #205071, #177834, #233932, #35429, #72121, #20761, #226562, #250749, #12828, #44828, #248481, #173313, #98096, #116064, #103034, #65705, #129162, #171955, #32040 ) ) ;
#149340=CYLINDRICAL_SURFACE ( 'NONE', #58984, 0.09999999999999939493 ) ;
#149379=CARTESIAN_POINT ( 'NONE',  ( 20.95595624212412744, 10.62389120310530544, -41.12963291412692257 ) ) ;
#149390=CARTESIAN_POINT ( 'NONE',  ( -20.94999999999999929, 10.29270135741298731, -72.45736188715193293 ) ) ;
#149454=TOROIDAL_SURFACE ( 'NONE', #182770, 0.2000000000000000111, 0.1000000000000000056 ) ;
#149460=DIRECTION ( 'NONE',  ( 0.000000000000000000, 0.000000000000000000, -1.000000000000000000 ) ) ;
#149464=CARTESIAN_POINT ( 'NONE',  ( 21.05000000000000071, 1.115600667400684642E-11, -33.50000000000000000 ) ) ;
#149465=CARTESIAN_POINT ( 'NONE',  ( -18.59999999999999787, 11.65000000001115232, -54.85000000000000142 ) ) ;
#149467=ORIENTED_EDGE ( 'NONE', *, *, #2294, .T. ) ;
#149470=DIRECTION ( 'NONE',  ( 0.000000000000000000, 0.000000000000000000, -1.000000000000000000 ) ) ;
#149491=EDGE_CURVE ( 'NONE', #136008, #222564, #198987, .T. ) ;
#149497=CARTESIAN_POINT ( 'NONE',  ( -20.54999999999999716, -9.499999999988846255, -57.10603087734755690 ) ) ;
#149499=DIRECTION ( 'NONE',  ( 0.000000000000000000, 0.000000000000000000, -1.000000000000000000 ) ) ;
#149500=VECTOR ( 'NONE', #176568, 1000.000000000000000 ) ;
#149525=CARTESIAN_POINT ( 'NONE',  ( 21.14999999999999858, -11.74999999998884448, -45.75000000000000711 ) ) ;
#149548=VERTEX_POINT ( 'NONE', #3001 ) ;
#149553=VECTOR ( 'NONE', #29028, 1000.000000000000000 ) ;
#149604=EDGE_CURVE ( 'NONE', #129105, #149548, #49143, .T. ) ;
#149612=DIRECTION ( 'NONE',  ( -1.000000000000000000, 0.000000000000000000, 0.000000000000000000 ) ) ;
#149633=CIRCLE ( 'NONE', #45373, 0.1000000000000028644 ) ;
#149647=CARTESIAN_POINT ( 'NONE',  ( -20.64999999999999858, 4.350000000011156054, -45.85000000000000142 ) ) ;
#149693=CARTESIAN_POINT ( 'NONE',  ( 23.14999999999999503, 11.65000000001116298, -59.98519422934606382 ) ) ;
#149752=VERTEX_POINT ( 'NONE', #154131 ) ;
#149763=ORIENTED_EDGE ( 'NONE', *, *, #108636, .F. ) ;
#149777=DIRECTION ( 'NONE',  ( 1.000000000000000000, -0.000000000000000000, -0.000000000000000000 ) ) ;
#149810=CYLINDRICAL_SURFACE ( 'NONE', #35272, 4.000000000000003553 ) ;
#149813=LINE ( 'NONE', #7724, #116169 ) ;
#149824=CARTESIAN_POINT ( 'NONE',  ( 21.13461538461538325, 10.61458296203669249, -45.85000000000000142 ) ) ;
#149844=CIRCLE ( 'NONE', #228935, 0.1000000000000002692 ) ;
#149910=EDGE_LOOP ( 'NONE', ( #197392, #254111, #76017, #16944, #58867 ) ) ;
#149923=CARTESIAN_POINT ( 'NONE',  ( -20.64999999999999858, 4.350000000011156054, -45.75000000000000711 ) ) ;
#149955=CYLINDRICAL_SURFACE ( 'NONE', #10844, 11.74999999999999645 ) ;
#149962=DIRECTION ( 'NONE',  ( 0.000000000000000000, 0.000000000000000000, -1.000000000000000000 ) ) ;
#149990=TOROIDAL_SURFACE ( 'NONE', #112564, 0.2000000000000000111, 0.1000000000000000056 ) ;
#150004=DIRECTION ( 'NONE',  ( 0.000000000000000000, 0.000000000000000000, -1.000000000000000000 ) ) ;
#150029=DIRECTION ( 'NONE',  ( -1.000000000000000000, -2.952720810173289112E-16, 0.000000000000000000 ) ) ;
#150055=EDGE_CURVE ( 'NONE', #13961, #22426, #23393, .T. ) ;
#150058=DIRECTION ( 'NONE',  ( 0.000000000000000000, 0.000000000000000000, 1.000000000000000000 ) ) ;
#150061=CARTESIAN_POINT ( 'NONE',  ( -21.05000000000000071, 1.115600667400684642E-11, -33.50000000000000000 ) ) ;
#150099=DIRECTION ( 'NONE',  ( 0.000000000000000000, 0.000000000000000000, -1.000000000000000000 ) ) ;
#150121=DIRECTION ( 'NONE',  ( 0.000000000000000000, -0.1298341882520124002, -0.9915357197604841577 ) ) ;
#150153=EDGE_LOOP ( 'NONE', ( #112070, #255418, #68664, #92760 ) ) ;
#150170=DIRECTION ( 'NONE',  ( 0.000000000000000000, 0.008583690987128059571, -0.9999631594459056361 ) ) ;
#150173=LINE ( 'NONE', #3238, #209882 ) ;
#150207=CARTESIAN_POINT ( 'NONE',  ( -18.41809261886924887, -9.682403314745313239, -73.65684355009136652 ) ) ;
#150219=CYLINDRICAL_SURFACE ( 'NONE', #1794, 0.09999999999999939493 ) ;
#150251=ORIENTED_EDGE ( 'NONE', *, *, #69120, .T. ) ;
#150266=AXIS2_PLACEMENT_3D ( 'NONE', #234323, #111829, #135212 ) ;
#150267=DIRECTION ( 'NONE',  ( 0.000000000000000000, -1.000000000000000000, -0.000000000000000000 ) ) ;
#150281=CARTESIAN_POINT ( 'NONE',  ( -21.05000000000000071, 6.257814610487270279, -33.40220970869120265 ) ) ;
#150315=LINE ( 'NONE', #125594, #54243 ) ;
#150339=EDGE_CURVE ( 'NONE', #196889, #135153, #82232, .T. ) ;
#150381=DIRECTION ( 'NONE',  ( 1.000000000000000000, 0.000000000000000000, 0.000000000000000000 ) ) ;
#150385=DIRECTION ( 'NONE',  ( 0.000000000000000000, 0.000000000000000000, -1.000000000000000000 ) ) ;
#150394=ORIENTED_EDGE ( 'NONE', *, *, #202755, .F. ) ;
#150400=EDGE_CURVE ( 'NONE', #203545, #72122, #212707, .T. ) ;
#150405=CARTESIAN_POINT ( 'NONE',  ( 18.49999999999999289, 6.450000000011156587, -54.65000000000000568 ) ) ;
#150427=VERTEX_POINT ( 'NONE', #203164 ) ;
#150438=CARTESIAN_POINT ( 'NONE',  ( -23.25000000000000000, -11.64999999998884483, -63.89999999999999858 ) ) ;
#150482=CARTESIAN_POINT ( 'NONE',  ( 21.05000000000000071, 6.540656951712401579, -33.60000000000000142 ) ) ;
#150510=ADVANCED_FACE ( 'NONE', ( #18762 ), #95721, .T. ) ;
#150526=TOROIDAL_SURFACE ( 'NONE', #208795, 0.2000000000000000111, 0.1000000000000000056 ) ;
#150537=B_SPLINE_CURVE_WITH_KNOTS ( 'NONE', 3,
 ( #175576, #15218, #30950, #12658, #192562, #96003, #170480, #249963, #32222, #111737 ),
 .UNSPECIFIED., .F., .F.,
 ( 4, 2, 2, 2, 4 ),
 ( 0.000000000000000000, 4.221631689687179134E-05, 8.443263379374358268E-05, 0.0001688652675874855933, 0.0003377305351749678797 ),
 .UNSPECIFIED. ) ;
#150552=ORIENTED_EDGE ( 'NONE', *, *, #207683, .T. ) ;
#150553=CARTESIAN_POINT ( 'NONE',  ( 20.84999999999998721, 10.33248238083634440, -72.59484654391314962 ) ) ;
#150564=CIRCLE ( 'NONE', #9102, 0.1000000000000028644 ) ;
#150589=ADVANCED_FACE ( 'NONE', ( #40934 ), #85122, .T. ) ;
#150635=ORIENTED_EDGE ( 'NONE', *, *, #164127, .F. ) ;
#150638=CARTESIAN_POINT ( 'NONE',  ( 20.95429693346636313, 10.54330487990693221, -41.06088253831304513 ) ) ;
#150641=CARTESIAN_POINT ( 'NONE',  ( -21.05000000000000071, 1.116121084443477685E-11, -36.39999999999999147 ) ) ;
#150664=ORIENTED_EDGE ( 'NONE', *, *, #189918, .T. ) ;
#150670=DIRECTION ( 'NONE',  ( 0.000000000000000000, -1.000000000000000000, 0.000000000000000000 ) ) ;
#150717=VECTOR ( 'NONE', #29306, 1000.000000000000000 ) ;
#150736=VECTOR ( 'NONE', #240903, 1000.000000000000000 ) ;
#150741=( BOUNDED_SURFACE ( )  B_SPLINE_SURFACE ( 3, 2, ( 
 ( #110003, #192140, #170036 ),
 ( #211702, #91735, #250799 ),
 ( #189563, #228695, #249537 ),
 ( #127007, #171328, #149160 ) ),
 .UNSPECIFIED., .F., .F., .T. ) 
 B_SPLINE_SURFACE_WITH_KNOTS ( ( 4, 4 ),
 ( 3, 3 ),
 ( -3.469446951953614189E-18, 0.001979672783031532438 ),
 ( 0.000000000000000000, 1.000000000000000000 ),
 .UNSPECIFIED. ) 
 GEOMETRIC_REPRESENTATION_ITEM ( )  RATIONAL_B_SPLINE_SURFACE ( (
 ( 1.000000000000000000, 0.7103081912008197829, 1.000000000000000000),
 ( 1.000000000000000000, 0.7104998333558649737, 1.000000000000000000),
 ( 1.000000000000000000, 0.7107238315755179947, 1.000000000000000000),
 ( 1.000000000000000000, 0.7110073749539376209, 1.000000000000000000) ) ) 
 REPRESENTATION_ITEM ( '' )  SURFACE ( )  );
#150761=CARTESIAN_POINT ( 'NONE',  ( -23.15000000000000213, 1.115650265596050101E-11, -29.45000000000000284 ) ) ;
#150765=CARTESIAN_POINT ( 'NONE',  ( -20.00857864376270001, 9.350000000011156942, -45.75000000000000000 ) ) ;
#150770=CARTESIAN_POINT ( 'NONE',  ( -22.57320508075687115, 11.75000000001115552, -33.50000000000000000 ) ) ;
#150783=CARTESIAN_POINT ( 'NONE',  ( 20.04142135623731136, 11.75000000001116263, -58.15000000000000568 ) ) ;
#150785=B_SPLINE_CURVE_WITH_KNOTS ( 'NONE', 3,
 ( #254229, #155189, #135569, #36522, #62480, #39078, #20797, #161597, #22077, #61185, #80726, #121196, #123736, #98993, #118614, #200700, #104143, #220278, #100283, #238535, #59874, #203260 ),
 .UNSPECIFIED., .F., .F.,
 ( 4, 3, 3, 3, 3, 3, 3, 4 ),
 ( 0.000000000000000000, 7.307836821077657032E-06, 4.161455748548155718E-05, 7.576591810647554650E-05, 0.0001098090429817538222, 0.0001438003617351105872, 0.0001777914035423655992, 0.0002117966137403026012 ),
 .UNSPECIFIED. ) ;
#150811=VERTEX_POINT ( 'NONE', #189406 ) ;
#150822=LINE ( 'NONE', #129956, #22601 ) ;
#150832=CARTESIAN_POINT ( 'NONE',  ( 21.08884785362045378, 6.357193367436396514, -33.45021690493315702 ) ) ;
#150886=EDGE_CURVE ( 'NONE', #1091, #83555, #107564, .T. ) ;
#150926=CARTESIAN_POINT ( 'NONE',  ( -21.05000000000000071, 1.162701749949165642, -41.60000000000000142 ) ) ;
#150971=TOROIDAL_SURFACE ( 'NONE', #254948, 0.4000000000000017431, 0.1000000000000000056 ) ;
#150983=CARTESIAN_POINT ( 'NONE',  ( -20.94560253601877164, 11.75000000001115197, -60.01008351251526562 ) ) ;
#151033=CIRCLE ( 'NONE', #17716, 0.1000000000000004496 ) ;
#151061=CARTESIAN_POINT ( 'NONE',  ( -21.05000000000000071, 5.900000000011162093, -56.78090023534363695 ) ) ;
#151098=LINE ( 'NONE', #32464, #16591 ) ;
#151162=CARTESIAN_POINT ( 'NONE',  ( -20.85000000000000142, 11.65000000001115232, -67.00000000000000000 ) ) ;
#151183=FACE_OUTER_BOUND ( 'NONE', #19834, .T. ) ;
#151239=AXIS2_PLACEMENT_3D ( 'NONE', #17952, #15417, #213587 ) ;
#151291=AXIS2_PLACEMENT_3D ( 'NONE', #158941, #242288, #59783 ) ;
#151294=LINE ( 'NONE', #172171, #118103 ) ;
#151296=FACE_OUTER_BOUND ( 'NONE', #134687, .T. ) ;
#151297=ORIENTED_EDGE ( 'NONE', *, *, #50445, .F. ) ;
#151302=CARTESIAN_POINT ( 'NONE',  ( -18.50000000000000000, 1.835341550235567887, -45.05515129256298223 ) ) ;
#151314=AXIS2_PLACEMENT_3D ( 'NONE', #202175, #23581, #103051 ) ;
#151322=AXIS2_PLACEMENT_3D ( 'NONE', #211117, #16460, #195097 ) ;
#151331=CIRCLE ( 'NONE', #5536, 0.09999999999999892308 ) ;
#151385=EDGE_CURVE ( 'NONE', #68820, #127120, #62520, .T. ) ;
#151391=AXIS2_PLACEMENT_3D ( 'NONE', #206509, #50004, #223488 ) ;
#151410=ORIENTED_EDGE ( 'NONE', *, *, #180822, .T. ) ;
#151447=DIRECTION ( 'NONE',  ( 1.000000000000000000, 0.000000000000000000, 0.000000000000000000 ) ) ;
#151448=CARTESIAN_POINT ( 'NONE',  ( 18.31325810956315436, -9.536388475996043113, -73.86844020630493901 ) ) ;
#151506=DIRECTION ( 'NONE',  ( 0.000000000000000000, 0.000000000000000000, -1.000000000000000000 ) ) ;
#151519=AXIS2_PLACEMENT_3D ( 'NONE', #33137, #113909, #16122 ) ;
#151528=ORIENTED_EDGE ( 'NONE', *, *, #139211, .F. ) ;
#151562=CIRCLE ( 'NONE', #18629, 0.1000000000000028644 ) ;
#151604=ORIENTED_EDGE ( 'NONE', *, *, #131507, .T. ) ;
#151668=EDGE_CURVE ( 'NONE', #35121, #45034, #103634, .T. ) ;
#151693=EDGE_LOOP ( 'NONE', ( #218281, #112575, #18367, #6014 ) ) ;
#151751=ORIENTED_EDGE ( 'NONE', *, *, #52184, .F. ) ;
#151814=AXIS2_PLACEMENT_3D ( 'NONE', #2621, #60023, #219097 ) ;
#151856=AXIS2_PLACEMENT_3D ( 'NONE', #2836, #220628, #42006 ) ;
#151868=AXIS2_PLACEMENT_3D ( 'NONE', #252538, #217253, #115606 ) ;
#151911=VERTEX_POINT ( 'NONE', #16068 ) ;
#151947=CARTESIAN_POINT ( 'NONE',  ( 21.04999999999999716, 10.54375127550677149, -41.05638780866501492 ) ) ;
#151983=ADVANCED_FACE ( 'NONE', ( #137258 ), #216794, .F. ) ;
#152002=ADVANCED_FACE ( 'NONE', ( #38187 ), #56428, .T. ) ;
#152013=DIRECTION ( 'NONE',  ( -1.000000000000000000, 0.000000000000000000, 0.000000000000000000 ) ) ;
#152028=VERTEX_POINT ( 'NONE', #120316 ) ;
#152058=CARTESIAN_POINT ( 'NONE',  ( 20.95512820512820440, 8.876151316299273120, -42.05862899514095687 ) ) ;
#152064=CYLINDRICAL_SURFACE ( 'NONE', #26887, 0.09999999999999939493 ) ;
#152069=DIRECTION ( 'NONE',  ( 0.000000000000000000, 0.000000000000000000, 1.000000000000000000 ) ) ;
#152081=ORIENTED_EDGE ( 'NONE', *, *, #40930, .F. ) ;
#152120=CARTESIAN_POINT ( 'NONE',  ( -20.94999999999999929, -1.851028230129704522, -45.15391326942249606 ) ) ;
#152126=ORIENTED_EDGE ( 'NONE', *, *, #57373, .F. ) ;
#152145=CARTESIAN_POINT ( 'NONE',  ( 21.08621493067296271, 6.349294291182824956, -33.44380516052389396 ) ) ;
#152152=AXIS2_PLACEMENT_3D ( 'NONE', #124253, #222025, #104634 ) ;
#152278=ORIENTED_EDGE ( 'NONE', *, *, #213642, .F. ) ;
#152286=CARTESIAN_POINT ( 'NONE',  ( -20.85000000106584750, 11.75000000001115197, -60.15550465647356049 ) ) ;
#152288=CARTESIAN_POINT ( 'NONE',  ( 23.14999999999999503, 11.65000000001116298, -59.98519422934606382 ) ) ;
#152303=STYLED_ITEM ( 'NONE', ( #38701 ), #228621 ) ;
#152309=EDGE_CURVE ( 'NONE', #186437, #26532, #149844, .T. ) ;
#152346=CARTESIAN_POINT ( 'NONE',  ( -20.85000000000000142, -1.263275465206102233, -74.90186466674640542 ) ) ;
#152352=LINE ( 'NONE', #250140, #94454 ) ;
#152364=EDGE_CURVE ( 'NONE', #237399, #70987, #183156, .T. ) ;
#152371=SPHERICAL_SURFACE ( 'NONE', #151239, 0.1000000000000000056 ) ;
#152393=DIRECTION ( 'NONE',  ( 0.000000000000000000, -0.1298341882520022694, -0.9915357197604853789 ) ) ;
#152415=ORIENTED_EDGE ( 'NONE', *, *, #74318, .T. ) ;
#152427=CARTESIAN_POINT ( 'NONE',  ( 23.14999999999999858, 1.115600667400684642E-11, -33.50000000000000000 ) ) ;
#152437=AXIS2_PLACEMENT_3D ( 'NONE', #222462, #234685, #114740 ) ;
#152439=ORIENTED_EDGE ( 'NONE', *, *, #163402, .T. ) ;
#152441=CARTESIAN_POINT ( 'NONE',  ( -21.05000000000000071, 1.250000000011155299, -41.50000000000000000 ) ) ;
#152448=DIRECTION ( 'NONE',  ( 1.000000000000000000, -0.000000000000000000, -0.000000000000000000 ) ) ;
#152452=CARTESIAN_POINT ( 'NONE',  ( 23.25000000000000000, -8.596261682231833845, -42.95012751715027832 ) ) ;
#152497=EDGE_CURVE ( 'NONE', #176243, #57243, #50048, .T. ) ;
#152514=EDGE_LOOP ( 'NONE', ( #120131, #57796, #10278, #212390 ) ) ;
#152542=ORIENTED_EDGE ( 'NONE', *, *, #247247, .F. ) ;
#152559=DIRECTION ( 'NONE',  ( 1.000000000000000000, -0.000000000000000000, -0.000000000000000000 ) ) ;
#152582=FACE_OUTER_BOUND ( 'NONE', #110328, .T. ) ;
#152583=DIRECTION ( 'NONE',  ( 0.000000000000000000, 0.000000000000000000, -1.000000000000000000 ) ) ;
#152600=DIRECTION ( 'NONE',  ( 0.000000000000000000, 0.000000000000000000, -1.000000000000000000 ) ) ;
#152608=LINE ( 'NONE', #212564, #12533 ) ;
#152641=DIRECTION ( 'NONE',  ( 1.000000000000000000, 0.000000000000000000, 0.000000000000000000 ) ) ;
#152659=CARTESIAN_POINT ( 'NONE',  ( -21.14999999999999858, -0.09999999998884338825, -27.25000000000000355 ) ) ;
#152688=EDGE_CURVE ( 'NONE', #81117, #11734, #72858, .T. ) ;
#152721=DIRECTION ( 'NONE',  ( 0.000000000000000000, 0.000000000000000000, -1.000000000000000000 ) ) ;
#152735=ORIENTED_EDGE ( 'NONE', *, *, #189918, .F. ) ;
#152747=CARTESIAN_POINT ( 'NONE',  ( -22.14074124539699895, 0.09905289585522827900, -26.10992214895623675 ) ) ;
#152754=DIRECTION ( 'NONE',  ( 0.000000000000000000, -0.000000000000000000, -1.000000000000000000 ) ) ;
#152755=ORIENTED_EDGE ( 'NONE', *, *, #173553, .F. ) ;
#152796=EDGE_CURVE ( 'NONE', #140862, #19748, #29251, .T. ) ;
#152844=CARTESIAN_POINT ( 'NONE',  ( 21.05000000000000071, 8.826429739528350638, -41.91405471294370244 ) ) ;
#152892=DIRECTION ( 'NONE',  ( 0.000000000000000000, 0.8660254037844411501, 0.4999999999999956701 ) ) ;
#152909=DIRECTION ( 'NONE',  ( 0.000000000000000000, 6.938893903907270030E-14, 1.000000000000000000 ) ) ;
#152916=CARTESIAN_POINT ( 'NONE',  ( 22.16821283564876666, 7.558973340791918183, -33.50000000000000000 ) ) ;
#152971=DIRECTION ( 'NONE',  ( 1.000000000000000000, -0.000000000000000000, -0.000000000000000000 ) ) ;
#152976=DIRECTION ( 'NONE',  ( 1.000000000000000000, -0.000000000000000000, -0.000000000000000000 ) ) ;
#152984=ORIENTED_EDGE ( 'NONE', *, *, #145450, .T. ) ;
#152989=CARTESIAN_POINT ( 'NONE',  ( -20.00857864376270001, 9.150000000011157653, -45.85000000000000142 ) ) ;
#153007=AXIS2_PLACEMENT_3D ( 'NONE', #102310, #24124, #181895 ) ;
#153082=CARTESIAN_POINT ( 'NONE',  ( 21.14999999999999858, 6.540656951712400691, -33.50000000000000000 ) ) ;
#153136=DIRECTION ( 'NONE',  ( 0.7071067811865474617, 0.7071067811865474617, 2.044391222244499837E-16 ) ) ;
#153159=EDGE_CURVE ( 'NONE', #194376, #183157, #115481, .T. ) ;
#153172=ORIENTED_EDGE ( 'NONE', *, *, #521, .T. ) ;
#153196=AXIS2_PLACEMENT_3D ( 'NONE', #156670, #214044, #111086 ) ;
#153202=DIRECTION ( 'NONE',  ( 0.000000000000000000, 0.000000000000000000, -1.000000000000000000 ) ) ;
#153215=CIRCLE ( 'NONE', #40792, 0.1000000000000002692 ) ;
#153239=CARTESIAN_POINT ( 'NONE',  ( 21.05000000000000071, 10.60832956796514104, -41.09168501329539680 ) ) ;
#153248=CARTESIAN_POINT ( 'NONE',  ( 18.52928932304149967, 10.27928932305266407, -58.17625343280370487 ) ) ;
#153258=ORIENTED_EDGE ( 'NONE', *, *, #73687, .T. ) ;
#153299=DIRECTION ( 'NONE',  ( 0.000000000000000000, 1.000000000000000000, 0.000000000000000000 ) ) ;
#153305=VECTOR ( 'NONE', #89311, 1000.000000000000000 ) ;
#153310=CARTESIAN_POINT ( 'NONE',  ( -22.50000000000000000, 7.790779598384560245, -33.39999999999999858 ) ) ;
#153340=DIRECTION ( 'NONE',  ( 1.000000000000000000, 0.000000000000000000, 0.000000000000000000 ) ) ;
#153343=EDGE_CURVE ( 'NONE', #7325, #103845, #129530, .T. ) ;
#153357=ADVANCED_FACE ( 'NONE', ( #24121 ), #133611, .F. ) ;
#153367=ADVANCED_FACE ( 'NONE', ( #91461 ), #92721, .T. ) ;
#153368=ORIENTED_EDGE ( 'NONE', *, *, #57373, .T. ) ;
#153371=CARTESIAN_POINT ( 'NONE',  ( 23.15000000000000213, -11.64999999998883595, -21.75000000000000355 ) ) ;
#153374=CARTESIAN_POINT ( 'NONE',  ( 20.94999999999999929, 6.550000000011156231, -45.65000000000000568 ) ) ;
#153394=VECTOR ( 'NONE', #147176, 1000.000000000000000 ) ;
#153399=CYLINDRICAL_SURFACE ( 'NONE', #202875, 0.09999999999999939493 ) ;
#153406=CIRCLE ( 'NONE', #57667, 0.1000000000000028644 ) ;
#153431=CARTESIAN_POINT ( 'NONE',  ( -21.05000000000000426, -0.02103547652895681672, -27.19554417805234792 ) ) ;
#153437=VECTOR ( 'NONE', #93069, 1000.000000000000000 ) ;
#153473=DIRECTION ( 'NONE',  ( 1.000000000000000000, 3.265361837132813093E-16, -0.000000000000000000 ) ) ;
#153479=EDGE_CURVE ( 'NONE', #67087, #190151, #19052, .T. ) ;
#153506=VERTEX_POINT ( 'NONE', #79569 ) ;
#153513=CARTESIAN_POINT ( 'NONE',  ( 0.000000000000000000, 0.000000000000000000, 0.000000000000000000 ) ) ;
#153542=ADVANCED_FACE ( 'NONE', ( #198247 ), #234817, .F. ) ;
#153555=EDGE_CURVE ( 'NONE', #80932, #238808, #8720, .T. ) ;
#153598=CARTESIAN_POINT ( 'NONE',  ( 20.04142135623730070, 11.75000000001115907, -21.75000000000000355 ) ) ;
#153651=CIRCLE ( 'NONE', #228442, 0.6000000000000033085 ) ;
#153685=ORIENTED_EDGE ( 'NONE', *, *, #45784, .T. ) ;
#153703=DIRECTION ( 'NONE',  ( 0.000000000000000000, 1.000000000000000000, 0.000000000000000000 ) ) ;
#153724=ADVANCED_FACE ( 'NONE', ( #147264 ), #237854, .T. ) ;
#153731=ADVANCED_FACE ( 'NONE', ( #183828 ), #163003, .T. ) ;
#153734=ORIENTED_EDGE ( 'NONE', *, *, #63460, .F. ) ;
#153741=ORIENTED_EDGE ( 'NONE', *, *, #69694, .T. ) ;
#153799=AXIS2_PLACEMENT_3D ( 'NONE', #251090, #192426, #202375 ) ;
#153803=CARTESIAN_POINT ( 'NONE',  ( -20.94999999999999929, 11.65000000001115588, -40.51480577065400013 ) ) ;
#153815=VERTEX_POINT ( 'NONE', #132857 ) ;
#153819=ORIENTED_EDGE ( 'NONE', *, *, #74007, .T. ) ;
#153867=DIRECTION ( 'NONE',  ( 0.000000000000000000, 0.000000000000000000, 1.000000000000000000 ) ) ;
#153879=VERTEX_POINT ( 'NONE', #70337 ) ;
#153906=CARTESIAN_POINT ( 'NONE',  ( -20.64999999999999858, 4.350000000011156054, -45.85000000000000142 ) ) ;
#153914=DIRECTION ( 'NONE',  ( 0.000000000000000000, 0.000000000000000000, -1.000000000000000000 ) ) ;
#153922=EDGE_LOOP ( 'NONE', ( #194363, #64207, #119048, #212755 ) ) ;
#153923=AXIS2_PLACEMENT_3D ( 'NONE', #172218, #76905, #212591 ) ;
#153969=DIRECTION ( 'NONE',  ( 0.000000000000000000, 6.308085367182471812E-16, 1.000000000000000000 ) ) ;
#154000=EDGE_LOOP ( 'NONE', ( #105660, #111777, #115434, #84285, #184892 ) ) ;
#154036=CIRCLE ( 'NONE', #179136, 0.1000000000000028644 ) ;
#154073=VERTEX_POINT ( 'NONE', #102665 ) ;
#154081=ORIENTED_EDGE ( 'NONE', *, *, #184782, .T. ) ;
#154100=ORIENTED_EDGE ( 'NONE', *, *, #168038, .T. ) ;
#154102=AXIS2_PLACEMENT_3D ( 'NONE', #145524, #45149, #146798 ) ;
#154131=CARTESIAN_POINT ( 'NONE',  ( -21.05000000000000071, 0.09779029131994770863, -27.24218538952388613 ) ) ;
#154139=EDGE_CURVE ( 'NONE', #52403, #22426, #50752, .T. ) ;
#154181=DIRECTION ( 'NONE',  ( 1.000000000000000000, 0.000000000000000000, 0.000000000000000000 ) ) ;
#154188=DIRECTION ( 'NONE',  ( 0.000000000000000000, 0.000000000000000000, -1.000000000000000000 ) ) ;
#154198=EDGE_LOOP ( 'NONE', ( #246654, #153741, #192958, #128001, #94915, #51355, #78402, #239269, #88057, #140243, #236873, #43661 ) ) ;
#154216=CARTESIAN_POINT ( 'NONE',  ( -23.15000000000000213, -9.499999999988848032, -43.39396912265245021 ) ) ;
#154218=ORIENTED_EDGE ( 'NONE', *, *, #149206, .F. ) ;
#154232=ORIENTED_EDGE ( 'NONE', *, *, #237753, .T. ) ;
#154255=CARTESIAN_POINT ( 'NONE',  ( 18.59999999999999432, 1.162701749949165642, -41.60000000000000142 ) ) ;
#154273=FACE_OUTER_BOUND ( 'NONE', #72934, .T. ) ;
#154280=AXIS2_PLACEMENT_3D ( 'NONE', #152989, #91692, #211659 ) ;
#154291=CARTESIAN_POINT ( 'NONE',  ( -23.25000000000000000, -1.835859311432481045, -78.50443916879852679 ) ) ;
#154298=CIRCLE ( 'NONE', #137466, 0.5000000000000004441 ) ;
#154312=EDGE_CURVE ( 'NONE', #135166, #241512, #209003, .T. ) ;
#154324=CARTESIAN_POINT ( 'NONE',  ( 23.14999999999999858, 1.115600667400684642E-11, -67.00000000000000000 ) ) ;
#154363=ORIENTED_EDGE ( 'NONE', *, *, #65366, .F. ) ;
#154367=CARTESIAN_POINT ( 'NONE',  ( 21.05000000000000426, 6.344359042054589892, -33.48514436510635051 ) ) ;
#154398=ORIENTED_EDGE ( 'NONE', *, *, #78451, .F. ) ;
#154408=VECTOR ( 'NONE', #111761, 1000.000000000000000 ) ;
#154413=CARTESIAN_POINT ( 'NONE',  ( 21.00000000000000000, 9.750000000011153745, -54.65000000000000568 ) ) ;
#154416=EDGE_CURVE ( 'NONE', #71915, #183810, #38501, .T. ) ;
#154429=EDGE_CURVE ( 'NONE', #19166, #206017, #253307, .T. ) ;
#154453=AXIS2_PLACEMENT_3D ( 'NONE', #93921, #173520, #114776 ) ;
#154458=FACE_OUTER_BOUND ( 'NONE', #45634, .T. ) ;
#154477=EDGE_CURVE ( 'NONE', #129700, #216121, #132088, .T. ) ;
#154489=DIRECTION ( 'NONE',  ( -1.000000000000000000, 0.000000000000000000, 0.000000000000000000 ) ) ;
#154598=ADVANCED_FACE ( 'NONE', ( #97692 ), #28094, .T. ) ;
#154611=DIRECTION ( 'NONE',  ( 0.000000000000000000, 0.000000000000000000, -1.000000000000000000 ) ) ;
#154623=ORIENTED_EDGE ( 'NONE', *, *, #83826, .T. ) ;
#154631=AXIS2_PLACEMENT_3D ( 'NONE', #185015, #5060, #84578 ) ;
#154658=ORIENTED_EDGE ( 'NONE', *, *, #138648, .T. ) ;
#154666=CARTESIAN_POINT ( 'NONE',  ( 19.97071067695831559, 11.72071067696947644, -58.17625343280366934 ) ) ;
#154677=DIRECTION ( 'NONE',  ( 1.000000000000000000, -0.000000000000000000, -0.000000000000000000 ) ) ;
#154705=ORIENTED_EDGE ( 'NONE', *, *, #69694, .F. ) ;
#154714=CARTESIAN_POINT ( 'NONE',  ( -21.05000000000000071, -1.360870587180885716, -41.57299792709095954 ) ) ;
#154736=VERTEX_POINT ( 'NONE', #115362 ) ;
#154760=ORIENTED_EDGE ( 'NONE', *, *, #230159, .F. ) ;
#154761=ORIENTED_EDGE ( 'NONE', *, *, #7650, .F. ) ;
#154763=ORIENTED_EDGE ( 'NONE', *, *, #29750, .F. ) ;
#154777=ORIENTED_EDGE ( 'NONE', *, *, #188022, .T. ) ;
#154793=CARTESIAN_POINT ( 'NONE',  ( -23.15000000000000213, 4.250000000011156409, -45.85000000000000142 ) ) ;
#154804=CARTESIAN_POINT ( 'NONE',  ( -18.50000000000000000, -1.164121893230052995, -74.71484808557160306 ) ) ;
#154806=EDGE_LOOP ( 'NONE', ( #106245, #242557, #197974, #31365 ) ) ;
#154828=CIRCLE ( 'NONE', #175662, 0.4000000000000045186 ) ;
#154848=CIRCLE ( 'NONE', #50740, 0.09999999999999939493 ) ;
#154849=ORIENTED_EDGE ( 'NONE', *, *, #230053, .T. ) ;
#154940=EDGE_CURVE ( 'NONE', #189515, #102738, #63034, .T. ) ;
#154955=DIRECTION ( 'NONE',  ( 0.000000000000000000, 0.000000000000000000, -1.000000000000000000 ) ) ;
#154958=CARTESIAN_POINT ( 'NONE',  ( 18.49999999999998934, 10.25000000001115552, -58.15000000000000568 ) ) ;
#154987=CARTESIAN_POINT ( 'NONE',  ( -20.94999999999999929, 11.60000000001115517, -60.07179676972450011 ) ) ;
#155028=DIRECTION ( 'NONE',  ( -1.000000000000000000, -0.000000000000000000, -0.000000000000000000 ) ) ;
#155049=CARTESIAN_POINT ( 'NONE',  ( -23.25000000000000000, 1.115600667400684642E-11, -67.00000000000000000 ) ) ;
#155063=EDGE_CURVE ( 'NONE', #184107, #2240, #250307, .T. ) ;
#155070=DIRECTION ( 'NONE',  ( 0.000000000000000000, -0.1350103645451876666, -0.9908441862701600211 ) ) ;
#155086=EDGE_CURVE ( 'NONE', #104231, #119881, #171237, .T. ) ;
#155102=ADVANCED_FACE ( 'NONE', ( #72102 ), #196316, .F. ) ;
#155128=DIRECTION ( 'NONE',  ( 0.000000000000000000, 0.000000000000000000, -1.000000000000000000 ) ) ;
#155160=AXIS2_PLACEMENT_3D ( 'NONE', #1750, #239103, #42192 ) ;
#155167=DIRECTION ( 'NONE',  ( -1.000000000000000000, 0.000000000000000000, 0.000000000000000000 ) ) ;
#155189=CARTESIAN_POINT ( 'NONE',  ( 20.95017935633852346, 10.47548927963648069, -41.07743979739048967 ) ) ;
#155201=FACE_OUTER_BOUND ( 'NONE', #156413, .T. ) ;
#155205=ORIENTED_EDGE ( 'NONE', *, *, #160082, .F. ) ;
#155255=ORIENTED_EDGE ( 'NONE', *, *, #193982, .F. ) ;
#155273=FACE_OUTER_BOUND ( 'NONE', #75150, .T. ) ;
#155314=CARTESIAN_POINT ( 'NONE',  ( 18.47135592147657235, -9.471088613254476485, -73.68359493984345931 ) ) ;
#155362=CARTESIAN_POINT ( 'NONE',  ( -18.43634282235122157, -9.679787199916759732, -73.66065188545398712 ) ) ;
#155385=AXIS2_PLACEMENT_3D ( 'NONE', #195831, #250626, #133264 ) ;
#155402=VECTOR ( 'NONE', #187073, 1000.000000000000000 ) ;
#155476=FACE_BOUND ( 'NONE', #249321, .T. ) ;
#155502=ADVANCED_FACE ( 'NONE', ( #52202 ), #53505, .F. ) ;
#155504=AXIS2_PLACEMENT_3D ( 'NONE', #234158, #231612, #195065 ) ;
#155552=LINE ( 'NONE', #176387, #190927 ) ;
#155575=CARTESIAN_POINT ( 'NONE',  ( 20.94999999999999929, 1.115600667400684642E-11, -67.00000000000000000 ) ) ;
#155580=ADVANCED_FACE ( 'NONE', ( #191767 ), #195608, .F. ) ;
#155588=CIRCLE ( 'NONE', #30664, 0.1000000000000028644 ) ;
#155617=AXIS2_PLACEMENT_3D ( 'NONE', #60229, #244000, #241454 ) ;
#155641=CARTESIAN_POINT ( 'NONE',  ( 21.05000000000000071, 6.257814610487288043, -33.40220970869120976 ) ) ;
#155671=EDGE_LOOP ( 'NONE', ( #250056, #64342, #171219, #169717 ) ) ;
#155717=AXIS2_PLACEMENT_3D ( 'NONE', #196944, #75737, #93989 ) ;
#155734=CIRCLE ( 'NONE', #105601, 0.1000000000000028644 ) ;
#155872=AXIS2_PLACEMENT_3D ( 'NONE', #196916, #200773, #139502 ) ;
#155893=ORIENTED_EDGE ( 'NONE', *, *, #68626, .F. ) ;
#155906=DIRECTION ( 'NONE',  ( 0.000000000000000000, 0.000000000000000000, -1.000000000000000000 ) ) ;
#155912=ORIENTED_EDGE ( 'NONE', *, *, #48179, .T. ) ;
#155918=DIRECTION ( 'NONE',  ( 0.000000000000000000, -2.428612866367527723E-14, -1.000000000000000000 ) ) ;
#155948=CARTESIAN_POINT ( 'NONE',  ( 19.97071067811865674, 11.72071067812981937, -58.15000000000000568 ) ) ;
#155976=ORIENTED_EDGE ( 'NONE', *, *, #90985, .F. ) ;
#155995=CARTESIAN_POINT ( 'NONE',  ( -21.44999999999999929, 7.250000000011155521, -45.85000000000000142 ) ) ;
#156009=CARTESIAN_POINT ( 'NONE',  ( 23.14999999999999858, 1.115600667400684642E-11, -67.00000000000000000 ) ) ;
#156015=CIRCLE ( 'NONE', #114292, 0.09999999999999939493 ) ;
#156021=EDGE_CURVE ( 'NONE', #150811, #147068, #96879, .T. ) ;
#156061=AXIS2_PLACEMENT_3D ( 'NONE', #220720, #42107, #182895 ) ;
#156106=DIRECTION ( 'NONE',  ( -1.000000000000000000, 0.000000000000000000, 0.000000000000000000 ) ) ;
#156107=SURFACE_STYLE_FILL_AREA ( #16583 ) ;
#156246=CARTESIAN_POINT ( 'NONE',  ( -18.47653818581420282, -9.465280387751807467, -40.62596081613983046 ) ) ;
#156252=EDGE_LOOP ( 'NONE', ( #220579, #172716, #115015, #35052 ) ) ;
#156263=AXIS2_PLACEMENT_3D ( 'NONE', #120712, #42429, #157272 ) ;
#156306=CARTESIAN_POINT ( 'NONE',  ( -20.15000000000000568, 9.291421356248463326, -54.65000000000000568 ) ) ;
#156312=AXIS2_PLACEMENT_3D ( 'NONE', #69497, #149032, #134561 ) ;
#156407=VERTEX_POINT ( 'NONE', #247890 ) ;
#156409=DIRECTION ( 'NONE',  ( 0.000000000000000000, 0.000000000000000000, 1.000000000000000000 ) ) ;
#156413=EDGE_LOOP ( 'NONE', ( #42835, #193510, #168510, #78761, #30973, #149125, #136455 ) ) ;
#156432=CARTESIAN_POINT ( 'NONE',  ( 23.24999999999999645, 1.115600667400684642E-11, -33.50000000000000000 ) ) ;
#156443=ORIENTED_EDGE ( 'NONE', *, *, #74980, .F. ) ;
#156467=CARTESIAN_POINT ( 'NONE',  ( -18.59999999999999787, -1.835859311432481045, -78.50443916879852679 ) ) ;
#156472=DIRECTION ( 'NONE',  ( 0.000000000000000000, 4.336808689941893885E-15, 1.000000000000000000 ) ) ;
#156485=CARTESIAN_POINT ( 'NONE',  ( 20.94999999999999574, 1.835341550235569663, -45.05515129256298223 ) ) ;
#156488=FACE_OUTER_BOUND ( 'NONE', #92518, .T. ) ;
#156520=FACE_OUTER_BOUND ( 'NONE', #87323, .T. ) ;
#156570=DIRECTION ( 'NONE',  ( 0.000000000000000000, 0.000000000000000000, -1.000000000000000000 ) ) ;
#156574=CARTESIAN_POINT ( 'NONE',  ( -21.04999999999999716, -9.599999999988844124, -40.53206939669966857 ) ) ;
#156592=CIRCLE ( 'NONE', #131598, 0.1000000000000028644 ) ;
#156604=CARTESIAN_POINT ( 'NONE',  ( 18.49362639424889210, -9.442604367877116545, -73.76444093351176434 ) ) ;
#156615=DIRECTION ( 'NONE',  ( -1.000000000000000000, 0.000000000000000000, 0.000000000000000000 ) ) ;
#156619=CARTESIAN_POINT ( 'NONE',  ( -20.94999999999999929, -11.74999999998884448, -63.89999999999999858 ) ) ;
#156670=CARTESIAN_POINT ( 'NONE',  ( 20.85000000000000142, -11.64999999998883595, -67.00000000000000000 ) ) ;
#156688=ORIENTED_EDGE ( 'NONE', *, *, #34729, .T. ) ;
#156689=EDGE_LOOP ( 'NONE', ( #173010, #42041, #82302, #163382 ) ) ;
#156703=CIRCLE ( 'NONE', #10942, 0.09999999999999939493 ) ;
#156724=EDGE_CURVE ( 'NONE', #247553, #80054, #255919, .T. ) ;
#156760=CARTESIAN_POINT ( 'NONE',  ( 20.94999999999999929, 1.115625160336667635E-11, -65.00000000000000000 ) ) ;
#156783=CARTESIAN_POINT ( 'NONE',  ( 18.39999999999999858, -9.499999999988842703, -40.53206939669966857 ) ) ;
#156787=DIRECTION ( 'NONE',  ( 1.000000000000000000, 0.000000000000000000, 0.000000000000000000 ) ) ;
#156826=DIRECTION ( 'NONE',  ( -1.000000000000000000, 0.000000000000000000, 0.000000000000000000 ) ) ;
#156832=CARTESIAN_POINT ( 'NONE',  ( 23.14999999999999503, 11.65000000001116298, -45.75000000000000711 ) ) ;
#156833=CARTESIAN_POINT ( 'NONE',  ( -20.64999999999999858, 1.115600667400684642E-11, -67.00000000000000000 ) ) ;
#156834=EDGE_LOOP ( 'NONE', ( #162332, #256391, #127636, #241335 ) ) ;
#156841=ORIENTED_EDGE ( 'NONE', *, *, #64497, .F. ) ;
#156844=EDGE_LOOP ( 'NONE', ( #242620, #71992, #24975, #252516 ) ) ;
#156897=DIRECTION ( 'NONE',  ( 0.000000000000000000, 0.4999999999999956701, -0.8660254037844411501 ) ) ;
#156900=ADVANCED_FACE ( 'NONE', ( #24720, #164213 ), #243736, .F. ) ;
#156947=DIRECTION ( 'NONE',  ( 1.000000000000000000, 0.000000000000000000, 0.000000000000000000 ) ) ;
#156961=VERTEX_POINT ( 'NONE', #212332 ) ;
#156967=ORIENTED_EDGE ( 'NONE', *, *, #5027, .F. ) ;
#156984=ORIENTED_EDGE ( 'NONE', *, *, #245641, .F. ) ;
#157000=EDGE_CURVE ( 'NONE', #203988, #73682, #110639, .T. ) ;
#157010=DIRECTION ( 'NONE',  ( 0.000000000000000000, 0.000000000000000000, -1.000000000000000000 ) ) ;
#157020=EDGE_LOOP ( 'NONE', ( #115656, #83039, #21783, #91711, #215006 ) ) ;
#157059=DIRECTION ( 'NONE',  ( 0.000000000000000000, 0.000000000000000000, -1.000000000000000000 ) ) ;
#157076=CARTESIAN_POINT ( 'NONE',  ( 21.05000000000000071, -0.09999999998884338825, -21.85042919245520210 ) ) ;
#157079=EDGE_LOOP ( 'NONE', ( #227676, #163619, #182094, #147804 ) ) ;
#157111=AXIS2_PLACEMENT_3D ( 'NONE', #230313, #186065, #209472 ) ;
#157158=VECTOR ( 'NONE', #182685, 1000.000000000000000 ) ;
#157175=DIRECTION ( 'NONE',  ( 0.000000000000000000, 0.000000000000000000, 1.000000000000000000 ) ) ;
#157207=CARTESIAN_POINT ( 'NONE',  ( 21.09546886439553504, 8.878553113026073973, -45.73709385055541077 ) ) ;
#157229=AXIS2_PLACEMENT_3D ( 'NONE', #2883, #137267, #236374 ) ;
#157246=DIRECTION ( 'NONE',  ( 0.000000000000000000, 0.000000000000000000, 1.000000000000000000 ) ) ;
#157271=DIRECTION ( 'NONE',  ( 0.000000000000000000, 0.000000000000000000, -1.000000000000000000 ) ) ;
#157272=DIRECTION ( 'NONE',  ( 0.000000000000000000, -0.1455152366551522025, -0.9893560106964505163 ) ) ;
#157283=VECTOR ( 'NONE', #219769, 1000.000000000000000 ) ;
#157319=DIRECTION ( 'NONE',  ( 1.000000000000000000, 0.000000000000000000, 0.000000000000000000 ) ) ;
#157390=AXIS2_PLACEMENT_3D ( 'NONE', #198960, #56851, #16501 ) ;
#157396=SURFACE_SIDE_STYLE ('',( #156107 ) ) ;
#157413=ORIENTED_EDGE ( 'NONE', *, *, #168683, .T. ) ;
#157415=EDGE_LOOP ( 'NONE', ( #24820, #127084 ) ) ;
#157443=TOROIDAL_SURFACE ( 'NONE', #78281, 7.800000000000000711, 0.1000000000000000056 ) ;
#157445=CARTESIAN_POINT ( 'NONE',  ( -21.05000000000000071, 11.65000000001115588, -33.60000000000000142 ) ) ;
#157472=DIRECTION ( 'NONE',  ( -1.000000000000000000, 0.000000000000000000, 0.000000000000000000 ) ) ;
#157492=DIRECTION ( 'NONE',  ( 1.000000000000000000, -0.000000000000000000, -0.000000000000000000 ) ) ;
#157503=DIRECTION ( 'NONE',  ( -0.9880948137434723000, 0.1538461538461483591, -0.000000000000000000 ) ) ;
#157527=ORIENTED_EDGE ( 'NONE', *, *, #174964, .T. ) ;
#157574=FACE_OUTER_BOUND ( 'NONE', #235633, .T. ) ;
#157576=CARTESIAN_POINT ( 'NONE',  ( -22.47071067811865319, 7.720074744509219933, -33.40090754529740025 ) ) ;
#157605=CARTESIAN_POINT ( 'NONE',  ( 20.94999999999999929, 11.65000000001115943, -60.15839931010294350 ) ) ;
#157640=VECTOR ( 'NONE', #104782, 1000.000000000000000 ) ;
#157665=EDGE_CURVE ( 'NONE', #76854, #221539, #139413, .T. ) ;
#157676=ORIENTED_EDGE ( 'NONE', *, *, #255374, .F. ) ;
#157697=AXIS2_PLACEMENT_3D ( 'NONE', #190259, #50703, #11626 ) ;
#157712=TOROIDAL_SURFACE ( 'NONE', #203455, 0.9750000000000019762, 0.1000000000000000056 ) ;
#157755=DIRECTION ( 'NONE',  ( -0.000000000000000000, -0.000000000000000000, 1.000000000000000000 ) ) ;
#157763=CARTESIAN_POINT ( 'NONE',  ( 18.59999999999999432, -1.135018845899022466, -74.71697688343232358 ) ) ;
#157795=DIRECTION ( 'NONE',  ( -0.000000000000000000, -0.000000000000000000, 1.000000000000000000 ) ) ;
#157804=ORIENTED_EDGE ( 'NONE', *, *, #220915, .T. ) ;
#157830=DIRECTION ( 'NONE',  ( 1.000000000000000000, 0.000000000000000000, -0.000000000000000000 ) ) ;
#157865=CARTESIAN_POINT ( 'NONE',  ( -22.00411653889210939, 0.09903810579712249429, -26.24655713235958032 ) ) ;
#157893=CARTESIAN_POINT ( 'NONE',  ( -23.25000000000000000, 11.75000000001115552, -33.50000000000000000 ) ) ;
#157899=CARTESIAN_POINT ( 'NONE',  ( -21.08621493067320429, 0.05619483948720500194, -27.15070570882805967 ) ) ;
#157904=ORIENTED_EDGE ( 'NONE', *, *, #69746, .F. ) ;
#157911=AXIS2_PLACEMENT_3D ( 'NONE', #125069, #25971, #222864 ) ;
#157983=EDGE_CURVE ( 'NONE', #244695, #82729, #107000, .T. ) ;
#158064=DIRECTION ( 'NONE',  ( -1.000000000000000000, 0.000000000000000000, 0.000000000000000000 ) ) ;
#158082=CARTESIAN_POINT ( 'NONE',  ( -20.64999999999999858, -8.999999999988844479, -57.10603087734755690 ) ) ;
#158107=CARTESIAN_POINT ( 'NONE',  ( -20.64999999999999858, 7.150000000011155876, -54.75000000000000000 ) ) ;
#158133=ADVANCED_FACE ( 'NONE', ( #93868 ), #54738, .T. ) ;
#158137=DIRECTION ( 'NONE',  ( -1.000000000000000000, 0.000000000000000000, 0.000000000000000000 ) ) ;
#158138=DIRECTION ( 'NONE',  ( 0.000000000000000000, -0.4930308989875313852, -0.8700118002898274971 ) ) ;
#158150=AXIS2_PLACEMENT_3D ( 'NONE', #158325, #39658, #134844 ) ;
#158200=AXIS2_PLACEMENT_3D ( 'NONE', #31078, #71473, #176998 ) ;
#158208=CARTESIAN_POINT ( 'NONE',  ( -22.45305610364634674, -0.1008583690875579225, -21.75043287651061164 ) ) ;
#158220=VECTOR ( 'NONE', #124787, 1000.000000000000000 ) ;
#158241=EDGE_CURVE ( 'NONE', #241724, #100962, #173171, .T. ) ;
#158285=CARTESIAN_POINT ( 'NONE',  ( -20.00857864376270001, 9.350000000011156942, -45.85000000000000142 ) ) ;
#158287=ORIENTED_EDGE ( 'NONE', *, *, #67965, .T. ) ;
#158293=ORIENTED_EDGE ( 'NONE', *, *, #83314, .F. ) ;
#158314=AXIS2_PLACEMENT_3D ( 'NONE', #143846, #223380, #245543 ) ;
#158325=CARTESIAN_POINT ( 'NONE',  ( -23.15000000000000213, 4.350000000011156054, -45.85000000000000142 ) ) ;
#158341=ORIENTED_EDGE ( 'NONE', *, *, #7129, .T. ) ;
#158352=CIRCLE ( 'NONE', #200016, 0.1000000000000028644 ) ;
#158374=ADVANCED_FACE ( 'NONE', ( #181344 ), #227276, .F. ) ;
#158383=ORIENTED_EDGE ( 'NONE', *, *, #215893, .F. ) ;
#158399=DIRECTION ( 'NONE',  ( 0.000000000000000000, 1.000000000000000000, 0.000000000000000000 ) ) ;
#158404=EDGE_LOOP ( 'NONE', ( #8943, #87238, #215312, #21375 ) ) ;
#158406=DIRECTION ( 'NONE',  ( 0.000000000000000000, 0.000000000000000000, -1.000000000000000000 ) ) ;
#158454=VERTEX_POINT ( 'NONE', #14261 ) ;
#158455=CARTESIAN_POINT ( 'NONE',  ( -21.07928932188134397, 0.09889514566555071551, -27.17148334360670248 ) ) ;
#158473=DIRECTION ( 'NONE',  ( 0.000000000000000000, 0.000000000000000000, 1.000000000000000000 ) ) ;
#158485=EDGE_LOOP ( 'NONE', ( #34841, #257825, #253277, #172073 ) ) ;
#158491=CARTESIAN_POINT ( 'NONE',  ( 20.95512820512820440, 8.876151316299269567, -45.65000000000000568 ) ) ;
#158497=DIRECTION ( 'NONE',  ( 2.952720810173289112E-16, -1.000000000000000000, 0.000000000000000000 ) ) ;
#158525=EDGE_CURVE ( 'NONE', #179511, #108455, #98066, .T. ) ;
#158530=ORIENTED_EDGE ( 'NONE', *, *, #201182, .T. ) ;
#158536=CARTESIAN_POINT ( 'NONE',  ( -21.59142135623730852, 7.850000000011158718, -45.85000000000000142 ) ) ;
#158541=DIRECTION ( 'NONE',  ( -1.000000000000000000, 0.000000000000000000, 0.000000000000000000 ) ) ;
#158543=ORIENTED_EDGE ( 'NONE', *, *, #141183, .F. ) ;
#158545=ORIENTED_EDGE ( 'NONE', *, *, #173324, .F. ) ;
#158575=EDGE_LOOP ( 'NONE', ( #62805, #69613, #182915, #77308 ) ) ;
#158599=CARTESIAN_POINT ( 'NONE',  ( 20.95512820512820440, 8.876151316299271343, -42.05862899514094977 ) ) ;
#158618=CIRCLE ( 'NONE', #79476, 0.09999999999999939493 ) ;
#158644=CARTESIAN_POINT ( 'NONE',  ( 23.24999999999999645, 1.115600667400684642E-11, -67.00000000000000000 ) ) ;
#158687=FACE_OUTER_BOUND ( 'NONE', #95089, .T. ) ;
#158690=CARTESIAN_POINT ( 'NONE',  ( -20.85000000000000142, -11.74999999998884448, -64.10000000000000853 ) ) ;
#158703=ORIENTED_EDGE ( 'NONE', *, *, #182951, .T. ) ;
#158774=CIRCLE ( 'NONE', #208651, 0.09999999999999939493 ) ;
#158775=AXIS2_PLACEMENT_3D ( 'NONE', #105535, #222941, #164279 ) ;
#158783=CARTESIAN_POINT ( 'NONE',  ( 20.77526135991777068, 8.932009016633434939, -41.96856854272417081 ) ) ;
#158787=EDGE_CURVE ( 'NONE', #197707, #31916, #102522, .T. ) ;
#158790=DIRECTION ( 'NONE',  ( 1.000000000000000000, 0.000000000000000000, -0.000000000000000000 ) ) ;
#158800=EDGE_CURVE ( 'NONE', #48124, #229112, #156592, .T. ) ;
#158826=EDGE_CURVE ( 'NONE', #36165, #47498, #166617, .T. ) ;
#158862=EDGE_CURVE ( 'NONE', #68820, #99123, #194166, .T. ) ;
#158866=EDGE_CURVE ( 'NONE', #88637, #201039, #2596, .T. ) ;
#158904=ORIENTED_EDGE ( 'NONE', *, *, #84988, .T. ) ;
#158907=DIRECTION ( 'NONE',  ( 0.000000000000000000, 0.000000000000000000, 1.000000000000000000 ) ) ;
#158911=DIRECTION ( 'NONE',  ( 1.000000000000000000, -0.000000000000000000, -0.000000000000000000 ) ) ;
#158922=B_SPLINE_CURVE_WITH_KNOTS ( 'NONE', 3,
 ( #187129, #245796, #67156, #204083, #123282, #144104, #45024, #247058, #68449, #227502, #241928, #124572, #5877, #128417, #65867, #184519 ),
 .UNSPECIFIED., .F., .F.,
 ( 4, 3, 3, 3, 3, 4 ),
 ( 0.000000000000000000, 2.209075297430740031E-05, 5.594258369009624354E-05, 8.979524372342012487E-05, 0.0001236472815274586301, 0.0001574990747609554737 ),
 .UNSPECIFIED. ) ;
#158941=CARTESIAN_POINT ( 'NONE',  ( -21.14999999999999858, 11.65000000001115588, -33.60000000000000142 ) ) ;
#158960=ORIENTED_EDGE ( 'NONE', *, *, #227183, .F. ) ;
#158968=EDGE_LOOP ( 'NONE', ( #117565, #240875, #140627, #118248 ) ) ;
#158991=EDGE_CURVE ( 'NONE', #242144, #14565, #256555, .T. ) ;
#158992=CARTESIAN_POINT ( 'NONE',  ( 22.37643362114956247, 7.625789993969535274, -33.40091862631862085 ) ) ;
#159013=CARTESIAN_POINT ( 'NONE',  ( -18.58671080940900566, -9.406932858815460818, -40.62415446490468440 ) ) ;
#159020=DIRECTION ( 'NONE',  ( 1.000000000000000000, 0.000000000000000000, 0.000000000000000000 ) ) ;
#159024=CARTESIAN_POINT ( 'NONE',  ( -21.45000000000000284, 7.708578643773852157, -54.75000000000000000 ) ) ;
#159026=LINE ( 'NONE', #181142, #229138 ) ;
#159050=DIRECTION ( 'NONE',  ( -1.000000000000000000, -0.000000000000000000, -0.000000000000000000 ) ) ;
#159060=VECTOR ( 'NONE', #28571, 1000.000000000000000 ) ;
#159097=EDGE_LOOP ( 'NONE', ( #25155, #41569, #248605, #192221 ) ) ;
#159098=CARTESIAN_POINT ( 'NONE',  ( -18.58735405345342073, -9.566478620325440829, -73.82271464626597890 ) ) ;
#159143=AXIS2_PLACEMENT_3D ( 'NONE', #182216, #205605, #105185 ) ;
#159164=FACE_OUTER_BOUND ( 'NONE', #251209, .T. ) ;
#159191=ORIENTED_EDGE ( 'NONE', *, *, #93551, .F. ) ;
#159196=ORIENTED_EDGE ( 'NONE', *, *, #203450, .F. ) ;
#159222=CYLINDRICAL_SURFACE ( 'NONE', #70641, 0.1000000000000000056 ) ;
#159244=EDGE_LOOP ( 'NONE', ( #23408, #8543, #166324, #58732 ) ) ;
#159251=VERTEX_POINT ( 'NONE', #177853 ) ;
#159256=EDGE_CURVE ( 'NONE', #65925, #14799, #133568, .T. ) ;
#159273=DIRECTION ( 'NONE',  ( -1.000000000000000000, 0.000000000000000000, 0.000000000000000000 ) ) ;
#159315=DIRECTION ( 'NONE',  ( -0.7071067811865388020, 0.7071067811865561215, 0.000000000000000000 ) ) ;
#159321=CARTESIAN_POINT ( 'NONE',  ( 21.07946286933444924, 0.07668384326756222391, -27.17096268099230372 ) ) ;
#159374=CARTESIAN_POINT ( 'NONE',  ( -20.94999999999999929, 7.021664781911246322, -70.83356540189728889 ) ) ;
#159379=ORIENTED_EDGE ( 'NONE', *, *, #114715, .T. ) ;
#159421=ORIENTED_EDGE ( 'NONE', *, *, #83808, .F. ) ;
#159433=AXIS2_PLACEMENT_3D ( 'NONE', #66004, #46430, #110257 ) ;
#159452=ORIENTED_EDGE ( 'NONE', *, *, #18426, .F. ) ;
#159453=CARTESIAN_POINT ( 'NONE',  ( -22.39999999999999858, -0.1008583690875579364, -21.75043287651061164 ) ) ;
#159459=CARTESIAN_POINT ( 'NONE',  ( -23.15000000000000213, 1.115600667400684642E-11, -33.50000000000000000 ) ) ;
#159496=EDGE_CURVE ( 'NONE', #191837, #201531, #231946, .T. ) ;
#159572=DIRECTION ( 'NONE',  ( 1.000000000000000000, -0.000000000000000000, -0.000000000000000000 ) ) ;
#159608=CARTESIAN_POINT ( 'NONE',  ( -23.25000000000000000, -11.64999999998884483, -36.60000000000000853 ) ) ;
#159620=EDGE_LOOP ( 'NONE', ( #65508, #152984, #151604, #219124, #234260, #158530, #229730, #14793 ) ) ;
#159640=ORIENTED_EDGE ( 'NONE', *, *, #44792, .F. ) ;
#159643=SURFACE_STYLE_USAGE ( .BOTH. , #220881 ) ;
#159646=TOROIDAL_SURFACE ( 'NONE', #109559, 11.65000000000000036, 0.1000000000000000056 ) ;
#159713=EDGE_LOOP ( 'NONE', ( #118064, #229160, #72365, #79041, #87032 ) ) ;
#159719=CARTESIAN_POINT ( 'NONE',  ( -21.11833042828140350, 0.007100509070575833880, -27.05435530614471773 ) ) ;
#159721=CARTESIAN_POINT ( 'NONE',  ( -22.50000000000000000, 0.1000000000111554016, -25.70922040162659883 ) ) ;
#159729=FACE_OUTER_BOUND ( 'NONE', #44294, .T. ) ;
#159730=EDGE_CURVE ( 'NONE', #67483, #210104, #162867, .T. ) ;
#159744=VECTOR ( 'NONE', #205265, 999.9999999999998863 ) ;
#159770=TOROIDAL_SURFACE ( 'NONE', #93115, 0.2000000000000000111, 0.1000000000000000056 ) ;
#159777=ADVANCED_FACE ( 'NONE', ( #126208 ), #214637, .F. ) ;
#159846=CARTESIAN_POINT ( 'NONE',  ( -20.89192007715127986, 10.32898536001801304, -72.58266832227644727 ) ) ;
#159848=CARTESIAN_POINT ( 'NONE',  ( -23.15000000000000213, 2.500000000011154633, -53.77537807723791019 ) ) ;
#159892=ORIENTED_EDGE ( 'NONE', *, *, #61408, .T. ) ;
#159922=CARTESIAN_POINT ( 'NONE',  ( 21.05315837390880418, 11.74999999924401273, -60.15835600047963538 ) ) ;
#159930=CARTESIAN_POINT ( 'NONE',  ( 21.05000000000000071, -9.399999999988844834, -57.10603087734755690 ) ) ;
#159940=VERTEX_POINT ( 'NONE', #80329 ) ;
#159946=EDGE_CURVE ( 'NONE', #38057, #127487, #119504, .T. ) ;
#159998=VERTEX_POINT ( 'NONE', #41271 ) ;
#160020=CIRCLE ( 'NONE', #168428, 0.09999999999999824307 ) ;
#160034=ORIENTED_EDGE ( 'NONE', *, *, #57080, .T. ) ;
#160060=ORIENTED_EDGE ( 'NONE', *, *, #79067, .F. ) ;
#160068=ORIENTED_EDGE ( 'NONE', *, *, #88974, .T. ) ;
#160082=EDGE_CURVE ( 'NONE', #36165, #209893, #57483, .T. ) ;
#160083=CARTESIAN_POINT ( 'NONE',  ( 21.05000000000000071, 1.115600667400684642E-11, -69.00000000000000000 ) ) ;
#160113=ORIENTED_EDGE ( 'NONE', *, *, #147360, .T. ) ;
#160150=ADVANCED_FACE ( 'NONE', ( #206727 ), #47628, .F. ) ;
#160153=VECTOR ( 'NONE', #247588, 1000.000000000000000 ) ;
#160168=CARTESIAN_POINT ( 'NONE',  ( 20.85000000000000142, -1.164121893230052995, -74.91484808557160591 ) ) ;
#160194=AXIS2_PLACEMENT_3D ( 'NONE', #95317, #212709, #53625 ) ;
#160200=DIRECTION ( 'NONE',  ( 1.000000000000000000, 0.000000000000000000, 0.000000000000000000 ) ) ;
#160212=ORIENTED_EDGE ( 'NONE', *, *, #91479, .T. ) ;
#160224=CARTESIAN_POINT ( 'NONE',  ( -18.59999999999999787, 5.950000000011100632, -43.80570230503486329 ) ) ;
#160241=EDGE_CURVE ( 'NONE', #72361, #15545, #128479, .T. ) ;
#160268=ORIENTED_EDGE ( 'NONE', *, *, #154416, .F. ) ;
#160272=CARTESIAN_POINT ( 'NONE',  ( 22.47071067811865319, 7.720074744509199505, -33.40090754529740025 ) ) ;
#160276=DIRECTION ( 'NONE',  ( 1.000000000000000000, 2.952720810173289112E-16, -0.000000000000000000 ) ) ;
#160282=DIRECTION ( 'NONE',  ( 0.000000000000000000, 8.881784197000696176E-16, -1.000000000000000000 ) ) ;
#160317=EDGE_LOOP ( 'NONE', ( #182249, #196768, #95720, #217123 ) ) ;
#160319=CARTESIAN_POINT ( 'NONE',  ( -22.39999999999999858, 0.1000000000111554016, -25.70922040162659883 ) ) ;
#160334=CARTESIAN_POINT ( 'NONE',  ( -20.94999999999999929, 1.162701749949165642, -41.60000000000000142 ) ) ;
#160371=ORIENTED_EDGE ( 'NONE', *, *, #21973, .F. ) ;
#160376=EDGE_CURVE ( 'NONE', #168461, #30860, #190616, .T. ) ;
#160390=CIRCLE ( 'NONE', #177140, 0.1000000000000002554 ) ;
#160436=CYLINDRICAL_SURFACE ( 'NONE', #225830, 0.1000000000000006162 ) ;
#160477=FACE_OUTER_BOUND ( 'NONE', #182923, .T. ) ;
#160482=CARTESIAN_POINT ( 'NONE',  ( 21.07094088545303734, 6.320167221927647461, -33.40110629744778237 ) ) ;
#160523=DIRECTION ( 'NONE',  ( 0.000000000000000000, 0.000000000000000000, -1.000000000000000000 ) ) ;
#160594=CIRCLE ( 'NONE', #18897, 0.09999999999999939493 ) ;
#160614=CARTESIAN_POINT ( 'NONE',  ( 21.08489834409762409, 10.62232389474667293, -45.85000000000001563 ) ) ;
#160629=EDGE_CURVE ( 'NONE', #153879, #102509, #153406, .T. ) ;
#160679=CYLINDRICAL_SURFACE ( 'NONE', #252993, 0.1000000000000028644 ) ;
#160707=AXIS2_PLACEMENT_3D ( 'NONE', #252767, #37602, #257860 ) ;
#160720=EDGE_CURVE ( 'NONE', #172722, #190117, #20102, .T. ) ;
#160722=FACE_OUTER_BOUND ( 'NONE', #79706, .T. ) ;
#160723=VERTEX_POINT ( 'NONE', #236261 ) ;
#160728=LINE ( 'NONE', #141139, #244665 ) ;
#160737=ADVANCED_FACE ( 'NONE', ( #73370 ), #133318, .T. ) ;
#160739=DIRECTION ( 'NONE',  ( 1.000000000000000000, 0.000000000000000000, 0.000000000000000000 ) ) ;
#160741=CYLINDRICAL_SURFACE ( 'NONE', #189008, 0.09999999999999939493 ) ;
#160753=AXIS2_PLACEMENT_3D ( 'NONE', #44335, #142135, #123875 ) ;
#160810=ORIENTED_EDGE ( 'NONE', *, *, #6174, .T. ) ;
#160811=CARTESIAN_POINT ( 'NONE',  ( -21.14999999999999858, 11.75000000001115552, -33.60000000000000142 ) ) ;
#160830=FACE_OUTER_BOUND ( 'NONE', #62966, .T. ) ;
#160902=CIRCLE ( 'NONE', #77462, 0.5000000000000004441 ) ;
#160913=VECTOR ( 'NONE', #187625, 1000.000000000000000 ) ;
#160915=AXIS2_PLACEMENT_3D ( 'NONE', #148930, #138096, #239789 ) ;
#160966=LINE ( 'NONE', #132102, #239313 ) ;
#161009=CIRCLE ( 'NONE', #119908, 0.2000000000000057288 ) ;
#161016=CARTESIAN_POINT ( 'NONE',  ( -20.64999999999999858, 1.115600667400684642E-11, -67.00000000000000000 ) ) ;
#161026=CARTESIAN_POINT ( 'NONE',  ( 21.05000000000000071, 5.400000000011154988, -45.90526601891310321 ) ) ;
#161027=ORIENTED_EDGE ( 'NONE', *, *, #53792, .T. ) ;
#161055=VERTEX_POINT ( 'NONE', #14376 ) ;
#161061=DIRECTION ( 'NONE',  ( 0.000000000000000000, 1.897661533703519897E-16, -1.000000000000000000 ) ) ;
#161074=CARTESIAN_POINT ( 'NONE',  ( -23.15000000000000213, 1.115600667400684642E-11, -67.00000000000000000 ) ) ;
#161122=CARTESIAN_POINT ( 'NONE',  ( -20.91682497891422798, 10.32263460347359363, -72.56059579686719019 ) ) ;
#161124=CARTESIAN_POINT ( 'NONE',  ( -1.739115166359751801E-14, 11.65000000001114699, -54.85000000000000142 ) ) ;
#161127=DIRECTION ( 'NONE',  ( 0.000000000000000000, 0.000000000000000000, 1.000000000000000000 ) ) ;
#161142=DIRECTION ( 'NONE',  ( 1.000000000000000000, 0.000000000000000000, -0.000000000000000000 ) ) ;
#161194=CARTESIAN_POINT ( 'NONE',  ( -23.15000000000000213, 11.65000000001115588, -54.85000000000000142 ) ) ;
#161205=DIRECTION ( 'NONE',  ( 0.000000000000000000, 0.000000000000000000, -1.000000000000000000 ) ) ;
#161214=ORIENTED_EDGE ( 'NONE', *, *, #37644, .T. ) ;
#161231=CARTESIAN_POINT ( 'NONE',  ( 23.14999999999999858, 5.000000000011153745, -54.59473398108690390 ) ) ;
#161235=EDGE_LOOP ( 'NONE', ( #116259, #102431, #142051, #220670, #93983, #83967, #150552, #123873, #189266, #131311, #242318, #224311 ) ) ;
#161253=ORIENTED_EDGE ( 'NONE', *, *, #38838, .F. ) ;
#161272=VERTEX_POINT ( 'NONE', #28174 ) ;
#161276=ORIENTED_EDGE ( 'NONE', *, *, #99233, .T. ) ;
#161288=DIRECTION ( 'NONE',  ( 0.000000000000000000, 0.000000000000000000, -1.000000000000000000 ) ) ;
#161289=AXIS2_PLACEMENT_3D ( 'NONE', #73070, #108310, #152600 ) ;
#161305=CYLINDRICAL_SURFACE ( 'NONE', #238746, 0.09999999999999939493 ) ;
#161311=CIRCLE ( 'NONE', #115496, 0.09999999999999939493 ) ;
#161314=VERTEX_POINT ( 'NONE', #208082 ) ;
#161321=CYLINDRICAL_SURFACE ( 'NONE', #233064, 11.74999999999999645 ) ;
#161338=EDGE_CURVE ( 'NONE', #178845, #35121, #162126, .T. ) ;
#161363=CARTESIAN_POINT ( 'NONE',  ( -18.51991288638512501, -9.392436789662260921, -40.64326640395893264 ) ) ;
#161370=ORIENTED_EDGE ( 'NONE', *, *, #195750, .T. ) ;
#161373=DIRECTION ( 'NONE',  ( 0.000000000000000000, 0.000000000000000000, -1.000000000000000000 ) ) ;
#161401=ADVANCED_FACE ( 'NONE', ( #134909 ), #214468, .T. ) ;
#161420=DIRECTION ( 'NONE',  ( 1.000000000000000000, 0.000000000000000000, -0.000000000000000000 ) ) ;
#161438=DIRECTION ( 'NONE',  ( 1.000000000000000000, 0.000000000000000000, 0.000000000000000000 ) ) ;
#161440=CARTESIAN_POINT ( 'NONE',  ( -20.94999999999999929, 1.115600667400684642E-11, -33.50000000000000000 ) ) ;
#161491=ORIENTED_EDGE ( 'NONE', *, *, #87554, .F. ) ;
#161507=CYLINDRICAL_SURFACE ( 'NONE', #140224, 0.1000000000000028644 ) ;
#161511=ORIENTED_EDGE ( 'NONE', *, *, #103927, .T. ) ;
#161525=FACE_OUTER_BOUND ( 'NONE', #113611, .T. ) ;
#161532=CARTESIAN_POINT ( 'NONE',  ( 18.59999999999999076, 10.20857864377385127, -54.85000000000000142 ) ) ;
#161596=ADVANCED_FACE ( 'NONE', ( #120540 ), #200056, .F. ) ;
#161597=CARTESIAN_POINT ( 'NONE',  ( 20.95325940946048249, 10.52339007070744437, -41.06446212924009131 ) ) ;
#161599=EDGE_CURVE ( 'NONE', #255894, #232658, #142037, .T. ) ;
#161645=CARTESIAN_POINT ( 'NONE',  ( 21.14999999999999858, 1.115600667400684642E-11, -33.50000000000000000 ) ) ;
#161666=VECTOR ( 'NONE', #190457, 1000.000000000000000 ) ;
#161686=CARTESIAN_POINT ( 'NONE',  ( 21.05000000000000071, 6.540656951712400691, -33.60000000000000142 ) ) ;
#161704=TOROIDAL_SURFACE ( 'NONE', #124276, 12.97499999999999787, 0.1000000000000000056 ) ;
#161720=CARTESIAN_POINT ( 'NONE',  ( 20.85000000000000142, -1.749999999988843813, -78.61895003862224485 ) ) ;
#161721=ORIENTED_EDGE ( 'NONE', *, *, #127846, .F. ) ;
#161733=CARTESIAN_POINT ( 'NONE',  ( 18.49999999999999289, 10.20857864377385127, -58.15000000000000568 ) ) ;
#161739=LINE ( 'NONE', #241265, #51811 ) ;
#161750=EDGE_LOOP ( 'NONE', ( #64392, #77079, #207963, #144702 ) ) ;
#161757=CARTESIAN_POINT ( 'NONE',  ( -18.50000000000000000, 11.65000000001115232, -45.65000000000000568 ) ) ;
#161808=LINE ( 'NONE', #255698, #19641 ) ;
#161838=CARTESIAN_POINT ( 'NONE',  ( 23.14999999999999503, 11.65000000001116298, -59.98519422934606382 ) ) ;
#161855=SPHERICAL_SURFACE ( 'NONE', #143256, 0.1000000000000000056 ) ;
#161862=CARTESIAN_POINT ( 'NONE',  ( 18.49999999999999645, 5.950000000011100632, -43.80570230503486329 ) ) ;
#161933=DIRECTION ( 'NONE',  ( 0.000000000000000000, 0.000000000000000000, -1.000000000000000000 ) ) ;
#161958=FACE_OUTER_BOUND ( 'NONE', #166186, .T. ) ;
#162000=ORIENTED_EDGE ( 'NONE', *, *, #110446, .T. ) ;
#162021=EDGE_CURVE ( 'NONE', #225961, #117247, #128407, .T. ) ;
#162027=AXIS2_PLACEMENT_3D ( 'NONE', #79924, #4265, #163365 ) ;
#162038=DIRECTION ( 'NONE',  ( 0.000000000000000000, 0.000000000000000000, 1.000000000000000000 ) ) ;
#162061=ORIENTED_EDGE ( 'NONE', *, *, #8192, .F. ) ;
#162103=ADVANCED_FACE ( 'NONE', ( #244671 ), #84269, .F. ) ;
#162119=AXIS2_PLACEMENT_3D ( 'NONE', #164716, #186861, #202552 ) ;
#162126=CIRCLE ( 'NONE', #245320, 0.09999999999999971412 ) ;
#162149=VERTEX_POINT ( 'NONE', #9924 ) ;
#162203=ORIENTED_EDGE ( 'NONE', *, *, #158787, .T. ) ;
#162223=CARTESIAN_POINT ( 'NONE',  ( -23.25000000000000000, 11.75000000001115552, -33.50000000000000000 ) ) ;
#162240=CARTESIAN_POINT ( 'NONE',  ( -22.45354308602486526, 2.198892876589933535E-07, -21.74956710954100814 ) ) ;
#162246=AXIS2_PLACEMENT_3D ( 'NONE', #64474, #203967, #185703 ) ;
#162268=CARTESIAN_POINT ( 'NONE',  ( -20.94999999999999929, 1.115600667400684642E-11, -67.00000000000000000 ) ) ;
#162272=DIRECTION ( 'NONE',  ( -0.000000000000000000, 1.000000000000000000, -0.000000000000000000 ) ) ;
#162284=LINE ( 'NONE', #24062, #171204 ) ;
#162290=ORIENTED_EDGE ( 'NONE', *, *, #165592, .T. ) ;
#162292=EDGE_LOOP ( 'NONE', ( #59285, #164126, #209172, #27914 ) ) ;
#162300=ORIENTED_EDGE ( 'NONE', *, *, #37578, .F. ) ;
#162319=ADVANCED_FACE ( 'NONE', ( #79829 ), #149454, .T. ) ;
#162323=ORIENTED_EDGE ( 'NONE', *, *, #229452, .T. ) ;
#162324=EDGE_CURVE ( 'NONE', #119487, #204355, #70363, .T. ) ;
#162332=ORIENTED_EDGE ( 'NONE', *, *, #228940, .T. ) ;
#162334=CARTESIAN_POINT ( 'NONE',  ( 18.59999999999999787, -1.851028230129704522, -45.15391326942249606 ) ) ;
#162388=EDGE_CURVE ( 'NONE', #132417, #27579, #149633, .T. ) ;
#162413=CARTESIAN_POINT ( 'NONE',  ( -20.87600722750343252, 10.33112638556969465, -72.59012289269746532 ) ) ;
#162420=DIRECTION ( 'NONE',  ( 0.7071067811865388020, -0.7071067811865561215, 0.000000000000000000 ) ) ;
#162431=ORIENTED_EDGE ( 'NONE', *, *, #66069, .T. ) ;
#162457=VERTEX_POINT ( 'NONE', #148830 ) ;
#162475=ORIENTED_EDGE ( 'NONE', *, *, #88227, .T. ) ;
#162482=CARTESIAN_POINT ( 'NONE',  ( -18.59117750673696889, 10.33248238083634796, -72.59484654391314962 ) ) ;
#162489=ADVANCED_FACE ( 'NONE', ( #173569 ), #74451, .T. ) ;
#162514=ORIENTED_EDGE ( 'NONE', *, *, #187468, .F. ) ;
#162534=CARTESIAN_POINT ( 'NONE',  ( 20.12500000000000000, 9.750000000011153745, -41.61177128211428311 ) ) ;
#162539=CIRCLE ( 'NONE', #50080, 0.09999999999999939493 ) ;
#162549=CARTESIAN_POINT ( 'NONE',  ( 23.25000000000000000, -9.599999999988845900, -43.39396912265245021 ) ) ;
#162553=CIRCLE ( 'NONE', #233289, 4.299999999999956302 ) ;
#162559=CARTESIAN_POINT ( 'NONE',  ( 21.05000000000000071, 8.776282895303634035, -41.98800072158436336 ) ) ;
#162564=DIRECTION ( 'NONE',  ( 0.000000000000000000, 0.000000000000000000, 1.000000000000000000 ) ) ;
#162566=EDGE_CURVE ( 'NONE', #115264, #126560, #120436, .T. ) ;
#162575=CARTESIAN_POINT ( 'NONE',  ( -21.05000000000000071, -11.41227409413852989, -36.50000000000000711 ) ) ;
#162581=ORIENTED_EDGE ( 'NONE', *, *, #11929, .T. ) ;
#162607=DIRECTION ( 'NONE',  ( 0.000000000000000000, 0.000000000000000000, 1.000000000000000000 ) ) ;
#162635=DIRECTION ( 'NONE',  ( 0.000000000000000000, 0.000000000000000000, 1.000000000000000000 ) ) ;
#162654=DIRECTION ( 'NONE',  ( 1.000000000000000000, 0.000000000000000000, 0.000000000000000000 ) ) ;
#162724=AXIS2_PLACEMENT_3D ( 'NONE', #26094, #67769, #148605 ) ;
#162734=EDGE_CURVE ( 'NONE', #186448, #68820, #82081, .T. ) ;
#162768=ORIENTED_EDGE ( 'NONE', *, *, #127284, .F. ) ;
#162800=CARTESIAN_POINT ( 'NONE',  ( 22.24259225415828567, 0.09906588346399246292, -26.00806212943458817 ) ) ;
#162853=B_SPLINE_CURVE_WITH_KNOTS ( 'NONE', 3,
 ( #193277, #78445, #94154, #237539, #15948, #96699, #176297, #138400, #217943, #219240 ),
 .UNSPECIFIED., .F., .F.,
 ( 4, 2, 2, 2, 4 ),
 ( 0.000000000000000000, 0.0001660831991682082409, 0.0002491247987523123749, 0.0002906455985443822092, 0.0003321663983364520978 ),
 .UNSPECIFIED. ) ;
#162863=DIRECTION ( 'NONE',  ( -0.000000000000000000, -0.000000000000000000, 1.000000000000000000 ) ) ;
#162867=B_SPLINE_CURVE_WITH_KNOTS ( 'NONE', 3,
 ( #225294, #141926, #83208, #102776, #182358, #123664, #25848, #204462, #162800, #84475 ),
 .UNSPECIFIED., .F., .F.,
 ( 4, 3, 3, 4 ),
 ( 3.469446951953614189E-18, 0.0002000000000008561227, 0.001000000000082977483, 0.001967863649483317639 ),
 .UNSPECIFIED. ) ;
#162869=FACE_OUTER_BOUND ( 'NONE', #161750, .T. ) ;
#162881=ORIENTED_EDGE ( 'NONE', *, *, #2294, .F. ) ;
#162900=DIRECTION ( 'NONE',  ( 0.000000000000000000, -0.1568667991644693838, -0.9876197685951279004 ) ) ;
#162930=ORIENTED_EDGE ( 'NONE', *, *, #62629, .T. ) ;
#162951=CIRCLE ( 'NONE', #83771, 1.899999999999999023 ) ;
#162998=CARTESIAN_POINT ( 'NONE',  ( -23.15000000000000213, -9.599999999988847676, -43.39396912265245021 ) ) ;
#163003=CYLINDRICAL_SURFACE ( 'NONE', #158775, 0.09999999999999939493 ) ;
#163014=CARTESIAN_POINT ( 'NONE',  ( -20.94999999999999929, -1.164121893230052995, -74.91484808557160591 ) ) ;
#163037=ADVANCED_FACE ( 'NONE', ( #148513 ), #231912, .T. ) ;
#163042=DIRECTION ( 'NONE',  ( -1.000000000000000000, -0.000000000000000000, -0.000000000000000000 ) ) ;
#163061=VERTEX_POINT ( 'NONE', #178361 ) ;
#163079=ORIENTED_EDGE ( 'NONE', *, *, #186868, .T. ) ;
#163094=ORIENTED_EDGE ( 'NONE', *, *, #165949, .T. ) ;
#163112=CARTESIAN_POINT ( 'NONE',  ( 23.14999999999999858, 6.650000000011155876, -45.85000000000000142 ) ) ;
#163127=DIRECTION ( 'NONE',  ( -0.000000000000000000, -0.000000000000000000, -1.000000000000000000 ) ) ;
#163130=VECTOR ( 'NONE', #72419, 1000.000000000000000 ) ;
#163136=EDGE_LOOP ( 'NONE', ( #167223, #199491, #39615 ) ) ;
#163151=VERTEX_POINT ( 'NONE', #96219 ) ;
#163171=CARTESIAN_POINT ( 'NONE',  ( -20.54999999999999716, 4.350000000011156054, -50.25000000000000000 ) ) ;
#163174=EDGE_CURVE ( 'NONE', #140969, #14771, #62241, .T. ) ;
#163208=ORIENTED_EDGE ( 'NONE', *, *, #20559, .T. ) ;
#163214=DIRECTION ( 'NONE',  ( 0.000000000000000000, 0.000000000000000000, -1.000000000000000000 ) ) ;
#163244=ADVANCED_FACE ( 'NONE', ( #24423 ), #101893, .T. ) ;
#163280=VERTEX_POINT ( 'NONE', #153374 ) ;
#163303=AXIS2_PLACEMENT_3D ( 'NONE', #130854, #210413, #31795 ) ;
#163365=DIRECTION ( 'NONE',  ( 0.000000000000000000, 0.000000000000000000, -1.000000000000000000 ) ) ;
#163370=DIRECTION ( 'NONE',  ( -0.000000000000000000, -1.000000000000000000, -1.734723475976807292E-15 ) ) ;
#163374=EDGE_CURVE ( 'NONE', #42457, #140969, #208184, .T. ) ;
#163382=ORIENTED_EDGE ( 'NONE', *, *, #217194, .T. ) ;
#163402=EDGE_CURVE ( 'NONE', #95143, #249646, #99745, .T. ) ;
#163410=DIRECTION ( 'NONE',  ( 2.952720810173289112E-16, -1.000000000000000000, -0.000000000000000000 ) ) ;
#163419=EDGE_CURVE ( 'NONE', #1139, #68228, #121747, .T. ) ;
#163442=VERTEX_POINT ( 'NONE', #175479 ) ;
#163476=CARTESIAN_POINT ( 'NONE',  ( 20.02499999999999858, 9.750000000011153745, -54.75000000000000711 ) ) ;
#163482=DIRECTION ( 'NONE',  ( -0.000000000000000000, 0.000000000000000000, -1.000000000000000000 ) ) ;
#163496=CARTESIAN_POINT ( 'NONE',  ( -21.07928932188134041, 6.328516656404449492, -33.40110485434561127 ) ) ;
#163502=FACE_OUTER_BOUND ( 'NONE', #164564, .T. ) ;
#163543=CARTESIAN_POINT ( 'NONE',  ( -20.64999999999999858, 1.115625160336667635E-11, -69.00000000000000000 ) ) ;
#163551=FACE_OUTER_BOUND ( 'NONE', #36392, .T. ) ;
#163562=CARTESIAN_POINT ( 'NONE',  ( -20.85000000000000142, -1.164121893230052995, -74.81484808557161159 ) ) ;
#163564=TOROIDAL_SURFACE ( 'NONE', #51097, 11.70000000000000639, 0.1000000000000000056 ) ;
#163599=ORIENTED_EDGE ( 'NONE', *, *, #180822, .F. ) ;
#163619=ORIENTED_EDGE ( 'NONE', *, *, #233866, .T. ) ;
#163638=ORIENTED_EDGE ( 'NONE', *, *, #195758, .F. ) ;
#163643=LINE ( 'NONE', #222289, #155402 ) ;
#163644=EDGE_LOOP ( 'NONE', ( #72303, #155255, #98050, #218336 ) ) ;
#163651=CARTESIAN_POINT ( 'NONE',  ( 23.14999999999999858, 1.115600667400684642E-11, -67.00000000000000000 ) ) ;
#163662=TOROIDAL_SURFACE ( 'NONE', #117856, 0.2000000000000000111, 0.1000000000000000056 ) ;
#163686=CARTESIAN_POINT ( 'NONE',  ( -20.86777300164945004, 10.33200063080771969, -72.59316749566428939 ) ) ;
#163689=CYLINDRICAL_SURFACE ( 'NONE', #77998, 0.09999999999999939493 ) ;
#163709=FACE_OUTER_BOUND ( 'NONE', #10105, .T. ) ;
#163723=DIRECTION ( 'NONE',  ( 1.000000000000000000, -0.000000000000000000, -0.000000000000000000 ) ) ;
#163729=ORIENTED_EDGE ( 'NONE', *, *, #4582, .F. ) ;
#163734=VECTOR ( 'NONE', #196111, 1000.000000000000114 ) ;
#163764=DIRECTION ( 'NONE',  ( 0.000000000000000000, -1.000000000000000000, 0.000000000000000000 ) ) ;
#163778=ADVANCED_FACE ( 'NONE', ( #13527 ), #122, .T. ) ;
#163789=CIRCLE ( 'NONE', #13948, 0.09999999999999892308 ) ;
#163798=CARTESIAN_POINT ( 'NONE',  ( -21.44999999999999929, 7.150000000011155876, -54.75000000000000000 ) ) ;
#163805=EDGE_CURVE ( 'NONE', #28235, #147882, #171069, .T. ) ;
#163810=DIRECTION ( 'NONE',  ( -1.836970198721029934E-16, 1.000000000000000000, 0.000000000000000000 ) ) ;
#163835=CARTESIAN_POINT ( 'NONE',  ( 21.07928932188134397, 6.328516656404459262, -33.40110485434561127 ) ) ;
#163872=ORIENTED_EDGE ( 'NONE', *, *, #198879, .T. ) ;
#163909=VERTEX_POINT ( 'NONE', #104578 ) ;
#163913=CIRCLE ( 'NONE', #130589, 0.1000000000000028644 ) ;
#163921=CARTESIAN_POINT ( 'NONE',  ( -18.46946985241261174, -9.509317228700407298, -40.48666256549965681 ) ) ;
#163933=FACE_OUTER_BOUND ( 'NONE', #228253, .T. ) ;
#163946=CARTESIAN_POINT ( 'NONE',  ( 21.14999999999999858, 1.115486826172573664E-11, -26.95934304829875927 ) ) ;
#164037=ORIENTED_EDGE ( 'NONE', *, *, #69252, .T. ) ;
#164048=TOROIDAL_SURFACE ( 'NONE', #234972, 0.2000000000000000111, 0.1000000000000000056 ) ;
#164070=AXIS2_PLACEMENT_3D ( 'NONE', #183436, #62203, #81720 ) ;
#164074=ORIENTED_EDGE ( 'NONE', *, *, #56746, .F. ) ;
#164099=CARTESIAN_POINT ( 'NONE',  ( 21.30740335185486245, 6.556657922039159203, -33.40106547422415417 ) ) ;
#164114=FACE_OUTER_BOUND ( 'NONE', #62145, .T. ) ;
#164126=ORIENTED_EDGE ( 'NONE', *, *, #253362, .T. ) ;
#164127=EDGE_CURVE ( 'NONE', #110138, #125075, #92079, .T. ) ;
#164159=CIRCLE ( 'NONE', #189100, 0.1000000000000028644 ) ;
#164164=EDGE_CURVE ( 'NONE', #135639, #148274, #246032, .T. ) ;
#164186=ADVANCED_FACE ( 'NONE', ( #179676 ), #187779, .F. ) ;
#164213=FACE_OUTER_BOUND ( 'NONE', #117120, .T. ) ;
#164215=CARTESIAN_POINT ( 'NONE',  ( -21.14999999999999858, -0.09999999998884338825, -21.85042919245520210 ) ) ;
#164222=CARTESIAN_POINT ( 'NONE',  ( -18.59999999999999787, -9.480686695267820596, -73.94111516875784673 ) ) ;
#164223=AXIS2_PLACEMENT_3D ( 'NONE', #183400, #167707, #204228 ) ;
#164237=DIRECTION ( 'NONE',  ( -0.000000000000000000, -0.1298341882519737922, -0.9915357197604890427 ) ) ;
#164249=ORIENTED_EDGE ( 'NONE', *, *, #85742, .F. ) ;
#164279=DIRECTION ( 'NONE',  ( 1.000000000000000000, 0.000000000000000000, 0.000000000000000000 ) ) ;
#164326=EDGE_LOOP ( 'NONE', ( #39308, #63791, #221471, #52343 ) ) ;
#164328=ORIENTED_EDGE ( 'NONE', *, *, #218705, .T. ) ;
#164369=CARTESIAN_POINT ( 'NONE',  ( 20.94999999999999929, 1.115600667400684642E-11, -67.00000000000000000 ) ) ;
#164375=VERTEX_POINT ( 'NONE', #189935 ) ;
#164378=EDGE_CURVE ( 'NONE', #241724, #119487, #183854, .T. ) ;
#164435=CARTESIAN_POINT ( 'NONE',  ( -20.54999999999999716, 2.000000000011154189, -46.22462192276210402 ) ) ;
#164451=DIRECTION ( 'NONE',  ( 1.000000000000000000, 0.000000000000000000, 0.000000000000000000 ) ) ;
#164479=CARTESIAN_POINT ( 'NONE',  ( 23.15000000000000213, -11.48912529306489994, -63.89999999999999858 ) ) ;
#164496=CIRCLE ( 'NONE', #135429, 11.65000000000000036 ) ;
#164513=ORIENTED_EDGE ( 'NONE', *, *, #60221, .F. ) ;
#164514=CIRCLE ( 'NONE', #43691, 4.099999999999992539 ) ;
#164519=EDGE_CURVE ( 'NONE', #214929, #2240, #101040, .T. ) ;
#164522=CARTESIAN_POINT ( 'NONE',  ( 20.94999999999999574, 8.926614585098251453, -41.97168301922312850 ) ) ;
#164534=ORIENTED_EDGE ( 'NONE', *, *, #146181, .T. ) ;
#164539=EDGE_LOOP ( 'NONE', ( #165469, #181712, #245490, #198939 ) ) ;
#164549=DIRECTION ( 'NONE',  ( -6.938893903907222067E-15, 1.000000000000000000, 2.891205793294679805E-16 ) ) ;
#164558=CARTESIAN_POINT ( 'NONE',  ( 18.50000324121758055, 10.29307482169091692, -72.45864214669397541 ) ) ;
#164564=EDGE_LOOP ( 'NONE', ( #126666, #44272, #195487, #121966 ) ) ;
#164641=ORIENTED_EDGE ( 'NONE', *, *, #179550, .F. ) ;
#164646=CARTESIAN_POINT ( 'NONE',  ( -23.25000000000000000, -11.74999999998884448, -67.00000000000000000 ) ) ;
#164708=ADVANCED_FACE ( 'NONE', ( #91809 ), #210481, .T. ) ;
#164716=CARTESIAN_POINT ( 'NONE',  ( -20.94999999999999929, 1.835341550235569663, -45.05515129256298223 ) ) ;
#164723=EDGE_CURVE ( 'NONE', #160723, #212737, #93080, .T. ) ;
#164749=ORIENTED_EDGE ( 'NONE', *, *, #175511, .T. ) ;
#164765=VECTOR ( 'NONE', #16755, 999.9999999999998863 ) ;
#164767=CARTESIAN_POINT ( 'NONE',  ( 18.39999999999999858, -9.599999999988845900, -73.60018939122203108 ) ) ;
#164773=CARTESIAN_POINT ( 'NONE',  ( -20.54999999999999716, -8.730841121484173684, -43.09807471898433562 ) ) ;
#164791=CARTESIAN_POINT ( 'NONE',  ( -22.39999999999999858, 1.115137594488420878E-11, -21.74956710754139522 ) ) ;
#164820=CARTESIAN_POINT ( 'NONE',  ( 21.14999999999999858, 6.540656951712400691, -33.50000000000000000 ) ) ;
#164859=AXIS2_PLACEMENT_3D ( 'NONE', #199303, #23251, #220149 ) ;
#164863=CARTESIAN_POINT ( 'NONE',  ( 20.84451136049629838, 10.62014191481791059, -40.99392455952863656 ) ) ;
#164869=AXIS2_PLACEMENT_3D ( 'NONE', #212208, #173116, #252587 ) ;
#164946=AXIS2_PLACEMENT_3D ( 'NONE', #80297, #215038, #93799 ) ;
#165026=DIRECTION ( 'NONE',  ( 1.000000000000000000, 7.304098846218134667E-16, 0.000000000000000000 ) ) ;
#165030=EDGE_LOOP ( 'NONE', ( #199824, #4116, #195830, #177404 ) ) ;
#165038=CIRCLE ( 'NONE', #27710, 0.1000000000000028644 ) ;
#165098=VERTEX_POINT ( 'NONE', #99039 ) ;
#165171=ORIENTED_EDGE ( 'NONE', *, *, #147124, .T. ) ;
#165188=CARTESIAN_POINT ( 'NONE',  ( 22.50927854361889047, -0.1008580735143522616, -21.75043287397308944 ) ) ;
#165212=CARTESIAN_POINT ( 'NONE',  ( -23.25000000000000000, -1.835859311432481045, -78.50443916879852679 ) ) ;
#165227=EDGE_CURVE ( 'NONE', #129700, #53755, #20759, .T. ) ;
#165252=DIRECTION ( 'NONE',  ( 0.000000000000000000, -1.000000000000000000, 0.000000000000000000 ) ) ;
#165283=AXIS2_PLACEMENT_3D ( 'NONE', #132967, #213772, #6893 ) ;
#165294=ORIENTED_EDGE ( 'NONE', *, *, #172912, .F. ) ;
#165301=CARTESIAN_POINT ( 'NONE',  ( -23.25000000000000000, 1.115650265596050101E-11, -29.45000000000000284 ) ) ;
#165311=ORIENTED_EDGE ( 'NONE', *, *, #215394, .T. ) ;
#165318=EDGE_CURVE ( 'NONE', #239491, #161272, #135768, .T. ) ;
#165326=CARTESIAN_POINT ( 'NONE',  ( -23.15000000000000213, -11.48912529306489816, -63.89999999999999858 ) ) ;
#165331=CARTESIAN_POINT ( 'NONE',  ( 21.05563370358598263, 10.72423035585766549, -45.68309081596307664 ) ) ;
#165353=CARTESIAN_POINT ( 'NONE',  ( 20.95512840106819752, 10.62384869378447583, -45.70247922079902025 ) ) ;
#165365=VERTEX_POINT ( 'NONE', #80923 ) ;
#165368=ORIENTED_EDGE ( 'NONE', *, *, #65366, .T. ) ;
#165390=DIRECTION ( 'NONE',  ( 1.000000000000000000, 0.000000000000000000, 0.000000000000000000 ) ) ;
#165441=CARTESIAN_POINT ( 'NONE',  ( -20.05000000000000426, 9.250000000011157297, -54.75000000000000000 ) ) ;
#165461=CARTESIAN_POINT ( 'NONE',  ( 22.59999985501178799, 11.74986979301414181, -33.43440133020061467 ) ) ;
#165469=ORIENTED_EDGE ( 'NONE', *, *, #77261, .F. ) ;
#165475=CARTESIAN_POINT ( 'NONE',  ( -23.25000000000000000, -9.599999999988838795, -57.10603087734755690 ) ) ;
#165514=CARTESIAN_POINT ( 'NONE',  ( 23.14999999999998437, -4.049999999988842525, -33.50000000000000000 ) ) ;
#165592=EDGE_CURVE ( 'NONE', #210104, #95143, #213419, .T. ) ;
#165595=B_SPLINE_CURVE_WITH_KNOTS ( 'NONE', 3,
 ( #114755, #237274, #198135, #74381, #18222, #177331, #59884, #213849, #99005, #255491, #254239, #116053, #97720, #174776, #139425, #195596 ),
 .UNSPECIFIED., .F., .F.,
 ( 4, 3, 3, 3, 3, 4 ),
 ( 0.000000000000000000, 2.209833635978076120E-05, 5.595056164119271882E-05, 8.979992002655370561E-05, 0.0001236482757198912198, 0.0001574984039362985287 ),
 .UNSPECIFIED. ) ;
#165605=CARTESIAN_POINT ( 'NONE',  ( 22.47007471830798764, 7.720710651937610081, -33.50000000000001421 ) ) ;
#165614=CIRCLE ( 'NONE', #53169, 0.09999999999999967248 ) ;
#165624=VERTEX_POINT ( 'NONE', #209891 ) ;
#165630=CARTESIAN_POINT ( 'NONE',  ( -20.64999999999999858, 2.000000000011154189, -53.77537807723790309 ) ) ;
#165647=EDGE_CURVE ( 'NONE', #165365, #152028, #130216, .T. ) ;
#165673=ORIENTED_EDGE ( 'NONE', *, *, #40930, .T. ) ;
#165691=ADVANCED_FACE ( 'NONE', ( #136743 ), #118496, .T. ) ;
#165697=DIRECTION ( 'NONE',  ( 0.000000000000000000, 0.000000000000000000, 1.000000000000000000 ) ) ;
#165708=VERTEX_POINT ( 'NONE', #76776 ) ;
#165717=CYLINDRICAL_SURFACE ( 'NONE', #63462, 0.09999999999999781286 ) ;
#165745=EDGE_CURVE ( 'NONE', #212748, #147427, #146775, .T. ) ;
#165773=ORIENTED_EDGE ( 'NONE', *, *, #216960, .T. ) ;
#165800=CIRCLE ( 'NONE', #132078, 0.9750000000000036415 ) ;
#165807=ORIENTED_EDGE ( 'NONE', *, *, #7650, .T. ) ;
#165821=ADVANCED_FACE ( 'NONE', ( #128427 ), #159646, .T. ) ;
#165847=CARTESIAN_POINT ( 'NONE',  ( 21.14999999999999503, 1.115600667400684642E-11, -27.25000000000000355 ) ) ;
#165878=DIRECTION ( 'NONE',  ( 0.000000000000000000, 0.1575844902526876978, 0.9875055080513731598 ) ) ;
#165880=CARTESIAN_POINT ( 'NONE',  ( 20.94999675878240808, 10.29307482169070909, -72.45864214669403225 ) ) ;
#165905=CIRCLE ( 'NONE', #53459, 0.3999999999999975797 ) ;
#165919=CIRCLE ( 'NONE', #232568, 11.74999999999999645 ) ;
#165920=LINE ( 'NONE', #62939, #228441 ) ;
#165938=DIRECTION ( 'NONE',  ( 1.000000000000000000, 0.000000000000000000, 0.000000000000000000 ) ) ;
#165949=EDGE_CURVE ( 'NONE', #45034, #240562, #38326, .T. ) ;
#165961=DIRECTION ( 'NONE',  ( 0.000000000000000000, -1.000000000000000000, 0.000000000000000000 ) ) ;
#165977=CARTESIAN_POINT ( 'NONE',  ( 20.94999999999999929, -1.164121893230052995, -74.91484808557160591 ) ) ;
#166008=VECTOR ( 'NONE', #79403, 1000.000000000000000 ) ;
#166057=ORIENTED_EDGE ( 'NONE', *, *, #3900, .T. ) ;
#166062=DIRECTION ( 'NONE',  ( -1.000000000000000000, 0.000000000000000000, 0.000000000000000000 ) ) ;
#166094=DIRECTION ( 'NONE',  ( 0.000000000000000000, 0.9999631594459056361, -0.008583690987128059571 ) ) ;
#166122=ORIENTED_EDGE ( 'NONE', *, *, #143004, .F. ) ;
#166135=ADVANCED_FACE ( 'NONE', ( #208941 ), #129403, .T. ) ;
#166152=FACE_OUTER_BOUND ( 'NONE', #58224, .T. ) ;
#166157=CIRCLE ( 'NONE', #211925, 0.1000000000000028644 ) ;
#166162=CARTESIAN_POINT ( 'NONE',  ( -21.05000000000000071, 1.250000000011155299, -41.50000000000000000 ) ) ;
#166175=CARTESIAN_POINT ( 'NONE',  ( 20.97217846901852312, 8.875441724720827708, -42.00122768393723760 ) ) ;
#166176=ORIENTED_EDGE ( 'NONE', *, *, #145352, .F. ) ;
#166186=EDGE_LOOP ( 'NONE', ( #134774, #191081, #220112, #36838 ) ) ;
#166206=EDGE_CURVE ( 'NONE', #36652, #204355, #213812, .T. ) ;
#166238=CARTESIAN_POINT ( 'NONE',  ( 22.45305468355010703, -0.1008583690885486023, -21.75043287651027768 ) ) ;
#166247=ADVANCED_FACE ( 'NONE', ( #25190 ), #168065, .T. ) ;
#166259=EDGE_CURVE ( 'NONE', #171197, #163151, #22288, .T. ) ;
#166281=EDGE_CURVE ( 'NONE', #131047, #31458, #94120, .T. ) ;
#166294=FACE_OUTER_BOUND ( 'NONE', #112463, .T. ) ;
#166324=ORIENTED_EDGE ( 'NONE', *, *, #229568, .T. ) ;
#166325=ORIENTED_EDGE ( 'NONE', *, *, #154429, .F. ) ;
#166330=ORIENTED_EDGE ( 'NONE', *, *, #11698, .T. ) ;
#166335=EDGE_LOOP ( 'NONE', ( #181073, #44116, #7433 ) ) ;
#166336=DIRECTION ( 'NONE',  ( 1.000000000000000000, 0.000000000000000000, -0.000000000000000000 ) ) ;
#166350=CARTESIAN_POINT ( 'NONE',  ( -18.56579813702275672, 10.33025634372637391, -72.58709292826389969 ) ) ;
#166373=CARTESIAN_POINT ( 'NONE',  ( 18.58685178364169488, -9.406733083793096029, -40.62442046908773818 ) ) ;
#166380=ORIENTED_EDGE ( 'NONE', *, *, #27939, .F. ) ;
#166397=ORIENTED_EDGE ( 'NONE', *, *, #56408, .F. ) ;
#166420=DIRECTION ( 'NONE',  ( -3.265361837132813093E-16, 1.000000000000000000, 0.000000000000000000 ) ) ;
#166424=DIRECTION ( 'NONE',  ( 1.000000000000000000, -7.304098846218135653E-16, -2.111765289898286048E-31 ) ) ;
#166456=EDGE_CURVE ( 'NONE', #171197, #165098, #63963, .T. ) ;
#166461=CIRCLE ( 'NONE', #91427, 0.09999999999999939493 ) ;
#166485=EDGE_CURVE ( 'NONE', #107516, #3690, #42534, .T. ) ;
#166500=ORIENTED_EDGE ( 'NONE', *, *, #179550, .T. ) ;
#166527=ADVANCED_FACE ( 'NONE', ( #43154 ), #202222, .F. ) ;
#166528=DIRECTION ( 'NONE',  ( -0.000000000000000000, 1.000000000000000000, 0.000000000000000000 ) ) ;
#166538=ORIENTED_EDGE ( 'NONE', *, *, #48272, .T. ) ;
#166565=EDGE_LOOP ( 'NONE', ( #69483, #234525, #23776, #5334 ) ) ;
#166572=ORIENTED_EDGE ( 'NONE', *, *, #7670, .T. ) ;
#166588=ORIENTED_EDGE ( 'NONE', *, *, #151668, .F. ) ;
#166601=EDGE_CURVE ( 'NONE', #43292, #84007, #129107, .T. ) ;
#166617=LINE ( 'NONE', #210849, #189865 ) ;
#166623=VECTOR ( 'NONE', #42914, 1000.000000000000000 ) ;
#166633=DIRECTION ( 'NONE',  ( 0.000000000000000000, -1.000000000000000000, -0.000000000000000000 ) ) ;
#166646=ORIENTED_EDGE ( 'NONE', *, *, #82594, .F. ) ;
#166655=CARTESIAN_POINT ( 'NONE',  ( -23.25000000000000000, 4.350000000011156054, -45.85000000000000142 ) ) ;
#166665=CARTESIAN_POINT ( 'NONE',  ( 21.05000012384953223, 10.62872029888669978, -45.67797733003531135 ) ) ;
#166666=DIRECTION ( 'NONE',  ( 0.000000000000000000, -1.000000000000000000, -0.000000000000000000 ) ) ;
#166667=AXIS2_PLACEMENT_3D ( 'NONE', #70507, #150029, #229557 ) ;
#166670=ORIENTED_EDGE ( 'NONE', *, *, #97825, .T. ) ;
#166693=DIRECTION ( 'NONE',  ( 0.000000000000000000, -0.9915357197604792727, 0.1298341882520475943 ) ) ;
#166699=DIRECTION ( 'NONE',  ( 0.000000000000000000, 0.000000000000000000, 1.000000000000000000 ) ) ;
#166728=FACE_OUTER_BOUND ( 'NONE', #212724, .T. ) ;
#166759=ORIENTED_EDGE ( 'NONE', *, *, #199017, .F. ) ;
#166767=ORIENTED_EDGE ( 'NONE', *, *, #242295, .T. ) ;
#166824=ADVANCED_FACE ( 'NONE', ( #50818 ), #191681, .F. ) ;
#166861=DIRECTION ( 'NONE',  ( -1.000000000000000000, -0.000000000000000000, -0.000000000000000000 ) ) ;
#166881=ORIENTED_EDGE ( 'NONE', *, *, #146510, .F. ) ;
#166895=EDGE_CURVE ( 'NONE', #168194, #208880, #180122, .T. ) ;
#166935=EDGE_CURVE ( 'NONE', #193788, #214956, #214075, .T. ) ;
#166959=VERTEX_POINT ( 'NONE', #198054 ) ;
#166970=CARTESIAN_POINT ( 'NONE',  ( 21.14999999999999858, 6.650000000011155876, -45.75000000000000711 ) ) ;
#166971=CARTESIAN_POINT ( 'NONE',  ( 21.14999999999999503, 11.65000000001116298, -33.60000000000000142 ) ) ;
#166977=DIRECTION ( 'NONE',  ( 0.000000000000000000, -0.6728971962616792091, 0.7397360091702790408 ) ) ;
#166979=CIRCLE ( 'NONE', #237849, 0.09999999999999939493 ) ;
#166996=LINE ( 'NONE', #28780, #186379 ) ;
#167027=FACE_OUTER_BOUND ( 'NONE', #94932, .T. ) ;
#167030=DIRECTION ( 'NONE',  ( -0.000000000000000000, -1.000000000000000000, 6.308085367188393199E-16 ) ) ;
#167043=DIRECTION ( 'NONE',  ( 0.000000000000000000, 0.000000000000000000, -1.000000000000000000 ) ) ;
#167074=CARTESIAN_POINT ( 'NONE',  ( 21.00000000000000000, 9.750000000011153745, -54.75000000000000000 ) ) ;
#167082=CARTESIAN_POINT ( 'NONE',  ( 21.05000000000000071, 1.115600667400684642E-11, -67.00000000000000000 ) ) ;
#167101=DIRECTION ( 'NONE',  ( -0.7071067811865475727, -0.7071067811865475727, -0.000000000000000000 ) ) ;
#167154=CARTESIAN_POINT ( 'NONE',  ( -21.44999999999999929, 7.250000000011155521, -54.65000000000000568 ) ) ;
#167160=AXIS2_PLACEMENT_3D ( 'NONE', #185086, #6439, #88528 ) ;
#167181=CARTESIAN_POINT ( 'NONE',  ( 20.94999999999999929, 10.29270135741298731, -72.45736188715193293 ) ) ;
#167183=ORIENTED_EDGE ( 'NONE', *, *, #144288, .T. ) ;
#167206=EDGE_CURVE ( 'NONE', #41950, #89935, #80964, .T. ) ;
#167216=CARTESIAN_POINT ( 'NONE',  ( -21.45000000000000284, 7.708578643773852157, -45.85000000000000142 ) ) ;
#167223=ORIENTED_EDGE ( 'NONE', *, *, #28530, .F. ) ;
#167230=ORIENTED_EDGE ( 'NONE', *, *, #233542, .T. ) ;
#167238=EDGE_CURVE ( 'NONE', #119881, #131987, #210085, .T. ) ;
#167244=DIRECTION ( 'NONE',  ( 0.000000000000000000, -0.5000000000000144329, -0.8660254037844302699 ) ) ;
#167249=DIRECTION ( 'NONE',  ( 1.000000000000000000, 0.000000000000000000, 0.000000000000000000 ) ) ;
#167262=ORIENTED_EDGE ( 'NONE', *, *, #153159, .T. ) ;
#167264=DIRECTION ( 'NONE',  ( 0.000000000000000000, 0.000000000000000000, -1.000000000000000000 ) ) ;
#167277=ORIENTED_EDGE ( 'NONE', *, *, #257941, .F. ) ;
#167300=AXIS2_PLACEMENT_3D ( 'NONE', #75818, #73283, #54941 ) ;
#167305=DIRECTION ( 'NONE',  ( 1.000000000000000000, 0.000000000000000000, 0.000000000000000000 ) ) ;
#167343=CARTESIAN_POINT ( 'NONE',  ( 21.97500000000000497, 9.750000000011153745, -54.75000000000000711 ) ) ;
#167417=AXIS2_PLACEMENT_3D ( 'NONE', #24612, #80680, #258002 ) ;
#167431=LINE ( 'NONE', #68312, #179026 ) ;
#167451=CYLINDRICAL_SURFACE ( 'NONE', #48061, 0.1000000000000028644 ) ;
#167461=EDGE_CURVE ( 'NONE', #164375, #32344, #206736, .T. ) ;
#167487=CARTESIAN_POINT ( 'NONE',  ( 23.14999999999999503, 6.550000000011156231, -54.65000000000000568 ) ) ;
#167506=AXIS2_PLACEMENT_3D ( 'NONE', #194327, #212592, #150058 ) ;
#167516=CARTESIAN_POINT ( 'NONE',  ( 22.60000000000000142, 0.04781839071596404728, -21.74997758095277334 ) ) ;
#167565=CARTESIAN_POINT ( 'NONE',  ( -18.59999999999999787, -1.637172712959223952, -45.08215336547201701 ) ) ;
#167569=DIRECTION ( 'NONE',  ( 0.000000000000000000, 0.5000000000000078826, 0.8660254037844340447 ) ) ;
#167573=CARTESIAN_POINT ( 'NONE',  ( 20.94999999999999929, 5.400000000011154988, -57.10603087734755690 ) ) ;
#167601=AXIS2_PLACEMENT_3D ( 'NONE', #86716, #8503, #68474 ) ;
#167610=ORIENTED_EDGE ( 'NONE', *, *, #99079, .T. ) ;
#167615=CARTESIAN_POINT ( 'NONE',  ( 23.24999999999999289, 11.75000000001116263, -21.75000000000000355 ) ) ;
#167626=VECTOR ( 'NONE', #158137, 1000.000000000000000 ) ;
#167650=ORIENTED_EDGE ( 'NONE', *, *, #103644, .T. ) ;
#167659=AXIS2_PLACEMENT_3D ( 'NONE', #174021, #93141, #253497 ) ;
#167668=EDGE_LOOP ( 'NONE', ( #216463, #162323, #82193, #175166 ) ) ;
#167699=DIRECTION ( 'NONE',  ( 1.000000000000000000, 3.265361837132813093E-16, -0.000000000000000000 ) ) ;
#167700=ORIENTED_EDGE ( 'NONE', *, *, #102890, .F. ) ;
#167707=DIRECTION ( 'NONE',  ( 1.000000000000000000, -0.000000000000000000, -0.000000000000000000 ) ) ;
#167723=AXIS2_PLACEMENT_3D ( 'NONE', #90671, #234037, #32021 ) ;
#167728=CARTESIAN_POINT ( 'NONE',  ( -23.15000000000000213, 2.000000000011154189, -53.77537807723790309 ) ) ;
#167741=AXIS2_PLACEMENT_3D ( 'NONE', #62833, #182804, #144918 ) ;
#167754=DIRECTION ( 'NONE',  ( 0.000000000000000000, 0.1350103645451904977, 0.9908441862701596881 ) ) ;
#167804=EDGE_LOOP ( 'NONE', ( #62825, #94892, #217267, #61712, #236944 ) ) ;
#167811=DIRECTION ( 'NONE',  ( -1.000000000000000000, 7.304098846218135653E-16, 0.000000000000000000 ) ) ;
#167813=AXIS2_PLACEMENT_3D ( 'NONE', #59355, #215877, #73862 ) ;
#167818=ORIENTED_EDGE ( 'NONE', *, *, #147637, .T. ) ;
#167819=VERTEX_POINT ( 'NONE', #169605 ) ;
#167833=EDGE_LOOP ( 'NONE', ( #137681, #153819, #29410, #175266 ) ) ;
#167834=CARTESIAN_POINT ( 'NONE',  ( -23.25000000000000000, -1.736705739456431807, -78.51742258762372728 ) ) ;
#167898=ADVANCED_FACE ( 'NONE', ( #151296 ), #83890, .F. ) ;
#167903=VECTOR ( 'NONE', #117464, 1000.000000000000000 ) ;
#167906=AXIS2_PLACEMENT_3D ( 'NONE', #42679, #221295, #6103 ) ;
#167907=CARTESIAN_POINT ( 'NONE',  ( -22.50000000000000000, 11.64957080755595520, -33.40000000000000568 ) ) ;
#167926=CARTESIAN_POINT ( 'NONE',  ( 21.14261333020286671, 10.71569264926606202, -45.75000000000021316 ) ) ;
#167933=DIRECTION ( 'NONE',  ( -3.265361837132813093E-16, 1.000000000000000000, 0.000000000000000000 ) ) ;
#167935=CARTESIAN_POINT ( 'NONE',  ( -21.65000000000000213, 7.750000000011155521, -45.85000000000000142 ) ) ;
#167986=LINE ( 'NONE', #247483, #218799 ) ;
#167989=ORIENTED_EDGE ( 'NONE', *, *, #144288, .F. ) ;
#168038=EDGE_CURVE ( 'NONE', #156961, #14219, #13231, .T. ) ;
#168058=CARTESIAN_POINT ( 'NONE',  ( 23.14999999999999858, 1.115600667400684642E-11, -67.00000000000000000 ) ) ;
#168065=TOROIDAL_SURFACE ( 'NONE', #55538, 4.149999999999999467, 0.1000000000000000056 ) ;
#168102=ORIENTED_EDGE ( 'NONE', *, *, #70752, .F. ) ;
#168142=DIRECTION ( 'NONE',  ( 0.000000000000000000, 0.000000000000000000, 1.000000000000000000 ) ) ;
#168158=CARTESIAN_POINT ( 'NONE',  ( -20.00857864376270001, 9.250000000011157297, -54.65000000000000568 ) ) ;
#168164=DIRECTION ( 'NONE',  ( -0.000000000000000000, -0.000000000000000000, 1.000000000000000000 ) ) ;
#168194=VERTEX_POINT ( 'NONE', #126257 ) ;
#168214=EDGE_CURVE ( 'NONE', #167819, #15533, #7607, .T. ) ;
#168215=ORIENTED_EDGE ( 'NONE', *, *, #125835, .T. ) ;
#168228=CIRCLE ( 'NONE', #172339, 0.1000000000000004496 ) ;
#168236=ORIENTED_EDGE ( 'NONE', *, *, #228184, .F. ) ;
#168254=( BOUNDED_SURFACE ( )  B_SPLINE_SURFACE ( 3, 2, ( 
 ( #32807, #232274, #212698 ),
 ( #95306, #174900, #135698 ),
 ( #255610, #14514, #130568 ),
 ( #191872, #151448, #94006 ),
 ( #194431, #230987, #52303 ),
 ( #17073, #133154, #75755 ),
 ( #155314, #96562, #233550 ),
 ( #156604, #73205, #234818 ),
 ( #91462, #56158, #92723 ),
 ( #215255, #131863, #213976 ) ),
 .UNSPECIFIED., .F., .F., .F. ) 
 B_SPLINE_SURFACE_WITH_KNOTS ( ( 4, 2, 2, 2, 4 ),
 ( 3, 3 ),
 ( 0.0001701955120502369480, 0.0002247052511886125372, 0.0002792149903269881264, 0.0003882344686037392505, 0.0006062734251572414988 ),
 ( 0.000000000000000000, 1.000000000000000000 ),
 .UNSPECIFIED. ) 
 GEOMETRIC_REPRESENTATION_ITEM ( )  RATIONAL_B_SPLINE_SURFACE ( (
 ( 1.000000000000000000, 0.2966190024560417804, 1.000000000000000000),
 ( 1.000000000000000000, 0.2964522492711926804, 1.000000000000000000),
 ( 1.000000000000000000, 0.3059923531883286807, 1.000000000000000000),
 ( 1.000000000000000000, 0.3355751146944992436, 1.000000000000000000),
 ( 1.000000000000000000, 0.3550672384964260742, 1.000000000000000000),
 ( 1.000000000000000000, 0.4157034672179444335, 1.000000000000000000),
 ( 1.000000000000000000, 0.4588031877653836466, 1.000000000000000000),
 ( 1.000000000000000000, 0.5771441759660936865, 1.000000000000000000),
 ( 1.000000000000000000, 0.6469377121771874295, 1.000000000000000000),
 ( 1.000000000000000000, 0.7071067811865376918, 1.000000000000000000) ) ) 
 REPRESENTATION_ITEM ( '' )  SURFACE ( )  );
#168298=CIRCLE ( 'NONE', #114059, 0.1999999999999987899 ) ;
#168301=EDGE_LOOP ( 'NONE', ( #149467, #175893, #213640, #69364 ) ) ;
#168324=DIRECTION ( 'NONE',  ( -1.000000000000000000, 0.000000000000000000, 0.000000000000000000 ) ) ;
#168349=EDGE_CURVE ( 'NONE', #204714, #95921, #100824, .T. ) ;
#168351=FACE_OUTER_BOUND ( 'NONE', #107490, .T. ) ;
#168379=DIRECTION ( 'NONE',  ( -1.000000000000000000, 0.000000000000000000, 0.000000000000000000 ) ) ;
#168411=DIRECTION ( 'NONE',  ( 0.000000000000000000, 0.000000000000000000, -1.000000000000000000 ) ) ;
#168419=VECTOR ( 'NONE', #178745, 1000.000000000000114 ) ;
#168428=AXIS2_PLACEMENT_3D ( 'NONE', #48, #114869, #37926 ) ;
#168461=VERTEX_POINT ( 'NONE', #42566 ) ;
#168490=EDGE_LOOP ( 'NONE', ( #115503, #192321, #256078 ) ) ;
#168499=CARTESIAN_POINT ( 'NONE',  ( 23.24999999999999289, 5.950000000011163692, -56.69429769496518645 ) ) ;
#168510=ORIENTED_EDGE ( 'NONE', *, *, #163419, .F. ) ;
#168512=LINE ( 'NONE', #191912, #102068 ) ;
#168526=CARTESIAN_POINT ( 'NONE',  ( -20.94999999999999929, 1.835341550235569663, -45.05515129256298223 ) ) ;
#168567=VECTOR ( 'NONE', #36356, 1000.000000000000000 ) ;
#168590=CYLINDRICAL_SURFACE ( 'NONE', #113651, 0.1000000000000028644 ) ;
#168619=CARTESIAN_POINT ( 'NONE',  ( 18.46082813848003212, -9.480749650896282077, -40.58437010271577350 ) ) ;
#168678=DIRECTION ( 'NONE',  ( 0.7071067811865474617, 0.7071067811865474617, -0.000000000000000000 ) ) ;
#168679=CARTESIAN_POINT ( 'NONE',  ( -20.94999999999999929, -11.74999999998884448, -36.60000000000000853 ) ) ;
#168683=EDGE_CURVE ( 'NONE', #14219, #73952, #38518, .T. ) ;
#168746=EDGE_CURVE ( 'NONE', #14799, #136029, #26066, .T. ) ;
#168750=ORIENTED_EDGE ( 'NONE', *, *, #62482, .T. ) ;
#168808=AXIS2_PLACEMENT_3D ( 'NONE', #251739, #73138, #232198 ) ;
#168824=ORIENTED_EDGE ( 'NONE', *, *, #218600, .F. ) ;
#168826=CARTESIAN_POINT ( 'NONE',  ( -18.59999999999999787, -1.835859311432481045, -78.50443916879852679 ) ) ;
#168868=CARTESIAN_POINT ( 'NONE',  ( 21.05000000000000071, 6.350000000011161383, -43.34382208968312966 ) ) ;
#168869=VERTEX_POINT ( 'NONE', #196200 ) ;
#168877=AXIS2_PLACEMENT_3D ( 'NONE', #131220, #210763, #32154 ) ;
#168881=( GEOMETRIC_REPRESENTATION_CONTEXT ( 3 ) GLOBAL_UNCERTAINTY_ASSIGNED_CONTEXT ( ( #24425 ) ) GLOBAL_UNIT_ASSIGNED_CONTEXT ( ( #216032, #173121, #253875 ) ) REPRESENTATION_CONTEXT ( 'NONE', 'WORKASPACE' ) );
#168913=DIRECTION ( 'NONE',  ( 1.000000000000000000, 0.000000000000000000, 0.000000000000000000 ) ) ;
#168917=CARTESIAN_POINT ( 'NONE',  ( -18.50000000000000000, 1.115600667400684642E-11, -33.50000000000000000 ) ) ;
#168936=DIRECTION ( 'NONE',  ( -3.265361837132813093E-16, 1.000000000000000000, 0.000000000000000000 ) ) ;
#168958=VERTEX_POINT ( 'NONE', #114616 ) ;
#168962=FACE_OUTER_BOUND ( 'NONE', #134904, .T. ) ;
#169021=EDGE_CURVE ( 'NONE', #217175, #64423, #122093, .T. ) ;
#169093=DIRECTION ( 'NONE',  ( 0.000000000000000000, 0.000000000000000000, -1.000000000000000000 ) ) ;
#169115=ORIENTED_EDGE ( 'NONE', *, *, #220529, .T. ) ;
#169151=CARTESIAN_POINT ( 'NONE',  ( -22.39999999999999858, 1.115600667400684642E-11, -25.70922040162659883 ) ) ;
#169177=CARTESIAN_POINT ( 'NONE',  ( -20.64999999999999858, 7.150000000011155876, -45.85000000000000142 ) ) ;
#169183=CIRCLE ( 'NONE', #31820, 2.000000000000001776 ) ;
#169260=( LENGTH_UNIT ( ) NAMED_UNIT ( * ) SI_UNIT ( .MILLI., .METRE. ) );
#169370=AXIS2_PLACEMENT_3D ( 'NONE', #231460, #108919, #132337 ) ;
#169371=EDGE_LOOP ( 'NONE', ( #187839, #246150, #125502, #170068, #239796 ) ) ;
#169417=CARTESIAN_POINT ( 'NONE',  ( -20.64999999999999858, 1.940186915899009490, -46.32911921105333164 ) ) ;
#169426=CARTESIAN_POINT ( 'NONE',  ( -21.05000000000000071, 1.835341550235567887, -45.15515129256298366 ) ) ;
#169441=EDGE_CURVE ( 'NONE', #232170, #194376, #126367, .T. ) ;
#169442=EDGE_CURVE ( 'NONE', #184107, #235379, #184619, .T. ) ;
#169458=CIRCLE ( 'NONE', #227845, 6.329289321881356400 ) ;
#169461=CYLINDRICAL_SURFACE ( 'NONE', #59503, 0.1000000000000000472 ) ;
#169511=CIRCLE ( 'NONE', #202778, 0.1000000000000028644 ) ;
#169525=EDGE_CURVE ( 'NONE', #22291, #88637, #163789, .T. ) ;
#169531=CIRCLE ( 'NONE', #69919, 11.79999999999999893 ) ;
#169543=DIRECTION ( 'NONE',  ( -1.000000000000000000, -0.000000000000000000, 0.000000000000000000 ) ) ;
#169583=CARTESIAN_POINT ( 'NONE',  ( 20.85000000000000142, -1.835859311432481045, -78.50443916879852679 ) ) ;
#169598=ORIENTED_EDGE ( 'NONE', *, *, #122687, .F. ) ;
#169605=CARTESIAN_POINT ( 'NONE',  ( -18.59999999999999787, -1.851028230129704522, -45.15391326942249606 ) ) ;
#169677=CARTESIAN_POINT ( 'NONE',  ( 20.85000000000000142, 11.65000000001115943, -60.21613433702191287 ) ) ;
#169684=DIRECTION ( 'NONE',  ( -1.000000000000000000, 0.000000000000000000, 0.000000000000000000 ) ) ;
#169696=CIRCLE ( 'NONE', #107279, 3.899999999999999467 ) ;
#169702=AXIS2_PLACEMENT_3D ( 'NONE', #144446, #101446, #45371 ) ;
#169706=ADVANCED_FACE ( 'NONE', ( #163709 ), #180709, .T. ) ;
#169717=ORIENTED_EDGE ( 'NONE', *, *, #19987, .F. ) ;
#169725=DIRECTION ( 'NONE',  ( 1.000000000000000000, 0.000000000000000000, 0.000000000000000000 ) ) ;
#169777=ORIENTED_EDGE ( 'NONE', *, *, #247536, .T. ) ;
#169790=FACE_OUTER_BOUND ( 'NONE', #204152, .T. ) ;
#169797=CARTESIAN_POINT ( 'NONE',  ( -18.50000000000000000, -9.480686695267820596, -73.94111516875786094 ) ) ;
#169806=FACE_OUTER_BOUND ( 'NONE', #81247, .T. ) ;
#169839=CIRCLE ( 'NONE', #82276, 0.09999999999999939493 ) ;
#169877=CARTESIAN_POINT ( 'NONE',  ( -21.05000000000000071, 6.413759733821432718, -33.58561306080397912 ) ) ;
#169884=EDGE_CURVE ( 'NONE', #123416, #39510, #39092, .T. ) ;
#169896=EDGE_CURVE ( 'NONE', #229112, #74863, #168298, .T. ) ;
#169897=ORIENTED_EDGE ( 'NONE', *, *, #166456, .T. ) ;
#169901=CARTESIAN_POINT ( 'NONE',  ( 18.46947024752518729, -9.509297157144928292, -40.48668944869792341 ) ) ;
#169931=EDGE_LOOP ( 'NONE', ( #167700, #98606, #156984, #170748 ) ) ;
#169947=DIRECTION ( 'NONE',  ( 0.000000000000000000, 0.000000000000000000, -1.000000000000000000 ) ) ;
#169954=CARTESIAN_POINT ( 'NONE',  ( 21.05000000000000071, -11.48912529306490349, -36.60000000000000142 ) ) ;
#169996=ORIENTED_EDGE ( 'NONE', *, *, #103779, .F. ) ;
#170019=EDGE_CURVE ( 'NONE', #178023, #233092, #55772, .T. ) ;
#170030=CYLINDRICAL_SURFACE ( 'NONE', #210555, 0.09999999999999939493 ) ;
#170033=DIRECTION ( 'NONE',  ( 0.000000000000000000, -1.000000000000000000, 0.000000000000000000 ) ) ;
#170036=CARTESIAN_POINT ( 'NONE',  ( 22.47071067811864964, 0.09909245471376176839, -25.77992525550196135 ) ) ;
#170060=ADVANCED_FACE ( 'NONE', ( #237804 ), #119147, .T. ) ;
#170068=ORIENTED_EDGE ( 'NONE', *, *, #74924, .F. ) ;
#170077=CARTESIAN_POINT ( 'NONE',  ( -18.39999999999999858, -9.499999999988849808, -40.53206939669966857 ) ) ;
#170079=CARTESIAN_POINT ( 'NONE',  ( 21.05000000000000071, 5.000000000011153745, -45.90526601891310321 ) ) ;
#170081=ADVANCED_FACE ( 'NONE', ( #21349 ), #230814, .T. ) ;
#170091=ADVANCED_FACE ( 'NONE', ( #44747 ), #61732, .T. ) ;
#170109=DIRECTION ( 'NONE',  ( 0.000000000000000000, 1.000000000000000000, 0.000000000000000000 ) ) ;
#170118=EDGE_CURVE ( 'NONE', #7520, #17436, #10227, .T. ) ;
#170126=ORIENTED_EDGE ( 'NONE', *, *, #65672, .F. ) ;
#170142=EDGE_LOOP ( 'NONE', ( #143752, #138681, #65064, #78797 ) ) ;
#170153=CARTESIAN_POINT ( 'NONE',  ( -20.64999999999999858, 7.150000000011155876, -45.85000000000000142 ) ) ;
#170202=LINE ( 'NONE', #51451, #153305 ) ;
#170242=CARTESIAN_POINT ( 'NONE',  ( -23.25000000000000000, 6.933893972137497030, -70.78564583437358237 ) ) ;
#170259=CARTESIAN_POINT ( 'NONE',  ( 18.49999999999999289, 10.20857864377384416, -58.15000000000000568 ) ) ;
#170278=ORIENTED_EDGE ( 'NONE', *, *, #128949, .F. ) ;
#170306=TOROIDAL_SURFACE ( 'NONE', #24527, 11.90000000000000213, 0.1000000000000000056 ) ;
#170324=DIRECTION ( 'NONE',  ( 1.000000000000000000, -0.000000000000000000, -0.000000000000000000 ) ) ;
#170359=CARTESIAN_POINT ( 'NONE',  ( 18.59999999999999432, -9.480686695267811714, -73.94111516875786094 ) ) ;
#170386=CARTESIAN_POINT ( 'NONE',  ( 23.14999999999999503, 6.650000000011155876, -54.85000000000000142 ) ) ;
#170403=CYLINDRICAL_SURFACE ( 'NONE', #4926, 0.1000000000000028644 ) ;
#170408=ORIENTED_EDGE ( 'NONE', *, *, #4800, .F. ) ;
#170415=DIRECTION ( 'NONE',  ( -0.000000000000000000, -0.9887567792719339499, -0.1495327102803676589 ) ) ;
#170416=AXIS2_PLACEMENT_3D ( 'NONE', #64648, #25540, #163764 ) ;
#170428=ORIENTED_EDGE ( 'NONE', *, *, #243861, .T. ) ;
#170460=ORIENTED_EDGE ( 'NONE', *, *, #223238, .F. ) ;
#170463=CARTESIAN_POINT ( 'NONE',  ( 19.97071067811864609, 11.72071067812981404, -58.15000000000000568 ) ) ;
#170465=CARTESIAN_POINT ( 'NONE',  ( 20.12500000000000000, 9.750000000011153745, -54.65000000000000568 ) ) ;
#170480=CARTESIAN_POINT ( 'NONE',  ( -18.47690164073606667, -9.464844538001081276, -73.70138093983609906 ) ) ;
#170497=ADVANCED_FACE ( 'NONE', ( #139654 ), #180108, .F. ) ;
#170501=CARTESIAN_POINT ( 'NONE',  ( -22.59999999999999787, 11.74956712350054744, -33.39914163090129762 ) ) ;
#170510=ORIENTED_EDGE ( 'NONE', *, *, #158866, .T. ) ;
#170559=DIRECTION ( 'NONE',  ( 0.000000000000000000, -1.000000000000000000, 1.713307136767217392E-15 ) ) ;
#170596=CARTESIAN_POINT ( 'NONE',  ( -20.87155475150660777, 11.75000000001115197, -60.09558652915745114 ) ) ;
#170602=CARTESIAN_POINT ( 'NONE',  ( -23.25000000000000000, 2.000000000011154189, -46.72462192276210402 ) ) ;
#170604=DIRECTION ( 'NONE',  ( 0.000000000000000000, 3.469446951953515108E-14, 1.000000000000000000 ) ) ;
#170638=ORIENTED_EDGE ( 'NONE', *, *, #215394, .F. ) ;
#170662=CARTESIAN_POINT ( 'NONE',  ( 18.59999999999999787, -1.835341550213255957, -45.05515129256298223 ) ) ;
#170663=VECTOR ( 'NONE', #10913, 1000.000000000000000 ) ;
#170669=DIRECTION ( 'NONE',  ( 1.000000000000000000, 2.952720810173289112E-16, -0.000000000000000000 ) ) ;
#170670=CIRCLE ( 'NONE', #228877, 0.09999999999999992228 ) ;
#170678=AXIS2_PLACEMENT_3D ( 'NONE', #201447, #85331, #181899 ) ;
#170686=ORIENTED_EDGE ( 'NONE', *, *, #11241, .T. ) ;
#170690=CARTESIAN_POINT ( 'NONE',  ( -23.25000000000000000, -1.249999999988843369, -74.80048075441509070 ) ) ;
#170699=ORIENTED_EDGE ( 'NONE', *, *, #37856, .T. ) ;
#170722=ADVANCED_FACE ( 'NONE', ( #37401 ), #197633, .T. ) ;
#170730=EDGE_CURVE ( 'NONE', #235569, #213025, #131179, .T. ) ;
#170740=CARTESIAN_POINT ( 'NONE',  ( -18.59999999999999787, 9.250000000011157297, -54.75000000000000000 ) ) ;
#170748=ORIENTED_EDGE ( 'NONE', *, *, #172912, .T. ) ;
#170762=FACE_OUTER_BOUND ( 'NONE', #217299, .T. ) ;
#170769=VERTEX_POINT ( 'NONE', #81601 ) ;
#170831=ORIENTED_EDGE ( 'NONE', *, *, #14656, .T. ) ;
#170872=VECTOR ( 'NONE', #4644, 1000.000000000000000 ) ;
#170883=CARTESIAN_POINT ( 'NONE',  ( -22.59999985501179154, 11.74986979301414358, -33.43440133020047256 ) ) ;
#170905=ORIENTED_EDGE ( 'NONE', *, *, #19987, .T. ) ;
#170928=CARTESIAN_POINT ( 'NONE',  ( -23.15000000000000213, 1.115625160336667635E-11, -69.00000000000000000 ) ) ;
#170958=AXIS2_PLACEMENT_3D ( 'NONE', #179069, #202452, #117773 ) ;
#171019=DIRECTION ( 'NONE',  ( 0.000000000000000000, 0.000000000000000000, -1.000000000000000000 ) ) ;
#171021=CARTESIAN_POINT ( 'NONE',  ( 21.97500000000000497, 9.750000000011153745, -54.65000000000000568 ) ) ;
#171032=EDGE_CURVE ( 'NONE', #73797, #63552, #10590, .T. ) ;
#171035=AXIS2_PLACEMENT_3D ( 'NONE', #240489, #197499, #97082 ) ;
#171041=FACE_OUTER_BOUND ( 'NONE', #43604, .T. ) ;
#171053=DIRECTION ( 'NONE',  ( 0.000000000000000000, -1.000000000000000000, 0.000000000000000000 ) ) ;
#171069=CIRCLE ( 'NONE', #179231, 0.1000000000000028644 ) ;
#171087=CARTESIAN_POINT ( 'NONE',  ( -18.40000000000000213, -9.499999999988849808, -73.92214984933045230 ) ) ;
#171093=VERTEX_POINT ( 'NONE', #55310 ) ;
#171098=CARTESIAN_POINT ( 'NONE',  ( -20.64999999999999858, 2.400000000011155432, -53.77537807723790309 ) ) ;
#171108=AXIS2_PLACEMENT_3D ( 'NONE', #256425, #116989, #196515 ) ;
#171125=VERTEX_POINT ( 'NONE', #198709 ) ;
#171139=ORIENTED_EDGE ( 'NONE', *, *, #21973, .T. ) ;
#171140=EDGE_CURVE ( 'NONE', #250359, #137736, #85362, .T. ) ;
#171157=DIRECTION ( 'NONE',  ( 0.000000000000000000, 0.000000000000000000, -1.000000000000000000 ) ) ;
#171169=CIRCLE ( 'NONE', #125333, 0.1000000000000017958 ) ;
#171170=VECTOR ( 'NONE', #168142, 1000.000000000000000 ) ;
#171179=ORIENTED_EDGE ( 'NONE', *, *, #187799, .F. ) ;
#171197=VERTEX_POINT ( 'NONE', #143861 ) ;
#171204=VECTOR ( 'NONE', #106118, 1000.000000000000114 ) ;
#171219=ORIENTED_EDGE ( 'NONE', *, *, #139760, .F. ) ;
#171237=LINE ( 'NONE', #116363, #246222 ) ;
#171250=AXIS2_PLACEMENT_3D ( 'NONE', #38887, #97522, #239642 ) ;
#171266=FACE_OUTER_BOUND ( 'NONE', #112174, .T. ) ;
#171275=DIRECTION ( 'NONE',  ( 0.000000000000000000, -1.000000000000000000, 0.000000000000000000 ) ) ;
#171281=CARTESIAN_POINT ( 'NONE',  ( 20.85000000000000142, 6.846123162363745074, -70.73772626684986164 ) ) ;
#171312=CARTESIAN_POINT ( 'NONE',  ( 23.15000000000000213, -9.499999999988848032, -43.39396912265245021 ) ) ;
#171318=CARTESIAN_POINT ( 'NONE',  ( -20.64999999999999858, 1.115600667400684642E-11, -33.50000000000000000 ) ) ;
#171320=CARTESIAN_POINT ( 'NONE',  ( 20.94999999999999574, 5.900000000011102586, -43.71909976465641989 ) ) ;
#171328=CARTESIAN_POINT ( 'NONE',  ( 21.07016717457011623, 1.115542603292150199E-11, -27.17905916189909377 ) ) ;
#171444=EDGE_CURVE ( 'NONE', #55352, #51091, #248107, .T. ) ;
#171459=AXIS2_PLACEMENT_3D ( 'NONE', #5703, #123121, #183100 ) ;
#171474=AXIS2_PLACEMENT_3D ( 'NONE', #226951, #45742, #47005 ) ;
#171490=DIRECTION ( 'NONE',  ( -0.000000000000000000, 0.000000000000000000, 1.000000000000000000 ) ) ;
#171496=ORIENTED_EDGE ( 'NONE', *, *, #150886, .F. ) ;
#171506=ORIENTED_EDGE ( 'NONE', *, *, #206753, .T. ) ;
#171525=VERTEX_POINT ( 'NONE', #15959 ) ;
#171553=CARTESIAN_POINT ( 'NONE',  ( 20.94999999999999929, 5.000000000011153745, -54.59473398108690390 ) ) ;
#171573=CARTESIAN_POINT ( 'NONE',  ( -18.59999999999999787, 11.65000000001115232, -54.85000000000000142 ) ) ;
#171609=CYLINDRICAL_SURFACE ( 'NONE', #153799, 0.09999999999999939493 ) ;
#171614=CARTESIAN_POINT ( 'NONE',  ( -23.15000000000000213, 1.115600667400684642E-11, -67.00000000000000000 ) ) ;
#171632=TOROIDAL_SURFACE ( 'NONE', #109043, 3.899999999999999467, 0.1000000000000000056 ) ;
#171688=ORIENTED_EDGE ( 'NONE', *, *, #207305, .F. ) ;
#171696=CARTESIAN_POINT ( 'NONE',  ( 20.85000000000000142, -1.835859311432481045, -78.50443916879852679 ) ) ;
#171698=EDGE_CURVE ( 'NONE', #247553, #28931, #244156, .T. ) ;
#171700=ORIENTED_EDGE ( 'NONE', *, *, #56023, .T. ) ;
#171716=CARTESIAN_POINT ( 'NONE',  ( 21.08376601933332495, 6.341947271286813681, -33.43622398907000104 ) ) ;
#171775=DIRECTION ( 'NONE',  ( -1.000000000000000000, 0.000000000000000000, -0.000000000000000000 ) ) ;
#171784=CYLINDRICAL_SURFACE ( 'NONE', #142850, 0.09999999999999939493 ) ;
#171795=AXIS2_PLACEMENT_3D ( 'NONE', #204177, #184624, #69838 ) ;
#171801=ORIENTED_EDGE ( 'NONE', *, *, #150339, .F. ) ;
#171811=ORIENTED_EDGE ( 'NONE', *, *, #11440, .F. ) ;
#171830=AXIS2_PLACEMENT_3D ( 'NONE', #187240, #145512, #226315 ) ;
#171844=EDGE_LOOP ( 'NONE', ( #120291, #183519, #129396, #221384 ) ) ;
#171914=AXIS2_PLACEMENT_3D ( 'NONE', #88547, #166861, #203391 ) ;
#171940=EDGE_CURVE ( 'NONE', #7325, #12615, #40393, .T. ) ;
#171955=ORIENTED_EDGE ( 'NONE', *, *, #249252, .T. ) ;
#172004=AXIS2_PLACEMENT_3D ( 'NONE', #69360, #68057, #207588 ) ;
#172008=ADVANCED_FACE ( 'NONE', ( #73073 ), #114728, .F. ) ;
#172014=CARTESIAN_POINT ( 'NONE',  ( 18.49999999999999645, 5.699452464332751767, -20.95772604343016710 ) ) ;
#172020=DIRECTION ( 'NONE',  ( 1.000000000000000000, 0.000000000000000000, 0.000000000000000000 ) ) ;
#172030=DIRECTION ( 'NONE',  ( 0.000000000000000000, 0.000000000000000000, -1.000000000000000000 ) ) ;
#172040=CARTESIAN_POINT ( 'NONE',  ( 18.50000000000000000, -9.499999999988842703, -40.53206939669966857 ) ) ;
#172073=ORIENTED_EDGE ( 'NONE', *, *, #107725, .F. ) ;
#172128=DIRECTION ( 'NONE',  ( 1.000000000000000000, -0.000000000000000000, 0.000000000000000000 ) ) ;
#172161=ORIENTED_EDGE ( 'NONE', *, *, #148768, .F. ) ;
#172171=CARTESIAN_POINT ( 'NONE',  ( -20.85000000000000142, 11.75000000001115197, -60.15839931010294350 ) ) ;
#172181=DIRECTION ( 'NONE',  ( 0.000000000000000000, 1.000000000000000000, 0.000000000000000000 ) ) ;
#172185=FACE_OUTER_BOUND ( 'NONE', #85498, .T. ) ;
#172218=CARTESIAN_POINT ( 'NONE',  ( 21.07928932188134397, 1.115600667400684642E-11, -33.50000000000000000 ) ) ;
#172247=AXIS2_PLACEMENT_3D ( 'NONE', #14458, #57386, #136941 ) ;
#172276=CARTESIAN_POINT ( 'NONE',  ( 18.59999999999998721, 19.85039924724470950, -35.78030305780136189 ) ) ;
#172280=CARTESIAN_POINT ( 'NONE',  ( -21.05000000000000071, -1.162701749926853712, -41.60000000000000142 ) ) ;
#172298=CIRCLE ( 'NONE', #51403, 0.6000000000000033085 ) ;
#172309=FACE_BOUND ( 'NONE', #122987, .T. ) ;
#172331=DIRECTION ( 'NONE',  ( 2.952720810173289112E-16, -1.000000000000000000, 0.000000000000000000 ) ) ;
#172339=AXIS2_PLACEMENT_3D ( 'NONE', #233506, #150121, #113537 ) ;
#172342=AXIS2_PLACEMENT_3D ( 'NONE', #204774, #242622, #26169 ) ;
#172383=EDGE_LOOP ( 'NONE', ( #49237, #222006, #53394, #171688 ) ) ;
#172419=DIRECTION ( 'NONE',  ( -3.265361837132813093E-16, 1.000000000000000000, 0.000000000000000000 ) ) ;
#172463=AXIS2_PLACEMENT_3D ( 'NONE', #161026, #1916, #237969 ) ;
#172481=DIRECTION ( 'NONE',  ( -0.000000000000000000, -0.000000000000000000, -1.000000000000000000 ) ) ;
#172501=EDGE_LOOP ( 'NONE', ( #235523, #190362, #10645, #55775 ) ) ;
#172508=DIRECTION ( 'NONE',  ( -0.000000000000000000, 0.000000000000000000, 1.000000000000000000 ) ) ;
#172543=CARTESIAN_POINT ( 'NONE',  ( 21.05000000000000071, 1.115600667400684642E-11, -33.50000000000000000 ) ) ;
#172551=EDGE_CURVE ( 'NONE', #54944, #110818, #94495, .T. ) ;
#172578=ORIENTED_EDGE ( 'NONE', *, *, #220377, .T. ) ;
#172605=DIRECTION ( 'NONE',  ( 1.000000000000000000, 2.952720810173289112E-16, -0.000000000000000000 ) ) ;
#172639=VERTEX_POINT ( 'NONE', #18540 ) ;
#172653=CARTESIAN_POINT ( 'NONE',  ( 21.05000000000000071, 6.413978881499668994, -33.58579911627400350 ) ) ;
#172716=ORIENTED_EDGE ( 'NONE', *, *, #103501, .T. ) ;
#172722=VERTEX_POINT ( 'NONE', #15997 ) ;
#172724=EDGE_CURVE ( 'NONE', #21983, #156407, #156703, .T. ) ;
#172729=FACE_OUTER_BOUND ( 'NONE', #248026, .T. ) ;
#172790=CARTESIAN_POINT ( 'NONE',  ( -23.15000000000000213, 1.115600667400684642E-11, -67.00000000000000000 ) ) ;
#172813=CARTESIAN_POINT ( 'NONE',  ( 21.05000000000000071, 10.68429367439828859, -41.02667393863730183 ) ) ;
#172819=DIRECTION ( 'NONE',  ( 1.000000000000000000, 0.000000000000000000, -0.000000000000000000 ) ) ;
#172836=VECTOR ( 'NONE', #134725, 1000.000000000000000 ) ;
#172845=CIRCLE ( 'NONE', #68744, 4.300000000000032685 ) ;
#172861=CARTESIAN_POINT ( 'NONE',  ( 19.97071067811864609, 11.72071067812981404, -54.85000000000000142 ) ) ;
#172890=CIRCLE ( 'NONE', #206166, 4.000000000000003553 ) ;
#172912=EDGE_CURVE ( 'NONE', #204996, #118577, #15035, .T. ) ;
#172915=AXIS2_PLACEMENT_3D ( 'NONE', #43773, #244530, #145428 ) ;
#172940=CARTESIAN_POINT ( 'NONE',  ( -23.15000000000000213, 4.350000000011156054, -54.85000000000000142 ) ) ;
#172958=CARTESIAN_POINT ( 'NONE',  ( -22.39999999999999503, 7.790779598384560245, -33.39999999999999858 ) ) ;
#172959=CARTESIAN_POINT ( 'NONE',  ( 19.80993210785492309, 11.75000000001021228, -58.26711774888664053 ) ) ;
#172962=LINE ( 'NONE', #33451, #185458 ) ;
#172969=FACE_OUTER_BOUND ( 'NONE', #99213, .T. ) ;
#172991=CARTESIAN_POINT ( 'NONE',  ( -21.04999999999999716, -0.08574093702224486191, -27.08617371118702977 ) ) ;
#173007=CIRCLE ( 'NONE', #114707, 0.5000000000000004441 ) ;
#173009=CARTESIAN_POINT ( 'NONE',  ( 18.59999999999999076, 5.950000000011100632, -43.80570230503486329 ) ) ;
#173010=ORIENTED_EDGE ( 'NONE', *, *, #161338, .T. ) ;
#173018=VERTEX_POINT ( 'NONE', #220220 ) ;
#173035=VERTEX_POINT ( 'NONE', #61131 ) ;
#173039=CARTESIAN_POINT ( 'NONE',  ( 18.59999999999999432, 1.162701749949165642, -41.60000000000000142 ) ) ;
#173045=CARTESIAN_POINT ( 'NONE',  ( -21.05000000000000071, -1.162701749926853712, -41.50000000000000000 ) ) ;
#173075=ORIENTED_EDGE ( 'NONE', *, *, #242793, .T. ) ;
#173076=ORIENTED_EDGE ( 'NONE', *, *, #253432, .F. ) ;
#173116=DIRECTION ( 'NONE',  ( -0.000000000000000000, -0.4791956752371546169, -0.8777080977375152360 ) ) ;
#173118=CARTESIAN_POINT ( 'NONE',  ( -20.64999999999999858, 1.115600667400684642E-11, -54.12500000000000711 ) ) ;
#173119=ORIENTED_EDGE ( 'NONE', *, *, #83640, .T. ) ;
#173121=( NAMED_UNIT ( * ) PLANE_ANGLE_UNIT ( ) SI_UNIT ( $, .RADIAN. ) );
#173125=ORIENTED_EDGE ( 'NONE', *, *, #169525, .F. ) ;
#173130=AXIS2_PLACEMENT_3D ( 'NONE', #171614, #72497, #174191 ) ;
#173132=CARTESIAN_POINT ( 'NONE',  ( -21.05000000000000071, 5.900000000011102586, -43.71909976465641989 ) ) ;
#173134=CARTESIAN_POINT ( 'NONE',  ( -20.54999999999999716, 1.115600667400684642E-11, -67.00000000000000000 ) ) ;
#173171=CIRCLE ( 'NONE', #73197, 0.1000000000000000472 ) ;
#173217=AXIS2_PLACEMENT_3D ( 'NONE', #1530, #122797, #22416 ) ;
#173220=DIRECTION ( 'NONE',  ( 1.000000000000000000, 0.000000000000000000, -0.000000000000000000 ) ) ;
#173271=ORIENTED_EDGE ( 'NONE', *, *, #169441, .F. ) ;
#173309=EDGE_CURVE ( 'NONE', #141325, #165624, #252510, .T. ) ;
#173313=ORIENTED_EDGE ( 'NONE', *, *, #45882, .F. ) ;
#173314=DIRECTION ( 'NONE',  ( 0.000000000000000000, 0.000000000000000000, -1.000000000000000000 ) ) ;
#173317=EDGE_CURVE ( 'NONE', #7520, #87561, #98619, .T. ) ;
#173321=VERTEX_POINT ( 'NONE', #235595 ) ;
#173324=EDGE_CURVE ( 'NONE', #171093, #121226, #240067, .T. ) ;
#173326=FACE_OUTER_BOUND ( 'NONE', #123970, .T. ) ;
#173361=CARTESIAN_POINT ( 'NONE',  ( -23.25000000000000000, -8.999999999988844479, -57.10603087734755690 ) ) ;
#173387=AXIS2_PLACEMENT_3D ( 'NONE', #2044, #234242, #116876 ) ;
#173389=VERTEX_POINT ( 'NONE', #139033 ) ;
#173401=AXIS2_PLACEMENT_3D ( 'NONE', #37337, #25475, #162420 ) ;
#173409=ORIENTED_EDGE ( 'NONE', *, *, #81930, .F. ) ;
#173433=TOROIDAL_SURFACE ( 'NONE', #210975, 0.2000000000000000111, 0.1000000000000000056 ) ;
#173437=CARTESIAN_POINT ( 'NONE',  ( 23.14999999999999858, 1.115600667400684642E-11, -67.00000000000000000 ) ) ;
#173447=ORIENTED_EDGE ( 'NONE', *, *, #112126, .T. ) ;
#173454=CARTESIAN_POINT ( 'NONE',  ( -22.49533356619860314, 11.65000000631534149, -33.43487741967728510 ) ) ;
#173464=AXIS2_PLACEMENT_3D ( 'NONE', #48379, #228320, #163214 ) ;
#173479=CARTESIAN_POINT ( 'NONE',  ( -22.00411653962166980, 7.253442868381237751, -33.40096189421771555 ) ) ;
#173520=DIRECTION ( 'NONE',  ( 1.000000000000000000, 7.304098846218134667E-16, -0.000000000000000000 ) ) ;
#173533=AXIS2_PLACEMENT_3D ( 'NONE', #83329, #189842, #90725 ) ;
#173548=CARTESIAN_POINT ( 'NONE',  ( 23.14999999999998792, 11.65000000001115588, -33.50000000000000000 ) ) ;
#173553=EDGE_CURVE ( 'NONE', #179315, #200421, #189754, .T. ) ;
#173567=AXIS2_PLACEMENT_3D ( 'NONE', #111654, #35988, #54236 ) ;
#173569=FACE_OUTER_BOUND ( 'NONE', #100711, .T. ) ;
#173574=DIRECTION ( 'NONE',  ( 0.000000000000000000, 0.000000000000000000, -1.000000000000000000 ) ) ;
#173588=CARTESIAN_POINT ( 'NONE',  ( 18.56579813702275317, 10.33025634372637924, -72.58709292826388548 ) ) ;
#173620=FACE_OUTER_BOUND ( 'NONE', #127983, .T. ) ;
#173631=CARTESIAN_POINT ( 'NONE',  ( -23.15000000000000213, -8.999999999988846255, -43.39396912265245021 ) ) ;
#173644=ADVANCED_FACE ( 'NONE', ( #56620 ), #81992, .F. ) ;
#173667=( BOUNDED_SURFACE ( )  B_SPLINE_SURFACE ( 3, 2, ( 
 ( #55493, #13845, #175506 ),
 ( #132507, #172959, #15134 ),
 ( #71270, #191225, #195069 ),
 ( #174244, #16431, #33447 ),
 ( #154666, #93368, #112948 ),
 ( #155948, #131213, #150783 ) ),
 .UNSPECIFIED., .F., .F., .T. ) 
 B_SPLINE_SURFACE_WITH_KNOTS ( ( 4, 2, 4 ),
 ( 3, 3 ),
 ( 4.712388980384689674, 5.497787143782137953, 6.283185307179586232 ),
 ( 0.000000000000000000, 1.000000000000000000 ),
 .UNSPECIFIED. ) 
 GEOMETRIC_REPRESENTATION_ITEM ( )  RATIONAL_B_SPLINE_SURFACE ( (
 ( 1.000000000000000000, 0.7071067811865536790, 1.000000000000000000),
 ( 1.000000000000000000, 0.7727932973488890189, 1.000000000000000000),
 ( 1.000000000000000000, 0.8282379607652868847, 1.000000000000000000),
 ( 1.000000000000000000, 0.9038128468036029650, 1.000000000000000000),
 ( 1.000000000000000000, 0.9240297172246195734, 1.000000000000000000),
 ( 1.000000000000000000, 0.9238795325112914014, 1.000000000000000000) ) ) 
 REPRESENTATION_ITEM ( '' )  SURFACE ( )  );
#173758=DIRECTION ( 'NONE',  ( 0.000000000000000000, -1.000000000000000000, 0.000000000000000000 ) ) ;
#173765=CARTESIAN_POINT ( 'NONE',  ( -23.15000000000000213, -9.499999999988848032, -43.39396912265245021 ) ) ;
#173777=DIRECTION ( 'NONE',  ( -1.000000000000000000, -0.000000000000000000, -0.000000000000000000 ) ) ;
#173781=CARTESIAN_POINT ( 'NONE',  ( 18.49999999999999289, 6.846123162363745074, -70.73772626684986164 ) ) ;
#173829=ORIENTED_EDGE ( 'NONE', *, *, #183240, .T. ) ;
#173841=VECTOR ( 'NONE', #117759, 1000.000000000000000 ) ;
#173855=DIRECTION ( 'NONE',  ( -0.000000000000000000, 0.000000000000000000, 1.000000000000000000 ) ) ;
#173861=ORIENTED_EDGE ( 'NONE', *, *, #65097, .F. ) ;
#173877=CARTESIAN_POINT ( 'NONE',  ( -21.05000000000000071, 1.162701749949165642, -41.50000000000000000 ) ) ;
#173887=ADVANCED_FACE ( 'NONE', ( #33967 ), #14384, .F. ) ;
#173896=LINE ( 'NONE', #132151, #221826 ) ;
#173915=AXIS2_PLACEMENT_3D ( 'NONE', #250139, #145885, #7685 ) ;
#173918=CARTESIAN_POINT ( 'NONE',  ( 20.93284271247462414, 11.75000000001116085, -59.98519422934605672 ) ) ;
#173955=CARTESIAN_POINT ( 'NONE',  ( 23.25000000000000000, -11.64999999998884483, -33.50000000000000000 ) ) ;
#173959=ADVANCED_FACE ( 'NONE', ( #237259 ), #3774, .T. ) ;
#173963=ORIENTED_EDGE ( 'NONE', *, *, #90233, .F. ) ;
#174000=CIRCLE ( 'NONE', #228131, 0.09999999999999939493 ) ;
#174021=CARTESIAN_POINT ( 'NONE',  ( -23.25000000000000000, 6.982009704867601307, -70.69615211825629331 ) ) ;
#174030=DIRECTION ( 'NONE',  ( -2.952720810173288619E-16, 1.000000000000000000, 0.000000000000000000 ) ) ;
#174037=EDGE_CURVE ( 'NONE', #51264, #19031, #220274, .T. ) ;
#174054=CARTESIAN_POINT ( 'NONE',  ( -21.14999999999999858, 11.65000000001115588, -33.50000000000000000 ) ) ;
#174060=ORIENTED_EDGE ( 'NONE', *, *, #152309, .T. ) ;
#174113=CARTESIAN_POINT ( 'NONE',  ( -23.15000000000000213, 4.350000000011156054, -54.64999999999999858 ) ) ;
#174114=CARTESIAN_POINT ( 'NONE',  ( -18.39999999999999858, -9.399999999988850163, -21.75000000000000355 ) ) ;
#174147=FACE_OUTER_BOUND ( 'NONE', #256044, .T. ) ;
#174178=ORIENTED_EDGE ( 'NONE', *, *, #147656, .F. ) ;
#174191=DIRECTION ( 'NONE',  ( 0.000000000000000000, 0.000000000000000000, -1.000000000000000000 ) ) ;
#174225=CARTESIAN_POINT ( 'NONE',  ( -20.54999999999999716, 7.150000000011155876, -50.25000000000000000 ) ) ;
#174230=ORIENTED_EDGE ( 'NONE', *, *, #86956, .F. ) ;
#174242=EDGE_CURVE ( 'NONE', #67087, #134912, #165614, .T. ) ;
#174244=CARTESIAN_POINT ( 'NONE',  ( 19.94784844284962944, 11.71308993304009682, -58.20219871729849359 ) ) ;
#174253=VECTOR ( 'NONE', #18673, 999.9999999999998863 ) ;
#174275=EDGE_CURVE ( 'NONE', #131987, #109174, #107327, .T. ) ;
#174315=AXIS2_PLACEMENT_3D ( 'NONE', #176026, #76887, #53488 ) ;
#174321=CARTESIAN_POINT ( 'NONE',  ( 18.49999999999999645, 1.115600667400684642E-11, -33.50000000000000000 ) ) ;
#174323=ORIENTED_EDGE ( 'NONE', *, *, #38468, .T. ) ;
#174324=CARTESIAN_POINT ( 'NONE',  ( 18.59999999999999787, -1.835341550213255957, -45.15515129256298366 ) ) ;
#174368=ORIENTED_EDGE ( 'NONE', *, *, #127975, .F. ) ;
#174471=EDGE_CURVE ( 'NONE', #122271, #181631, #10017, .T. ) ;
#174504=ADVANCED_FACE ( 'NONE', ( #242064 ), #157443, .T. ) ;
#174521=DIRECTION ( 'NONE',  ( 1.000000000000000000, 0.000000000000000000, 0.000000000000000000 ) ) ;
#174524=CARTESIAN_POINT ( 'NONE',  ( -18.59999999999999787, 1.835341550235567887, -45.15515129256298366 ) ) ;
#174563=PLANE ( 'NONE',  #146875 ) ;
#174608=AXIS2_PLACEMENT_3D ( 'NONE', #89022, #126882, #249406 ) ;
#174613=DIRECTION ( 'NONE',  ( 0.7071067811865388020, -0.7071067811865561215, 0.000000000000000000 ) ) ;
#174620=DIRECTION ( 'NONE',  ( 0.000000000000000000, 0.000000000000000000, 1.000000000000000000 ) ) ;
#174628=ORIENTED_EDGE ( 'NONE', *, *, #249421, .T. ) ;
#174643=DIRECTION ( 'NONE',  ( 0.000000000000000000, 2.891205793294679805E-16, -1.000000000000000000 ) ) ;
#174692=ORIENTED_EDGE ( 'NONE', *, *, #148433, .F. ) ;
#174698=ORIENTED_EDGE ( 'NONE', *, *, #150400, .F. ) ;
#174723=ORIENTED_EDGE ( 'NONE', *, *, #38838, .T. ) ;
#174727=DIRECTION ( 'NONE',  ( -0.000000000000000000, 0.000000000000000000, 1.000000000000000000 ) ) ;
#174732=DIRECTION ( 'NONE',  ( 0.000000000000000000, -1.000000000000000000, 0.000000000000000000 ) ) ;
#174735=ORIENTED_EDGE ( 'NONE', *, *, #146295, .T. ) ;
#174776=CARTESIAN_POINT ( 'NONE',  ( 22.49806830649814060, 0.07746431633666321648, -21.85011034516092465 ) ) ;
#174796=VERTEX_POINT ( 'NONE', #16318 ) ;
#174806=EDGE_CURVE ( 'NONE', #76854, #186448, #82534, .T. ) ;
#174867=CARTESIAN_POINT ( 'NONE',  ( -21.55000000000000426, 7.750000000011159074, -54.65000000000000568 ) ) ;
#174869=DIRECTION ( 'NONE',  ( -1.000000000000000000, -2.952720810173289112E-16, 0.000000000000000000 ) ) ;
#174881=FACE_OUTER_BOUND ( 'NONE', #122860, .T. ) ;
#174885=AXIS2_PLACEMENT_3D ( 'NONE', #157763, #79435, #76876 ) ;
#174899=CARTESIAN_POINT ( 'NONE',  ( -21.30740335185486245, 0.09893452578700702438, -26.94334207797199809 ) ) ;
#174900=CARTESIAN_POINT ( 'NONE',  ( 18.36493879433266940, -9.500000806178647395, -73.92214866035172349 ) ) ;
#174911=ORIENTED_EDGE ( 'NONE', *, *, #54084, .F. ) ;
#174943=AXIS2_PLACEMENT_3D ( 'NONE', #103736, #142865, #205419 ) ;
#174948=ORIENTED_EDGE ( 'NONE', *, *, #50445, .T. ) ;
#174964=EDGE_CURVE ( 'NONE', #163061, #14704, #27886, .T. ) ;
#175013=DIRECTION ( 'NONE',  ( -1.000000000000000000, 0.000000000000000000, 0.000000000000000000 ) ) ;
#175037=ORIENTED_EDGE ( 'NONE', *, *, #196329, .T. ) ;
#175050=CARTESIAN_POINT ( 'NONE',  ( -20.64999999999999858, 2.500000000011154633, -53.77537807723790309 ) ) ;
#175053=CARTESIAN_POINT ( 'NONE',  ( 23.24999999999999645, 1.115600667400684642E-11, -67.00000000000000000 ) ) ;
#175074=ORIENTED_EDGE ( 'NONE', *, *, #48403, .T. ) ;
#175077=FACE_OUTER_BOUND ( 'NONE', #139941, .T. ) ;
#175106=DIRECTION ( 'NONE',  ( 1.000000000000000000, -0.000000000000000000, -0.000000000000000000 ) ) ;
#175111=ORIENTED_EDGE ( 'NONE', *, *, #234695, .F. ) ;
#175132=FACE_OUTER_BOUND ( 'NONE', #67514, .T. ) ;
#175135=ORIENTED_EDGE ( 'NONE', *, *, #107365, .T. ) ;
#175166=ORIENTED_EDGE ( 'NONE', *, *, #197098, .F. ) ;
#175216=CARTESIAN_POINT ( 'NONE',  ( -20.54999999999999716, 7.150000000011155876, -54.65000000000000568 ) ) ;
#175229=ORIENTED_EDGE ( 'NONE', *, *, #109988, .T. ) ;
#175266=ORIENTED_EDGE ( 'NONE', *, *, #104062, .F. ) ;
#175338=CIRCLE ( 'NONE', #212739, 0.09999999999999939493 ) ;
#175347=AXIS2_PLACEMENT_3D ( 'NONE', #22101, #220300, #182459 ) ;
#175354=CARTESIAN_POINT ( 'NONE',  ( -21.45000000000000284, 7.708578643773852157, -45.85000000000000142 ) ) ;
#175399=FACE_OUTER_BOUND ( 'NONE', #8750, .T. ) ;
#175415=DIRECTION ( 'NONE',  ( 0.000000000000000000, 1.000000000000000000, -6.308085367188393199E-16 ) ) ;
#175420=FACE_OUTER_BOUND ( 'NONE', #159713, .T. ) ;
#175461=ORIENTED_EDGE ( 'NONE', *, *, #203124, .F. ) ;
#175464=ADVANCED_FACE ( 'NONE', ( #179591 ), #87197, .T. ) ;
#175466=EDGE_CURVE ( 'NONE', #147427, #136008, #218677, .T. ) ;
#175472=CARTESIAN_POINT ( 'NONE',  ( 20.95263205890719149, 8.895740107905213634, -41.98950840694161712 ) ) ;
#175479=CARTESIAN_POINT ( 'NONE',  ( -21.05000000000000071, -1.162701749926853712, -41.40000000000000568 ) ) ;
#175502=FACE_OUTER_BOUND ( 'NONE', #227582, .T. ) ;
#175506=CARTESIAN_POINT ( 'NONE',  ( 19.75857864376269291, 11.75000000001116263, -58.35000000000000853 ) ) ;
#175511=EDGE_CURVE ( 'NONE', #203548, #179043, #205534, .T. ) ;
#175522=AXIS2_PLACEMENT_3D ( 'NONE', #17585, #116696, #137529 ) ;
#175533=EDGE_CURVE ( 'NONE', #116556, #204714, #106421, .T. ) ;
#175576=CARTESIAN_POINT ( 'NONE',  ( -18.39999999999999858, -9.499999999988849808, -73.60018939122203108 ) ) ;
#175589=CARTESIAN_POINT ( 'NONE',  ( 18.46858270002953262, -9.474202674699412796, -40.60202193470386334 ) ) ;
#175615=EDGE_LOOP ( 'NONE', ( #156841, #174735, #14284 ) ) ;
#175662=AXIS2_PLACEMENT_3D ( 'NONE', #51075, #250591, #193212 ) ;
#175684=EDGE_CURVE ( 'NONE', #12615, #194376, #112873, .T. ) ;
#175716=CARTESIAN_POINT ( 'NONE',  ( 20.94999999999999574, -1.249999999988843369, -41.50000000000000000 ) ) ;
#175723=DIRECTION ( 'NONE',  ( 0.000000000000000000, 1.000000000000000000, 0.000000000000000000 ) ) ;
#175729=AXIS2_PLACEMENT_3D ( 'NONE', #58310, #33690, #97426 ) ;
#175730=CARTESIAN_POINT ( 'NONE',  ( -23.15000000000000213, -11.64999999998884483, -21.75000000000000355 ) ) ;
#175736=DIRECTION ( 'NONE',  ( 0.000000000000000000, 0.000000000000000000, 1.000000000000000000 ) ) ;
#175773=LINE ( 'NONE', #111948, #189356 ) ;
#175783=AXIS2_PLACEMENT_3D ( 'NONE', #143984, #5744, #226072 ) ;
#175792=DIRECTION ( 'NONE',  ( -1.000000000000000000, -2.952720810173289112E-16, 0.000000000000000000 ) ) ;
#175798=CARTESIAN_POINT ( 'NONE',  ( -18.44362607810620602, -9.490496158073668198, -40.55795386684712156 ) ) ;
#175827=EDGE_CURVE ( 'NONE', #127487, #22210, #145255, .T. ) ;
#175831=VERTEX_POINT ( 'NONE', #104820 ) ;
#175858=ORIENTED_EDGE ( 'NONE', *, *, #180196, .T. ) ;
#175893=ORIENTED_EDGE ( 'NONE', *, *, #129478, .F. ) ;
#175901=EDGE_CURVE ( 'NONE', #131047, #192117, #167431, .T. ) ;
#175980=EDGE_CURVE ( 'NONE', #2240, #65925, #130842, .T. ) ;
#175984=DIRECTION ( 'NONE',  ( -1.000000000000000000, 7.304098846218134667E-16, -4.217023435051678980E-16 ) ) ;
#175992=ORIENTED_EDGE ( 'NONE', *, *, #94177, .F. ) ;
#176026=CARTESIAN_POINT ( 'NONE',  ( 20.85000000000000142, 1.115600667400684642E-11, -67.00000000000000000 ) ) ;
#176037=AXIS2_PLACEMENT_3D ( 'NONE', #130373, #110813, #11746 ) ;
#176043=CARTESIAN_POINT ( 'NONE',  ( -21.05000000000000426, 11.60000000001115872, -40.42820323027555673 ) ) ;
#176046=VECTOR ( 'NONE', #130996, 1000.000000000000000 ) ;
#176048=EDGE_CURVE ( 'NONE', #224583, #135153, #248230, .T. ) ;
#176089=AXIS2_PLACEMENT_3D ( 'NONE', #154291, #53859, #176393 ) ;
#176103=ORIENTED_EDGE ( 'NONE', *, *, #219501, .T. ) ;
#176115=VECTOR ( 'NONE', #107627, 1000.000000000000000 ) ;
#176122=FACE_OUTER_BOUND ( 'NONE', #27156, .T. ) ;
#176123=CARTESIAN_POINT ( 'NONE',  ( -22.39999999999999503, 1.115541036281197940E-11, -25.70922040162659883 ) ) ;
#176140=DIRECTION ( 'NONE',  ( 0.000000000000000000, 0.9998779222360096863, -0.01562500000001061998 ) ) ;
#176148=DIRECTION ( 'NONE',  ( 0.000000000000000000, 1.000000000000000000, -1.224646799147353207E-16 ) ) ;
#176152=CARTESIAN_POINT ( 'NONE',  ( 20.94999999999999929, 1.115600667400684642E-11, -67.00000000000000000 ) ) ;
#176164=AXIS2_PLACEMENT_3D ( 'NONE', #95476, #172508, #73388 ) ;
#176174=ORIENTED_EDGE ( 'NONE', *, *, #97391, .F. ) ;
#176210=DIRECTION ( 'NONE',  ( 1.000000000000000000, 3.265361837132813093E-16, -0.000000000000000000 ) ) ;
#176215=CYLINDRICAL_SURFACE ( 'NONE', #16459, 0.09999999999999939493 ) ;
#176221=SPHERICAL_SURFACE ( 'NONE', #239570, 0.1000000000000000056 ) ;
#176222=ORIENTED_EDGE ( 'NONE', *, *, #145605, .T. ) ;
#176243=VERTEX_POINT ( 'NONE', #176919 ) ;
#176261=ORIENTED_EDGE ( 'NONE', *, *, #250772, .F. ) ;
#176262=EDGE_CURVE ( 'NONE', #79923, #176243, #119495, .T. ) ;
#176296=EDGE_CURVE ( 'NONE', #133079, #72361, #158352, .T. ) ;
#176297=CARTESIAN_POINT ( 'NONE',  ( 18.44444291854883033, -9.490101180932070335, -73.62890396489098066 ) ) ;
#176305=PLANE ( 'NONE',  #16348 ) ;
#176313=CARTESIAN_POINT ( 'NONE',  ( -21.07928932188134041, 1.115600667400684642E-11, -33.50000000000000000 ) ) ;
#176315=CARTESIAN_POINT ( 'NONE',  ( -21.37071067811865532, 8.070710678129811910, -54.65000000000000568 ) ) ;
#176371=EDGE_CURVE ( 'NONE', #216334, #201073, #33457, .T. ) ;
#176387=CARTESIAN_POINT ( 'NONE',  ( -23.25000000000000000, -9.682403433465239573, -73.65684337741279819 ) ) ;
#176393=DIRECTION ( 'NONE',  ( 0.000000000000000000, 0.000000000000000000, -1.000000000000000000 ) ) ;
#176405=ORIENTED_EDGE ( 'NONE', *, *, #90568, .F. ) ;
#176416=AXIS2_PLACEMENT_3D ( 'NONE', #69451, #246769, #130680 ) ;
#176430=CARTESIAN_POINT ( 'NONE',  ( 23.15000000000000213, -11.64999999998883595, -63.89999999999999858 ) ) ;
#176431=CARTESIAN_POINT ( 'NONE',  ( 23.14999999999999858, 5.600000000011153389, -54.59473398108690390 ) ) ;
#176532=ADVANCED_FACE ( 'NONE', ( #189730 ), #149340, .T. ) ;
#176539=ORIENTED_EDGE ( 'NONE', *, *, #21799, .F. ) ;
#176568=DIRECTION ( 'NONE',  ( 0.000000000000000000, -0.000000000000000000, 1.000000000000000000 ) ) ;
#176584=CARTESIAN_POINT ( 'NONE',  ( 18.50000000000000000, -9.499999999988842703, -21.75000000000000355 ) ) ;
#176598=ADVANCED_FACE ( 'NONE', ( #18481, #30680 ), #254489, .T. ) ;
#176628=CARTESIAN_POINT ( 'NONE',  ( -23.25000000000000000, -1.835859311432481045, -78.50443916879852679 ) ) ;
#176670=ADVANCED_FACE ( 'NONE', ( #120190 ), #62747, .T. ) ;
#176675=AXIS2_PLACEMENT_3D ( 'NONE', #42658, #20558, #122208 ) ;
#176688=EDGE_LOOP ( 'NONE', ( #96083, #99622, #178400 ) ) ;
#176721=CARTESIAN_POINT ( 'NONE',  ( -21.05000000000000071, -0.02110330804785487402, -27.19548367073597461 ) ) ;
#176723=FACE_OUTER_BOUND ( 'NONE', #217310, .T. ) ;
#176724=ORIENTED_EDGE ( 'NONE', *, *, #90568, .T. ) ;
#176776=ADVANCED_FACE ( 'NONE', ( #91300 ), #254772, .T. ) ;
#176823=ADVANCED_FACE ( 'NONE', ( #105687 ), #38191, .T. ) ;
#176829=ADVANCED_FACE ( 'NONE', ( #70486 ), #165717, .F. ) ;
#176874=LINE ( 'NONE', #257604, #144091 ) ;
#176891=VERTEX_POINT ( 'NONE', #136828 ) ;
#176919=CARTESIAN_POINT ( 'NONE',  ( 21.05000000000000071, -11.64999999998883595, -64.00000000000000000 ) ) ;
#176948=EDGE_LOOP ( 'NONE', ( #183285, #187056, #234620, #102822 ) ) ;
#176998=DIRECTION ( 'NONE',  ( 0.000000000000000000, 0.6728971962616697722, 0.7397360091702875895 ) ) ;
#177005=EDGE_LOOP ( 'NONE', ( #256342, #103275, #97147, #230859 ) ) ;
#177029=ORIENTED_EDGE ( 'NONE', *, *, #143030, .F. ) ;
#177054=DIRECTION ( 'NONE',  ( 0.000000000000000000, -2.168404344970984413E-15, -1.000000000000000000 ) ) ;
#177060=CARTESIAN_POINT ( 'NONE',  ( 20.41140022480507454, 10.41043084241319683, -41.11500130363457117 ) ) ;
#177140=AXIS2_PLACEMENT_3D ( 'NONE', #167216, #104600, #146320 ) ;
#177146=ADVANCED_FACE ( 'NONE', ( #164114 ), #150971, .F. ) ;
#177201=DIRECTION ( 'NONE',  ( -1.000000000000000000, -0.000000000000000000, -0.000000000000000000 ) ) ;
#177227=ORIENTED_EDGE ( 'NONE', *, *, #163174, .T. ) ;
#177254=ORIENTED_EDGE ( 'NONE', *, *, #103779, .T. ) ;
#177275=FACE_OUTER_BOUND ( 'NONE', #181191, .T. ) ;
#177289=CARTESIAN_POINT ( 'NONE',  ( 21.05000000000000071, 5.850000000011105428, -43.63249722427796939 ) ) ;
#177298=ORIENTED_EDGE ( 'NONE', *, *, #227507, .T. ) ;
#177331=CARTESIAN_POINT ( 'NONE',  ( 22.44352723754029810, 0.009277095054436624438, -21.85027865465129437 ) ) ;
#177337=FACE_OUTER_BOUND ( 'NONE', #210881, .T. ) ;
#177338=VERTEX_POINT ( 'NONE', #242039 ) ;
#177348=PRODUCT_CONTEXT ( 'NONE', #190631, 'mechanical' ) ;
#177359=CARTESIAN_POINT ( 'NONE',  ( 21.05281448260627641, 8.776010158548784190, -45.67355791181142166 ) ) ;
#177392=ORIENTED_EDGE ( 'NONE', *, *, #245653, .F. ) ;
#177397=CARTESIAN_POINT ( 'NONE',  ( 21.05000000000000071, -0.09999999998884338825, -26.95934304829875927 ) ) ;
#177404=ORIENTED_EDGE ( 'NONE', *, *, #157665, .T. ) ;
#177413=CARTESIAN_POINT ( 'NONE',  ( -21.53699400385237794, 1.034126895667923527E-11, -26.71228820676542526 ) ) ;
#177444=CARTESIAN_POINT ( 'NONE',  ( -21.08198257630413508, 0.07264332379574613141, -27.16340326598493604 ) ) ;
#177454=DIRECTION ( 'NONE',  ( -1.000000000000000000, 0.000000000000000000, 0.000000000000000000 ) ) ;
#177457=ADVANCED_FACE ( 'NONE', ( #67257 ), #47674, .T. ) ;
#177486=AXIS2_PLACEMENT_3D ( 'NONE', #81547, #21619, #161127 ) ;
#177513=ORIENTED_EDGE ( 'NONE', *, *, #218457, .T. ) ;
#177516=CIRCLE ( 'NONE', #252283, 3.900000000000000799 ) ;
#177526=CIRCLE ( 'NONE', #123321, 0.1000000000000028644 ) ;
#177537=VERTEX_POINT ( 'NONE', #30732 ) ;
#177545=ORIENTED_EDGE ( 'NONE', *, *, #168214, .F. ) ;
#177554=ADVANCED_FACE ( 'NONE', ( #210619 ), #61429, .T. ) ;
#177570=CARTESIAN_POINT ( 'NONE',  ( -20.54999999999999716, 1.925233644870972816, -46.23024353312612789 ) ) ;
#177582=ORIENTED_EDGE ( 'NONE', *, *, #166259, .T. ) ;
#177604=ORIENTED_EDGE ( 'NONE', *, *, #209430, .F. ) ;
#177653=ORIENTED_EDGE ( 'NONE', *, *, #95664, .T. ) ;
#177696=CIRCLE ( 'NONE', #181752, 12.77500000000000036 ) ;
#177710=AXIS2_PLACEMENT_3D ( 'NONE', #19547, #8958, #226706 ) ;
#177718=ORIENTED_EDGE ( 'NONE', *, *, #41232, .T. ) ;
#177724=DIRECTION ( 'NONE',  ( 0.000000000000000000, 0.000000000000000000, 1.000000000000000000 ) ) ;
#177741=ORIENTED_EDGE ( 'NONE', *, *, #8687, .F. ) ;
#177747=VECTOR ( 'NONE', #13710, 1000.000000000000000 ) ;
#177754=EDGE_CURVE ( 'NONE', #86704, #182014, #161009, .T. ) ;
#177776=DIRECTION ( 'NONE',  ( 1.000000000000000000, 2.952720810173289112E-16, -0.000000000000000000 ) ) ;
#177787=DIRECTION ( 'NONE',  ( -1.000000000000000000, 0.000000000000000000, 0.000000000000000000 ) ) ;
#177808=EDGE_CURVE ( 'NONE', #207476, #147427, #76229, .T. ) ;
#177830=CIRCLE ( 'NONE', #231992, 0.09999999999999939493 ) ;
#177834=ORIENTED_EDGE ( 'NONE', *, *, #120212, .T. ) ;
#177844=ORIENTED_EDGE ( 'NONE', *, *, #167238, .T. ) ;
#177851=CIRCLE ( 'NONE', #148814, 0.09999999999999781286 ) ;
#177853=CARTESIAN_POINT ( 'NONE',  ( -23.15000000000000213, -11.74999999998884448, -33.50000000000000000 ) ) ;
#177867=AXIS2_PLACEMENT_3D ( 'NONE', #130379, #30035, #89964 ) ;
#177868=PLANE ( 'NONE',  #11326 ) ;
#177892=CARTESIAN_POINT ( 'NONE',  ( -21.00857864376268935, 11.60000000001115161, -40.42820323027555673 ) ) ;
#177903=ORIENTED_EDGE ( 'NONE', *, *, #235673, .T. ) ;
#177961=PLANE ( 'NONE',  #171035 ) ;
#177980=CIRCLE ( 'NONE', #186354, 0.1999999999999987899 ) ;
#178007=CARTESIAN_POINT ( 'NONE',  ( -21.05000000000000071, 0.01485563490482383515, -27.15564095795645727 ) ) ;
#178012=EDGE_CURVE ( 'NONE', #88661, #254615, #23665, .T. ) ;
#178023=VERTEX_POINT ( 'NONE', #209033 ) ;
#178029=DIRECTION ( 'NONE',  ( 1.000000000000000000, 0.000000000000000000, -0.000000000000000000 ) ) ;
#178034=AXIS2_PLACEMENT_3D ( 'NONE', #22567, #79917, #219449 ) ;
#178042=AXIS2_PLACEMENT_3D ( 'NONE', #23275, #124922, #127479 ) ;
#178065=DIRECTION ( 'NONE',  ( 0.000000000000000000, 0.1575844902526835067, 0.9875055080513738259 ) ) ;
#178086=EDGE_CURVE ( 'NONE', #171525, #55518, #198587, .T. ) ;
#178129=DIRECTION ( 'NONE',  ( 1.000000000000000000, 3.265361837132813093E-16, -0.000000000000000000 ) ) ;
#178166=CARTESIAN_POINT ( 'NONE',  ( 18.44364597020196328, -9.490487317151108826, -40.55797788968387607 ) ) ;
#178176=ORIENTED_EDGE ( 'NONE', *, *, #3827, .T. ) ;
#178185=ORIENTED_EDGE ( 'NONE', *, *, #216023, .T. ) ;
#178209=CARTESIAN_POINT ( 'NONE',  ( 20.99551997958364424, 11.75000000001111644, -60.15165913768996120 ) ) ;
#178223=ORIENTED_EDGE ( 'NONE', *, *, #253778, .T. ) ;
#178227=AXIS2_PLACEMENT_3D ( 'NONE', #142818, #67162, #146668 ) ;
#178278=CIRCLE ( 'NONE', #99112, 4.049999999999998046 ) ;
#178291=FACE_OUTER_BOUND ( 'NONE', #20113, .T. ) ;
#178343=CARTESIAN_POINT ( 'NONE',  ( 20.12518398540832365, 9.975088720679844201, -41.49666825246991664 ) ) ;
#178361=CARTESIAN_POINT ( 'NONE',  ( -20.64999999999999858, 7.250000000011155521, -54.65000000000000568 ) ) ;
#178373=ORIENTED_EDGE ( 'NONE', *, *, #175684, .T. ) ;
#178382=FACE_OUTER_BOUND ( 'NONE', #254525, .T. ) ;
#178400=ORIENTED_EDGE ( 'NONE', *, *, #228940, .F. ) ;
#178427=EDGE_CURVE ( 'NONE', #15533, #1348, #252937, .T. ) ;
#178450=ADVANCED_FACE ( 'NONE', ( #178291 ), #82973, .T. ) ;
#178464=CIRCLE ( 'NONE', #82722, 0.1000000000000000472 ) ;
#178466=CARTESIAN_POINT ( 'NONE',  ( -23.25000000000000000, 11.65000000001115588, -33.50000000000000000 ) ) ;
#178485=DIRECTION ( 'NONE',  ( 0.000000000000000000, -0.9999176327611369874, 0.01283462868041984617 ) ) ;
#178488=LINE ( 'NONE', #215013, #46626 ) ;
#178541=EDGE_CURVE ( 'NONE', #77793, #233092, #244552, .T. ) ;
#178543=DIRECTION ( 'NONE',  ( -1.000000000000000000, 0.000000000000000000, 0.000000000000000000 ) ) ;
#178572=CIRCLE ( 'NONE', #149330, 2.000000000000001776 ) ;
#178580=CARTESIAN_POINT ( 'NONE',  ( 18.50000000000000000, -9.399999999988843058, -40.49928567783884858 ) ) ;
#178638=CARTESIAN_POINT ( 'NONE',  ( 21.05000000000000071, 8.776282895303632259, -45.65000000000000568 ) ) ;
#178651=DIRECTION ( 'NONE',  ( 0.000000000000000000, 1.000000000000000000, 0.000000000000000000 ) ) ;
#178696=ORIENTED_EDGE ( 'NONE', *, *, #176262, .F. ) ;
#178721=DIRECTION ( 'NONE',  ( 0.000000000000000000, -0.1298341882520022694, -0.9915357197604852679 ) ) ;
#178729=DIRECTION ( 'NONE',  ( 0.000000000000000000, -1.000000000000000000, 0.000000000000000000 ) ) ;
#178733=CARTESIAN_POINT ( 'NONE',  ( 18.49999999999999645, 1.866714910068465239, -45.25267524628200988 ) ) ;
#178745=DIRECTION ( 'NONE',  ( 0.7071067811865474617, 0.7071067811865474617, 0.000000000000000000 ) ) ;
#178778=CIRCLE ( 'NONE', #245386, 0.09999999999999939493 ) ;
#178789=DIRECTION ( 'NONE',  ( 0.000000000000000000, 0.000000000000000000, -1.000000000000000000 ) ) ;
#178796=ORIENTED_EDGE ( 'NONE', *, *, #18802, .F. ) ;
#178805=FACE_OUTER_BOUND ( 'NONE', #193287, .T. ) ;
#178810=ORIENTED_EDGE ( 'NONE', *, *, #162566, .T. ) ;
#178816=CARTESIAN_POINT ( 'NONE',  ( -23.15000000000000213, 1.115600667400684642E-11, -33.50000000000000000 ) ) ;
#178843=CARTESIAN_POINT ( 'NONE',  ( 23.14999999999999858, 11.65000000001116298, -59.98519422934606382 ) ) ;
#178845=VERTEX_POINT ( 'NONE', #76273 ) ;
#178860=CARTESIAN_POINT ( 'NONE',  ( -22.39999999999999858, 11.65000000001115588, -33.40000000000000568 ) ) ;
#178876=DIRECTION ( 'NONE',  ( 0.000000000000000000, -0.9654727137038715545, 0.2605042016806676242 ) ) ;
#178897=CARTESIAN_POINT ( 'NONE',  ( -18.59999999999999787, -1.162701749926853712, -41.60000000000000142 ) ) ;
#178898=FACE_OUTER_BOUND ( 'NONE', #72650, .T. ) ;
#179004=CIRCLE ( 'NONE', #141528, 0.1000000000000028644 ) ;
#179026=VECTOR ( 'NONE', #147855, 1000.000000000000000 ) ;
#179031=AXIS2_PLACEMENT_3D ( 'NONE', #187890, #92608, #47059 ) ;
#179042=AXIS2_PLACEMENT_3D ( 'NONE', #129154, #229543, #50864 ) ;
#179043=VERTEX_POINT ( 'NONE', #164820 ) ;
#179061=FACE_OUTER_BOUND ( 'NONE', #238029, .T. ) ;
#179065=LINE ( 'NONE', #120379, #174253 ) ;
#179069=CARTESIAN_POINT ( 'NONE',  ( 21.14999999999999858, 1.115600667400684642E-11, -33.60000000000000142 ) ) ;
#179074=CARTESIAN_POINT ( 'NONE',  ( 23.24999999999999289, 6.450000000011156587, -54.65000000000000568 ) ) ;
#179084=ORIENTED_EDGE ( 'NONE', *, *, #241675, .T. ) ;
#179101=AXIS2_PLACEMENT_3D ( 'NONE', #236670, #73790, #58022 ) ;
#179108=CARTESIAN_POINT ( 'NONE',  ( 20.94999999999999574, 1.162701749949165642, -41.50000000000000000 ) ) ;
#179136=AXIS2_PLACEMENT_3D ( 'NONE', #113447, #251671, #109582 ) ;
#179150=CARTESIAN_POINT ( 'NONE',  ( 21.05000000000000071, -11.39257802169451139, -63.92605042016806749 ) ) ;
#179164=FACE_OUTER_BOUND ( 'NONE', #120071, .T. ) ;
#179183=CARTESIAN_POINT ( 'NONE',  ( 20.85000000000000142, -1.149570369564537842, -74.81591248450196474 ) ) ;
#179231=AXIS2_PLACEMENT_3D ( 'NONE', #78612, #193456, #53928 ) ;
#179244=FACE_OUTER_BOUND ( 'NONE', #197716, .T. ) ;
#179278=CIRCLE ( 'NONE', #208303, 0.1000000000000028644 ) ;
#179286=CARTESIAN_POINT ( 'NONE',  ( 18.49999999999999289, 6.650000000011155876, -54.85000000000000142 ) ) ;
#179290=FACE_OUTER_BOUND ( 'NONE', #213793, .T. ) ;
#179298=CARTESIAN_POINT ( 'NONE',  ( -20.64999999999999858, 4.250000000011156409, -54.64999999999999858 ) ) ;
#179315=VERTEX_POINT ( 'NONE', #77255 ) ;
#179328=VECTOR ( 'NONE', #92232, 1000.000000000000000 ) ;
#179333=CARTESIAN_POINT ( 'NONE',  ( 21.09787244211750945, 8.775370707348422172, -45.73925338431762810 ) ) ;
#179367=CARTESIAN_POINT ( 'NONE',  ( -20.54999999999999716, 2.000000000011154189, -46.72462192276210402 ) ) ;
#179417=ORIENTED_EDGE ( 'NONE', *, *, #169021, .F. ) ;
#179428=EDGE_CURVE ( 'NONE', #225825, #24660, #240843, .T. ) ;
#179484=DIRECTION ( 'NONE',  ( 0.000000000000000000, 0.9915357197604794948, -0.1298341882520470392 ) ) ;
#179485=CARTESIAN_POINT ( 'NONE',  ( 20.96428641294217954, 11.75000000001150013, -60.17489317794084513 ) ) ;
#179499=ADVANCED_FACE ( 'NONE', ( #108393 ), #90996, .F. ) ;
#179511=VERTEX_POINT ( 'NONE', #25025 ) ;
#179513=ORIENTED_EDGE ( 'NONE', *, *, #87881, .T. ) ;
#179529=ORIENTED_EDGE ( 'NONE', *, *, #142522, .T. ) ;
#179531=CARTESIAN_POINT ( 'NONE',  ( 18.59999999999999076, 10.49142135624846439, -58.35000000000000142 ) ) ;
#179550=EDGE_CURVE ( 'NONE', #230716, #130418, #24378, .T. ) ;
#179553=CIRCLE ( 'NONE', #208764, 0.1000000000000008937 ) ;
#179585=CARTESIAN_POINT ( 'NONE',  ( 18.59999999999999076, 11.75000000001115907, -41.60000000000000142 ) ) ;
#179591=FACE_OUTER_BOUND ( 'NONE', #177005, .T. ) ;
#179619=CARTESIAN_POINT ( 'NONE',  ( 20.86036036209909383, 10.62104277658211871, -41.16634841850498816 ) ) ;
#179642=DIRECTION ( 'NONE',  ( -0.000000000000000000, -0.000000000000000000, 1.000000000000000000 ) ) ;
#179674=DIRECTION ( 'NONE',  ( 0.000000000000000000, -0.4930308989875324399, -0.8700118002898268310 ) ) ;
#179676=FACE_OUTER_BOUND ( 'NONE', #113259, .T. ) ;
#179684=CIRCLE ( 'NONE', #233843, 7.800000000000000711 ) ;
#179710=ORIENTED_EDGE ( 'NONE', *, *, #152688, .T. ) ;
#179722=DIRECTION ( 'NONE',  ( 0.000000000000000000, 0.000000000000000000, 1.000000000000000000 ) ) ;
#179748=DIRECTION ( 'NONE',  ( 0.000000000000000000, 1.000000000000000000, 2.891205793294679805E-16 ) ) ;
#179798=EDGE_LOOP ( 'NONE', ( #105664, #211060, #110614, #55908 ) ) ;
#179867=EDGE_CURVE ( 'NONE', #135153, #41243, #53087, .T. ) ;
#179889=EDGE_CURVE ( 'NONE', #110818, #54944, #257715, .T. ) ;
#179905=ADVANCED_FACE ( 'NONE', ( #192292 ), #210565, .F. ) ;
#179936=FACE_OUTER_BOUND ( 'NONE', #195849, .T. ) ;
#179940=AXIS2_PLACEMENT_3D ( 'NONE', #238434, #119794, #100173 ) ;
#179945=CIRCLE ( 'NONE', #34220, 0.1000000000000028644 ) ;
#179981=FACE_OUTER_BOUND ( 'NONE', #251849, .T. ) ;
#180010=DIRECTION ( 'NONE',  ( 1.000000000000000000, 1.836970198721029934E-16, -0.000000000000000000 ) ) ;
#180020=ADVANCED_FACE ( 'NONE', ( #188422 ), #230120, .T. ) ;
#180101=DIRECTION ( 'NONE',  ( 0.000000000000000000, 0.000000000000000000, -1.000000000000000000 ) ) ;
#180108=CYLINDRICAL_SURFACE ( 'NONE', #26982, 0.1000000000000028644 ) ;
#180122=CIRCLE ( 'NONE', #176037, 0.09999999999999939493 ) ;
#180165=EDGE_CURVE ( 'NONE', #127078, #182882, #41325, .T. ) ;
#180196=EDGE_CURVE ( 'NONE', #116181, #154736, #99524, .T. ) ;
#180200=CARTESIAN_POINT ( 'NONE',  ( 21.05000000000000071, -11.48912529306490349, -36.39999999999999858 ) ) ;
#180249=DIRECTION ( 'NONE',  ( -1.000000000000000000, -1.836970198721029934E-16, 0.000000000000000000 ) ) ;
#180272=EDGE_LOOP ( 'NONE', ( #215102, #11237, #253229, #51486 ) ) ;
#180291=CARTESIAN_POINT ( 'NONE',  ( -18.59999999999999787, -1.162701749926853712, -41.60000000000000142 ) ) ;
#180308=DIRECTION ( 'NONE',  ( 1.000000000000000000, 0.000000000000000000, 0.000000000000000000 ) ) ;
#180315=ORIENTED_EDGE ( 'NONE', *, *, #248990, .T. ) ;
#180395=EDGE_CURVE ( 'NONE', #43175, #12448, #58015, .T. ) ;
#180447=EDGE_CURVE ( 'NONE', #190117, #130981, #117585, .T. ) ;
#180458=ORIENTED_EDGE ( 'NONE', *, *, #42067, .F. ) ;
#180464=EDGE_CURVE ( 'NONE', #171125, #101473, #162853, .T. ) ;
#180493=AXIS2_PLACEMENT_3D ( 'NONE', #238783, #60121, #139648 ) ;
#180494=CARTESIAN_POINT ( 'NONE',  ( -18.50000000000000000, -9.499999999988849808, -21.75000000000000355 ) ) ;
#180518=AXIS2_PLACEMENT_3D ( 'NONE', #145997, #89870, #246395 ) ;
#180524=CARTESIAN_POINT ( 'NONE',  ( -21.05000000000000071, -1.851028230129704522, -45.15391326942249606 ) ) ;
#180596=DIRECTION ( 'NONE',  ( 0.5000000000001141309, 0.000000000000000000, -0.8660254037843729824 ) ) ;
#180603=FACE_OUTER_BOUND ( 'NONE', #68765, .T. ) ;
#180613=AXIS2_PLACEMENT_3D ( 'NONE', #199845, #104537, #182853 ) ;
#180620=VECTOR ( 'NONE', #208043, 1000.000000000000000 ) ;
#180684=CARTESIAN_POINT ( 'NONE',  ( -20.94403535211772294, 10.30632246271647467, -72.50418367788957141 ) ) ;
#180704=AXIS2_PLACEMENT_3D ( 'NONE', #197318, #78651, #96908 ) ;
#180709=PLANE ( 'NONE',  #230615 ) ;
#180713=PLANE ( 'NONE',  #173387 ) ;
#180715=CARTESIAN_POINT ( 'NONE',  ( 20.04142135623730070, 11.65000000001115943, -54.85000000000000142 ) ) ;
#180750=VERTEX_POINT ( 'NONE', #177289 ) ;
#180762=CIRCLE ( 'NONE', #176675, 0.1000000000000028644 ) ;
#180785=CIRCLE ( 'NONE', #85063, 0.09999999999999939493 ) ;
#180822=EDGE_CURVE ( 'NONE', #55121, #212737, #195810, .T. ) ;
#180857=ORIENTED_EDGE ( 'NONE', *, *, #69577, .T. ) ;
#180866=AXIS2_PLACEMENT_3D ( 'NONE', #19027, #80248, #20337 ) ;
#180915=CARTESIAN_POINT ( 'NONE',  ( 20.04142135623730070, 11.65000000001115943, -58.15000000000000568 ) ) ;
#180917=CARTESIAN_POINT ( 'NONE',  ( -18.50000000000000355, -9.399999999988818189, -40.79725975966328377 ) ) ;
#180952=VERTEX_POINT ( 'NONE', #186252 ) ;
#181028=CARTESIAN_POINT ( 'NONE',  ( 18.59999999999999787, -1.362429037182151470, -74.88888124792120493 ) ) ;
#181036=CARTESIAN_POINT ( 'NONE',  ( -23.15000000000000213, 11.65000000001115588, -45.65000000000000568 ) ) ;
#181048=ORIENTED_EDGE ( 'NONE', *, *, #89382, .T. ) ;
#181073=ORIENTED_EDGE ( 'NONE', *, *, #174242, .F. ) ;
#181082=CIRCLE ( 'NONE', #68641, 0.1000000000000028644 ) ;
#181103=ORIENTED_EDGE ( 'NONE', *, *, #115016, .T. ) ;
#181108=DIRECTION ( 'NONE',  ( 0.000000000000000000, 1.000000000000000000, 0.000000000000000000 ) ) ;
#181133=LINE ( 'NONE', #178580, #181230 ) ;
#181142=CARTESIAN_POINT ( 'NONE',  ( -22.39999999999999858, 1.115600667400684642E-11, -27.25000000000000355 ) ) ;
#181143=DIRECTION ( 'NONE',  ( 0.000000000000000000, 0.000000000000000000, -1.000000000000000000 ) ) ;
#181160=EDGE_CURVE ( 'NONE', #192209, #129105, #33510, .T. ) ;
#181191=EDGE_LOOP ( 'NONE', ( #53546, #212542, #10468, #120539 ) ) ;
#181209=DIRECTION ( 'NONE',  ( 0.000000000000000000, 0.000000000000000000, 1.000000000000000000 ) ) ;
#181230=VECTOR ( 'NONE', #157755, 1000.000000000000000 ) ;
#181237=CIRCLE ( 'NONE', #14840, 0.09999999999999939493 ) ;
#181265=DIRECTION ( 'NONE',  ( 0.7071359030027766224, 0.000000000000000000, -0.7070776581709024011 ) ) ;
#181270=AXIS2_PLACEMENT_3D ( 'NONE', #62063, #240688, #25507 ) ;
#181271=EDGE_LOOP ( 'NONE', ( #178796, #79112, #86644, #187333 ) ) ;
#181319=CARTESIAN_POINT ( 'NONE',  ( 21.53752568617663243, 6.786807874515133676, -33.40102553874074687 ) ) ;
#181334=MECHANICAL_DESIGN_GEOMETRIC_PRESENTATION_REPRESENTATION('',(#152303),#168881);
#181344=FACE_OUTER_BOUND ( 'NONE', #156834, .T. ) ;
#181357=CARTESIAN_POINT ( 'NONE',  ( -20.95000000000000284, 11.65000000001115232, -59.98519422934605672 ) ) ;
#181382=EDGE_CURVE ( 'NONE', #88661, #119088, #30397, .T. ) ;
#181454=DIRECTION ( 'NONE',  ( 0.000000000000000000, 1.000000000000000000, 2.891205793294679805E-16 ) ) ;
#181461=EDGE_CURVE ( 'NONE', #87677, #248271, #225157, .T. ) ;
#181463=CARTESIAN_POINT ( 'NONE',  ( 21.05000000000000071, 8.876614585098254295, -41.88508047884467800 ) ) ;
#181497=ADVANCED_FACE ( 'NONE', ( #175077 ), #62878, .F. ) ;
#181506=CIRCLE ( 'NONE', #31118, 12.87499999999999822 ) ;
#181514=ORIENTED_EDGE ( 'NONE', *, *, #81258, .T. ) ;
#181589=CARTESIAN_POINT ( 'NONE',  ( -20.94999999999999929, -11.39257802169451672, -36.57394957983193251 ) ) ;
#181631=VERTEX_POINT ( 'NONE', #181463 ) ;
#181632=CARTESIAN_POINT ( 'NONE',  ( -20.94999999999999929, 6.846123162363745074, -70.73772626684986164 ) ) ;
#181648=VERTEX_POINT ( 'NONE', #170928 ) ;
#181652=ORIENTED_EDGE ( 'NONE', *, *, #68181, .F. ) ;
#181712=ORIENTED_EDGE ( 'NONE', *, *, #199017, .T. ) ;
#181752=AXIS2_PLACEMENT_3D ( 'NONE', #156432, #160276, #217621 ) ;
#181765=DIRECTION ( 'NONE',  ( -0.000000000000000000, 0.1350103645451904977, 0.9908441862701597991 ) ) ;
#181775=AXIS2_PLACEMENT_3D ( 'NONE', #22756, #83932, #142653 ) ;
#181799=CARTESIAN_POINT ( 'NONE',  ( -21.05000000000000071, 6.258842723548718290, -33.46798630681211506 ) ) ;
#181825=EDGE_CURVE ( 'NONE', #141325, #249646, #165595, .T. ) ;
#181827=FACE_OUTER_BOUND ( 'NONE', #249363, .T. ) ;
#181849=CARTESIAN_POINT ( 'NONE',  ( 18.59999999999999787, 1.115600667400684642E-11, -33.50000000000000000 ) ) ;
#181868=EDGE_CURVE ( 'NONE', #225961, #61206, #104700, .T. ) ;
#181883=CARTESIAN_POINT ( 'NONE',  ( 21.05000000000000071, 8.776282895303626930, -45.65000000000000568 ) ) ;
#181895=DIRECTION ( 'NONE',  ( 0.000000000000000000, 1.000000000000000000, 0.000000000000000000 ) ) ;
#181899=DIRECTION ( 'NONE',  ( 1.000000000000000000, 0.000000000000000000, 0.000000000000000000 ) ) ;
#181915=AXIS2_PLACEMENT_3D ( 'NONE', #178860, #17195, #114989 ) ;
#181952=VERTEX_POINT ( 'NONE', #220290 ) ;
#181968=DIRECTION ( 'NONE',  ( 1.000000000000000000, 0.000000000000000000, 0.000000000000000000 ) ) ;
#182004=ORIENTED_EDGE ( 'NONE', *, *, #203808, .T. ) ;
#182014=VERTEX_POINT ( 'NONE', #61196 ) ;
#182035=CARTESIAN_POINT ( 'NONE',  ( 20.96077737575326694, 11.62390063401587170, -60.14079195710662162 ) ) ;
#182042=VECTOR ( 'NONE', #167811, 1000.000000000000000 ) ;
#182047=EDGE_LOOP ( 'NONE', ( #110594, #109783, #173963, #174368 ) ) ;
#182077=DIRECTION ( 'NONE',  ( 0.000000000000000000, -1.000000000000000000, 0.000000000000000000 ) ) ;
#182094=ORIENTED_EDGE ( 'NONE', *, *, #87188, .T. ) ;
#182104=FACE_OUTER_BOUND ( 'NONE', #33503, .T. ) ;
#182129=B_SPLINE_CURVE_WITH_KNOTS ( 'NONE', 3,
 ( #204160, #106333, #166373, #245876, #122084, #141634, #224997, #184611 ),
 .UNSPECIFIED., .F., .F.,
 ( 4, 2, 2, 4 ),
 ( 0.000000000000000000, 0.0002114466876442047964, 0.0003171700314663110300, 0.0004228933752884172907 ),
 .UNSPECIFIED. ) ;
#182151=LINE ( 'NONE', #4756, #19410 ) ;
#182159=CARTESIAN_POINT ( 'NONE',  ( -23.15000000000000213, 11.65000000001115588, -45.65000000000000568 ) ) ;
#182198=CARTESIAN_POINT ( 'NONE',  ( -21.05000000000000071, 1.115600667400684642E-11, -67.00000000000000000 ) ) ;
#182204=DIRECTION ( 'NONE',  ( 0.000000000000000000, -1.000000000000000000, 0.000000000000000000 ) ) ;
#182205=EDGE_LOOP ( 'NONE', ( #129308, #200093, #106478, #88259 ) ) ;
#182206=EDGE_LOOP ( 'NONE', ( #150251, #185352, #187114, #207324 ) ) ;
#182215=CARTESIAN_POINT ( 'NONE',  ( -23.25000000000000000, 1.115600667400684642E-11, -67.00000000000000000 ) ) ;
#182216=CARTESIAN_POINT ( 'NONE',  ( 18.59999999999999076, 11.65000000001115943, -21.75000000000000355 ) ) ;
#182230=CARTESIAN_POINT ( 'NONE',  ( 21.05000000000000071, -0.09999993529482767429, -27.02192177890524150 ) ) ;
#182239=ORIENTED_EDGE ( 'NONE', *, *, #247175, .F. ) ;
#182249=ORIENTED_EDGE ( 'NONE', *, *, #92443, .T. ) ;
#182292=CYLINDRICAL_SURFACE ( 'NONE', #31773, 0.09999999999999939493 ) ;
#182299=ORIENTED_EDGE ( 'NONE', *, *, #123749, .T. ) ;
#182303=AXIS2_PLACEMENT_3D ( 'NONE', #188693, #88282, #53029 ) ;
#182304=EDGE_CURVE ( 'NONE', #48144, #8827, #125767, .T. ) ;
#182313=EDGE_CURVE ( 'NONE', #172639, #82065, #154848, .T. ) ;
#182314=AXIS2_PLACEMENT_3D ( 'NONE', #16408, #197580, #1937 ) ;
#182341=VERTEX_POINT ( 'NONE', #236958 ) ;
#182358=CARTESIAN_POINT ( 'NONE',  ( 21.40925344232283223, 0.09895018863080314031, -26.84148114060954526 ) ) ;
#182376=VECTOR ( 'NONE', #212398, 1000.000000000000114 ) ;
#182447=PLANE ( 'NONE',  #132090 ) ;
#182459=DIRECTION ( 'NONE',  ( 0.000000000000000000, 0.000000000000000000, -1.000000000000000000 ) ) ;
#182461=DIRECTION ( 'NONE',  ( 0.000000000000000000, 0.000000000000000000, 1.000000000000000000 ) ) ;
#182468=FACE_OUTER_BOUND ( 'NONE', #104027, .T. ) ;
#182475=ORIENTED_EDGE ( 'NONE', *, *, #23809, .T. ) ;
#182504=CARTESIAN_POINT ( 'NONE',  ( -23.25000000000000000, 2.000000000011154189, -54.37537807723790451 ) ) ;
#182514=TOROIDAL_SURFACE ( 'NONE', #215787, 0.4000000000000009104, 0.1000000000000000056 ) ;
#182573=ORIENTED_EDGE ( 'NONE', *, *, #246052, .F. ) ;
#182599=CARTESIAN_POINT ( 'NONE',  ( 20.94999999999999929, 11.65000000001115943, -60.21613433702191287 ) ) ;
#182653=ORIENTED_EDGE ( 'NONE', *, *, #174242, .T. ) ;
#182672=EDGE_CURVE ( 'NONE', #159251, #55121, #112853, .T. ) ;
#182685=DIRECTION ( 'NONE',  ( 0.000000000000000000, 0.000000000000000000, -1.000000000000000000 ) ) ;
#182724=EDGE_CURVE ( 'NONE', #16861, #241304, #213219, .T. ) ;
#182728=DIRECTION ( 'NONE',  ( 0.000000000000000000, 1.000000000000000000, 0.000000000000000000 ) ) ;
#182736=LINE ( 'NONE', #163171, #110896 ) ;
#182757=CARTESIAN_POINT ( 'NONE',  ( -23.25000000000000000, 11.75000000001115552, -45.65000000000000568 ) ) ;
#182769=VECTOR ( 'NONE', #128763, 1000.000000000000000 ) ;
#182770=AXIS2_PLACEMENT_3D ( 'NONE', #21200, #100665, #180249 ) ;
#182772=CARTESIAN_POINT ( 'NONE',  ( 21.00000000000000000, 9.750000000011153745, -54.75000000000000000 ) ) ;
#182804=DIRECTION ( 'NONE',  ( -1.000000000000000000, 9.012599976028471648E-15, 6.882867235861662930E-14 ) ) ;
#182806=ORIENTED_EDGE ( 'NONE', *, *, #2605, .F. ) ;
#182853=DIRECTION ( 'NONE',  ( 0.000000000000000000, 0.000000000000000000, -1.000000000000000000 ) ) ;
#182864=AXIS2_PLACEMENT_3D ( 'NONE', #253985, #37531, #177054 ) ;
#182878=DIRECTION ( 'NONE',  ( 0.000000000000000000, 0.9999631594459056361, -0.008583690987128059571 ) ) ;
#182881=CARTESIAN_POINT ( 'NONE',  ( -20.64999999999999858, 7.250000000011155521, -45.85000000000000142 ) ) ;
#182882=VERTEX_POINT ( 'NONE', #47420 ) ;
#182884=ORIENTED_EDGE ( 'NONE', *, *, #138548, .T. ) ;
#182890=EDGE_LOOP ( 'NONE', ( #230521, #41139, #13121, #177392 ) ) ;
#182895=DIRECTION ( 'NONE',  ( 0.000000000000000000, 0.000000000000000000, 1.000000000000000000 ) ) ;
#182902=ADVANCED_FACE ( 'NONE', ( #188237 ), #145241, .F. ) ;
#182915=ORIENTED_EDGE ( 'NONE', *, *, #110834, .F. ) ;
#182923=EDGE_LOOP ( 'NONE', ( #199816, #170408, #120118, #82142 ) ) ;
#182940=DIRECTION ( 'NONE',  ( -1.000000000000000000, -7.304098846218135653E-16, 4.607487905232624742E-31 ) ) ;
#182951=EDGE_CURVE ( 'NONE', #79720, #147882, #26614, .T. ) ;
#183038=DIRECTION ( 'NONE',  ( 0.000000000000000000, -1.000000000000000000, 0.000000000000000000 ) ) ;
#183042=ADVANCED_FACE ( 'NONE', ( #95226 ), #150526, .T. ) ;
#183046=ADVANCED_FACE ( 'NONE', ( #136919 ), #196887, .T. ) ;
#183073=ORIENTED_EDGE ( 'NONE', *, *, #13164, .T. ) ;
#183085=CARTESIAN_POINT ( 'NONE',  ( -20.64999999999999858, 7.250000000011155521, -45.75000000000000000 ) ) ;
#183093=ORIENTED_EDGE ( 'NONE', *, *, #38371, .F. ) ;
#183100=DIRECTION ( 'NONE',  ( 0.000000000000000000, 0.000000000000000000, -1.000000000000000000 ) ) ;
#183156=CIRCLE ( 'NONE', #216454, 0.09999999999999939493 ) ;
#183157=VERTEX_POINT ( 'NONE', #221566 ) ;
#183168=ORIENTED_EDGE ( 'NONE', *, *, #76886, .T. ) ;
#183169=B_SPLINE_CURVE_WITH_KNOTS ( 'NONE', 3,
 ( #232444, #72075, #14685, #133324, #55040, #152916, #94178 ),
 .UNSPECIFIED., .F., .F.,
 ( 4, 3, 4 ),
 ( 0.000000000000000000, 0.0007844235214594269838, 0.001767853679404345069 ),
 .UNSPECIFIED. ) ;
#183198=EDGE_LOOP ( 'NONE', ( #175229, #15145, #163208, #10557, #104088 ) ) ;
#183218=AXIS2_PLACEMENT_3D ( 'NONE', #2365, #178485, #238431 ) ;
#183220=ORIENTED_EDGE ( 'NONE', *, *, #56923, .F. ) ;
#183236=ORIENTED_EDGE ( 'NONE', *, *, #169896, .F. ) ;
#183240=EDGE_CURVE ( 'NONE', #127487, #16805, #25445, .T. ) ;
#183268=VECTOR ( 'NONE', #83301, 1000.000000000000000 ) ;
#183281=CARTESIAN_POINT ( 'NONE',  ( -23.25000000000000000, 2.600000000011156054, -46.72462192276210402 ) ) ;
#183285=ORIENTED_EDGE ( 'NONE', *, *, #85878, .F. ) ;
#183290=DIRECTION ( 'NONE',  ( 0.000000000000000000, 0.000000000000000000, -1.000000000000000000 ) ) ;
#183305=ADVANCED_FACE ( 'NONE', ( #70258 ), #191488, .T. ) ;
#183319=EDGE_LOOP ( 'NONE', ( #167183, #12595, #186665, #130676 ) ) ;
#183322=CARTESIAN_POINT ( 'NONE',  ( -18.39999999999999858, -9.499999999988849808, -73.60018939122203108 ) ) ;
#183361=DIRECTION ( 'NONE',  ( -1.000000000000000000, 0.000000000000000000, 0.000000000000000000 ) ) ;
#183368=DIRECTION ( 'NONE',  ( -5.603264701231743991E-32, 1.897661533703520143E-16, -1.000000000000000000 ) ) ;
#183396=ADVANCED_FACE ( 'NONE', ( #63329, #205407, #3347 ), #226239, .F. ) ;
#183400=CARTESIAN_POINT ( 'NONE',  ( -23.25000000000000000, 1.115600667400684642E-11, -33.50000000000000000 ) ) ;
#183429=AXIS2_PLACEMENT_3D ( 'NONE', #238124, #240709, #241984 ) ;
#183436=CARTESIAN_POINT ( 'NONE',  ( 21.05000000000000071, 1.115600667400684642E-11, -33.50000000000000000 ) ) ;
#183446=DIRECTION ( 'NONE',  ( 0.000000000000000000, 0.000000000000000000, 1.000000000000000000 ) ) ;
#183459=ADVANCED_FACE ( 'NONE', ( #53682 ), #91531, .F. ) ;
#183469=ORIENTED_EDGE ( 'NONE', *, *, #186282, .F. ) ;
#183475=CARTESIAN_POINT ( 'NONE',  ( 22.59999954896768770, -0.008828232233014684030, -21.74949132593200574 ) ) ;
#183484=CARTESIAN_POINT ( 'NONE',  ( -18.52186455168988388, -9.481018481431377154, -40.52501647791446970 ) ) ;
#183519=ORIENTED_EDGE ( 'NONE', *, *, #113065, .F. ) ;
#183522=EDGE_CURVE ( 'NONE', #47428, #102195, #237985, .T. ) ;
#183535=CONICAL_SURFACE ( 'NONE', #83542, 4.299999999999956302, 0.7853981633974466137 ) ;
#183536=EDGE_LOOP ( 'NONE', ( #42143, #77004, #66188, #95245 ) ) ;
#183539=DIRECTION ( 'NONE',  ( 0.000000000000000000, 0.000000000000000000, -1.000000000000000000 ) ) ;
#183556=EDGE_CURVE ( 'NONE', #2313, #224490, #14585, .T. ) ;
#183587=DIRECTION ( 'NONE',  ( 1.000000000000000000, -0.000000000000000000, -0.000000000000000000 ) ) ;
#183596=EDGE_CURVE ( 'NONE', #214564, #145730, #154828, .T. ) ;
#183597=CARTESIAN_POINT ( 'NONE',  ( -18.50000000000000000, 9.250000000011157297, -54.75000000000000000 ) ) ;
#183638=CARTESIAN_POINT ( 'NONE',  ( 21.04999999999999716, 10.62872031401550466, -45.64999999999999858 ) ) ;
#183658=DIRECTION ( 'NONE',  ( 0.000000000000000000, 0.000000000000000000, 1.000000000000000000 ) ) ;
#183665=ORIENTED_EDGE ( 'NONE', *, *, #29121, .F. ) ;
#183680=VERTEX_POINT ( 'NONE', #99205 ) ;
#183686=AXIS2_PLACEMENT_3D ( 'NONE', #256579, #40183, #77984 ) ;
#183700=FACE_OUTER_BOUND ( 'NONE', #229661, .T. ) ;
#183706=ADVANCED_FACE ( 'NONE', ( #58792 ), #41850, .T. ) ;
#183736=DIRECTION ( 'NONE',  ( -0.000000000000000000, -0.000000000000000000, 1.000000000000000000 ) ) ;
#183738=LINE ( 'NONE', #238569, #92526 ) ;
#183776=CARTESIAN_POINT ( 'NONE',  ( -18.52328366898032286, -9.642321089030096104, -73.71481933757003446 ) ) ;
#183799=CARTESIAN_POINT ( 'NONE',  ( 23.24999999999997513, 11.75000000001116263, -59.98519422934606382 ) ) ;
#183801=ORIENTED_EDGE ( 'NONE', *, *, #190788, .F. ) ;
#183802=CARTESIAN_POINT ( 'NONE',  ( -20.00857864376270001, 9.150000000011157653, -54.75000000000000000 ) ) ;
#183810=VERTEX_POINT ( 'NONE', #86048 ) ;
#183828=FACE_OUTER_BOUND ( 'NONE', #101230, .T. ) ;
#183829=DIRECTION ( 'NONE',  ( 0.000000000000000000, -0.4791956752371546169, -0.8777080977375152360 ) ) ;
#183841=CYLINDRICAL_SURFACE ( 'NONE', #129263, 0.09999999999999939493 ) ;
#183848=FACE_OUTER_BOUND ( 'NONE', #167668, .T. ) ;
#183854=CIRCLE ( 'NONE', #54659, 7.900000000000000355 ) ;
#183863=DIRECTION ( 'NONE',  ( -0.000000000000000000, 1.000000000000000000, 0.000000000000000000 ) ) ;
#183919=EDGE_CURVE ( 'NONE', #9029, #241512, #230748, .T. ) ;
#183938=DIRECTION ( 'NONE',  ( 0.000000000000000000, -0.8700118002898321601, 0.4930308989875230030 ) ) ;
#183950=CYLINDRICAL_SURFACE ( 'NONE', #103859, 0.09999999999999939493 ) ;
#183977=EDGE_LOOP ( 'NONE', ( #253063, #235630, #214134, #148445 ) ) ;
#183995=CIRCLE ( 'NONE', #71588, 0.1000000000000028644 ) ;
#184003=EDGE_CURVE ( 'NONE', #7325, #195498, #178488, .T. ) ;
#184038=EDGE_LOOP ( 'NONE', ( #221371, #92054, #30953, #144672, #72620 ) ) ;
#184040=VECTOR ( 'NONE', #224052, 1000.000000000000000 ) ;
#184046=EDGE_CURVE ( 'NONE', #131237, #224599, #25803, .T. ) ;
#184066=DIRECTION ( 'NONE',  ( 0.000000000000000000, 0.000000000000000000, -1.000000000000000000 ) ) ;
#184076=FACE_OUTER_BOUND ( 'NONE', #154806, .T. ) ;
#184098=EDGE_LOOP ( 'NONE', ( #174628, #125724, #223279, #126803, #198661, #108891 ) ) ;
#184107=VERTEX_POINT ( 'NONE', #59765 ) ;
#184168=CARTESIAN_POINT ( 'NONE',  ( -18.49372193242239959, -9.442484523346879044, -73.76478126003453895 ) ) ;
#184225=ORIENTED_EDGE ( 'NONE', *, *, #111455, .T. ) ;
#184231=EDGE_CURVE ( 'NONE', #201531, #19748, #71045, .T. ) ;
#184236=CARTESIAN_POINT ( 'NONE',  ( 23.14999999999999503, 6.650000000011155876, -45.65000000000000568 ) ) ;
#184243=PLANE ( 'NONE',  #34563 ) ;
#184249=DIRECTION ( 'NONE',  ( 1.000000000000000000, 0.000000000000000000, 0.000000000000000000 ) ) ;
#184258=ORIENTED_EDGE ( 'NONE', *, *, #123670, .F. ) ;
#184262=SPHERICAL_SURFACE ( 'NONE', #127916, 0.1000000000000000056 ) ;
#184264=EDGE_CURVE ( 'NONE', #163442, #89935, #210537, .T. ) ;
#184303=ADVANCED_FACE ( 'NONE', ( #72322 ), #192270, .F. ) ;
#184304=ORIENTED_EDGE ( 'NONE', *, *, #3981, .F. ) ;
#184307=AXIS2_PLACEMENT_3D ( 'NONE', #224198, #105507, #245057 ) ;
#184312=TOROIDAL_SURFACE ( 'NONE', #217617, 11.65000000000000036, 0.1000000000000000056 ) ;
#184327=CARTESIAN_POINT ( 'NONE',  ( -21.09610168723073187, 6.378955715235940183, -33.46641049310851201 ) ) ;
#184343=CARTESIAN_POINT ( 'NONE',  ( 21.05000000000000071, 10.42338541492406279, -40.99205192387010044 ) ) ;
#184375=EDGE_LOOP ( 'NONE', ( #208279, #189404, #146349, #80865 ) ) ;
#184402=CARTESIAN_POINT ( 'NONE',  ( -21.05000000000000071, 11.65000000001115232, -40.28386566297815108 ) ) ;
#184417=AXIS2_PLACEMENT_3D ( 'NONE', #211144, #174643, #192877 ) ;
#184420=AXIS2_PLACEMENT_3D ( 'NONE', #232294, #191891, #131885 ) ;
#184461=CARTESIAN_POINT ( 'NONE',  ( 23.24999999999999289, 6.650000000011155876, -45.85000000000000142 ) ) ;
#184483=CARTESIAN_POINT ( 'NONE',  ( -20.94999999999999929, 1.115600667400684642E-11, -63.00000000000000000 ) ) ;
#184484=ORIENTED_EDGE ( 'NONE', *, *, #167461, .F. ) ;
#184516=ORIENTED_EDGE ( 'NONE', *, *, #8192, .T. ) ;
#184519=CARTESIAN_POINT ( 'NONE',  ( -22.39999999999999858, 1.115600667400684642E-11, -21.85042919245520210 ) ) ;
#184525=VECTOR ( 'NONE', #115399, 1000.000000000000000 ) ;
#184556=VERTEX_POINT ( 'NONE', #29065 ) ;
#184559=ADVANCED_FACE ( 'NONE', ( #90261 ), #184243, .T. ) ;
#184611=CARTESIAN_POINT ( 'NONE',  ( 18.39999999999999858, -9.519327731081283162, -40.47297637655933755 ) ) ;
#184619=CIRCLE ( 'NONE', #101369, 0.1999999999999987899 ) ;
#184624=DIRECTION ( 'NONE',  ( 1.000000000000000000, 0.000000000000000000, 0.000000000000000000 ) ) ;
#184633=CARTESIAN_POINT ( 'NONE',  ( -20.94999999999999929, 11.75000000001115197, -40.51480577065400013 ) ) ;
#184653=ADVANCED_FACE ( 'NONE', ( #245515 ), #168590, .F. ) ;
#184655=CARTESIAN_POINT ( 'NONE',  ( 21.05000000000000071, 8.876614585098254295, -41.88508047884467800 ) ) ;
#184682=ADVANCED_FACE ( 'NONE', ( #208945 ), #30326, .F. ) ;
#184725=CARTESIAN_POINT ( 'NONE',  ( 20.94999999999999574, 1.115600667400684642E-11, -33.50000000000000000 ) ) ;
#184782=EDGE_CURVE ( 'NONE', #100799, #22210, #63770, .T. ) ;
#184804=VECTOR ( 'NONE', #206626, 1000.000000000000000 ) ;
#184805=AXIS2_PLACEMENT_3D ( 'NONE', #77418, #98246, #56559 ) ;
#184806=ORIENTED_EDGE ( 'NONE', *, *, #146181, .F. ) ;
#184858=CARTESIAN_POINT ( 'NONE',  ( -22.48660254037843487, 11.65000000001115588, -33.45000000000002416 ) ) ;
#184892=ORIENTED_EDGE ( 'NONE', *, *, #32491, .T. ) ;
#184898=CARTESIAN_POINT ( 'NONE',  ( -21.05000000000000071, 1.835341550235569663, -45.05515129256298223 ) ) ;
#184922=DIRECTION ( 'NONE',  ( -1.000000000000000000, 0.000000000000000000, 0.000000000000000000 ) ) ;
#184927=AXIS2_PLACEMENT_3D ( 'NONE', #230998, #57457, #32817 ) ;
#184934=CIRCLE ( 'NONE', #139106, 7.800000000000001599 ) ;
#184944=DIRECTION ( 'NONE',  ( 0.000000000000000000, 0.000000000000000000, 1.000000000000000000 ) ) ;
#184969=CIRCLE ( 'NONE', #205811, 0.09999999999999939493 ) ;
#184975=CARTESIAN_POINT ( 'NONE',  ( -20.94999999999999929, -11.64999999998884483, -64.10000000000000853 ) ) ;
#185001=CARTESIAN_POINT ( 'NONE',  ( -18.59999999999999787, 7.070967871809997973, -70.74656422186831151 ) ) ;
#185015=CARTESIAN_POINT ( 'NONE',  ( 23.14999999999999503, 11.65000000001116298, -45.65000000000000568 ) ) ;
#185019=ORIENTED_EDGE ( 'NONE', *, *, #247258, .F. ) ;
#185052=EDGE_CURVE ( 'NONE', #79373, #226022, #97214, .T. ) ;
#185083=EDGE_CURVE ( 'NONE', #77835, #34405, #55964, .T. ) ;
#185086=CARTESIAN_POINT ( 'NONE',  ( 20.94999999999999929, 1.115600667400684642E-11, -33.50000000000000000 ) ) ;
#185099=ADVANCED_FACE ( 'NONE', ( #232081 ), #188855, .F. ) ;
#185108=DIRECTION ( 'NONE',  ( 0.000000000000000000, 0.000000000000000000, 1.000000000000000000 ) ) ;
#185112=TOROIDAL_SURFACE ( 'NONE', #239279, 4.149999999999999467, 0.1000000000000000056 ) ;
#185129=VECTOR ( 'NONE', #255109, 1000.000000000000000 ) ;
#185163=ORIENTED_EDGE ( 'NONE', *, *, #67965, .F. ) ;
#185247=ORIENTED_EDGE ( 'NONE', *, *, #115299, .F. ) ;
#185286=DIRECTION ( 'NONE',  ( 0.000000000000000000, 0.000000000000000000, -1.000000000000000000 ) ) ;
#185306=AXIS2_PLACEMENT_3D ( 'NONE', #69205, #167030, #148728 ) ;
#185322=ORIENTED_EDGE ( 'NONE', *, *, #188023, .T. ) ;
#185338=EDGE_CURVE ( 'NONE', #201436, #46286, #4969, .T. ) ;
#185343=CARTESIAN_POINT ( 'NONE',  ( -21.59142135623730852, 7.850000000011158718, -54.65000000000000568 ) ) ;
#185351=CARTESIAN_POINT ( 'NONE',  ( 21.30000000000002558, 1.115600667400684642E-11, -33.50000000000000000 ) ) ;
#185352=ORIENTED_EDGE ( 'NONE', *, *, #191972, .T. ) ;
#185376=LINE ( 'NONE', #47120, #219825 ) ;
#185400=ORIENTED_EDGE ( 'NONE', *, *, #196005, .F. ) ;
#185402=EDGE_CURVE ( 'NONE', #153506, #214929, #134834, .T. ) ;
#185410=AXIS2_PLACEMENT_3D ( 'NONE', #52818, #71136, #50246 ) ;
#185424=CARTESIAN_POINT ( 'NONE',  ( 20.89192007715127986, 10.32898536001801304, -72.58266832227644727 ) ) ;
#185458=VECTOR ( 'NONE', #193767, 1000.000000000000000 ) ;
#185492=CARTESIAN_POINT ( 'NONE',  ( 18.59999999999999076, 11.65000000001115943, -58.25000000000000000 ) ) ;
#185494=ORIENTED_EDGE ( 'NONE', *, *, #40277, .T. ) ;
#185495=DIRECTION ( 'NONE',  ( -1.000000000000000000, 0.000000000000000000, 0.000000000000000000 ) ) ;
#185500=VECTOR ( 'NONE', #145805, 1000.000000000000000 ) ;
#185512=ORIENTED_EDGE ( 'NONE', *, *, #127365, .F. ) ;
#185530=FACE_OUTER_BOUND ( 'NONE', #207666, .T. ) ;
#185534=DIRECTION ( 'NONE',  ( 0.000000000000000000, 0.000000000000000000, -1.000000000000000000 ) ) ;
#185553=DIRECTION ( 'NONE',  ( 0.000000000000000000, 1.000000000000000000, 0.000000000000000000 ) ) ;
#185566=DIRECTION ( 'NONE',  ( -1.000000000000000000, -2.952720810173289112E-16, 0.000000000000000000 ) ) ;
#185600=ORIENTED_EDGE ( 'NONE', *, *, #220458, .T. ) ;
#185603=ORIENTED_EDGE ( 'NONE', *, *, #230053, .F. ) ;
#185613=AXIS2_PLACEMENT_3D ( 'NONE', #125424, #147545, #227068 ) ;
#185653=CARTESIAN_POINT ( 'NONE',  ( -21.05000000000000071, 6.344723404101344499, -33.48528214347599885 ) ) ;
#185657=FACE_OUTER_BOUND ( 'NONE', #36593, .T. ) ;
#185668=DIRECTION ( 'NONE',  ( 1.000000000000000000, -0.000000000000000000, -0.000000000000000000 ) ) ;
#185687=DIRECTION ( 'NONE',  ( 1.000000000000000000, 0.000000000000000000, 0.000000000000000000 ) ) ;
#185696=EDGE_CURVE ( 'NONE', #31610, #156407, #36137, .T. ) ;
#185698=CARTESIAN_POINT ( 'NONE',  ( -23.15000000000000213, 1.115600667400684642E-11, -69.10000000000000853 ) ) ;
#185703=DIRECTION ( 'NONE',  ( 1.000000000000000000, 0.000000000000000000, 0.000000000000000000 ) ) ;
#185704=AXIS2_PLACEMENT_3D ( 'NONE', #85717, #149612, #47905 ) ;
#185708=CARTESIAN_POINT ( 'NONE',  ( 20.21567752745019320, 10.19811410124265905, -41.38262034765165964 ) ) ;
#185740=EDGE_LOOP ( 'NONE', ( #131450, #80762, #58283, #225633 ) ) ;
#185745=CARTESIAN_POINT ( 'NONE',  ( -21.07928932188134041, 0.09889514566555068775, -27.17148334360670958 ) ) ;
#185779=CARTESIAN_POINT ( 'NONE',  ( 18.59999999999998366, 1.115600667400684642E-11, -67.00000000000000000 ) ) ;
#185790=CYLINDRICAL_SURFACE ( 'NONE', #238564, 0.1000000000000028644 ) ;
#185838=AXIS2_PLACEMENT_3D ( 'NONE', #193920, #93513, #73996 ) ;
#185843=LINE ( 'NONE', #64602, #50856 ) ;
#185859=ORIENTED_EDGE ( 'NONE', *, *, #127914, .T. ) ;
#185877=DIRECTION ( 'NONE',  ( -1.000000000000000000, -0.000000000000000000, -0.000000000000000000 ) ) ;
#185889=SPHERICAL_SURFACE ( 'NONE', #142986, 0.1000000000000000056 ) ;
#185916=DIRECTION ( 'NONE',  ( 0.000000000000000000, 0.000000000000000000, -1.000000000000000000 ) ) ;
#185933=ORIENTED_EDGE ( 'NONE', *, *, #123483, .T. ) ;
#185934=EDGE_CURVE ( 'NONE', #102195, #206017, #76782, .T. ) ;
#185959=DIRECTION ( 'NONE',  ( -1.000000000000000000, 0.000000000000000000, 0.000000000000000000 ) ) ;
#185989=AXIS2_PLACEMENT_3D ( 'NONE', #82543, #202528, #145106 ) ;
#186034=ORIENTED_EDGE ( 'NONE', *, *, #72632, .T. ) ;
#186039=CARTESIAN_POINT ( 'NONE',  ( 20.94999999999999929, 5.500000000011153745, -54.59473398108690390 ) ) ;
#186063=EDGE_CURVE ( 'NONE', #25677, #45011, #22368, .T. ) ;
#186065=DIRECTION ( 'NONE',  ( -0.000000000000000000, 0.000000000000000000, -1.000000000000000000 ) ) ;
#186070=CARTESIAN_POINT ( 'NONE',  ( 20.94999999999999929, -11.39257802169451317, -63.92605042016806749 ) ) ;
#186093=CIRCLE ( 'NONE', #252714, 0.09999999999999939493 ) ;
#186112=CARTESIAN_POINT ( 'NONE',  ( 21.09813707148777340, 6.385062105747658201, -33.46864850047048634 ) ) ;
#186202=CARTESIAN_POINT ( 'NONE',  ( 20.95512820512820440, 10.62384868372303259, -45.65000000000000568 ) ) ;
#186211=DIRECTION ( 'NONE',  ( 0.000000000000000000, 0.000000000000000000, -1.000000000000000000 ) ) ;
#186236=CARTESIAN_POINT ( 'NONE',  ( -21.05000000000000071, 1.115600667400684642E-11, -67.00000000000000000 ) ) ;
#186252=CARTESIAN_POINT ( 'NONE',  ( -18.59999999999999787, 1.162701749949165642, -41.50000000000000000 ) ) ;
#186257=ORIENTED_EDGE ( 'NONE', *, *, #170730, .T. ) ;
#186265=DIRECTION ( 'NONE',  ( 1.000000000000000000, -0.000000000000000000, -0.000000000000000000 ) ) ;
#186269=CARTESIAN_POINT ( 'NONE',  ( 23.24999999999997513, 11.65000000001116298, -59.98519422934606382 ) ) ;
#186282=EDGE_CURVE ( 'NONE', #203548, #9287, #6222, .T. ) ;
#186297=TOROIDAL_SURFACE ( 'NONE', #36472, 0.6000000000000015321, 0.1000000000000000056 ) ;
#186298=VERTEX_POINT ( 'NONE', #87442 ) ;
#186307=EDGE_CURVE ( 'NONE', #15545, #134939, #106168, .T. ) ;
#186354=AXIS2_PLACEMENT_3D ( 'NONE', #102385, #181968, #3299 ) ;
#186365=DIRECTION ( 'NONE',  ( 0.7071067811865474617, 0.7071067811865474617, 0.000000000000000000 ) ) ;
#186366=DIRECTION ( 'NONE',  ( -1.000000000000000000, -2.952720810173289112E-16, 0.000000000000000000 ) ) ;
#186375=CARTESIAN_POINT ( 'NONE',  ( -20.64999999999999858, 4.350000000011156054, -54.65000000000000568 ) ) ;
#186379=VECTOR ( 'NONE', #247773, 1000.000000000000000 ) ;
#186406=EDGE_CURVE ( 'NONE', #110700, #27581, #14828, .T. ) ;
#186408=DIRECTION ( 'NONE',  ( -1.000000000000000000, 0.000000000000000000, 0.000000000000000000 ) ) ;
#186414=CARTESIAN_POINT ( 'NONE',  ( 23.15000000000000213, -8.999999999988842703, -57.10603087734755690 ) ) ;
#186416=CARTESIAN_POINT ( 'NONE',  ( -21.11101077989000174, 0.01528526892543598421, -27.07631526527388033 ) ) ;
#186426=CARTESIAN_POINT ( 'NONE',  ( 22.50000000000000000, 7.790779598384538929, -33.39999999999999858 ) ) ;
#186437=VERTEX_POINT ( 'NONE', #135553 ) ;
#186448=VERTEX_POINT ( 'NONE', #92576 ) ;
#186499=CARTESIAN_POINT ( 'NONE',  ( -20.94999999999999929, -11.48912529306490349, -36.39999999999999858 ) ) ;
#186533=FACE_OUTER_BOUND ( 'NONE', #211181, .T. ) ;
#186540=EDGE_LOOP ( 'NONE', ( #212998, #65853, #166646, #136840 ) ) ;
#186557=EDGE_CURVE ( 'NONE', #171125, #171525, #181133, .T. ) ;
#186562=CIRCLE ( 'NONE', #11598, 2.000000000000002665 ) ;
#186569=ORIENTED_EDGE ( 'NONE', *, *, #162388, .T. ) ;
#186602=EDGE_LOOP ( 'NONE', ( #66101, #30611, #62917, #141064 ) ) ;
#186621=ORIENTED_EDGE ( 'NONE', *, *, #220377, .F. ) ;
#186638=FACE_OUTER_BOUND ( 'NONE', #145645, .T. ) ;
#186665=ORIENTED_EDGE ( 'NONE', *, *, #178541, .F. ) ;
#186677=DIRECTION ( 'NONE',  ( -1.000000000000000000, 0.000000000000000000, 0.000000000000000000 ) ) ;
#186693=CARTESIAN_POINT ( 'NONE',  ( 18.52643265882457868, 10.31973158071402885, -72.55053347133544150 ) ) ;
#186731=CIRCLE ( 'NONE', #20126, 0.3999999999999975797 ) ;
#186751=CARTESIAN_POINT ( 'NONE',  ( 22.39999999999999858, 7.790779598384538929, -33.39999999999999858 ) ) ;
#186792=DIRECTION ( 'NONE',  ( 1.301042606982683418E-14, -0.8660254037844330455, 0.5000000000000096589 ) ) ;
#186793=CARTESIAN_POINT ( 'NONE',  ( -18.59999999999999787, 1.115600667400684642E-11, -33.50000000000000000 ) ) ;
#186835=ADVANCED_FACE ( 'NONE', ( #111854 ), #191417, .F. ) ;
#186839=AXIS2_PLACEMENT_3D ( 'NONE', #137141, #75876, #36792 ) ;
#186859=CARTESIAN_POINT ( 'NONE',  ( 18.59999994388910238, -9.363566187060008872, -40.68111723680090108 ) ) ;
#186861=DIRECTION ( 'NONE',  ( 1.000000000000000000, 0.000000000000000000, 0.000000000000000000 ) ) ;
#186868=EDGE_CURVE ( 'NONE', #216334, #36408, #69642, .T. ) ;
#186899=ORIENTED_EDGE ( 'NONE', *, *, #165227, .F. ) ;
#186922=VECTOR ( 'NONE', #45702, 1000.000000000000114 ) ;
#186933=DIRECTION ( 'NONE',  ( 1.000000000000000000, 0.000000000000000000, -0.000000000000000000 ) ) ;
#187056=ORIENTED_EDGE ( 'NONE', *, *, #18803, .T. ) ;
#187062=DIRECTION ( 'NONE',  ( 1.000000000000000000, 2.952720810173289112E-16, -0.000000000000000000 ) ) ;
#187073=DIRECTION ( 'NONE',  ( 1.000000000000000000, -0.000000000000000000, -0.000000000000000000 ) ) ;
#187089=ORIENTED_EDGE ( 'NONE', *, *, #95041, .F. ) ;
#187114=ORIENTED_EDGE ( 'NONE', *, *, #18803, .F. ) ;
#187121=ORIENTED_EDGE ( 'NONE', *, *, #149078, .F. ) ;
#187129=CARTESIAN_POINT ( 'NONE',  ( -22.50000000000000000, 0.1000000000111554016, -21.85042919245520210 ) ) ;
#187172=DIRECTION ( 'NONE',  ( -1.000000000000000000, 0.000000000000000000, 0.000000000000000000 ) ) ;
#187191=AXIS2_PLACEMENT_3D ( 'NONE', #238499, #234651, #174732 ) ;
#187220=FACE_OUTER_BOUND ( 'NONE', #29078, .T. ) ;
#187240=CARTESIAN_POINT ( 'NONE',  ( -20.64999999999999858, 1.115600667400684642E-11, -67.00000000000000000 ) ) ;
#187264=FACE_OUTER_BOUND ( 'NONE', #105896, .T. ) ;
#187308=CARTESIAN_POINT ( 'NONE',  ( -20.54999999999999716, 1.115600667400684642E-11, -33.50000000000000000 ) ) ;
#187324=CARTESIAN_POINT ( 'NONE',  ( -22.59999999999999787, 0.1008583691098682150, -21.75043287651061164 ) ) ;
#187328=CARTESIAN_POINT ( 'NONE',  ( 21.14999999999999858, 11.65000000001115943, -33.60000000000000142 ) ) ;
#187333=ORIENTED_EDGE ( 'NONE', *, *, #181160, .F. ) ;
#187336=ADVANCED_FACE ( 'NONE', ( #246735 ), #189724, .F. ) ;
#187340=CARTESIAN_POINT ( 'NONE',  ( -18.59999999999999787, 1.115600667400684642E-11, -33.50000000000000000 ) ) ;
#187380=EDGE_CURVE ( 'NONE', #189010, #189515, #8148, .T. ) ;
#187383=CARTESIAN_POINT ( 'NONE',  ( -21.05000000000000071, -11.48912529306489994, -63.89999999999999858 ) ) ;
#187426=CARTESIAN_POINT ( 'NONE',  ( 18.52928932188133970, 10.27928932189250411, -58.25000000000000000 ) ) ;
#187439=AXIS2_PLACEMENT_3D ( 'NONE', #195362, #175792, #255250 ) ;
#187447=CARTESIAN_POINT ( 'NONE',  ( -18.39999999999999858, -9.599999999988844124, -40.53206939669966857 ) ) ;
#187456=ORIENTED_EDGE ( 'NONE', *, *, #18531, .T. ) ;
#187468=EDGE_CURVE ( 'NONE', #12767, #219135, #91684, .T. ) ;
#187473=EDGE_LOOP ( 'NONE', ( #196526, #15529, #45422, #62408 ) ) ;
#187476=CARTESIAN_POINT ( 'NONE',  ( 21.05193202509564543, 10.72393601970834354, -45.67253460332576509 ) ) ;
#187479=EDGE_CURVE ( 'NONE', #137139, #178845, #65007, .T. ) ;
#187527=EDGE_LOOP ( 'NONE', ( #216593, #48824, #38286, #81556 ) ) ;
#187532=CARTESIAN_POINT ( 'NONE',  ( -1.739115166359751801E-14, 11.65000000001114699, -45.75000000000000711 ) ) ;
#187534=FACE_OUTER_BOUND ( 'NONE', #149294, .T. ) ;
#187539=ORIENTED_EDGE ( 'NONE', *, *, #204546, .F. ) ;
#187551=VECTOR ( 'NONE', #180010, 1000.000000000000000 ) ;
#187567=DIRECTION ( 'NONE',  ( 7.304098846218134667E-16, -1.000000000000000000, 0.000000000000000000 ) ) ;
#187569=CARTESIAN_POINT ( 'NONE',  ( 22.39999999999999858, 7.790779598384538929, -33.39999999999999858 ) ) ;
#187600=CARTESIAN_POINT ( 'NONE',  ( 22.49544290803764213, 11.74987023786834683, -33.43468804074238676 ) ) ;
#187613=CARTESIAN_POINT ( 'NONE',  ( -23.25000000000000000, 1.115600667400684642E-11, -33.50000000000000000 ) ) ;
#187625=DIRECTION ( 'NONE',  ( 1.000000000000000000, -0.000000000000000000, -0.000000000000000000 ) ) ;
#187637=TOROIDAL_SURFACE ( 'NONE', #187439, 3.899999999999999467, 0.1000000000000000056 ) ;
#187647=CIRCLE ( 'NONE', #104394, 0.1000000000000028644 ) ;
#187721=EDGE_CURVE ( 'NONE', #200421, #126100, #192732, .T. ) ;
#187737=VERTEX_POINT ( 'NONE', #26278 ) ;
#187753=EDGE_CURVE ( 'NONE', #81578, #127685, #23354, .T. ) ;
#187773=AXIS2_PLACEMENT_3D ( 'NONE', #13136, #29212, #153969 ) ;
#187779=CONICAL_SURFACE ( 'NONE', #183686, 4.049999999999998046, 0.7853981633974604915 ) ;
#187780=DIRECTION ( 'NONE',  ( 1.000000000000000000, 0.000000000000000000, 0.000000000000000000 ) ) ;
#187786=ORIENTED_EDGE ( 'NONE', *, *, #36816, .T. ) ;
#187787=EDGE_LOOP ( 'NONE', ( #173829, #165773, #177029, #43533 ) ) ;
#187795=DIRECTION ( 'NONE',  ( 0.000000000000000000, 0.000000000000000000, -1.000000000000000000 ) ) ;
#187799=EDGE_CURVE ( 'NONE', #161314, #141916, #102381, .T. ) ;
#187805=ORIENTED_EDGE ( 'NONE', *, *, #6174, .F. ) ;
#187806=AXIS2_PLACEMENT_3D ( 'NONE', #140858, #176148, #80855 ) ;
#187837=AXIS2_PLACEMENT_3D ( 'NONE', #77906, #194043, #117053 ) ;
#187839=ORIENTED_EDGE ( 'NONE', *, *, #206611, .T. ) ;
#187890=CARTESIAN_POINT ( 'NONE',  ( 21.00000000000000000, 9.750000000011153745, -45.75000000000000711 ) ) ;
#187915=AXIS2_PLACEMENT_3D ( 'NONE', #257804, #158790, #238284 ) ;
#187921=CARTESIAN_POINT ( 'NONE',  ( 19.99999999999998934, 11.75000000001115552, -54.85000000000000142 ) ) ;
#187943=DIRECTION ( 'NONE',  ( -0.000000000000000000, 0.8660254037844502539, 0.4999999999999799605 ) ) ;
#187951=CARTESIAN_POINT ( 'NONE',  ( -21.05000000000000071, 1.115600667400684642E-11, -62.90000000000001279 ) ) ;
#187977=VERTEX_POINT ( 'NONE', #140433 ) ;
#187993=DIRECTION ( 'NONE',  ( 0.000000000000000000, 0.000000000000000000, -1.000000000000000000 ) ) ;
#187994=CARTESIAN_POINT ( 'NONE',  ( 18.49999999999999645, 1.162701749949165642, -41.60000000000000142 ) ) ;
#188019=ORIENTED_EDGE ( 'NONE', *, *, #229562, .T. ) ;
#188022=EDGE_CURVE ( 'NONE', #83334, #67212, #182151, .T. ) ;
#188023=EDGE_CURVE ( 'NONE', #186298, #82173, #2644, .T. ) ;
#188060=AXIS2_PLACEMENT_3D ( 'NONE', #39138, #254288, #139480 ) ;
#188076=ORIENTED_EDGE ( 'NONE', *, *, #72504, .F. ) ;
#188103=DIRECTION ( 'NONE',  ( 0.000000000000000000, 0.000000000000000000, -1.000000000000000000 ) ) ;
#188112=DIRECTION ( 'NONE',  ( 0.000000000000000000, 0.8700118002898321601, -0.4930308989875230030 ) ) ;
#188143=CARTESIAN_POINT ( 'NONE',  ( 21.05000000000000071, 5.500000000011153745, -54.59473398108690390 ) ) ;
#188190=CARTESIAN_POINT ( 'NONE',  ( -20.94999999999999929, -11.64999999998884483, -36.39999999999999858 ) ) ;
#188201=FACE_OUTER_BOUND ( 'NONE', #168301, .T. ) ;
#188237=FACE_OUTER_BOUND ( 'NONE', #209663, .T. ) ;
#188281=CARTESIAN_POINT ( 'NONE',  ( 23.14999999999999858, 1.115600667400684642E-11, -67.00000000000000000 ) ) ;
#188296=CARTESIAN_POINT ( 'NONE',  ( -21.05000000000000071, -1.835341550213255957, -45.05515129256298223 ) ) ;
#188312=AXIS2_PLACEMENT_3D ( 'NONE', #128112, #68135, #70729 ) ;
#188326=ADVANCED_FACE ( 'NONE', ( #37208 ), #236661, .F. ) ;
#188358=VERTEX_POINT ( 'NONE', #163562 ) ;
#188359=ADVANCED_FACE ( 'NONE', ( #243086 ), #77836, .T. ) ;
#188387=LINE ( 'NONE', #9749, #68539 ) ;
#188422=FACE_OUTER_BOUND ( 'NONE', #144781, .T. ) ;
#188428=CIRCLE ( 'NONE', #171914, 0.1000000000000028644 ) ;
#188478=DIRECTION ( 'NONE',  ( 0.000000000000000000, 0.000000000000000000, 1.000000000000000000 ) ) ;
#188515=ORIENTED_EDGE ( 'NONE', *, *, #48834, .F. ) ;
#188532=CARTESIAN_POINT ( 'NONE',  ( 19.92426406871192412, 11.75000000001116085, -58.35000000000000142 ) ) ;
#188557=ADVANCED_FACE ( 'NONE', ( #147860 ), #228687, .F. ) ;
#188580=ADVANCED_FACE ( 'NONE', ( #90427 ), #170030, .T. ) ;
#188591=DIRECTION ( 'NONE',  ( -2.952720810173289112E-16, 1.000000000000000000, 0.000000000000000000 ) ) ;
#188612=DIRECTION ( 'NONE',  ( 0.000000000000000000, 0.4999999999999956701, -0.8660254037844411501 ) ) ;
#188621=LINE ( 'NONE', #111657, #111317 ) ;
#188639=FACE_OUTER_BOUND ( 'NONE', #27736, .T. ) ;
#188640=ORIENTED_EDGE ( 'NONE', *, *, #218600, .T. ) ;
#188642=VERTEX_POINT ( 'NONE', #171320 ) ;
#188671=AXIS2_PLACEMENT_3D ( 'NONE', #249367, #150267, #244194 ) ;
#188674=CARTESIAN_POINT ( 'NONE',  ( 21.08198257630413508, 6.336596734026219480, -33.42735667621539619 ) ) ;
#188693=CARTESIAN_POINT ( 'NONE',  ( 21.05000000000000071, -8.999999999988844479, -43.39396912265245021 ) ) ;
#188726=ORIENTED_EDGE ( 'NONE', *, *, #55778, .F. ) ;
#188730=ORIENTED_EDGE ( 'NONE', *, *, #125002, .F. ) ;
#188772=CARTESIAN_POINT ( 'NONE',  ( -18.59999999999999787, -1.835859311432481045, -78.60443916879853532 ) ) ;
#188789=FACE_OUTER_BOUND ( 'NONE', #64291, .T. ) ;
#188791=FACE_OUTER_BOUND ( 'NONE', #66618, .T. ) ;
#188813=EDGE_LOOP ( 'NONE', ( #160810, #56723, #58798, #69782 ) ) ;
#188815=CARTESIAN_POINT ( 'NONE',  ( -20.85000000000000142, 7.120270961708750512, -70.65956304183931991 ) ) ;
#188823=CIRCLE ( 'NONE', #59794, 0.1000000000000000472 ) ;
#188840=CIRCLE ( 'NONE', #26352, 11.65000000000000036 ) ;
#188855=TOROIDAL_SURFACE ( 'NONE', #122216, 0.2000000000000000111, 0.1000000000000000056 ) ;
#188880=FACE_OUTER_BOUND ( 'NONE', #158485, .T. ) ;
#188916=EDGE_CURVE ( 'NONE', #187737, #99123, #39888, .T. ) ;
#188919=DIRECTION ( 'NONE',  ( 0.000000000000000000, -0.9915357197604853789, 0.1298341882520022694 ) ) ;
#188921=EDGE_CURVE ( 'NONE', #200640, #82011, #73225, .T. ) ;
#188928=CARTESIAN_POINT ( 'NONE',  ( 19.75857864376268935, 11.65000000001115943, -58.25000000000000000 ) ) ;
#188967=AXIS2_PLACEMENT_3D ( 'NONE', #215832, #100992, #217112 ) ;
#188968=CARTESIAN_POINT ( 'NONE',  ( -21.12757541349819590, 0.005161215820883788274, -27.02661942874843604 ) ) ;
#188978=ORIENTED_EDGE ( 'NONE', *, *, #7129, .F. ) ;
#188985=EDGE_LOOP ( 'NONE', ( #254438, #30159, #131911, #116967 ) ) ;
#188988=DIRECTION ( 'NONE',  ( 0.000000000000000000, 1.776356839400155604E-15, 1.000000000000000000 ) ) ;
#189008=AXIS2_PLACEMENT_3D ( 'NONE', #124161, #101980, #242801 ) ;
#189010=VERTEX_POINT ( 'NONE', #230958 ) ;
#189044=ORIENTED_EDGE ( 'NONE', *, *, #190314, .F. ) ;
#189055=EDGE_LOOP ( 'NONE', ( #144626, #158341, #66131, #171139 ) ) ;
#189063=AXIS2_PLACEMENT_3D ( 'NONE', #193017, #252966, #14397 ) ;
#189099=EDGE_LOOP ( 'NONE', ( #221005, #248096, #244180, #87355 ) ) ;
#189100=AXIS2_PLACEMENT_3D ( 'NONE', #67387, #146899, #90783 ) ;
#189177=EDGE_CURVE ( 'NONE', #191642, #248843, #215012, .T. ) ;
#189187=DIRECTION ( 'NONE',  ( 0.000000000000000000, 0.000000000000000000, -1.000000000000000000 ) ) ;
#189199=DIRECTION ( 'NONE',  ( 0.000000000000000000, 0.000000000000000000, -1.000000000000000000 ) ) ;
#189201=DIRECTION ( 'NONE',  ( -0.000000000000000000, -0.000000000000000000, -1.000000000000000000 ) ) ;
#189211=VERTEX_POINT ( 'NONE', #12 ) ;
#189220=AXIS2_PLACEMENT_3D ( 'NONE', #15814, #74515, #56170 ) ;
#189223=VERTEX_POINT ( 'NONE', #100378 ) ;
#189229=CIRCLE ( 'NONE', #76779, 0.5000000000000004441 ) ;
#189266=ORIENTED_EDGE ( 'NONE', *, *, #77341, .T. ) ;
#189312=DIRECTION ( 'NONE',  ( 1.000000000000000000, 0.000000000000000000, 0.000000000000000000 ) ) ;
#189354=CARTESIAN_POINT ( 'NONE',  ( -22.50000000000000000, 1.115600667400684642E-11, -21.85042919245520210 ) ) ;
#189356=VECTOR ( 'NONE', #255230, 1000.000000000000000 ) ;
#189404=ORIENTED_EDGE ( 'NONE', *, *, #132995, .T. ) ;
#189406=CARTESIAN_POINT ( 'NONE',  ( -18.59999999999999787, -1.851617760457748618, -78.60318971960367662 ) ) ;
#189418=CIRCLE ( 'NONE', #22269, 11.65000000000000036 ) ;
#189419=CARTESIAN_POINT ( 'NONE',  ( 18.52165635395191146, -9.481150711271022047, -40.52483758286248161 ) ) ;
#189424=VERTEX_POINT ( 'NONE', #149824 ) ;
#189472=DIRECTION ( 'NONE',  ( 1.000000000000000000, 2.952720810173289112E-16, -0.000000000000000000 ) ) ;
#189488=ORIENTED_EDGE ( 'NONE', *, *, #223923, .F. ) ;
#189515=VERTEX_POINT ( 'NONE', #19275 ) ;
#189523=ORIENTED_EDGE ( 'NONE', *, *, #138807, .T. ) ;
#189531=ORIENTED_EDGE ( 'NONE', *, *, #196590, .T. ) ;
#189563=CARTESIAN_POINT ( 'NONE',  ( 21.46681500597532377, 1.115542391533913547E-11, -26.64248884056870281 ) ) ;
#189599=CARTESIAN_POINT ( 'NONE',  ( -21.05000000000000071, 11.60000000001115517, -60.07179676972450011 ) ) ;
#189625=B_SPLINE_CURVE_WITH_KNOTS ( 'NONE', 3,
 ( #131266, #11325, #210808, #92141, #53005, #32194, #111707, #186112, #249937, #150832, #152145, #171716, #188674, #10036, #148265, #72602, #132560, #7466, #191275 ),
 .UNSPECIFIED., .F., .F.,
 ( 4, 3, 3, 3, 3, 3, 4 ),
 ( 0.000000000000000000, 7.110282409889913185E-05, 0.0001508797727291428831, 0.0002027344179858457109, 0.0002343294522349018149, 0.0002454816334821171078, 0.0002619873080085533793 ),
 .UNSPECIFIED. ) ;
#189724=TOROIDAL_SURFACE ( 'NONE', #48070, 11.70000000000000107, 0.1000000000000000056 ) ;
#189730=FACE_OUTER_BOUND ( 'NONE', #49091, .T. ) ;
#189734=CARTESIAN_POINT ( 'NONE',  ( -18.55807992284872299, 10.32898536001801304, -72.58266832227644727 ) ) ;
#189754=LINE ( 'NONE', #11124, #198548 ) ;
#189755=TOROIDAL_SURFACE ( 'NONE', #52368, 0.2000000000000000111, 0.1000000000000000056 ) ;
#189762=CARTESIAN_POINT ( 'NONE',  ( 20.95595012432476523, 10.60417921308728495, -41.09576933021813971 ) ) ;
#189775=DIRECTION ( 'NONE',  ( 0.000000000000000000, 0.000000000000000000, 1.000000000000000000 ) ) ;
#189802=CARTESIAN_POINT ( 'NONE',  ( -21.45000000000000284, 7.708578643773852157, -54.65000000000000568 ) ) ;
#189803=DIRECTION ( 'NONE',  ( 0.000000000000000000, 0.000000000000000000, -1.000000000000000000 ) ) ;
#189817=CARTESIAN_POINT ( 'NONE',  ( 20.94999999999999929, 6.450000000011156587, -43.51702717044002355 ) ) ;
#189835=FACE_OUTER_BOUND ( 'NONE', #81916, .T. ) ;
#189842=DIRECTION ( 'NONE',  ( -1.000000000000000000, 0.000000000000000000, -0.000000000000000000 ) ) ;
#189861=EDGE_CURVE ( 'NONE', #1409, #135375, #83603, .T. ) ;
#189865=VECTOR ( 'NONE', #111749, 1000.000000000000000 ) ;
#189883=CARTESIAN_POINT ( 'NONE',  ( -21.05000000000000071, 14.05000000001115623, -39.01369507076099552 ) ) ;
#189918=EDGE_CURVE ( 'NONE', #85875, #63552, #7082, .T. ) ;
#189935=CARTESIAN_POINT ( 'NONE',  ( -23.15000000000000213, -11.64999999998884483, -64.00000000000000000 ) ) ;
#189946=ORIENTED_EDGE ( 'NONE', *, *, #207607, .T. ) ;
#189962=CIRCLE ( 'NONE', #10912, 0.1000000000000000472 ) ;
#189975=CARTESIAN_POINT ( 'NONE',  ( 18.59999999999999076, 10.49142135624846439, -58.25000000000000000 ) ) ;
#190006=FACE_OUTER_BOUND ( 'NONE', #106410, .T. ) ;
#190026=ORIENTED_EDGE ( 'NONE', *, *, #115859, .F. ) ;
#190053=VECTOR ( 'NONE', #235234, 1000.000000000000000 ) ;
#190112=CARTESIAN_POINT ( 'NONE',  ( -21.02374657821573933, 11.60000000083169702, -60.07179677019823316 ) ) ;
#190117=VERTEX_POINT ( 'NONE', #32812 ) ;
#190151=VERTEX_POINT ( 'NONE', #36656 ) ;
#190163=CIRCLE ( 'NONE', #177710, 0.09999999999999939493 ) ;
#190168=CIRCLE ( 'NONE', #244307, 0.09999999999999892308 ) ;
#190181=DIRECTION ( 'NONE',  ( -6.938893903907222856E-15, 1.000000000000000000, 0.000000000000000000 ) ) ;
#190195=CARTESIAN_POINT ( 'NONE',  ( 21.05000000000000071, 5.000000000011153745, -54.59473398108690390 ) ) ;
#190221=FACE_OUTER_BOUND ( 'NONE', #21544, .T. ) ;
#190240=EDGE_LOOP ( 'NONE', ( #47899, #30388, #45710, #60327, #208686, #90974, #212688, #9085, #165171 ) ) ;
#190242=CIRCLE ( 'NONE', #56917, 0.1000000000000020595 ) ;
#190252=DIRECTION ( 'NONE',  ( 0.000000000000000000, 1.265107689135680095E-16, -1.000000000000000000 ) ) ;
#190257=VERTEX_POINT ( 'NONE', #161733 ) ;
#190259=CARTESIAN_POINT ( 'NONE',  ( 18.59999999999998366, 7.021664781911246322, -70.83356540189728889 ) ) ;
#190263=DIRECTION ( 'NONE',  ( 0.000000000000000000, 0.000000000000000000, 1.000000000000000000 ) ) ;
#190265=ORIENTED_EDGE ( 'NONE', *, *, #27861, .T. ) ;
#190273=DIRECTION ( 'NONE',  ( 0.000000000000000000, -1.000000000000000000, 0.000000000000000000 ) ) ;
#190293=TOROIDAL_SURFACE ( 'NONE', #31901, 0.2000000000000000111, 0.1000000000000000056 ) ;
#190314=EDGE_CURVE ( 'NONE', #101718, #116556, #102997, .T. ) ;
#190339=DIRECTION ( 'NONE',  ( -0.000000000000000000, 1.000000000000000000, 1.734723475976807292E-15 ) ) ;
#190357=ORIENTED_EDGE ( 'NONE', *, *, #33328, .T. ) ;
#190362=ORIENTED_EDGE ( 'NONE', *, *, #231644, .T. ) ;
#190364=CARTESIAN_POINT ( 'NONE',  ( -23.25000000000000000, 1.115600667400684642E-11, -67.00000000000000000 ) ) ;
#190382=ORIENTED_EDGE ( 'NONE', *, *, #116423, .T. ) ;
#190410=CARTESIAN_POINT ( 'NONE',  ( -23.25000000000000000, 1.115600667400684642E-11, -67.00000000000000000 ) ) ;
#190436=ORIENTED_EDGE ( 'NONE', *, *, #152796, .T. ) ;
#190441=DIRECTION ( 'NONE',  ( -0.000000000000000000, -1.000000000000000000, 0.000000000000000000 ) ) ;
#190445=CARTESIAN_POINT ( 'NONE',  ( 23.14999999999998437, 1.115600667400684642E-11, -33.50000000000000000 ) ) ;
#190454=EDGE_CURVE ( 'NONE', #77793, #138330, #99014, .T. ) ;
#190457=DIRECTION ( 'NONE',  ( -0.000000000000000000, 1.000000000000000000, -0.000000000000000000 ) ) ;
#190509=CARTESIAN_POINT ( 'NONE',  ( -18.59999999999999787, 9.350000000011156942, -45.85000000000000142 ) ) ;
#190516=CARTESIAN_POINT ( 'NONE',  ( -23.15000000000000213, -8.999999999988844479, -57.10603087734755690 ) ) ;
#190530=CIRCLE ( 'NONE', #86409, 0.1000000000000002692 ) ;
#190540=DIRECTION ( 'NONE',  ( -3.469446951953604722E-14, -0.9999176327611370985, -0.01283462868040260302 ) ) ;
#190567=EDGE_LOOP ( 'NONE', ( #31300, #95368, #103978, #65952 ) ) ;
#190568=LINE ( 'NONE', #114861, #117712 ) ;
#190574=AXIS2_PLACEMENT_3D ( 'NONE', #101995, #187993, #6781 ) ;
#190577=ADVANCED_FACE ( 'NONE', ( #32509 ), #257206, .T. ) ;
#190616=CIRCLE ( 'NONE', #15843, 0.1000000000000028644 ) ;
#190625=ORIENTED_EDGE ( 'NONE', *, *, #87220, .T. ) ;
#190631=APPLICATION_CONTEXT ( 'automotive_design' ) ;
#190674=CLOSED_SHELL ( 'NONE', ( #256682, #121188, #86046, #238067, #31342, #166247, #236399, #89743, #142586, #143679, #64716, #40104, #62963, #61498, #104214, #49157, #235022, #167898, #248925, #22599, #103878, #179905, #3581, #241122, #248270, #2262, #44863, #65837, #160150, #24941, #6593, #12323, #245033, #30913, #49466, #223343, #18934, #47307, #170060, #232570, #101279, #164186, #252762, #15831, #211855, #233045, #229561, #239094, #232628, #191848, #67972, #76240, #245422, #136440, #208574, #1300, #232279, #178450, #183396, #165691, #128504, #202983, #103527, #156900, #73700, #42177, #136866, #209562, #80146, #233120, #51619, #238863, #127386, #139858, #151983, #79958, #5821, #8090, #233736, #199440, #240323, #184303, #226284, #50192, #207191, #161596, #105828, #254192, #239084, #166824, #183459, #69873, #122885, #40009, #41833, #208083, #207547, #68926, #198807, #144480, #176598, #5006, #256524, #162103, #44595, #24071, #6788, #65855, #228682, #84474, #90184, #115020, #9906, #47342, #226044, #208018, #204199, #243780, #128605, #240612, #241686, #117012, #66057, #113862, #108486, #83704, #87976, #140559, #198877, #31007, #160737, #186835, #166135, #146327, #22525, #184559, #55173, #166527, #141098, #234428, #122284, #205354, #215215, #120630, #115366, #147909, #28408, #54634, #51024, #169706, #153357, #112931, #92408, #146484, #197861, #254743, #19607, #170497, #25990, #46995, #98292, #199537, #38463, #82049, #115972, #246699, #172008, #143663, #184653, #231630, #37106, #59234, #76041, #196394, #9829, #183706, #104399, #210686, #254294, #173644, #38605, #16786, #132193, #195669, #205425, #6049, #118722, #73498, #232870, #46204, #176670, #74409, #5181, #238112, #37166, #124668, #51975, #37660, #205177, #101743, #211682, #170722, #187336, #240724, #114480, #255699, #25824, #58492, #33148, #203300, #161401, #149007, #80462, #67314, #16941, #213705, #214096, #183305, #73336, #91922, #176532, #12391, #15299, #68400, #227673, #36062, #203640, #22628, #120826, #29927, #14786, #18494, #65771, #183042, #206315, #144998, #77076, #40221, #47863, #170091, #150589, #67012, #165821, #222157, #146620, #253295, #102966, #110757, #120230, #73824, #155580, #31713, #176829, #236802, #131240, #58701, #13254, #115240, #251229, #253393, #25302, #75102, #244081, #153367, #90324, #136569, #159777, #102399, #225118, #15747, #63212, #108236, #188580, #31431, #256002, #176823, #152002, #28181, #124648, #224090, #148535, #52063, #251076, #202765, #184682, #74379, #13096, #244899, #106548, #188557, #241986, #216750, #249903, #83166, #112871, #4886, #183046, #214558, #124062, #241387, #173959, #209363, #35564, #17993, #224296, #195718, #163778, #132947, #31862, #174504, #258094, #133748, #82368, #69449, #164708, #97525, #117568, #162489, #105791, #56763, #137700, #7496, #150510, #69557, #520, #163037, #7603, #45656, #145346, #95054, #148603, #125409, #204445, #3772, #133153, #62214, #210672, #193209, #256575, #175464, #21189, #76200, #179499, #30236, #10038, #200782, #127683, #83588, #100576, #1912, #50815, #114866, #177554, #47535, #16258, #12027, #248375, #245267, #5465, #26048, #118812, #211850, #19326, #246874, #72345, #255179, #233968, #203370, #155502, #188326, #76445, #185099, #73039, #143344, #196837, #255415, #135326, #226327, #121724, #51652, #20136, #158374, #162319, #155102, #111774, #28642, #228986, #141780, #224718, #200324, #252519, #200085, #27761, #51184, #29227, #146455, #106032, #2102, #72300, #213788, #177146, #173887, #63773, #181497, #131767, #80717, #83960, #217103, #242766, #80892, #237903, #16642, #74833, #86972, #42646, #50459, #106898, #26463, #176776, #242150, #201350, #244952, #215211, #14253, #55603, #177457, #231329, #153724, #188359, #63185, #82342, #232811, #114413, #170081, #55626, #182902, #59468, #250635, #121355, #100344, #125858, #75481, #91196, #123686, #14939, #236522, #238021, #241941, #118804, #207245, #206568, #220560, #31516, #238610, #67017, #212112, #106392, #73159, #12378, #218338, #158133, #154598, #207922, #194684, #153542, #47057, #133481, #127494, #180020, #212734, #163244, #190577, #11721, #37277, #145963, #255053, #153731, #251399 ) ) ;
#190692=CARTESIAN_POINT ( 'NONE',  ( 18.59999999999999076, 11.75000000001115907, -21.75000000000000355 ) ) ;
#190770=AXIS2_PLACEMENT_3D ( 'NONE', #58985, #138524, #43316 ) ;
#190772=EDGE_CURVE ( 'NONE', #83555, #82173, #247337, .T. ) ;
#190788=EDGE_CURVE ( 'NONE', #250359, #193526, #225191, .T. ) ;
#190799=CIRCLE ( 'NONE', #3293, 11.80000000000000426 ) ;
#190816=AXIS2_PLACEMENT_3D ( 'NONE', #92887, #232436, #96720 ) ;
#190833=CARTESIAN_POINT ( 'NONE',  ( -21.14999999999999858, 11.75000000001115552, -33.50000000000000000 ) ) ;
#190857=DIRECTION ( 'NONE',  ( 1.000000000000000000, -0.000000000000000000, -0.000000000000000000 ) ) ;
#190894=CIRCLE ( 'NONE', #253398, 0.1000000000000028644 ) ;
#190913=CIRCLE ( 'NONE', #7526, 4.000000000000003553 ) ;
#190927=VECTOR ( 'NONE', #235064, 1000.000000000000000 ) ;
#190983=ORIENTED_EDGE ( 'NONE', *, *, #147961, .F. ) ;
#190992=CARTESIAN_POINT ( 'NONE',  ( 20.85000000000000142, 1.115600667400684642E-11, -67.00000000000000000 ) ) ;
#191003=LINE ( 'NONE', #86711, #82625 ) ;
#191011=VECTOR ( 'NONE', #56382, 1000.000000000000000 ) ;
#191040=CARTESIAN_POINT ( 'NONE',  ( -18.50000000000000000, 10.29270135741298375, -72.45736188715194714 ) ) ;
#191044=CARTESIAN_POINT ( 'NONE',  ( -18.59999999999999787, -26.43935341558978891, -51.64150860750746119 ) ) ;
#191053=VECTOR ( 'NONE', #32624, 1000.000000000000227 ) ;
#191081=ORIENTED_EDGE ( 'NONE', *, *, #43092, .F. ) ;
#191093=DIRECTION ( 'NONE',  ( 0.000000000000000000, 0.2605042016806715099, 0.9654727137038706664 ) ) ;
#191161=FACE_OUTER_BOUND ( 'NONE', #64887, .T. ) ;
#191186=CARTESIAN_POINT ( 'NONE',  ( 21.05000000000000071, 1.115600667400684642E-11, -68.90000000000000568 ) ) ;
#191187=CIRCLE ( 'NONE', #78714, 11.74999999999999645 ) ;
#191190=TOROIDAL_SURFACE ( 'NONE', #157911, 4.099999999999999645, 0.1000000000000000056 ) ;
#191225=CARTESIAN_POINT ( 'NONE',  ( 19.87657994472040457, 11.75000000001104716, -58.26578812462643242 ) ) ;
#191227=DIRECTION ( 'NONE',  ( 0.000000000000000000, 1.000000000000000000, 0.000000000000000000 ) ) ;
#191243=ORIENTED_EDGE ( 'NONE', *, *, #192964, .T. ) ;
#191250=DIRECTION ( 'NONE',  ( -1.000000000000000000, 0.000000000000000000, 0.000000000000000000 ) ) ;
#191251=ORIENTED_EDGE ( 'NONE', *, *, #105244, .T. ) ;
#191260=EDGE_CURVE ( 'NONE', #67554, #971, #232699, .T. ) ;
#191270=EDGE_CURVE ( 'NONE', #115688, #196889, #224339, .T. ) ;
#191275=CARTESIAN_POINT ( 'NONE',  ( 21.07928932188134397, 6.328516656404459262, -33.40110485434561127 ) ) ;
#191312=ORIENTED_EDGE ( 'NONE', *, *, #208667, .F. ) ;
#191322=CARTESIAN_POINT ( 'NONE',  ( 20.04142135623730070, 11.65000000001115943, -54.75000000000000000 ) ) ;
#191334=ORIENTED_EDGE ( 'NONE', *, *, #184046, .F. ) ;
#191341=ORIENTED_EDGE ( 'NONE', *, *, #233542, .F. ) ;
#191356=DIRECTION ( 'NONE',  ( 0.000000000000000000, 0.000000000000000000, -1.000000000000000000 ) ) ;
#191388=ORIENTED_EDGE ( 'NONE', *, *, #142096, .F. ) ;
#191393=DIRECTION ( 'NONE',  ( 1.000000000000000000, -0.000000000000000000, -0.000000000000000000 ) ) ;
#191417=PLANE ( 'NONE',  #211090 ) ;
#191421=LINE ( 'NONE', #209668, #242058 ) ;
#191438=CARTESIAN_POINT ( 'NONE',  ( 21.05000000000000071, 1.115649653272650466E-11, -63.00000000000000000 ) ) ;
#191448=EDGE_LOOP ( 'NONE', ( #4002, #94491, #146550, #86566 ) ) ;
#191488=CYLINDRICAL_SURFACE ( 'NONE', #25628, 0.09999999999999939493 ) ;
#191496=DIRECTION ( 'NONE',  ( 0.000000000000000000, 0.000000000000000000, -1.000000000000000000 ) ) ;
#191523=CARTESIAN_POINT ( 'NONE',  ( -18.39999999999999858, -9.499999999988849808, -40.53206939669966857 ) ) ;
#191567=ORIENTED_EDGE ( 'NONE', *, *, #3805, .F. ) ;
#191601=DIRECTION ( 'NONE',  ( 0.000000000000000000, 0.000000000000000000, -1.000000000000000000 ) ) ;
#191628=DIRECTION ( 'NONE',  ( 0.000000000000000000, 0.000000000000000000, -1.000000000000000000 ) ) ;
#191642=VERTEX_POINT ( 'NONE', #61105 ) ;
#191681=CYLINDRICAL_SURFACE ( 'NONE', #217499, 11.80000000000000426 ) ;
#191718=DIRECTION ( 'NONE',  ( -0.000000000000000000, -0.000000000000000000, 1.000000000000000000 ) ) ;
#191734=DIRECTION ( 'NONE',  ( 1.000000000000000000, 0.000000000000000000, 0.000000000000000000 ) ) ;
#191740=AXIS2_PLACEMENT_3D ( 'NONE', #109338, #250159, #230602 ) ;
#191762=AXIS2_PLACEMENT_3D ( 'NONE', #176315, #96718, #159315 ) ;
#191765=FACE_OUTER_BOUND ( 'NONE', #144145, .T. ) ;
#191767=FACE_OUTER_BOUND ( 'NONE', #251219, .T. ) ;
#191779=DIRECTION ( 'NONE',  ( -1.000000000000000000, -0.000000000000000000, -0.000000000000000000 ) ) ;
#191793=ORIENTED_EDGE ( 'NONE', *, *, #24088, .F. ) ;
#191814=ORIENTED_EDGE ( 'NONE', *, *, #15764, .T. ) ;
#191837=VERTEX_POINT ( 'NONE', #154793 ) ;
#191848=ADVANCED_FACE ( 'NONE', ( #116923 ), #235571, .F. ) ;
#191871=DIRECTION ( 'NONE',  ( -1.000000000000000000, 0.000000000000000000, 0.000000000000000000 ) ) ;
#191872=CARTESIAN_POINT ( 'NONE',  ( 18.43466021071411021, -9.494190690445394765, -73.61706156012773761 ) ) ;
#191891=DIRECTION ( 'NONE',  ( -0.000000000000000000, 1.000000000000000000, -0.000000000000000000 ) ) ;
#191895=TOROIDAL_SURFACE ( 'NONE', #121167, 0.2000000000000000111, 0.1000000000000000056 ) ;
#191912=CARTESIAN_POINT ( 'NONE',  ( 21.87500000000000355, 9.750000000011153745, -54.75000000000000000 ) ) ;
#191941=CARTESIAN_POINT ( 'NONE',  ( 23.15000000000000213, -9.499999999988844479, -57.10603087734755690 ) ) ;
#191972=EDGE_CURVE ( 'NONE', #11734, #201436, #16590, .T. ) ;
#191985=CARTESIAN_POINT ( 'NONE',  ( 19.97071067811864609, 11.72071067812981404, -58.15000000000000568 ) ) ;
#191996=ORIENTED_EDGE ( 'NONE', *, *, #183556, .T. ) ;
#192003=ORIENTED_EDGE ( 'NONE', *, *, #125960, .F. ) ;
#192004=B_SPLINE_CURVE_WITH_KNOTS ( 'NONE', 3,
 ( #170501, #212152, #113042, #209577 ),
 .UNSPECIFIED., .F., .F.,
 ( 4, 4 ),
 ( 0.000000000000000000, 0.0001048066582182386071 ),
 .UNSPECIFIED. ) ;
#192026=AXIS2_PLACEMENT_3D ( 'NONE', #64458, #145254, #185687 ) ;
#192027=FACE_OUTER_BOUND ( 'NONE', #31186, .T. ) ;
#192042=EDGE_CURVE ( 'NONE', #107953, #189223, #28038, .T. ) ;
#192067=EDGE_LOOP ( 'NONE', ( #113932, #16000, #36994, #140103 ) ) ;
#192080=DIRECTION ( 'NONE',  ( 0.000000000000000000, -1.000000000000000000, -0.000000000000000000 ) ) ;
#192116=VECTOR ( 'NONE', #88092, 1000.000000000000000 ) ;
#192117=VERTEX_POINT ( 'NONE', #249705 ) ;
#192140=CARTESIAN_POINT ( 'NONE',  ( 22.47007471830798053, 1.115784124149148083E-11, -25.77928934807354722 ) ) ;
#192174=DIRECTION ( 'NONE',  ( 1.000000000000000000, 0.000000000000000000, 0.000000000000000000 ) ) ;
#192181=DIRECTION ( 'NONE',  ( 0.000000000000000000, -6.938893903907222067E-15, -1.000000000000000000 ) ) ;
#192199=FACE_OUTER_BOUND ( 'NONE', #91880, .T. ) ;
#192209=VERTEX_POINT ( 'NONE', #179183 ) ;
#192214=DIRECTION ( 'NONE',  ( 0.000000000000000000, 0.000000000000000000, -1.000000000000000000 ) ) ;
#192217=EDGE_LOOP ( 'NONE', ( #102816, #26711, #132301, #210860 ) ) ;
#192221=ORIENTED_EDGE ( 'NONE', *, *, #98583, .F. ) ;
#192228=AXIS2_PLACEMENT_3D ( 'NONE', #86735, #166336, #245839 ) ;
#192245=ORIENTED_EDGE ( 'NONE', *, *, #10989, .T. ) ;
#192248=CARTESIAN_POINT ( 'NONE',  ( -18.50000000000000000, -1.866714910046153308, -45.25267524628200988 ) ) ;
#192270=PLANE ( 'NONE',  #167659 ) ;
#192292=FACE_OUTER_BOUND ( 'NONE', #115974, .T. ) ;
#192301=DIRECTION ( 'NONE',  ( 4.377807931758638789E-15, 0.2605042016806672911, 0.9654727137038716656 ) ) ;
#192309=DIRECTION ( 'NONE',  ( 0.000000000000000000, 0.000000000000000000, -1.000000000000000000 ) ) ;
#192311=CARTESIAN_POINT ( 'NONE',  ( -18.59999999999999787, 1.162701749949165642, -41.60000000000000142 ) ) ;
#192314=LINE ( 'NONE', #51479, #114139 ) ;
#192321=ORIENTED_EDGE ( 'NONE', *, *, #166935, .T. ) ;
#192367=CIRCLE ( 'NONE', #242234, 1.899999999999999023 ) ;
#192414=AXIS2_PLACEMENT_3D ( 'NONE', #58620, #235980, #142020 ) ;
#192426=DIRECTION ( 'NONE',  ( 0.000000000000000000, 0.000000000000000000, -1.000000000000000000 ) ) ;
#192444=EDGE_LOOP ( 'NONE', ( #60422, #223567, #179417, #214411 ) ) ;
#192457=CARTESIAN_POINT ( 'NONE',  ( 18.59999999999999076, 1.750000000011155743, -45.16951155790165018 ) ) ;
#192478=LINE ( 'NONE', #252427, #93097 ) ;
#192491=CARTESIAN_POINT ( 'NONE',  ( -18.50000000000000000, 9.350000000011156942, -54.65000000000000568 ) ) ;
#192494=EDGE_CURVE ( 'NONE', #40541, #86338, #4455, .T. ) ;
#192526=LINE ( 'NONE', #112990, #211821 ) ;
#192562=CARTESIAN_POINT ( 'NONE',  ( -18.45140287520618472, -9.486077739518409047, -73.64052312668613354 ) ) ;
#192613=DIRECTION ( 'NONE',  ( 0.000000000000000000, -1.000000000000000000, 0.000000000000000000 ) ) ;
#192629=( BOUNDED_SURFACE ( )  B_SPLINE_SURFACE ( 3, 2, ( 
 ( #99889, #77774, #238139 ),
 ( #59475, #159922, #2092 ),
 ( #202868, #217283, #197738 ),
 ( #182035, #178209, #19098 ),
 ( #62087, #179485, #790 ),
 ( #118207, #139008, #24261 ) ),
 .UNSPECIFIED., .F., .F., .F. ) 
 B_SPLINE_SURFACE_WITH_KNOTS ( ( 4, 2, 4 ),
 ( 3, 3 ),
 ( -1.776356839400250465E-15, 0.7853981633974468357, 1.570796326794895448 ),
 ( 0.000000000000000000, 1.000000000000000000 ),
 .UNSPECIFIED. ) 
 GEOMETRIC_REPRESENTATION_ITEM ( )  RATIONAL_B_SPLINE_SURFACE ( (
 ( 1.000000000000000000, 0.4999999999999960587, 1.000000000000000000),
 ( 1.000000000000000000, 0.4993418825336311540, 1.000000000000000000),
 ( 1.000000000000000000, 0.5278258667054654962, 1.000000000000000000),
 ( 1.000000000000000000, 0.6092287576699327856, 1.000000000000000000),
 ( 1.000000000000000000, 0.6611148371776465194, 1.000000000000000000),
 ( 1.000000000000000000, 0.7071067811865658914, 1.000000000000000000) ) ) 
 REPRESENTATION_ITEM ( '' )  SURFACE ( )  );
#192654=EDGE_CURVE ( 'NONE', #36652, #116043, #137712, .T. ) ;
#192683=DIRECTION ( 'NONE',  ( 1.000000000000000000, -0.000000000000000000, -0.000000000000000000 ) ) ;
#192720=DIRECTION ( 'NONE',  ( 0.000000000000000000, -1.734723475976757554E-14, 1.000000000000000000 ) ) ;
#192732=LINE ( 'NONE', #48388, #244072 ) ;
#192742=DIRECTION ( 'NONE',  ( 0.000000000000000000, 0.000000000000000000, 1.000000000000000000 ) ) ;
#192802=AXIS2_PLACEMENT_3D ( 'NONE', #160334, #159050, #199453 ) ;
#192837=CIRCLE ( 'NONE', #96918, 0.09999999999999939493 ) ;
#192877=DIRECTION ( 'NONE',  ( 0.000000000000000000, 1.000000000000000000, 2.891205793294679805E-16 ) ) ;
#192878=ORIENTED_EDGE ( 'NONE', *, *, #140878, .T. ) ;
#192889=AXIS2_PLACEMENT_3D ( 'NONE', #128663, #90789, #208204 ) ;
#192937=ORIENTED_EDGE ( 'NONE', *, *, #210980, .F. ) ;
#192958=ORIENTED_EDGE ( 'NONE', *, *, #11698, .F. ) ;
#192964=EDGE_CURVE ( 'NONE', #113714, #176243, #195647, .T. ) ;
#192980=CARTESIAN_POINT ( 'NONE',  ( 22.39999999999999503, 7.790779598384535376, -33.50000000000000000 ) ) ;
#192985=ORIENTED_EDGE ( 'NONE', *, *, #90233, .T. ) ;
#192992=CARTESIAN_POINT ( 'NONE',  ( -21.07016717456946608, 6.320940838111406279, -33.50000000000000711 ) ) ;
#193017=CARTESIAN_POINT ( 'NONE',  ( -20.94999999999999929, 14.05000000001115623, -61.48630492923908974 ) ) ;
#193037=ORIENTED_EDGE ( 'NONE', *, *, #146782, .T. ) ;
#193043=CIRCLE ( 'NONE', #213873, 0.1000000000000028644 ) ;
#193063=EDGE_LOOP ( 'NONE', ( #226471, #57448, #71330, #101303 ) ) ;
#193072=DIRECTION ( 'NONE',  ( -1.000000000000000000, -0.000000000000000000, 0.000000000000000000 ) ) ;
#193082=CARTESIAN_POINT ( 'NONE',  ( -23.15000000000000213, 1.115600667400684642E-11, -63.00000000000000000 ) ) ;
#193114=CIRCLE ( 'NONE', #205544, 0.09999999999999939493 ) ;
#193148=AXIS2_PLACEMENT_3D ( 'NONE', #25093, #225801, #223249 ) ;
#193162=AXIS2_PLACEMENT_3D ( 'NONE', #33706, #113194, #233168 ) ;
#193171=ORIENTED_EDGE ( 'NONE', *, *, #169021, .T. ) ;
#193178=EDGE_CURVE ( 'NONE', #182882, #100505, #93235, .T. ) ;
#193193=CARTESIAN_POINT ( 'NONE',  ( -18.50000000000000000, 11.65000000001115232, -40.51480577065400013 ) ) ;
#193206=CARTESIAN_POINT ( 'NONE',  ( 21.07199075132371746, 8.774944999127242795, -45.71353216161286070 ) ) ;
#193209=ADVANCED_FACE ( 'NONE', ( #59206 ), #193633, .F. ) ;
#193212=DIRECTION ( 'NONE',  ( 0.000000000000000000, 0.000000000000000000, -1.000000000000000000 ) ) ;
#193222=ORIENTED_EDGE ( 'NONE', *, *, #138232, .T. ) ;
#193258=AXIS2_PLACEMENT_3D ( 'NONE', #64722, #185959, #162564 ) ;
#193277=CARTESIAN_POINT ( 'NONE',  ( 18.50000000000000000, -9.399999999988843058, -73.88204184817267617 ) ) ;
#193287=EDGE_LOOP ( 'NONE', ( #73775, #211775, #152735, #222049 ) ) ;
#193289=CARTESIAN_POINT ( 'NONE',  ( 22.60000000000000142, 11.74956712350054744, -33.39914163090129762 ) ) ;
#193293=TOROIDAL_SURFACE ( 'NONE', #14240, 0.2000000000000000111, 0.1000000000000000056 ) ;
#193359=CARTESIAN_POINT ( 'NONE',  ( 18.59999999999999432, -1.162701749926853712, -41.60000000000000142 ) ) ;
#193366=MANIFOLD_SOLID_BREP ( 'Stock-MAS-200-1', #190674 ) ;
#193387=FACE_OUTER_BOUND ( 'NONE', #65086, .T. ) ;
#193395=EDGE_CURVE ( 'NONE', #73952, #201073, #5668, .T. ) ;
#193414=ORIENTED_EDGE ( 'NONE', *, *, #255629, .T. ) ;
#193427=DIRECTION ( 'NONE',  ( -1.000000000000000000, -0.000000000000000000, -0.000000000000000000 ) ) ;
#193431=EDGE_CURVE ( 'NONE', #251013, #237327, #12660, .T. ) ;
#193445=AXIS2_PLACEMENT_3D ( 'NONE', #230662, #128993, #226790 ) ;
#193450=CARTESIAN_POINT ( 'NONE',  ( 20.85000000000000142, 11.75000000001115907, -60.21613433702191287 ) ) ;
#193456=DIRECTION ( 'NONE',  ( 1.000000000000000000, -0.000000000000000000, 0.000000000000000000 ) ) ;
#193462=CARTESIAN_POINT ( 'NONE',  ( 21.05000000000000071, 6.540656951712399803, -33.50000000000000000 ) ) ;
#193472=AXIS2_PLACEMENT_3D ( 'NONE', #85680, #42742, #206954 ) ;
#193482=LINE ( 'NONE', #115208, #153437 ) ;
#193490=DIRECTION ( 'NONE',  ( 0.000000000000000000, 0.000000000000000000, -1.000000000000000000 ) ) ;
#193508=AXIS2_PLACEMENT_3D ( 'NONE', #179367, #41146, #157246 ) ;
#193510=ORIENTED_EDGE ( 'NONE', *, *, #78744, .T. ) ;
#193526=VERTEX_POINT ( 'NONE', #168679 ) ;
#193537=DIRECTION ( 'NONE',  ( 1.000000000000000000, -0.000000000000000000, -0.000000000000000000 ) ) ;
#193571=CARTESIAN_POINT ( 'NONE',  ( 20.85000000000000142, 7.120270961708750512, -70.65956304183931991 ) ) ;
#193578=EDGE_CURVE ( 'NONE', #41950, #45390, #96755, .T. ) ;
#193589=DIRECTION ( 'NONE',  ( -1.000000000000000000, -7.304098846218134667E-16, 0.000000000000000000 ) ) ;
#193605=ORIENTED_EDGE ( 'NONE', *, *, #7670, .F. ) ;
#193621=DIRECTION ( 'NONE',  ( 1.000000000000000000, 0.000000000000000000, -0.000000000000000000 ) ) ;
#193633=CYLINDRICAL_SURFACE ( 'NONE', #220570, 0.09999999999999939493 ) ;
#193638=EDGE_CURVE ( 'NONE', #172639, #138742, #65358, .T. ) ;
#193652=ORIENTED_EDGE ( 'NONE', *, *, #190772, .T. ) ;
#193694=FACE_OUTER_BOUND ( 'NONE', #125275, .T. ) ;
#193704=DIRECTION ( 'NONE',  ( 1.000000000000000000, 0.000000000000000000, 0.000000000000000000 ) ) ;
#193722=TOROIDAL_SURFACE ( 'NONE', #102102, 1.900000000000002576, 0.1000000000000000056 ) ;
#193733=DIRECTION ( 'NONE',  ( 0.000000000000000000, 0.000000000000000000, -1.000000000000000000 ) ) ;
#193737=AXIS2_PLACEMENT_3D ( 'NONE', #2527, #39127, #79496 ) ;
#193767=DIRECTION ( 'NONE',  ( -0.000000000000000000, -1.000000000000000000, -0.000000000000000000 ) ) ;
#193788=VERTEX_POINT ( 'NONE', #202310 ) ;
#193795=ORIENTED_EDGE ( 'NONE', *, *, #108537, .F. ) ;
#193802=B_SPLINE_CURVE_WITH_KNOTS ( 'NONE', 3,
 ( #215193, #104215, #65104, #183776, #219034, #159098, #224173, #164222 ),
 .UNSPECIFIED., .F., .F.,
 ( 4, 2, 2, 4 ),
 ( 0.000000000000000000, 0.0001094981963948490336, 0.0002189963927896980671, 0.0004379927855793961343 ),
 .UNSPECIFIED. ) ;
#193814=VECTOR ( 'NONE', #129894, 1000.000000000000000 ) ;
#193827=VECTOR ( 'NONE', #163370, 1000.000000000000000 ) ;
#193843=SPHERICAL_SURFACE ( 'NONE', #157390, 0.1000000000000000056 ) ;
#193876=CIRCLE ( 'NONE', #114770, 0.2000000000000057288 ) ;
#193879=ORIENTED_EDGE ( 'NONE', *, *, #82606, .F. ) ;
#193884=ORIENTED_EDGE ( 'NONE', *, *, #127211, .T. ) ;
#193920=CARTESIAN_POINT ( 'NONE',  ( -22.50000000000000000, 1.115600667400684642E-11, -33.50000000000000000 ) ) ;
#193928=ORIENTED_EDGE ( 'NONE', *, *, #197098, .T. ) ;
#193957=VECTOR ( 'NONE', #172419, 1000.000000000000000 ) ;
#193969=CARTESIAN_POINT ( 'NONE',  ( -21.04386569057627909, 11.75000000001120526, -60.14283735177934886 ) ) ;
#193982=EDGE_CURVE ( 'NONE', #217509, #158454, #17124, .T. ) ;
#194000=EDGE_CURVE ( 'NONE', #151911, #250000, #141994, .T. ) ;
#194043=DIRECTION ( 'NONE',  ( 1.000000000000000000, 0.000000000000000000, 0.000000000000000000 ) ) ;
#194082=EDGE_LOOP ( 'NONE', ( #248613, #249045, #83316 ) ) ;
#194114=CARTESIAN_POINT ( 'NONE',  ( -21.59780538579341425, 6.847090529954407145, -33.40102133040201693 ) ) ;
#194133=ORIENTED_EDGE ( 'NONE', *, *, #16209, .F. ) ;
#194162=SPHERICAL_SURFACE ( 'NONE', #105735, 0.1000000000000000056 ) ;
#194164=FACE_OUTER_BOUND ( 'NONE', #79630, .T. ) ;
#194166=CIRCLE ( 'NONE', #115045, 0.09999999999999736877 ) ;
#194218=EDGE_CURVE ( 'NONE', #170769, #252337, #58766, .T. ) ;
#194295=EDGE_CURVE ( 'NONE', #231817, #82011, #2128, .T. ) ;
#194312=CARTESIAN_POINT ( 'NONE',  ( -18.59999999999999787, 1.250000000011155299, -41.50000000000000000 ) ) ;
#194327=CARTESIAN_POINT ( 'NONE',  ( -18.59999999999999787, -1.164121893230052995, -74.91484808557160591 ) ) ;
#194350=CYLINDRICAL_SURFACE ( 'NONE', #77689, 0.09999999999999939493 ) ;
#194360=VECTOR ( 'NONE', #220500, 1000.000000000000000 ) ;
#194363=ORIENTED_EDGE ( 'NONE', *, *, #243309, .T. ) ;
#194376=VERTEX_POINT ( 'NONE', #256140 ) ;
#194387=DIRECTION ( 'NONE',  ( -2.827886303505249259E-16, 0.8660254037844412611, 0.4999999999999956701 ) ) ;
#194388=CARTESIAN_POINT ( 'NONE',  ( 21.05000000000000426, 0.06570161033324307953, -27.24168394266797222 ) ) ;
#194390=DIRECTION ( 'NONE',  ( 0.000000000000000000, 0.000000000000000000, -1.000000000000000000 ) ) ;
#194404=CYLINDRICAL_SURFACE ( 'NONE', #146689, 4.049999999999998046 ) ;
#194413=EDGE_CURVE ( 'NONE', #205356, #228375, #17305, .T. ) ;
#194430=CARTESIAN_POINT ( 'NONE',  ( -21.95218792049438861, 0.09902843981107177507, -26.29849243875332121 ) ) ;
#194431=CARTESIAN_POINT ( 'NONE',  ( 18.44206774312970865, -9.491027357528929898, -73.62622750469815003 ) ) ;
#194433=VERTEX_POINT ( 'NONE', #39764 ) ;
#194446=LINE ( 'NONE', #198264, #204253 ) ;
#194448=LINE ( 'NONE', #211421, #167903 ) ;
#194452=EDGE_CURVE ( 'NONE', #40042, #241304, #513, .T. ) ;
#194462=CIRCLE ( 'NONE', #95032, 12.87499999999999822 ) ;
#194482=ORIENTED_EDGE ( 'NONE', *, *, #37021, .T. ) ;
#194573=VECTOR ( 'NONE', #117465, 1000.000000000000000 ) ;
#194594=DIRECTION ( 'NONE',  ( 0.000000000000000000, 0.000000000000000000, 1.000000000000000000 ) ) ;
#194611=EDGE_LOOP ( 'NONE', ( #174323, #43519 ) ) ;
#194649=CIRCLE ( 'NONE', #86260, 0.1000000000000028644 ) ;
#194660=DIRECTION ( 'NONE',  ( 0.000000000000000000, 1.224646799142057732E-16, 1.000000000000000000 ) ) ;
#194676=CARTESIAN_POINT ( 'NONE',  ( 22.50000000000000000, 0.1000000000111554016, -25.70922040162662014 ) ) ;
#194684=ADVANCED_FACE ( 'NONE', ( #110582 ), #91023, .T. ) ;
#194718=AXIS2_PLACEMENT_3D ( 'NONE', #217367, #200396, #238226 ) ;
#194761=CARTESIAN_POINT ( 'NONE',  ( -23.15000000000000213, -8.999999999988844479, -57.60603087734755690 ) ) ;
#194781=DIRECTION ( 'NONE',  ( 0.000000000000000000, -0.8660254037844411501, -0.4999999999999956701 ) ) ;
#194802=ORIENTED_EDGE ( 'NONE', *, *, #120076, .T. ) ;
#194844=VERTEX_POINT ( 'NONE', #96136 ) ;
#194849=DIRECTION ( 'NONE',  ( -1.000000000000000000, -0.000000000000000000, -0.000000000000000000 ) ) ;
#194855=LINE ( 'NONE', #16218, #145190 ) ;
#194874=AXIS2_PLACEMENT_3D ( 'NONE', #180494, #42950, #66363 ) ;
#194900=EDGE_LOOP ( 'NONE', ( #161214, #13064, #31953, #125655 ) ) ;
#194903=VERTEX_POINT ( 'NONE', #81684 ) ;
#194932=CYLINDRICAL_SURFACE ( 'NONE', #185410, 0.1000000000000028644 ) ;
#194933=DIRECTION ( 'NONE',  ( 0.000000000000000000, 0.000000000000000000, 1.000000000000000000 ) ) ;
#194934=EDGE_LOOP ( 'NONE', ( #55550, #10155, #56247, #193222, #118932, #170699, #228345, #32045 ) ) ;
#194956=AXIS2_PLACEMENT_3D ( 'NONE', #202342, #23740, #103219 ) ;
#194966=CARTESIAN_POINT ( 'NONE',  ( -23.15000000000000213, 11.65000000001115588, -45.65000000000000568 ) ) ;
#194976=DIRECTION ( 'NONE',  ( 0.000000000000000000, 0.9999631594459058581, 0.008583690987093516023 ) ) ;
#195031=AXIS2_PLACEMENT_3D ( 'NONE', #249484, #152976, #150385 ) ;
#195044=CARTESIAN_POINT ( 'NONE',  ( -20.94999999999999929, -11.48912529306489994, -63.89999999999999858 ) ) ;
#195058=CARTESIAN_POINT ( 'NONE',  ( 20.84999999999998721, 10.33248238083634440, -72.59484654391314962 ) ) ;
#195063=DIRECTION ( 'NONE',  ( 2.259780016855445309E-14, 0.9875055080513753802, -0.1575844902526748192 ) ) ;
#195065=DIRECTION ( 'NONE',  ( 0.000000000000000000, 1.000000000000000000, 0.000000000000000000 ) ) ;
#195069=CARTESIAN_POINT ( 'NONE',  ( 19.90621891164687440, 11.75000000001116263, -58.32844527787765543 ) ) ;
#195077=VERTEX_POINT ( 'NONE', #107704 ) ;
#195097=DIRECTION ( 'NONE',  ( 1.000000000000000000, 0.000000000000000000, 0.000000000000000000 ) ) ;
#195182=CIRCLE ( 'NONE', #12017, 0.5000000000000004441 ) ;
#195215=CARTESIAN_POINT ( 'NONE',  ( 21.05000000000000071, -9.499999999988848032, -43.39396912265245021 ) ) ;
#195219=DIRECTION ( 'NONE',  ( 0.000000000000000000, 0.000000000000000000, -1.000000000000000000 ) ) ;
#195227=VECTOR ( 'NONE', #167249, 1000.000000000000000 ) ;
#195268=ORIENTED_EDGE ( 'NONE', *, *, #64906, .T. ) ;
#195290=SPHERICAL_SURFACE ( 'NONE', #238287, 0.1000000000000000056 ) ;
#195303=AXIS2_PLACEMENT_3D ( 'NONE', #203502, #246472, #104369 ) ;
#195317=ORIENTED_EDGE ( 'NONE', *, *, #200813, .F. ) ;
#195330=CARTESIAN_POINT ( 'NONE',  ( 20.85000000000000142, -11.74999999998883560, -64.10000000000000853 ) ) ;
#195362=CARTESIAN_POINT ( 'NONE',  ( 23.14999999999999858, 1.115600667400684642E-11, -67.00000000000000000 ) ) ;
#195384=CARTESIAN_POINT ( 'NONE',  ( -23.15000000000000213, 2.500000000011154633, -53.77537807723790309 ) ) ;
#195389=AXIS2_PLACEMENT_3D ( 'NONE', #31630, #73327, #171157 ) ;
#195392=AXIS2_PLACEMENT_3D ( 'NONE', #34524, #192301, #178876 ) ;
#195406=DIRECTION ( 'NONE',  ( 0.000000000000000000, -1.000000000000000000, 0.000000000000000000 ) ) ;
#195441=DIRECTION ( 'NONE',  ( 1.000000000000000000, -0.000000000000000000, 0.000000000000000000 ) ) ;
#195443=VECTOR ( 'NONE', #33579, 999.9999999999998863 ) ;
#195445=DIRECTION ( 'NONE',  ( 0.000000000000000000, 0.000000000000000000, -1.000000000000000000 ) ) ;
#195471=DIRECTION ( 'NONE',  ( 0.000000000000000000, 0.000000000000000000, -1.000000000000000000 ) ) ;
#195475=CARTESIAN_POINT ( 'NONE',  ( 21.05000000000000071, -1.849084418615859926, -45.15601052144712213 ) ) ;
#195487=ORIENTED_EDGE ( 'NONE', *, *, #193431, .F. ) ;
#195498=VERTEX_POINT ( 'NONE', #52556 ) ;
#195512=VECTOR ( 'NONE', #121326, 1000.000000000000000 ) ;
#195525=VERTEX_POINT ( 'NONE', #226033 ) ;
#195545=VERTEX_POINT ( 'NONE', #31760 ) ;
#195547=LINE ( 'NONE', #15635, #74899 ) ;
#195564=CARTESIAN_POINT ( 'NONE',  ( -21.00219873199057474, 11.60538868788778721, -40.41264742829478962 ) ) ;
#195565=CARTESIAN_POINT ( 'NONE',  ( 23.24999999999999645, 1.115600667400684642E-11, -67.00000000000000000 ) ) ;
#195583=ORIENTED_EDGE ( 'NONE', *, *, #76572, .T. ) ;
#195596=CARTESIAN_POINT ( 'NONE',  ( 22.50000000000000000, 0.1000000000111554016, -21.85042919245520210 ) ) ;
#195608=CYLINDRICAL_SURFACE ( 'NONE', #192414, 0.09999999999999939493 ) ;
#195630=CARTESIAN_POINT ( 'NONE',  ( -20.54999999999999716, 1.115624548013267999E-11, -65.10000000000000853 ) ) ;
#195633=CARTESIAN_POINT ( 'NONE',  ( -20.54999999999999716, -11.74999999998884448, -50.25000000000000000 ) ) ;
#195647=CIRCLE ( 'NONE', #199741, 0.09999999999999939493 ) ;
#195669=ADVANCED_FACE ( 'NONE', ( #193387 ), #113688, .T. ) ;
#195715=CARTESIAN_POINT ( 'NONE',  ( 23.14999999999999147, 4.150000000011154988, -33.50000000000000000 ) ) ;
#195717=VECTOR ( 'NONE', #122338, 1000.000000000000000 ) ;
#195718=ADVANCED_FACE ( 'NONE', ( #198495 ), #116407, .T. ) ;
#195737=CARTESIAN_POINT ( 'NONE',  ( -18.50000000000000000, 11.75000000001115197, -33.60000000000000142 ) ) ;
#195739=LINE ( 'NONE', #99153, #254880 ) ;
#195750=EDGE_CURVE ( 'NONE', #242609, #146650, #213838, .T. ) ;
#195758=EDGE_CURVE ( 'NONE', #183157, #205018, #58954, .T. ) ;
#195786=ORIENTED_EDGE ( 'NONE', *, *, #145605, .F. ) ;
#195809=DIRECTION ( 'NONE',  ( 0.000000000000000000, 1.000000000000000000, 0.000000000000000000 ) ) ;
#195810=CIRCLE ( 'NONE', #41678, 0.09999999999999939493 ) ;
#195830=ORIENTED_EDGE ( 'NONE', *, *, #174806, .F. ) ;
#195831=CARTESIAN_POINT ( 'NONE',  ( 20.94999999999999929, -1.835341550213257733, -45.05515129256298223 ) ) ;
#195834=AXIS2_PLACEMENT_3D ( 'NONE', #49310, #187567, #88412 ) ;
#195849=EDGE_LOOP ( 'NONE', ( #243902, #21618, #210184, #8779 ) ) ;
#195854=DIRECTION ( 'NONE',  ( -0.4999999999999799050, 0.000000000000000000, -0.8660254037844502539 ) ) ;
#195860=PLANE ( 'NONE',  #59739 ) ;
#195878=CARTESIAN_POINT ( 'NONE',  ( -23.25000000000000000, -11.74999999998884448, -63.89999999999999858 ) ) ;
#195891=AXIS2_PLACEMENT_3D ( 'NONE', #87692, #69454, #146376 ) ;
#195932=AXIS2_PLACEMENT_3D ( 'NONE', #28821, #67894, #209986 ) ;
#195980=ORIENTED_EDGE ( 'NONE', *, *, #144939, .T. ) ;
#195982=EDGE_CURVE ( 'NONE', #72990, #200797, #63817, .T. ) ;
#196005=EDGE_CURVE ( 'NONE', #212748, #30860, #75378, .T. ) ;
#196052=ORIENTED_EDGE ( 'NONE', *, *, #224739, .T. ) ;
#196104=AXIS2_PLACEMENT_3D ( 'NONE', #12206, #90419, #72171 ) ;
#196111=DIRECTION ( 'NONE',  ( -0.000000000000000000, 0.8660254037844383745, -0.5000000000000003331 ) ) ;
#196121=LINE ( 'NONE', #232690, #149500 ) ;
#196150=CARTESIAN_POINT ( 'NONE',  ( -23.15000000000000213, 11.75000000001115552, -54.85000000000000142 ) ) ;
#196152=EDGE_CURVE ( 'NONE', #19663, #3284, #22974, .T. ) ;
#196174=CIRCLE ( 'NONE', #46318, 0.1000000000000028644 ) ;
#196199=LINE ( 'NONE', #111531, #177747 ) ;
#196200=CARTESIAN_POINT ( 'NONE',  ( -20.85000000000000142, -11.74999999998884448, -67.00000000000000000 ) ) ;
#196204=EDGE_CURVE ( 'NONE', #96705, #152028, #239433, .T. ) ;
#196209=AXIS2_PLACEMENT_3D ( 'NONE', #196688, #121047, #18057 ) ;
#196216=CARTESIAN_POINT ( 'NONE',  ( 18.59999999999999787, 1.866714910068465239, -45.25267524628200988 ) ) ;
#196303=FACE_OUTER_BOUND ( 'NONE', #214112, .T. ) ;
#196316=TOROIDAL_SURFACE ( 'NONE', #129685, 0.2000000000000000111, 0.1000000000000000056 ) ;
#196329=EDGE_CURVE ( 'NONE', #257458, #17700, #172845, .T. ) ;
#196360=DIRECTION ( 'NONE',  ( -1.000000000000000000, -3.265361837132813093E-16, 0.000000000000000000 ) ) ;
#196363=CARTESIAN_POINT ( 'NONE',  ( -18.50000000000000000, 9.350000000011156942, -45.85000000000000142 ) ) ;
#196382=AXIS2_PLACEMENT_3D ( 'NONE', #252193, #73606, #227499 ) ;
#196394=ADVANCED_FACE ( 'NONE', ( #95869 ), #115441, .T. ) ;
#196456=CARTESIAN_POINT ( 'NONE',  ( -22.59999999999999787, 11.74956712350054744, -33.39914163090129762 ) ) ;
#196491=ORIENTED_EDGE ( 'NONE', *, *, #253647, .T. ) ;
#196514=CIRCLE ( 'NONE', #225712, 4.000000000000003553 ) ;
#196515=DIRECTION ( 'NONE',  ( 0.000000000000000000, 0.5000000000000078826, -0.8660254037844340447 ) ) ;
#196526=ORIENTED_EDGE ( 'NONE', *, *, #48018, .T. ) ;
#196566=CARTESIAN_POINT ( 'NONE',  ( 21.05000000000000071, 4.850467289730772791, -45.53426740900168568 ) ) ;
#196587=CARTESIAN_POINT ( 'NONE',  ( 20.22516295850462598, 9.899364295460458152, -41.41006571209138798 ) ) ;
#196590=EDGE_CURVE ( 'NONE', #133244, #55828, #138642, .T. ) ;
#196616=ORIENTED_EDGE ( 'NONE', *, *, #140100, .T. ) ;
#196630=CIRCLE ( 'NONE', #142464, 0.1000000000000010186 ) ;
#196649=DIRECTION ( 'NONE',  ( -1.000000000000000000, -3.265361837132813093E-16, 0.000000000000000000 ) ) ;
#196657=DIRECTION ( 'NONE',  ( 0.000000000000000000, -0.8660254037844384856, 0.5000000000000003331 ) ) ;
#196669=SPHERICAL_SURFACE ( 'NONE', #218380, 0.1000000000000000056 ) ;
#196678=DIRECTION ( 'NONE',  ( 0.000000000000000000, 0.000000000000000000, -1.000000000000000000 ) ) ;
#196688=CARTESIAN_POINT ( 'NONE',  ( 20.94999999999999929, -8.999999999988842703, -57.10603087734755690 ) ) ;
#196691=PLANE ( 'NONE',  #234573 ) ;
#196692=AXIS2_PLACEMENT_3D ( 'NONE', #126927, #115064, #52504 ) ;
#196729=CYLINDRICAL_SURFACE ( 'NONE', #207710, 0.09999999999999939493 ) ;
#196768=ORIENTED_EDGE ( 'NONE', *, *, #141381, .F. ) ;
#196801=LINE ( 'NONE', #13068, #79325 ) ;
#196825=AXIS2_PLACEMENT_3D ( 'NONE', #16049, #57694, #116416 ) ;
#196837=ADVANCED_FACE ( 'NONE', ( #60301 ), #255892, .F. ) ;
#196876=CARTESIAN_POINT ( 'NONE',  ( 21.04999999999908411, 8.776282895301829257, -45.65790900265250229 ) ) ;
#196887=SPHERICAL_SURFACE ( 'NONE', #87944, 0.1000000000000000056 ) ;
#196889=VERTEX_POINT ( 'NONE', #21221 ) ;
#196916=CARTESIAN_POINT ( 'NONE',  ( -18.59999999999999787, 11.65000000001115232, -45.65000000000000568 ) ) ;
#196922=FACE_OUTER_BOUND ( 'NONE', #204857, .T. ) ;
#196934=CARTESIAN_POINT ( 'NONE',  ( -21.93340585898929973, 1.115541036281197940E-11, -26.17585297787465137 ) ) ;
#196944=CARTESIAN_POINT ( 'NONE',  ( 21.14999999999999858, 11.65000000001115943, -45.65000000000000568 ) ) ;
#196969=ORIENTED_EDGE ( 'NONE', *, *, #95881, .F. ) ;
#197005=ORIENTED_EDGE ( 'NONE', *, *, #96368, .T. ) ;
#197009=ORIENTED_EDGE ( 'NONE', *, *, #222460, .F. ) ;
#197028=DIRECTION ( 'NONE',  ( 1.000000000000000000, 0.000000000000000000, 0.000000000000000000 ) ) ;
#197038=VERTEX_POINT ( 'NONE', #167154 ) ;
#197075=DIRECTION ( 'NONE',  ( 0.000000000000000000, 0.000000000000000000, -1.000000000000000000 ) ) ;
#197098=EDGE_CURVE ( 'NONE', #57195, #108495, #193043, .T. ) ;
#197129=CARTESIAN_POINT ( 'NONE',  ( 21.07928932188134397, 0.09889514566555242248, -27.17148334360669537 ) ) ;
#197144=DIRECTION ( 'NONE',  ( 0.000000000000000000, -0.4999999999999649170, 0.8660254037844589137 ) ) ;
#197176=ORIENTED_EDGE ( 'NONE', *, *, #112424, .T. ) ;
#197232=CIRCLE ( 'NONE', #13890, 0.1999999999999987899 ) ;
#197240=DIRECTION ( 'NONE',  ( -1.000000000000000000, 0.000000000000000000, 0.000000000000000000 ) ) ;
#197278=EDGE_CURVE ( 'NONE', #24103, #159940, #18421, .T. ) ;
#197318=CARTESIAN_POINT ( 'NONE',  ( -23.15000000000000213, 2.000000000011154189, -46.72462192276210402 ) ) ;
#197337=ORIENTED_EDGE ( 'NONE', *, *, #194295, .F. ) ;
#197355=ORIENTED_EDGE ( 'NONE', *, *, #190788, .T. ) ;
#197365=EDGE_CURVE ( 'NONE', #80895, #18621, #72429, .T. ) ;
#197381=CARTESIAN_POINT ( 'NONE',  ( 20.94999999999999574, -11.64999999998883595, -36.39999999999999858 ) ) ;
#197392=ORIENTED_EDGE ( 'NONE', *, *, #101632, .T. ) ;
#197406=VECTOR ( 'NONE', #11426, 1000.000000000000000 ) ;
#197429=CARTESIAN_POINT ( 'NONE',  ( -20.94999999999999929, 11.60000000001115161, -40.42820323027555673 ) ) ;
#197451=ORIENTED_EDGE ( 'NONE', *, *, #50581, .T. ) ;
#197454=CARTESIAN_POINT ( 'NONE',  ( -21.05000000000000071, -11.39257802169451139, -63.92605042016806749 ) ) ;
#197455=CARTESIAN_POINT ( 'NONE',  ( 20.94999999999999929, 10.47338541492405817, -41.07865446424855094 ) ) ;
#197484=CARTESIAN_POINT ( 'NONE',  ( 22.39999999999999858, 1.115600667400684642E-11, -33.50000000000000000 ) ) ;
#197499=DIRECTION ( 'NONE',  ( 1.000000000000000000, 0.000000000000000000, -0.000000000000000000 ) ) ;
#197510=CARTESIAN_POINT ( 'NONE',  ( -23.15000000000000213, -11.74999999998884448, -21.75000000000000355 ) ) ;
#197518=ORIENTED_EDGE ( 'NONE', *, *, #82606, .T. ) ;
#197537=VERTEX_POINT ( 'NONE', #136647 ) ;
#197576=CARTESIAN_POINT ( 'NONE',  ( 21.13461538461538325, 8.885417037985614996, -45.74999999999999289 ) ) ;
#197580=DIRECTION ( 'NONE',  ( 0.000000000000000000, -0.8660254037844247188, 0.5000000000000245359 ) ) ;
#197582=PLANE ( 'NONE',  #104561 ) ;
#197598=PLANE ( 'NONE',  #63889 ) ;
#197610=ORIENTED_EDGE ( 'NONE', *, *, #52569, .T. ) ;
#197623=ORIENTED_EDGE ( 'NONE', *, *, #162021, .T. ) ;
#197633=TOROIDAL_SURFACE ( 'NONE', #43708, 11.65000000000000036, 0.1000000000000000056 ) ;
#197645=DIRECTION ( 'NONE',  ( -7.304098846218201720E-16, 1.000000000000000000, 0.000000000000000000 ) ) ;
#197677=AXIS2_PLACEMENT_3D ( 'NONE', #4491, #241826, #142717 ) ;
#197684=CARTESIAN_POINT ( 'NONE',  ( 20.95083306685154056, 8.916842641901356004, -41.97732485325835938 ) ) ;
#197686=DIRECTION ( 'NONE',  ( -0.000000000000000000, -0.000000000000000000, 1.000000000000000000 ) ) ;
#197707=VERTEX_POINT ( 'NONE', #170077 ) ;
#197716=EDGE_LOOP ( 'NONE', ( #164641, #173119, #255387, #11526 ) ) ;
#197738=CARTESIAN_POINT ( 'NONE',  ( 20.94560253601876809, 11.75000000001115907, -60.01008351251527984 ) ) ;
#197752=ORIENTED_EDGE ( 'NONE', *, *, #215893, .T. ) ;
#197761=SURFACE_STYLE_USAGE ( .BOTH. , #157396 ) ;
#197774=DIRECTION ( 'NONE',  ( 0.000000000000000000, 0.000000000000000000, -1.000000000000000000 ) ) ;
#197787=VERTEX_POINT ( 'NONE', #29282 ) ;
#197804=ORIENTED_EDGE ( 'NONE', *, *, #139903, .T. ) ;
#197818=CARTESIAN_POINT ( 'NONE',  ( 21.14999999999999858, 11.65000000001115943, -45.65000000000000568 ) ) ;
#197861=ADVANCED_FACE ( 'NONE', ( #236418 ), #233859, .F. ) ;
#197881=AXIS2_PLACEMENT_3D ( 'NONE', #79348, #136759, #200598 ) ;
#197915=ORIENTED_EDGE ( 'NONE', *, *, #177808, .T. ) ;
#197927=FACE_OUTER_BOUND ( 'NONE', #135444, .T. ) ;
#197953=CARTESIAN_POINT ( 'NONE',  ( 20.85000000000000142, 11.75000000001115907, -60.21613433702191287 ) ) ;
#197974=ORIENTED_EDGE ( 'NONE', *, *, #97323, .F. ) ;
#197995=CARTESIAN_POINT ( 'NONE',  ( -18.59999999999999787, 9.350000000011156942, -54.65000000000000568 ) ) ;
#198054=CARTESIAN_POINT ( 'NONE',  ( 23.24999999999999289, 11.65000000001116298, -54.85000000000000142 ) ) ;
#198055=ORIENTED_EDGE ( 'NONE', *, *, #87734, .F. ) ;
#198129=AXIS2_PLACEMENT_3D ( 'NONE', #134409, #69344, #172331 ) ;
#198135=CARTESIAN_POINT ( 'NONE',  ( 22.41477678272288188, 0.0008238657741001866345, -21.85041471548460379 ) ) ;
#198140=ORIENTED_EDGE ( 'NONE', *, *, #92716, .F. ) ;
#198149=FACE_OUTER_BOUND ( 'NONE', #189099, .T. ) ;
#198165=PLANE ( 'NONE',  #98620 ) ;
#198186=CARTESIAN_POINT ( 'NONE',  ( -23.25000000000000000, 1.115650265596050101E-11, -29.45000000000000284 ) ) ;
#198189=ORIENTED_EDGE ( 'NONE', *, *, #118525, .F. ) ;
#198192=ORIENTED_EDGE ( 'NONE', *, *, #82167, .F. ) ;
#198219=ORIENTED_EDGE ( 'NONE', *, *, #132167, .F. ) ;
#198221=CARTESIAN_POINT ( 'NONE',  ( -21.00023020733502932, 1.115542391533913547E-11, -27.10913075473164824 ) ) ;
#198247=FACE_OUTER_BOUND ( 'NONE', #163136, .T. ) ;
#198252=CARTESIAN_POINT ( 'NONE',  ( -21.33487959338958362, 6.725558151922345296, -33.50000000000000000 ) ) ;
#198264=CARTESIAN_POINT ( 'NONE',  ( -23.15000000000000213, 4.250000000011156409, -45.75000000000000000 ) ) ;
#198362=CARTESIAN_POINT ( 'NONE',  ( -20.64999999999999858, 2.000000000011154189, -53.77537807723790309 ) ) ;
#198376=DIRECTION ( 'NONE',  ( 0.000000000000000000, 0.000000000000000000, -1.000000000000000000 ) ) ;
#198389=AXIS2_PLACEMENT_3D ( 'NONE', #120965, #182204, #217448 ) ;
#198410=CARTESIAN_POINT ( 'NONE',  ( -18.59999999999999787, 11.65000000001115232, -40.51480577065400013 ) ) ;
#198464=AXIS2_PLACEMENT_3D ( 'NONE', #100869, #157059, #166062 ) ;
#198495=FACE_OUTER_BOUND ( 'NONE', #176948, .T. ) ;
#198533=FACE_OUTER_BOUND ( 'NONE', #230031, .T. ) ;
#198545=ORIENTED_EDGE ( 'NONE', *, *, #175901, .F. ) ;
#198548=VECTOR ( 'NONE', #90636, 1000.000000000000000 ) ;
#198575=CARTESIAN_POINT ( 'NONE',  ( -20.85000000000000142, -1.736705739456431807, -78.51742258762372728 ) ) ;
#198587=CIRCLE ( 'NONE', #236003, 11.90000000000000213 ) ;
#198630=VECTOR ( 'NONE', #210463, 1000.000000000000000 ) ;
#198661=ORIENTED_EDGE ( 'NONE', *, *, #141803, .F. ) ;
#198669=CARTESIAN_POINT ( 'NONE',  ( 23.14999999999999503, 11.65000000001116298, -59.98519422934606382 ) ) ;
#198707=CARTESIAN_POINT ( 'NONE',  ( -23.15000000000000213, 1.115600667400684642E-11, -67.00000000000000000 ) ) ;
#198709=CARTESIAN_POINT ( 'NONE',  ( 18.50000000000000000, -9.399999999988843058, -73.88204184817267617 ) ) ;
#198737=EDGE_CURVE ( 'NONE', #87561, #183680, #81476, .T. ) ;
#198741=DIRECTION ( 'NONE',  ( 1.000000000000000000, 0.000000000000000000, -0.000000000000000000 ) ) ;
#198764=DIRECTION ( 'NONE',  ( -0.000000000000000000, 0.8660254037844383745, -0.5000000000000003331 ) ) ;
#198807=ADVANCED_FACE ( 'NONE', ( #24349 ), #108675, .F. ) ;
#198861=ORIENTED_EDGE ( 'NONE', *, *, #11499, .T. ) ;
#198862=AXIS2_PLACEMENT_3D ( 'NONE', #29693, #171775, #128773 ) ;
#198867=CARTESIAN_POINT ( 'NONE',  ( 20.97462148592277131, 8.874737576461731337, -45.75464433173102918 ) ) ;
#198874=DIRECTION ( 'NONE',  ( 0.000000000000000000, 0.000000000000000000, 1.000000000000000000 ) ) ;
#198877=ADVANCED_FACE ( 'NONE', ( #38144 ), #134632, .T. ) ;
#198879=EDGE_CURVE ( 'NONE', #159940, #115264, #122662, .T. ) ;
#198930=DIRECTION ( 'NONE',  ( 1.000000000000000000, 7.304098846218134667E-16, 0.000000000000000000 ) ) ;
#198937=ORIENTED_EDGE ( 'NONE', *, *, #181868, .F. ) ;
#198939=ORIENTED_EDGE ( 'NONE', *, *, #149078, .T. ) ;
#198945=DIRECTION ( 'NONE',  ( 1.000000000000000000, 7.304098846218134667E-16, 0.000000000000000000 ) ) ;
#198949=ORIENTED_EDGE ( 'NONE', *, *, #246657, .T. ) ;
#198960=CARTESIAN_POINT ( 'NONE',  ( -23.15000000000000213, 11.65000000001115588, -54.85000000000000142 ) ) ;
#198983=CIRCLE ( 'NONE', #57502, 0.09999999999999971412 ) ;
#198984=CARTESIAN_POINT ( 'NONE',  ( 18.50000000000000355, -9.419209763398097124, -40.74776946275895284 ) ) ;
#198987=CIRCLE ( 'NONE', #203275, 0.1000000000000028644 ) ;
#199017=EDGE_CURVE ( 'NONE', #3690, #141829, #120270, .T. ) ;
#199033=DIRECTION ( 'NONE',  ( 4.408576920032447355E-17, -0.1350103645451876666, -0.9908441862701600211 ) ) ;
#199055=CARTESIAN_POINT ( 'NONE',  ( -23.15000000000000213, 1.115600667400684642E-11, -67.00000000000000000 ) ) ;
#199066=DIRECTION ( 'NONE',  ( 0.000000000000000000, 0.000000000000000000, -1.000000000000000000 ) ) ;
#199095=EDGE_CURVE ( 'NONE', #1409, #226915, #226871, .T. ) ;
#199097=DIRECTION ( 'NONE',  ( -0.000000000000000000, -0.000000000000000000, 1.000000000000000000 ) ) ;
#199100=VERTEX_POINT ( 'NONE', #247878 ) ;
#199130=DIRECTION ( 'NONE',  ( -3.265361837132813093E-16, 1.000000000000000000, 0.000000000000000000 ) ) ;
#199134=EDGE_CURVE ( 'NONE', #88637, #55402, #47088, .T. ) ;
#199165=CARTESIAN_POINT ( 'NONE',  ( 20.59588692710267921, 10.36872342118021528, -41.13908109451047324 ) ) ;
#199167=FACE_OUTER_BOUND ( 'NONE', #40521, .T. ) ;
#199183=DIRECTION ( 'NONE',  ( 0.000000000000000000, 1.000000000000000000, 0.000000000000000000 ) ) ;
#199184=VERTEX_POINT ( 'NONE', #228329 ) ;
#199189=PRODUCT_DEFINITION_CONTEXT ( 'detailed design', #229068, 'design' ) ;
#199208=VECTOR ( 'NONE', #155028, 1000.000000000000000 ) ;
#199255=DIRECTION ( 'NONE',  ( 0.000000000000000000, -0.9908441862701600211, -0.1350103645451876666 ) ) ;
#199272=DIRECTION ( 'NONE',  ( 0.000000000000000000, -1.000000000000000000, 0.000000000000000000 ) ) ;
#199303=CARTESIAN_POINT ( 'NONE',  ( 23.14999999999999858, 5.000000000011153745, -45.90526601891310321 ) ) ;
#199308=CARTESIAN_POINT ( 'NONE',  ( -20.94999999999999929, -1.162701749926853712, -41.40000000000000568 ) ) ;
#199309=CIRCLE ( 'NONE', #232644, 11.80000000000000426 ) ;
#199373=LINE ( 'NONE', #138082, #37680 ) ;
#199386=EDGE_LOOP ( 'NONE', ( #67327, #67924, #205459, #135785 ) ) ;
#199395=LINE ( 'NONE', #96400, #41101 ) ;
#199419=CARTESIAN_POINT ( 'NONE',  ( 20.94999999999999929, 8.776282895303628706, -42.05862899514094977 ) ) ;
#199440=ADVANCED_FACE ( 'NONE', ( #122506 ), #121253, .T. ) ;
#199453=DIRECTION ( 'NONE',  ( 0.000000000000000000, 0.000000000000000000, -1.000000000000000000 ) ) ;
#199462=CIRCLE ( 'NONE', #182314, 0.09999999999999910349 ) ;
#199491=ORIENTED_EDGE ( 'NONE', *, *, #244147, .F. ) ;
#199495=( BOUNDED_CURVE ( )  B_SPLINE_CURVE ( 3, ( #123751, #104159, #227978, #243688 ),
 .UNSPECIFIED., .F., .F. ) 
 B_SPLINE_CURVE_WITH_KNOTS ( ( 4, 4 ),
 ( 4.712388980384689674, 6.283185307179586232 ),
 .UNSPECIFIED. ) 
 CURVE ( )  GEOMETRIC_REPRESENTATION_ITEM ( )  RATIONAL_B_SPLINE_CURVE ( ( 1.000000000000000000, 0.8047378541243649375, 0.8047378541243649375, 1.000000000000000000 ) ) 
 REPRESENTATION_ITEM ( '' )  );
#199537=ADVANCED_FACE ( 'NONE', ( #224149 ), #246297, .F. ) ;
#199575=DIRECTION ( 'NONE',  ( 0.000000000000000000, -1.000000000000000000, 6.308085367188393199E-16 ) ) ;
#199608=VECTOR ( 'NONE', #241246, 999.9999999999998863 ) ;
#199643=ORIENTED_EDGE ( 'NONE', *, *, #3827, .F. ) ;
#199665=ORIENTED_EDGE ( 'NONE', *, *, #33516, .T. ) ;
#199672=EDGE_LOOP ( 'NONE', ( #197451, #18736, #71735 ) ) ;
#199691=CIRCLE ( 'NONE', #216407, 0.09999999999999939493 ) ;
#199692=CARTESIAN_POINT ( 'NONE',  ( -20.64999999999999858, 2.400000000011155432, -53.77537807723790309 ) ) ;
#199693=DIRECTION ( 'NONE',  ( 0.000000000000000000, 0.4930308989875324399, 0.8700118002898268310 ) ) ;
#199711=CARTESIAN_POINT ( 'NONE',  ( -20.54999999999999361, 11.65000000001115232, -54.85000000000000142 ) ) ;
#199719=ORIENTED_EDGE ( 'NONE', *, *, #85801, .T. ) ;
#199741=AXIS2_PLACEMENT_3D ( 'NONE', #105059, #163810, #64692 ) ;
#199784=DIRECTION ( 'NONE',  ( 0.000000000000000000, 0.000000000000000000, -1.000000000000000000 ) ) ;
#199790=DIRECTION ( 'NONE',  ( 1.000000000000000000, -0.000000000000000000, -0.000000000000000000 ) ) ;
#199816=ORIENTED_EDGE ( 'NONE', *, *, #196204, .T. ) ;
#199824=ORIENTED_EDGE ( 'NONE', *, *, #232783, .T. ) ;
#199830=DIRECTION ( 'NONE',  ( -1.836970198721029934E-16, 1.000000000000000000, 0.000000000000000000 ) ) ;
#199845=CARTESIAN_POINT ( 'NONE',  ( 20.94999999999999929, 1.115600667400684642E-11, -67.00000000000000000 ) ) ;
#199892=DIRECTION ( 'NONE',  ( -1.000000000000000000, -1.836970198721029934E-16, 0.000000000000000000 ) ) ;
#199970=EDGE_CURVE ( 'NONE', #225394, #80895, #131377, .T. ) ;
#200016=AXIS2_PLACEMENT_3D ( 'NONE', #2084, #218562, #137742 ) ;
#200028=FACE_OUTER_BOUND ( 'NONE', #63522, .T. ) ;
#200036=ORIENTED_EDGE ( 'NONE', *, *, #103644, .F. ) ;
#200056=PLANE ( 'NONE',  #194874 ) ;
#200068=EDGE_LOOP ( 'NONE', ( #162431, #61351, #166380, #233565 ) ) ;
#200085=ADVANCED_FACE ( 'NONE', ( #32093 ), #27383, .T. ) ;
#200093=ORIENTED_EDGE ( 'NONE', *, *, #215253, .F. ) ;
#200119=DIRECTION ( 'NONE',  ( 2.952720810173289112E-16, -1.000000000000000000, 0.000000000000000000 ) ) ;
#200128=CARTESIAN_POINT ( 'NONE',  ( 19.75857864376268935, 11.75000000001115907, -58.35000000000000142 ) ) ;
#200130=CARTESIAN_POINT ( 'NONE',  ( 21.05000000000000071, 6.650000000011155876, -43.51702717044002355 ) ) ;
#200171=CARTESIAN_POINT ( 'NONE',  ( -21.55000000000000426, 7.708578643773852157, -54.65000000000000568 ) ) ;
#200198=DIRECTION ( 'NONE',  ( 0.000000000000000000, 0.9908441862701596881, 0.1350103645451904977 ) ) ;
#200206=ORIENTED_EDGE ( 'NONE', *, *, #123749, .F. ) ;
#200239=CARTESIAN_POINT ( 'NONE',  ( -20.94788355080264353, 10.30207779525983014, -72.48955207167824710 ) ) ;
#200255=AXIS2_PLACEMENT_3D ( 'NONE', #207878, #29254, #110024 ) ;
#200324=ADVANCED_FACE ( 'NONE', ( #159729 ), #123377, .T. ) ;
#200334=DIRECTION ( 'NONE',  ( -1.000000000000000000, -0.000000000000000000, 0.000000000000000000 ) ) ;
#200396=DIRECTION ( 'NONE',  ( 1.000000000000000000, 0.000000000000000000, 0.000000000000000000 ) ) ;
#200407=ORIENTED_EDGE ( 'NONE', *, *, #155086, .T. ) ;
#200421=VERTEX_POINT ( 'NONE', #65758 ) ;
#200452=ORIENTED_EDGE ( 'NONE', *, *, #242321, .T. ) ;
#200475=EDGE_CURVE ( 'NONE', #151911, #27454, #244349, .T. ) ;
#200478=CARTESIAN_POINT ( 'NONE',  ( 18.59999999999999787, 5.900000000011102586, -43.71909976465641989 ) ) ;
#200482=DIRECTION ( 'NONE',  ( 0.000000000000000000, -1.000000000000000000, 0.000000000000000000 ) ) ;
#200501=CARTESIAN_POINT ( 'NONE',  ( 21.04999999999988702, 0.01471785653530134283, -27.15527659590986431 ) ) ;
#200509=VERTEX_POINT ( 'NONE', #130864 ) ;
#200555=CARTESIAN_POINT ( 'NONE',  ( 21.14999999999999503, -11.64999999998883595, -21.75000000000000355 ) ) ;
#200574=CARTESIAN_POINT ( 'NONE',  ( 18.59999999999999432, -1.261786168553869603, -41.58649896354548048 ) ) ;
#200581=ORIENTED_EDGE ( 'NONE', *, *, #174037, .T. ) ;
#200592=DIRECTION ( 'NONE',  ( 0.000000000000000000, 1.000000000000000000, 0.000000000000000000 ) ) ;
#200598=DIRECTION ( 'NONE',  ( 1.000000000000000000, 0.000000000000000000, 0.000000000000000000 ) ) ;
#200630=CARTESIAN_POINT ( 'NONE',  ( 21.05000000000000071, 10.72371711693665652, -45.67623960113817816 ) ) ;
#200635=VERTEX_POINT ( 'NONE', #230631 ) ;
#200640=VERTEX_POINT ( 'NONE', #188928 ) ;
#200661=DIRECTION ( 'NONE',  ( 0.000000000000000000, -0.1350103645451876666, 0.9908441862701600211 ) ) ;
#200700=CARTESIAN_POINT ( 'NONE',  ( 20.95568717954149562, 10.60199405390297400, -41.10250836826865140 ) ) ;
#200712=VECTOR ( 'NONE', #34883, 1000.000000000000000 ) ;
#200732=DIRECTION ( 'NONE',  ( 0.000000000000000000, 1.000000000000000000, 0.000000000000000000 ) ) ;
#200754=CARTESIAN_POINT ( 'NONE',  ( 21.05000000000000071, 1.115600667400684642E-11, -67.00000000000000000 ) ) ;
#200757=EDGE_CURVE ( 'NONE', #197707, #41986, #46406, .T. ) ;
#200758=EDGE_CURVE ( 'NONE', #167819, #153879, #11131, .T. ) ;
#200773=DIRECTION ( 'NONE',  ( 1.000000000000000000, 0.000000000000000000, 0.000000000000000000 ) ) ;
#200781=DIRECTION ( 'NONE',  ( 0.000000000000000000, 0.9915357197604973694, -0.1298341882519105928 ) ) ;
#200782=ADVANCED_FACE ( 'NONE', ( #79219 ), #34157, .T. ) ;
#200797=VERTEX_POINT ( 'NONE', #239610 ) ;
#200813=EDGE_CURVE ( 'NONE', #179043, #13961, #52629, .T. ) ;
#200860=DIRECTION ( 'NONE',  ( 0.000000000000000000, 0.000000000000000000, 1.000000000000000000 ) ) ;
#200868=ORIENTED_EDGE ( 'NONE', *, *, #51924, .F. ) ;
#200872=VERTEX_POINT ( 'NONE', #205591 ) ;
#200939=DIRECTION ( 'NONE',  ( 0.000000000000000000, 1.000000000000000000, 0.000000000000000000 ) ) ;
#200972=AXIS2_PLACEMENT_3D ( 'NONE', #181036, #100164, #16830 ) ;
#201039=VERTEX_POINT ( 'NONE', #72536 ) ;
#201073=VERTEX_POINT ( 'NONE', #16416 ) ;
#201087=VECTOR ( 'NONE', #47865, 1000.000000000000000 ) ;
#201096=ORIENTED_EDGE ( 'NONE', *, *, #131343, .F. ) ;
#201100=LINE ( 'NONE', #240245, #65607 ) ;
#201110=AXIS2_PLACEMENT_3D ( 'NONE', #192491, #154677, #217163 ) ;
#201128=FACE_OUTER_BOUND ( 'NONE', #183319, .T. ) ;
#201134=CIRCLE ( 'NONE', #180866, 0.1000000000000001027 ) ;
#201168=LINE ( 'NONE', #62944, #126322 ) ;
#201178=FACE_OUTER_BOUND ( 'NONE', #226007, .T. ) ;
#201182=EDGE_CURVE ( 'NONE', #109070, #33939, #61202, .T. ) ;
#201200=VERTEX_POINT ( 'NONE', #42379 ) ;
#201216=EDGE_CURVE ( 'NONE', #233728, #55518, #61378, .T. ) ;
#201318=CARTESIAN_POINT ( 'NONE',  ( 20.94999999999999574, -1.360870587180885716, -41.57299792709095954 ) ) ;
#201331=AXIS2_PLACEMENT_3D ( 'NONE', #48541, #186792, #167244 ) ;
#201345=DIRECTION ( 'NONE',  ( 2.557131231893037478E-16, -0.8660254037844385966, 0.5000000000000003331 ) ) ;
#201350=ADVANCED_FACE ( 'NONE', ( #94334 ), #186297, .T. ) ;
#201357=CARTESIAN_POINT ( 'NONE',  ( -21.11825140030082082, 6.445407565431136021, -33.49279637936726317 ) ) ;
#201375=AXIS2_PLACEMENT_3D ( 'NONE', #132232, #34447, #91819 ) ;
#201382=CARTESIAN_POINT ( 'NONE',  ( 23.15000000000000213, -11.48912529306489994, -63.89999999999999858 ) ) ;
#201394=CARTESIAN_POINT ( 'NONE',  ( 21.07928932188134397, 0.09889514566555242248, -27.17148334360669537 ) ) ;
#201396=CARTESIAN_POINT ( 'NONE',  ( -21.09096482362052782, 0.03944827878522684517, -27.13645563459557053 ) ) ;
#201418=VERTEX_POINT ( 'NONE', #134736 ) ;
#201421=EDGE_CURVE ( 'NONE', #213770, #229112, #33138, .T. ) ;
#201436=VERTEX_POINT ( 'NONE', #198575 ) ;
#201442=AXIS2_PLACEMENT_3D ( 'NONE', #236682, #215827, #100986 ) ;
#201447=CARTESIAN_POINT ( 'NONE',  ( -20.85000000000000142, -11.64999999998884483, -64.10000000000000853 ) ) ;
#201460=EDGE_LOOP ( 'NONE', ( #128759, #112065, #29747, #16580 ) ) ;
#201485=AXIS2_PLACEMENT_3D ( 'NONE', #23815, #203703, #103291 ) ;
#201491=LINE ( 'NONE', #703, #157283 ) ;
#201493=AXIS2_PLACEMENT_3D ( 'NONE', #78848, #220933, #77558 ) ;
#201513=EDGE_CURVE ( 'NONE', #36910, #53762, #24240, .T. ) ;
#201530=AXIS2_PLACEMENT_3D ( 'NONE', #164369, #122689, #215648 ) ;
#201531=VERTEX_POINT ( 'NONE', #136877 ) ;
#201563=ORIENTED_EDGE ( 'NONE', *, *, #57873, .T. ) ;
#201585=DIRECTION ( 'NONE',  ( 3.469446951953635015E-14, -0.000000000000000000, 1.000000000000000000 ) ) ;
#201612=VERTEX_POINT ( 'NONE', #69139 ) ;
#201623=CARTESIAN_POINT ( 'NONE',  ( 22.50000000000000000, 1.115600667400684642E-11, -33.50000000000000000 ) ) ;
#201647=ORIENTED_EDGE ( 'NONE', *, *, #79120, .T. ) ;
#201659=CARTESIAN_POINT ( 'NONE',  ( 20.94999999999999929, 10.72371710471867701, -41.16491356908760935 ) ) ;
#201739=VERTEX_POINT ( 'NONE', #228200 ) ;
#201750=CARTESIAN_POINT ( 'NONE',  ( -18.40000000000000213, -9.519327731081286714, -40.47297637655933045 ) ) ;
#201842=ORIENTED_EDGE ( 'NONE', *, *, #150055, .F. ) ;
#201862=CARTESIAN_POINT ( 'NONE',  ( 21.05000000000000071, 5.000000000011153745, -45.90526601891310321 ) ) ;
#201889=DIRECTION ( 'NONE',  ( 0.000000000000000000, 0.5000000000000014433, -0.8660254037844378194 ) ) ;
#201896=CIRCLE ( 'NONE', #151856, 0.09999999999999982514 ) ;
#201922=DIRECTION ( 'NONE',  ( -0.000000000000000000, 0.1298341882520022694, 0.9915357197604853789 ) ) ;
#201926=DIRECTION ( 'NONE',  ( 0.000000000000000000, 0.000000000000000000, -1.000000000000000000 ) ) ;
#201928=CARTESIAN_POINT ( 'NONE',  ( -20.64999999999999858, 2.000000000011154189, -54.27537807723790309 ) ) ;
#201941=CARTESIAN_POINT ( 'NONE',  ( 22.14074124539698829, 7.390077851054901892, -33.40094710415593227 ) ) ;
#201951=ORIENTED_EDGE ( 'NONE', *, *, #53749, .F. ) ;
#201976=DIRECTION ( 'NONE',  ( -0.000000000000000000, 0.000000000000000000, 1.000000000000000000 ) ) ;
#201977=CYLINDRICAL_SURFACE ( 'NONE', #204223, 0.09999999999999939493 ) ;
#201981=AXIS2_PLACEMENT_3D ( 'NONE', #256286, #178129, #232969 ) ;
#202015=ORIENTED_EDGE ( 'NONE', *, *, #246433, .F. ) ;
#202018=AXIS2_PLACEMENT_3D ( 'NONE', #173009, #212101, #251192 ) ;
#202041=CARTESIAN_POINT ( 'NONE',  ( 23.24999999999999645, -3.899999999988843502, -67.00000000000000000 ) ) ;
#202082=DIRECTION ( 'NONE',  ( 0.000000000000000000, 0.000000000000000000, 1.000000000000000000 ) ) ;
#202103=LINE ( 'NONE', #102976, #71775 ) ;
#202114=CARTESIAN_POINT ( 'NONE',  ( -21.07971444708686093, 0.08782343632898161057, -27.17020791837345328 ) ) ;
#202124=EDGE_CURVE ( 'NONE', #201531, #81754, #115919, .T. ) ;
#202150=CARTESIAN_POINT ( 'NONE',  ( 21.93340585971920476, 7.324147022865875378, -33.50000000000000711 ) ) ;
#202175=CARTESIAN_POINT ( 'NONE',  ( 18.59999999999999076, 6.650000000011155876, -54.65000000000000568 ) ) ;
#202186=ORIENTED_EDGE ( 'NONE', *, *, #190454, .F. ) ;
#202222=CYLINDRICAL_SURFACE ( 'NONE', #180493, 11.79999999999999716 ) ;
#202226=DIRECTION ( 'NONE',  ( 0.000000000000000000, 0.5000000000000209832, 0.8660254037844264952 ) ) ;
#202227=ORIENTED_EDGE ( 'NONE', *, *, #257468, .T. ) ;
#202275=ORIENTED_EDGE ( 'NONE', *, *, #239528, .F. ) ;
#202282=DIRECTION ( 'NONE',  ( 0.000000000000000000, 0.000000000000000000, 1.000000000000000000 ) ) ;
#202286=DIRECTION ( 'NONE',  ( 0.000000000000000000, 0.000000000000000000, -1.000000000000000000 ) ) ;
#202305=DIRECTION ( 'NONE',  ( 1.000000000000000000, -0.000000000000000000, -0.000000000000000000 ) ) ;
#202306=LINE ( 'NONE', #67926, #230017 ) ;
#202310=CARTESIAN_POINT ( 'NONE',  ( -21.05000000000000071, -0.09999999998884338825, -21.85042919245520210 ) ) ;
#202315=DIRECTION ( 'NONE',  ( -0.000000000000000000, 0.1350103645451876666, 0.9908441862701600211 ) ) ;
#202326=DIRECTION ( 'NONE',  ( 1.000000000000000000, 0.000000000000000000, 0.000000000000000000 ) ) ;
#202342=CARTESIAN_POINT ( 'NONE',  ( -20.54999999999999716, 1.115600667400684642E-11, -67.00000000000000000 ) ) ;
#202355=EDGE_CURVE ( 'NONE', #45873, #84436, #199309, .T. ) ;
#202367=AXIS2_PLACEMENT_3D ( 'NONE', #12215, #227378, #26638 ) ;
#202372=CIRCLE ( 'NONE', #219110, 12.77499999999999503 ) ;
#202375=DIRECTION ( 'NONE',  ( -1.000000000000000000, 0.000000000000000000, 0.000000000000000000 ) ) ;
#202392=CARTESIAN_POINT ( 'NONE',  ( -20.85000000000000142, 7.021664781911246322, -70.83356540189728889 ) ) ;
#202414=DIRECTION ( 'NONE',  ( 1.000000000000000000, -0.000000000000000000, -0.000000000000000000 ) ) ;
#202425=FACE_OUTER_BOUND ( 'NONE', #216310, .T. ) ;
#202448=CIRCLE ( 'NONE', #164859, 0.5000000000000013323 ) ;
#202452=DIRECTION ( 'NONE',  ( 0.000000000000000000, 1.000000000000000000, -6.308085367188393199E-16 ) ) ;
#202455=ORIENTED_EDGE ( 'NONE', *, *, #199970, .F. ) ;
#202484=ORIENTED_EDGE ( 'NONE', *, *, #20559, .F. ) ;
#202528=DIRECTION ( 'NONE',  ( 1.000000000000000000, 2.952720810173289112E-16, -0.000000000000000000 ) ) ;
#202536=EDGE_LOOP ( 'NONE', ( #96913, #52360, #71066, #85788 ) ) ;
#202552=DIRECTION ( 'NONE',  ( 0.000000000000000000, 0.000000000000000000, -1.000000000000000000 ) ) ;
#202558=CARTESIAN_POINT ( 'NONE',  ( -18.50000000000000000, -9.399999999988850163, -73.91465834296965909 ) ) ;
#202632=AXIS2_PLACEMENT_3D ( 'NONE', #176628, #256075, #94488 ) ;
#202654=AXIS2_PLACEMENT_3D ( 'NONE', #30739, #125944, #29467 ) ;
#202755=EDGE_CURVE ( 'NONE', #188642, #186448, #240410, .T. ) ;
#202765=ADVANCED_FACE ( 'NONE', ( #210281 ), #53921, .T. ) ;
#202778=AXIS2_PLACEMENT_3D ( 'NONE', #86060, #24869, #225577 ) ;
#202789=VERTEX_POINT ( 'NONE', #12094 ) ;
#202801=CARTESIAN_POINT ( 'NONE',  ( -20.92356734117541706, 10.31973158071402175, -72.55053347133544150 ) ) ;
#202804=ORIENTED_EDGE ( 'NONE', *, *, #152688, .F. ) ;
#202858=CARTESIAN_POINT ( 'NONE',  ( 18.59999999999999076, 10.25000000001115552, -58.25000000000000000 ) ) ;
#202868=CARTESIAN_POINT ( 'NONE',  ( 20.99780126800942526, 11.60538868788779432, -60.08735257170526722 ) ) ;
#202873=DIRECTION ( 'NONE',  ( 1.000000000000000000, 0.000000000000000000, 0.000000000000000000 ) ) ;
#202875=AXIS2_PLACEMENT_3D ( 'NONE', #135048, #52957, #75130 ) ;
#202890=DIRECTION ( 'NONE',  ( 0.000000000000000000, 0.000000000000000000, 1.000000000000000000 ) ) ;
#202935=ORIENTED_EDGE ( 'NONE', *, *, #146295, .F. ) ;
#202966=ORIENTED_EDGE ( 'NONE', *, *, #241089, .T. ) ;
#202978=VECTOR ( 'NONE', #10614, 1000.000000000000000 ) ;
#202983=ADVANCED_FACE ( 'NONE', ( #155476, #234979 ), #176305, .T. ) ;
#203011=VECTOR ( 'NONE', #168164, 1000.000000000000000 ) ;
#203021=CARTESIAN_POINT ( 'NONE',  ( 22.49999999999999645, 0.1008583691098678403, -21.75043287651060808 ) ) ;
#203124=EDGE_CURVE ( 'NONE', #115688, #197537, #233008, .T. ) ;
#203164=CARTESIAN_POINT ( 'NONE',  ( -18.50000000000000000, 6.846123162363745074, -70.73772626684986164 ) ) ;
#203168=CARTESIAN_POINT ( 'NONE',  ( 18.43709777086140278, -9.682403433465236020, -73.65684337741278398 ) ) ;
#203233=TOROIDAL_SURFACE ( 'NONE', #40942, 7.800000000000000711, 0.1000000000000000056 ) ;
#203257=( BOUNDED_SURFACE ( )  B_SPLINE_SURFACE ( 3, 2, ( 
 ( #236696, #197576, #140160 ),
 ( #120646, #77609, #637 ),
 ( #98436, #157207, #179333 ),
 ( #198867, #58052, #101002 ),
 ( #257497, #22832, #17651 ),
 ( #158491, #219707, #181883 ) ),
 .UNSPECIFIED., .F., .F., .F. ) 
 B_SPLINE_SURFACE_WITH_KNOTS ( ( 4, 2, 4 ),
 ( 3, 3 ),
 ( 0.0001381104793128061785, 0.0002947094729387697305, 0.0004513084665647332824 ),
 ( 0.000000000000000000, 1.000000000000000000 ),
 .UNSPECIFIED. ) 
 GEOMETRIC_REPRESENTATION_ITEM ( )  RATIONAL_B_SPLINE_SURFACE ( (
 ( 1.000000000000000000, 0.7071067811865494601, 1.000000000000000000),
 ( 1.000000000000000000, 0.6919563088099112136, 1.000000000000000000),
 ( 1.000000000000000000, 0.6959445945717440685, 1.000000000000000000),
 ( 1.000000000000000000, 0.7137882985313291906, 1.000000000000000000),
 ( 1.000000000000000000, 0.7257496306096311578, 1.000000000000000000),
 ( 1.000000000000000000, 0.7250110520819876836, 1.000000000000000000) ) ) 
 REPRESENTATION_ITEM ( '' )  SURFACE ( )  );
#203260=CARTESIAN_POINT ( 'NONE',  ( 20.95512820512820440, 10.62384868372303615, -41.16491356908760935 ) ) ;
#203275=AXIS2_PLACEMENT_3D ( 'NONE', #158285, #223336, #40897 ) ;
#203298=CIRCLE ( 'NONE', #95151, 0.1000000000000028644 ) ;
#203300=ADVANCED_FACE ( 'NONE', ( #167027 ), #228260, .F. ) ;
#203332=EDGE_CURVE ( 'NONE', #212737, #164375, #212344, .T. ) ;
#203333=FACE_OUTER_BOUND ( 'NONE', #86559, .T. ) ;
#203339=EDGE_CURVE ( 'NONE', #95688, #102195, #208059, .T. ) ;
#203362=DIRECTION ( 'NONE',  ( 0.000000000000000000, 0.000000000000000000, 1.000000000000000000 ) ) ;
#203366=ORIENTED_EDGE ( 'NONE', *, *, #164127, .T. ) ;
#203370=ADVANCED_FACE ( 'NONE', ( #158687 ), #2131, .T. ) ;
#203391=DIRECTION ( 'NONE',  ( 0.000000000000000000, 0.000000000000000000, -1.000000000000000000 ) ) ;
#203394=EDGE_CURVE ( 'NONE', #253488, #126100, #136498, .T. ) ;
#203437=CARTESIAN_POINT ( 'NONE',  ( 21.53699400380134676, 6.787711793207312994, -33.50000000000000711 ) ) ;
#203441=CIRCLE ( 'NONE', #82766, 12.97499999999999964 ) ;
#203450=EDGE_CURVE ( 'NONE', #147029, #23656, #141399, .T. ) ;
#203454=ORIENTED_EDGE ( 'NONE', *, *, #197278, .F. ) ;
#203455=AXIS2_PLACEMENT_3D ( 'NONE', #219316, #120266, #202326 ) ;
#203502=CARTESIAN_POINT ( 'NONE',  ( -20.64999999999999858, 4.350000000011156054, -54.65000000000000568 ) ) ;
#203539=CIRCLE ( 'NONE', #215976, 0.09999999999999939493 ) ;
#203545=VERTEX_POINT ( 'NONE', #82932 ) ;
#203548=VERTEX_POINT ( 'NONE', #204184 ) ;
#203601=FACE_OUTER_BOUND ( 'NONE', #183536, .T. ) ;
#203640=ADVANCED_FACE ( 'NONE', ( #131074 ), #105681, .T. ) ;
#203645=ORIENTED_EDGE ( 'NONE', *, *, #55475, .T. ) ;
#203649=CARTESIAN_POINT ( 'NONE',  ( 21.05000000000000071, 1.115600667400684642E-11, -67.00000000000000000 ) ) ;
#203680=TOROIDAL_SURFACE ( 'NONE', #99580, 0.2000000000000000111, 0.1000000000000000056 ) ;
#203703=DIRECTION ( 'NONE',  ( 2.879366945564059217E-14, -0.9875055080513751582, 0.1575844902526747915 ) ) ;
#203706=CARTESIAN_POINT ( 'NONE',  ( -21.98333005346336932, 1.115600667400684642E-11, -26.12592467094331994 ) ) ;
#203748=ORIENTED_EDGE ( 'NONE', *, *, #174806, .T. ) ;
#203758=CIRCLE ( 'NONE', #12248, 0.1999999999999987899 ) ;
#203771=CARTESIAN_POINT ( 'NONE',  ( -20.94999999999999929, -11.41227409413852989, -36.50000000000000711 ) ) ;
#203808=EDGE_CURVE ( 'NONE', #189424, #252337, #49446, .T. ) ;
#203827=EDGE_CURVE ( 'NONE', #244974, #201200, #178464, .T. ) ;
#203848=EDGE_CURVE ( 'NONE', #74863, #207108, #65656, .T. ) ;
#203889=VERTEX_POINT ( 'NONE', #86478 ) ;
#203891=CARTESIAN_POINT ( 'NONE',  ( -20.54999999999999716, 1.115600667400684642E-11, -54.12500000000000711 ) ) ;
#203895=CARTESIAN_POINT ( 'NONE',  ( -21.08479644141222664, 6.345038657743046429, -33.44144555743587688 ) ) ;
#203904=EDGE_CURVE ( 'NONE', #61363, #125880, #66008, .T. ) ;
#203967=DIRECTION ( 'NONE',  ( 0.000000000000000000, 1.000000000000000000, 0.000000000000000000 ) ) ;
#203982=AXIS2_PLACEMENT_3D ( 'NONE', #75422, #179642, #57081 ) ;
#203988=VERTEX_POINT ( 'NONE', #232465 ) ;
#203995=TOROIDAL_SURFACE ( 'NONE', #104017, 0.6000000000000013101, 0.1000000000000000056 ) ;
#204017=ORIENTED_EDGE ( 'NONE', *, *, #253911, .T. ) ;
#204035=CIRCLE ( 'NONE', #8248, 0.1000000000000028644 ) ;
#204055=AXIS2_PLACEMENT_3D ( 'NONE', #94152, #173758, #154188 ) ;
#204083=CARTESIAN_POINT ( 'NONE',  ( -22.49756042579671700, 0.07804633702833754794, -21.85013503889767605 ) ) ;
#204139=VERTEX_POINT ( 'NONE', #156783 ) ;
#204140=CARTESIAN_POINT ( 'NONE',  ( 23.24999999999999289, 11.75000000001116263, -45.65000000000000568 ) ) ;
#204152=EDGE_LOOP ( 'NONE', ( #49852, #234640, #256634, #220044 ) ) ;
#204154=CARTESIAN_POINT ( 'NONE',  ( -23.25000000000000000, 1.115600667400684642E-11, -67.00000000000000000 ) ) ;
#204156=VECTOR ( 'NONE', #25280, 1000.000000000000000 ) ;
#204160=CARTESIAN_POINT ( 'NONE',  ( 18.60000000000000142, -9.321008403350125704, -40.73593824907789696 ) ) ;
#204161=AXIS2_PLACEMENT_3D ( 'NONE', #73413, #87784, #130780 ) ;
#204177=CARTESIAN_POINT ( 'NONE',  ( 20.94999999999999929, 1.115600667400684642E-11, -67.00000000000000000 ) ) ;
#204184=CARTESIAN_POINT ( 'NONE',  ( 21.14999999999999503, 11.65000000001116298, -33.50000000000000000 ) ) ;
#204187=CARTESIAN_POINT ( 'NONE',  ( -20.94999999999999929, 11.60000000001115339, -40.42820323027555673 ) ) ;
#204199=ADVANCED_FACE ( 'NONE', ( #82320 ), #124064, .F. ) ;
#204208=ORIENTED_EDGE ( 'NONE', *, *, #74318, .F. ) ;
#204223=AXIS2_PLACEMENT_3D ( 'NONE', #143273, #123724, #87142 ) ;
#204228=DIRECTION ( 'NONE',  ( 0.000000000000000000, 0.000000000000000000, -1.000000000000000000 ) ) ;
#204253=VECTOR ( 'NONE', #78309, 1000.000000000000000 ) ;
#204287=ORIENTED_EDGE ( 'NONE', *, *, #120550, .T. ) ;
#204355=VERTEX_POINT ( 'NONE', #7967 ) ;
#204370=CARTESIAN_POINT ( 'NONE',  ( 21.14999999999999858, 6.650000000011155876, -45.65000000000000568 ) ) ;
#204426=EDGE_CURVE ( 'NONE', #170769, #72122, #208044, .T. ) ;
#204445=ADVANCED_FACE ( 'NONE', ( #39097 ), #4011, .T. ) ;
#204462=CARTESIAN_POINT ( 'NONE',  ( 22.01447462590973458, 0.09903700007069084210, -26.23619979877009101 ) ) ;
#204470=ORIENTED_EDGE ( 'NONE', *, *, #95299, .T. ) ;
#204500=ORIENTED_EDGE ( 'NONE', *, *, #133041, .T. ) ;
#204511=EDGE_CURVE ( 'NONE', #208600, #67483, #70683, .T. ) ;
#204515=ORIENTED_EDGE ( 'NONE', *, *, #227215, .T. ) ;
#204535=ORIENTED_EDGE ( 'NONE', *, *, #79424, .T. ) ;
#204546=EDGE_CURVE ( 'NONE', #15533, #158454, #170670, .T. ) ;
#204556=DIRECTION ( 'NONE',  ( 0.000000000000000000, -0.000000000000000000, 1.000000000000000000 ) ) ;
#204575=FACE_OUTER_BOUND ( 'NONE', #223303, .T. ) ;
#204577=CIRCLE ( 'NONE', #4647, 11.70000000000000284 ) ;
#204660=CARTESIAN_POINT ( 'NONE',  ( -21.10320863425827298, 0.02502225123826237740, -27.09972261354077006 ) ) ;
#204674=EDGE_CURVE ( 'NONE', #163151, #234522, #99013, .T. ) ;
#204698=ORIENTED_EDGE ( 'NONE', *, *, #62969, .T. ) ;
#204699=CIRCLE ( 'NONE', #92286, 0.1999999999999987899 ) ;
#204702=EDGE_CURVE ( 'NONE', #130418, #255894, #87389, .T. ) ;
#204710=ORIENTED_EDGE ( 'NONE', *, *, #116114, .T. ) ;
#204714=VERTEX_POINT ( 'NONE', #243691 ) ;
#204741=ORIENTED_EDGE ( 'NONE', *, *, #91189, .F. ) ;
#204765=CARTESIAN_POINT ( 'NONE',  ( -18.50000000000000000, 3.912899247244609580, -44.98182297301097066 ) ) ;
#204774=CARTESIAN_POINT ( 'NONE',  ( 23.15000000000000213, -11.48912529306489994, -63.89999999999999858 ) ) ;
#204804=AXIS2_PLACEMENT_3D ( 'NONE', #50625, #132774, #251413 ) ;
#204835=EDGE_CURVE ( 'NONE', #138742, #25677, #67616, .T. ) ;
#204857=EDGE_LOOP ( 'NONE', ( #147945, #40005, #55674, #127770 ) ) ;
#204920=DIRECTION ( 'NONE',  ( 0.000000000000000000, 0.000000000000000000, -1.000000000000000000 ) ) ;
#204923=CARTESIAN_POINT ( 'NONE',  ( -21.14999999999999858, 11.65000000001115588, -33.60000000000000142 ) ) ;
#204932=DIRECTION ( 'NONE',  ( -1.000000000000000000, -0.000000000000000000, -0.000000000000000000 ) ) ;
#204996=VERTEX_POINT ( 'NONE', #74076 ) ;
#204999=ORIENTED_EDGE ( 'NONE', *, *, #95881, .T. ) ;
#205018=VERTEX_POINT ( 'NONE', #92312 ) ;
#205056=CIRCLE ( 'NONE', #196692, 0.6000000000000015321 ) ;
#205071=ORIENTED_EDGE ( 'NONE', *, *, #192654, .F. ) ;
#205073=DIRECTION ( 'NONE',  ( 1.000000000000000000, 0.000000000000000000, 0.000000000000000000 ) ) ;
#205080=DIRECTION ( 'NONE',  ( 0.000000000000000000, 0.000000000000000000, -1.000000000000000000 ) ) ;
#205089=ORIENTED_EDGE ( 'NONE', *, *, #42067, .T. ) ;
#205100=EDGE_LOOP ( 'NONE', ( #190382, #120623, #11957, #31140 ) ) ;
#205113=DIRECTION ( 'NONE',  ( 0.7071067811865487940, 8.659560562354918067E-17, 0.7071067811865463515 ) ) ;
#205142=VERTEX_POINT ( 'NONE', #12182 ) ;
#205165=CIRCLE ( 'NONE', #213354, 0.1000000000000028644 ) ;
#205177=ADVANCED_FACE ( 'NONE', ( #229922 ), #104313, .F. ) ;
#205194=CARTESIAN_POINT ( 'NONE',  ( -21.05000000000000071, 6.540656951712400691, -33.50000000000000000 ) ) ;
#205217=CYLINDRICAL_SURFACE ( 'NONE', #66701, 0.09999999999999939493 ) ;
#205243=DIRECTION ( 'NONE',  ( 0.000000000000000000, -1.000000000000000000, 0.000000000000000000 ) ) ;
#205245=CARTESIAN_POINT ( 'NONE',  ( 20.21494484322224849, 9.303170737879936425, -41.84026519177099601 ) ) ;
#205265=DIRECTION ( 'NONE',  ( -0.000000000000000000, 0.8660254037844411501, 0.4999999999999956701 ) ) ;
#205279=DIRECTION ( 'NONE',  ( 1.000000000000000000, -0.000000000000000000, -0.000000000000000000 ) ) ;
#205285=CARTESIAN_POINT ( 'NONE',  ( 18.59999999999999076, 10.20857864377385127, -54.85000000000000142 ) ) ;
#205299=DIRECTION ( 'NONE',  ( 0.000000000000000000, -0.9908441862701600211, -0.1350103645451876666 ) ) ;
#205307=CARTESIAN_POINT ( 'NONE',  ( 22.60000000000000142, 0.1008583691098682150, -21.75043287651061164 ) ) ;
#205339=CIRCLE ( 'NONE', #17915, 0.1000000000000028644 ) ;
#205354=ADVANCED_FACE ( 'NONE', ( #214495, #60552 ), #177961, .F. ) ;
#205356=VERTEX_POINT ( 'NONE', #236622 ) ;
#205361=EDGE_LOOP ( 'NONE', ( #43233, #207857, #251980, #247560 ) ) ;
#205365=CARTESIAN_POINT ( 'NONE',  ( -23.15000000000000213, -4.831324760611774849, -50.46969694219875180 ) ) ;
#205384=CARTESIAN_POINT ( 'NONE',  ( 23.14999999999999858, 1.115600667400684642E-11, -46.37500000000000000 ) ) ;
#205407=FACE_BOUND ( 'NONE', #194611, .T. ) ;
#205419=DIRECTION ( 'NONE',  ( 0.000000000000000000, 0.000000000000000000, -1.000000000000000000 ) ) ;
#205423=CARTESIAN_POINT ( 'NONE',  ( 18.49999999999998934, 6.650000000011155876, -45.85000000000000142 ) ) ;
#205424=CARTESIAN_POINT ( 'NONE',  ( -18.53317502108577131, 10.32263460347359540, -72.56059579686720440 ) ) ;
#205425=ADVANCED_FACE ( 'NONE', ( #256127 ), #98359, .T. ) ;
#205438=VECTOR ( 'NONE', #173220, 1000.000000000000000 ) ;
#205439=CIRCLE ( 'NONE', #9642, 0.09999999999999939493 ) ;
#205442=CARTESIAN_POINT ( 'NONE',  ( 21.14999999999998082, -11.74999999998884448, -33.50000000000000000 ) ) ;
#205452=AXIS2_PLACEMENT_3D ( 'NONE', #145674, #165252, #244773 ) ;
#205459=ORIENTED_EDGE ( 'NONE', *, *, #184046, .T. ) ;
#205504=DIRECTION ( 'NONE',  ( 1.000000000000000000, 0.000000000000000000, 0.000000000000000000 ) ) ;
#205534=LINE ( 'NONE', #208141, #82895 ) ;
#205544=AXIS2_PLACEMENT_3D ( 'NONE', #249287, #70667, #232302 ) ;
#205556=EDGE_LOOP ( 'NONE', ( #13317, #77743, #52991, #148361 ) ) ;
#205564=DIRECTION ( 'NONE',  ( 0.000000000000000000, 0.3738317757009345654, 0.9274965247785492695 ) ) ;
#205591=CARTESIAN_POINT ( 'NONE',  ( 20.94999999999999574, -11.64999999998883595, -36.50000000000000711 ) ) ;
#205605=DIRECTION ( 'NONE',  ( 0.000000000000000000, 0.000000000000000000, -1.000000000000000000 ) ) ;
#205615=EDGE_LOOP ( 'NONE', ( #153368, #95888, #173125, #61447 ) ) ;
#205625=EDGE_LOOP ( 'NONE', ( #218613, #204741, #125529, #216998 ) ) ;
#205677=ORIENTED_EDGE ( 'NONE', *, *, #134860, .F. ) ;
#205731=CARTESIAN_POINT ( 'NONE',  ( 18.60000000000000142, -9.523946312306550865, -73.88202799533824816 ) ) ;
#205743=EDGE_LOOP ( 'NONE', ( #43446, #16740, #53099, #36312 ) ) ;
#205763=VERTEX_POINT ( 'NONE', #156832 ) ;
#205774=ORIENTED_EDGE ( 'NONE', *, *, #11778, .F. ) ;
#205811=AXIS2_PLACEMENT_3D ( 'NONE', #77530, #237912, #55390 ) ;
#205818=CARTESIAN_POINT ( 'NONE',  ( 21.05000000000000071, -8.663551401858002876, -43.02410111806730697 ) ) ;
#205838=PLANE ( 'NONE',  #246663 ) ;
#205862=CARTESIAN_POINT ( 'NONE',  ( 23.14999999999999503, 11.75000000001116263, -45.65000000000000568 ) ) ;
#205921=ORIENTED_EDGE ( 'NONE', *, *, #134033, .F. ) ;
#205929=DIRECTION ( 'NONE',  ( 0.000000000000000000, 0.1495327102803689356, -0.9887567792719336168 ) ) ;
#205937=EDGE_CURVE ( 'NONE', #86338, #43174, #1093, .T. ) ;
#205950=DIRECTION ( 'NONE',  ( 0.000000000000000000, 0.000000000000000000, -1.000000000000000000 ) ) ;
#205951=ORIENTED_EDGE ( 'NONE', *, *, #89405, .T. ) ;
#205953=CARTESIAN_POINT ( 'NONE',  ( 23.14999999999999503, 11.75000000001116263, -59.98519422934606382 ) ) ;
#205957=CARTESIAN_POINT ( 'NONE',  ( -21.11927991906891222, 0.009083679485027933501, -27.05150688150849092 ) ) ;
#205968=LINE ( 'NONE', #27380, #26926 ) ;
#205980=DIRECTION ( 'NONE',  ( 2.557131231893036985E-16, -0.8660254037844383745, 0.5000000000000003331 ) ) ;
#205996=CARTESIAN_POINT ( 'NONE',  ( -21.14999999999999858, 11.65000000001115588, -33.60000000000000142 ) ) ;
#206017=VERTEX_POINT ( 'NONE', #208776 ) ;
#206063=CARTESIAN_POINT ( 'NONE',  ( -22.59999999999999787, 1.115600667400684642E-11, -33.50000000000000000 ) ) ;
#206100=CARTESIAN_POINT ( 'NONE',  ( 18.59999999999999787, 1.115600667400684642E-11, -33.50000000000000000 ) ) ;
#206166=AXIS2_PLACEMENT_3D ( 'NONE', #198707, #100844, #96998 ) ;
#206172=ORIENTED_EDGE ( 'NONE', *, *, #167206, .T. ) ;
#206196=DIRECTION ( 'NONE',  ( -1.000000000000000000, 0.000000000000000000, 0.000000000000000000 ) ) ;
#206209=ORIENTED_EDGE ( 'NONE', *, *, #95041, .T. ) ;
#206211=EDGE_CURVE ( 'NONE', #61821, #142140, #242210, .T. ) ;
#206237=VERTEX_POINT ( 'NONE', #36585 ) ;
#206242=CARTESIAN_POINT ( 'NONE',  ( 18.51024323315077069, 10.31104185824064068, -72.52045169831059468 ) ) ;
#206265=CARTESIAN_POINT ( 'NONE',  ( 22.50000000000000000, 7.750000000011162626, -33.39999999999999858 ) ) ;
#206292=CIRCLE ( 'NONE', #218724, 0.1000000000000000472 ) ;
#206293=CIRCLE ( 'NONE', #97916, 0.09999999999999939493 ) ;
#206315=ADVANCED_FACE ( 'NONE', ( #44261 ), #108929, .T. ) ;
#206328=VECTOR ( 'NONE', #45613, 1000.000000000000000 ) ;
#206329=DIRECTION ( 'NONE',  ( -0.000000000000000000, 0.000000000000000000, 1.000000000000000000 ) ) ;
#206356=ORIENTED_EDGE ( 'NONE', *, *, #114467, .F. ) ;
#206405=CARTESIAN_POINT ( 'NONE',  ( 18.43473516226069009, -9.494942282747068418, -40.54589868334937108 ) ) ;
#206471=VECTOR ( 'NONE', #112410, 999.9999999999998863 ) ;
#206503=DIRECTION ( 'NONE',  ( 1.000000000000000000, -0.000000000000000000, -0.000000000000000000 ) ) ;
#206509=CARTESIAN_POINT ( 'NONE',  ( -22.39999999999999858, 1.115600667400684642E-11, -33.50000000000000000 ) ) ;
#206513=CIRCLE ( 'NONE', #256315, 12.87499999999999822 ) ;
#206528=VECTOR ( 'NONE', #30728, 1000.000000000000000 ) ;
#206538=ORIENTED_EDGE ( 'NONE', *, *, #212159, .T. ) ;
#206554=EDGE_LOOP ( 'NONE', ( #56267, #173409, #229630, #257961 ) ) ;
#206566=DIRECTION ( 'NONE',  ( 2.952720810173289112E-16, -1.000000000000000000, 0.000000000000000000 ) ) ;
#206568=ADVANCED_FACE ( 'NONE', ( #56715 ), #77489, .T. ) ;
#206580=DIRECTION ( 'NONE',  ( 1.000000000000000000, 0.000000000000000000, 0.000000000000000000 ) ) ;
#206603=ORIENTED_EDGE ( 'NONE', *, *, #56408, .T. ) ;
#206611=EDGE_CURVE ( 'NONE', #130418, #74897, #121626, .T. ) ;
#206626=DIRECTION ( 'NONE',  ( -0.000000000000000000, -0.1350103645451876666, -0.9908441862701600211 ) ) ;
#206657=CIRCLE ( 'NONE', #94220, 0.1000000000000001860 ) ;
#206723=FACE_OUTER_BOUND ( 'NONE', #140347, .T. ) ;
#206727=FACE_OUTER_BOUND ( 'NONE', #219144, .T. ) ;
#206736=LINE ( 'NONE', #82900, #176115 ) ;
#206753=EDGE_CURVE ( 'NONE', #227593, #86031, #238104, .T. ) ;
#206799=CARTESIAN_POINT ( 'NONE',  ( 21.05000000000000071, 8.776282895303632259, -42.05862899514094977 ) ) ;
#206811=CARTESIAN_POINT ( 'NONE',  ( -20.54999999999999716, 2.400000000011155432, -57.10603087734755690 ) ) ;
#206848=CARTESIAN_POINT ( 'NONE',  ( 18.49999999999999645, 1.115600667400684642E-11, -67.00000000000000000 ) ) ;
#206874=CARTESIAN_POINT ( 'NONE',  ( 23.25000000000000000, -9.599999999988849453, -21.75000000000000355 ) ) ;
#206881=CARTESIAN_POINT ( 'NONE',  ( 23.14999999999999503, 11.75000000001115552, -54.75000000000000000 ) ) ;
#206905=DIRECTION ( 'NONE',  ( -4.239556034732056743E-17, 0.1298341882520022694, 0.9915357197604853789 ) ) ;
#206915=CARTESIAN_POINT ( 'NONE',  ( -20.94999999999999929, 1.115600667400684642E-11, -67.00000000000000000 ) ) ;
#206942=SPHERICAL_SURFACE ( 'NONE', #13947, 0.1000000000000000056 ) ;
#206949=AXIS2_PLACEMENT_3D ( 'NONE', #120656, #241857, #41120 ) ;
#206954=DIRECTION ( 'NONE',  ( 0.000000000000000000, 0.000000000000000000, 1.000000000000000000 ) ) ;
#206993=ORIENTED_EDGE ( 'NONE', *, *, #244258, .F. ) ;
#206999=LINE ( 'NONE', #165301, #215422 ) ;
#207024=ORIENTED_EDGE ( 'NONE', *, *, #34965, .T. ) ;
#207049=LINE ( 'NONE', #79698, #55732 ) ;
#207075=EDGE_CURVE ( 'NONE', #3284, #126100, #77933, .T. ) ;
#207078=DIRECTION ( 'NONE',  ( -1.000000000000000000, 0.000000000000000000, 0.000000000000000000 ) ) ;
#207081=SPHERICAL_SURFACE ( 'NONE', #209258, 0.1000000000000000056 ) ;
#207091=EDGE_LOOP ( 'NONE', ( #105175, #233892, #181652, #199643 ) ) ;
#207108=VERTEX_POINT ( 'NONE', #129274 ) ;
#207149=CARTESIAN_POINT ( 'NONE',  ( 22.60000000000000142, 11.74956712350054744, -33.39914163090129762 ) ) ;
#207151=EDGE_CURVE ( 'NONE', #90926, #72361, #215225, .T. ) ;
#207153=DIRECTION ( 'NONE',  ( -1.000000000000000000, -2.952720810173289112E-16, 0.000000000000000000 ) ) ;
#207178=DIRECTION ( 'NONE',  ( -1.000000000000000000, -8.673617379884087537E-15, 0.000000000000000000 ) ) ;
#207191=ADVANCED_FACE ( 'NONE', ( #35344 ), #194404, .F. ) ;
#207194=AXIS2_PLACEMENT_3D ( 'NONE', #71133, #134903, #189775 ) ;
#207201=ORIENTED_EDGE ( 'NONE', *, *, #84988, .F. ) ;
#207237=CARTESIAN_POINT ( 'NONE',  ( 20.94999999999999574, -11.41227409413852989, -36.39999999999999858 ) ) ;
#207243=ORIENTED_EDGE ( 'NONE', *, *, #67735, .T. ) ;
#207245=ADVANCED_FACE ( 'NONE', ( #120009 ), #212348, .F. ) ;
#207257=CARTESIAN_POINT ( 'NONE',  ( 21.14999999999999858, -11.64999999998883595, -33.50000000000000000 ) ) ;
#207305=EDGE_CURVE ( 'NONE', #252337, #53762, #5225, .T. ) ;
#207319=ORIENTED_EDGE ( 'NONE', *, *, #200475, .F. ) ;
#207324=ORIENTED_EDGE ( 'NONE', *, *, #158525, .F. ) ;
#207339=DIRECTION ( 'NONE',  ( 0.000000000000000000, 1.000000000000000000, 0.000000000000000000 ) ) ;
#207348=CARTESIAN_POINT ( 'NONE',  ( 21.05000000000000071, 6.257814610487280937, -33.40220970869120265 ) ) ;
#207422=CARTESIAN_POINT ( 'NONE',  ( -21.44999999999999929, 7.350000000011155166, -45.85000000000000142 ) ) ;
#207443=DIRECTION ( 'NONE',  ( 0.000000000000000000, -1.000000000000000000, 0.000000000000000000 ) ) ;
#207460=EDGE_CURVE ( 'NONE', #225834, #110138, #46927, .T. ) ;
#207466=DIRECTION ( 'NONE',  ( -0.000000000000000000, -0.000000000000000000, 1.000000000000000000 ) ) ;
#207476=VERTEX_POINT ( 'NONE', #108119 ) ;
#207478=ORIENTED_EDGE ( 'NONE', *, *, #31639, .T. ) ;
#207535=AXIS2_PLACEMENT_3D ( 'NONE', #234405, #55742, #135301 ) ;
#207547=ADVANCED_FACE ( 'NONE', ( #178382 ), #174563, .F. ) ;
#207587=DIRECTION ( 'NONE',  ( 0.000000000000000000, 0.000000000000000000, -1.000000000000000000 ) ) ;
#207588=DIRECTION ( 'NONE',  ( -1.000000000000000000, 0.000000000000000000, 0.000000000000000000 ) ) ;
#207598=EDGE_LOOP ( 'NONE', ( #142790, #175992, #94368, #149239 ) ) ;
#207607=EDGE_CURVE ( 'NONE', #90674, #225961, #59566, .T. ) ;
#207663=CARTESIAN_POINT ( 'NONE',  ( -21.05000000000000071, 1.115600667400684642E-11, -37.79999999999996163 ) ) ;
#207666=EDGE_LOOP ( 'NONE', ( #15889, #67869, #141159 ) ) ;
#207683=EDGE_CURVE ( 'NONE', #130981, #160723, #55287, .T. ) ;
#207692=CARTESIAN_POINT ( 'NONE',  ( -20.85000000000000142, 10.33248238083635151, -72.59484654391314962 ) ) ;
#207695=ORIENTED_EDGE ( 'NONE', *, *, #14009, .T. ) ;
#207705=ORIENTED_EDGE ( 'NONE', *, *, #224833, .F. ) ;
#207710=AXIS2_PLACEMENT_3D ( 'NONE', #97603, #64916, #147014 ) ;
#207762=CARTESIAN_POINT ( 'NONE',  ( 23.14999999999998437, 1.115600667400684642E-11, -33.50000000000000000 ) ) ;
#207799=EDGE_CURVE ( 'NONE', #82729, #248843, #9707, .T. ) ;
#207836=EDGE_CURVE ( 'NONE', #40541, #100962, #12579, .T. ) ;
#207842=DIRECTION ( 'NONE',  ( -1.000000000000000000, 0.000000000000000000, 0.000000000000000000 ) ) ;
#207857=ORIENTED_EDGE ( 'NONE', *, *, #231528, .T. ) ;
#207865=DIRECTION ( 'NONE',  ( 0.000000000000000000, -0.1298341882520079038, -0.9915357197604846018 ) ) ;
#207878=CARTESIAN_POINT ( 'NONE',  ( 21.00000000000000000, 9.750000000011153745, -54.65000000000000568 ) ) ;
#207908=CARTESIAN_POINT ( 'NONE',  ( 21.05000000000000071, -8.730841121484171907, -43.09807471898433562 ) ) ;
#207911=DIRECTION ( 'NONE',  ( 0.000000000000000000, 0.1350103645451876666, -0.9908441862701600211 ) ) ;
#207922=ADVANCED_FACE ( 'NONE', ( #175502 ), #133777, .T. ) ;
#207930=DIRECTION ( 'NONE',  ( 0.000000000000000000, 0.5000000000000144329, 0.8660254037844302699 ) ) ;
#207963=ORIENTED_EDGE ( 'NONE', *, *, #158866, .F. ) ;
#207975=VERTEX_POINT ( 'NONE', #75125 ) ;
#207986=ORIENTED_EDGE ( 'NONE', *, *, #80160, .T. ) ;
#208004=EDGE_CURVE ( 'NONE', #235258, #1091, #192478, .T. ) ;
#208011=LINE ( 'NONE', #107598, #233142 ) ;
#208012=CARTESIAN_POINT ( 'NONE',  ( 20.94999999999999929, -1.835341550213257733, -45.05515129256298223 ) ) ;
#208018=ADVANCED_FACE ( 'NONE', ( #217144 ), #197598, .F. ) ;
#208028=CARTESIAN_POINT ( 'NONE',  ( -18.50596464788227635, 10.30632246271647112, -72.50418367788957141 ) ) ;
#208043=DIRECTION ( 'NONE',  ( -1.000000000000000000, 0.000000000000000000, 0.000000000000000000 ) ) ;
#208044=CIRCLE ( 'NONE', #179031, 0.9750000000000036415 ) ;
#208045=EDGE_CURVE ( 'NONE', #119088, #178023, #147586, .T. ) ;
#208051=AXIS2_PLACEMENT_3D ( 'NONE', #59426, #217234, #93445 ) ;
#208059=CIRCLE ( 'NONE', #103962, 0.09999999999999939493 ) ;
#208082=CARTESIAN_POINT ( 'NONE',  ( -21.59142135623730852, 7.850000000011158718, -54.75000000000000000 ) ) ;
#208083=ADVANCED_FACE ( 'NONE', ( #48478 ), #140178, .F. ) ;
#208099=DIRECTION ( 'NONE',  ( 0.000000000000000000, 0.000000000000000000, -1.000000000000000000 ) ) ;
#208141=CARTESIAN_POINT ( 'NONE',  ( 21.14999999999999503, 11.75000000001115552, -33.50000000000000000 ) ) ;
#208174=DIRECTION ( 'NONE',  ( 0.000000000000000000, -0.6728971962616697722, 0.7397360091702875895 ) ) ;
#208184=LINE ( 'NONE', #192457, #241563 ) ;
#208186=DIRECTION ( 'NONE',  ( 0.000000000000000000, 0.000000000000000000, 1.000000000000000000 ) ) ;
#208191=DIRECTION ( 'NONE',  ( 1.000000000000000000, 0.000000000000000000, 0.000000000000000000 ) ) ;
#208196=AXIS2_PLACEMENT_3D ( 'NONE', #180291, #142436, #1629 ) ;
#208204=DIRECTION ( 'NONE',  ( 0.000000000000000000, 0.000000000000000000, -1.000000000000000000 ) ) ;
#208211=AXIS2_PLACEMENT_3D ( 'NONE', #176431, #177724, #120331 ) ;
#208213=VERTEX_POINT ( 'NONE', #249266 ) ;
#208271=DIRECTION ( 'NONE',  ( 0.000000000000000000, 0.8660254037844482555, 0.4999999999999837907 ) ) ;
#208279=ORIENTED_EDGE ( 'NONE', *, *, #154139, .F. ) ;
#208303=AXIS2_PLACEMENT_3D ( 'NONE', #156467, #92588, #153914 ) ;
#208312=DIRECTION ( 'NONE',  ( 0.000000000000000000, 0.000000000000000000, -1.000000000000000000 ) ) ;
#208333=ORIENTED_EDGE ( 'NONE', *, *, #201421, .T. ) ;
#208382=DIRECTION ( 'NONE',  ( 0.000000000000000000, 0.5000000000000078826, -0.8660254037844340447 ) ) ;
#208407=CARTESIAN_POINT ( 'NONE',  ( 20.94999999999997442, -1.263275465206102233, -74.90186466674640542 ) ) ;
#208413=DIRECTION ( 'NONE',  ( 0.000000000000000000, 1.000000000000000000, -3.469446951953635015E-14 ) ) ;
#208448=CARTESIAN_POINT ( 'NONE',  ( 22.48660254037844552, 11.75000000001115730, -33.45000000000000995 ) ) ;
#208463=LINE ( 'NONE', #48074, #159060 ) ;
#208486=TOROIDAL_SURFACE ( 'NONE', #204161, 0.2000000000000000111, 0.1000000000000000056 ) ;
#208487=ORIENTED_EDGE ( 'NONE', *, *, #139836, .F. ) ;
#208531=VECTOR ( 'NONE', #108819, 1000.000000000000000 ) ;
#208574=ADVANCED_FACE ( 'NONE', ( #127270 ), #7316, .F. ) ;
#208600=VERTEX_POINT ( 'NONE', #163835 ) ;
#208608=CARTESIAN_POINT ( 'NONE',  ( -20.85000000000000142, -1.835859311432481045, -78.50443916879852679 ) ) ;
#208649=ORIENTED_EDGE ( 'NONE', *, *, #156724, .T. ) ;
#208651=AXIS2_PLACEMENT_3D ( 'NONE', #78880, #18923, #16386 ) ;
#208667=EDGE_CURVE ( 'NONE', #39957, #55352, #64254, .T. ) ;
#208685=EDGE_LOOP ( 'NONE', ( #220539, #103773, #167989, #173447 ) ) ;
#208686=ORIENTED_EDGE ( 'NONE', *, *, #127846, .T. ) ;
#208708=CYLINDRICAL_SURFACE ( 'NONE', #161289, 0.1000000000000028644 ) ;
#208751=CYLINDRICAL_SURFACE ( 'NONE', #110621, 0.8750000000000007772 ) ;
#208764=AXIS2_PLACEMENT_3D ( 'NONE', #7379, #8673, #208174 ) ;
#208776=CARTESIAN_POINT ( 'NONE',  ( 23.14999999999999858, 1.115649653272650466E-11, -63.00000000000000000 ) ) ;
#208782=DIRECTION ( 'NONE',  ( 0.000000000000000000, 0.000000000000000000, -1.000000000000000000 ) ) ;
#208791=DIRECTION ( 'NONE',  ( 0.000000000000000000, 0.4999999999999649170, -0.8660254037844589137 ) ) ;
#208795=AXIS2_PLACEMENT_3D ( 'NONE', #36579, #58643, #57364 ) ;
#208812=DIRECTION ( 'NONE',  ( 0.000000000000000000, -0.4930308989875248349, -0.8700118002898312719 ) ) ;
#208829=DIRECTION ( 'NONE',  ( 0.000000000000000000, -0.9999631594459056361, -0.008583690987124413183 ) ) ;
#208867=ORIENTED_EDGE ( 'NONE', *, *, #152497, .F. ) ;
#208880=VERTEX_POINT ( 'NONE', #1106 ) ;
#208909=ORIENTED_EDGE ( 'NONE', *, *, #111455, .F. ) ;
#208912=CIRCLE ( 'NONE', #96465, 0.09999999999999749367 ) ;
#208935=VECTOR ( 'NONE', #51251, 1000.000000000000000 ) ;
#208941=FACE_OUTER_BOUND ( 'NONE', #46138, .T. ) ;
#208945=FACE_OUTER_BOUND ( 'NONE', #184098, .T. ) ;
#208970=CARTESIAN_POINT ( 'NONE',  ( 18.58703555225022797, -9.406336740777579308, -40.62494464124684157 ) ) ;
#208974=EDGE_LOOP ( 'NONE', ( #241782, #159892, #143769, #61710 ) ) ;
#208986=DIRECTION ( 'NONE',  ( 0.000000000000000000, 0.000000000000000000, -1.000000000000000000 ) ) ;
#209003=CIRCLE ( 'NONE', #96550, 0.09999999999999892308 ) ;
#209033=CARTESIAN_POINT ( 'NONE',  ( 21.05000000000000071, -11.64999999998883595, -33.50000000000000000 ) ) ;
#209040=EDGE_CURVE ( 'NONE', #40550, #14005, #18644, .T. ) ;
#209075=LINE ( 'NONE', #190833, #208935 ) ;
#209118=DIRECTION ( 'NONE',  ( -1.000000000000000000, -3.265361837132813093E-16, 0.000000000000000000 ) ) ;
#209166=TOROIDAL_SURFACE ( 'NONE', #167506, 0.2000000000000000111, 0.1000000000000000056 ) ;
#209172=ORIENTED_EDGE ( 'NONE', *, *, #112642, .F. ) ;
#209213=CARTESIAN_POINT ( 'NONE',  ( -18.59999999999999787, 5.900000000011102586, -43.71909976465641989 ) ) ;
#209219=CARTESIAN_POINT ( 'NONE',  ( -23.15000000000000213, 1.115600667400684642E-11, -46.37500000000000000 ) ) ;
#209258=AXIS2_PLACEMENT_3D ( 'NONE', #149693, #33622, #50536 ) ;
#209295=EDGE_CURVE ( 'NONE', #95688, #228463, #122313, .T. ) ;
#209314=CARTESIAN_POINT ( 'NONE',  ( -22.39999999999999858, 7.790779598384560245, -33.39999999999999858 ) ) ;
#209321=CARTESIAN_POINT ( 'NONE',  ( 18.49999999999999289, 10.25000000001115730, -58.14999999999999858 ) ) ;
#209331=FACE_OUTER_BOUND ( 'NONE', #78859, .T. ) ;
#209358=FACE_OUTER_BOUND ( 'NONE', #241896, .T. ) ;
#209363=ADVANCED_FACE ( 'NONE', ( #206723 ), #222401, .F. ) ;
#209414=CARTESIAN_POINT ( 'NONE',  ( -18.50000000000000000, 1.866714910068465239, -45.25267524628200988 ) ) ;
#209430=EDGE_CURVE ( 'NONE', #46223, #42536, #146719, .T. ) ;
#209471=FACE_OUTER_BOUND ( 'NONE', #169931, .T. ) ;
#209472=DIRECTION ( 'NONE',  ( 1.000000000000000000, 0.000000000000000000, 0.000000000000000000 ) ) ;
#209530=EDGE_CURVE ( 'NONE', #55402, #253110, #134552, .T. ) ;
#209532=CARTESIAN_POINT ( 'NONE',  ( -20.85000000000000142, 7.021664781911246322, -70.73356540189729458 ) ) ;
#209562=ADVANCED_FACE ( 'NONE', ( #212840 ), #195860, .F. ) ;
#209577=CARTESIAN_POINT ( 'NONE',  ( -22.57320508075687115, 11.75000000001115552, -33.50000000000000000 ) ) ;
#209599=FACE_OUTER_BOUND ( 'NONE', #238437, .T. ) ;
#209602=ORIENTED_EDGE ( 'NONE', *, *, #110975, .T. ) ;
#209635=ORIENTED_EDGE ( 'NONE', *, *, #202755, .T. ) ;
#209663=EDGE_LOOP ( 'NONE', ( #25548, #213076, #25014, #7060, #159452 ) ) ;
#209668=CARTESIAN_POINT ( 'NONE',  ( -23.25000000000000000, -11.74999999998884448, -33.50000000000000000 ) ) ;
#209730=DIRECTION ( 'NONE',  ( -1.000000000000000000, -0.000000000000000000, -0.000000000000000000 ) ) ;
#209796=CARTESIAN_POINT ( 'NONE',  ( -18.50000000000000000, 9.150000000011157653, -21.75000000000000355 ) ) ;
#209806=CARTESIAN_POINT ( 'NONE',  ( 22.49999999999999645, 11.64976291804307884, -33.41119002361307366 ) ) ;
#209839=CARTESIAN_POINT ( 'NONE',  ( -20.94999999999999929, -1.835341550213255957, -45.15515129256298366 ) ) ;
#209866=DIRECTION ( 'NONE',  ( 1.000000000000000000, -0.000000000000000000, -0.000000000000000000 ) ) ;
#209870=ORIENTED_EDGE ( 'NONE', *, *, #180447, .F. ) ;
#209882=VECTOR ( 'NONE', #142748, 1000.000000000000000 ) ;
#209891=CARTESIAN_POINT ( 'NONE',  ( 22.39999999999999503, -0.1008583690875579364, -21.75043287651061164 ) ) ;
#209893=VERTEX_POINT ( 'NONE', #28804 ) ;
#209909=ORIENTED_EDGE ( 'NONE', *, *, #222378, .F. ) ;
#209949=DIRECTION ( 'NONE',  ( 0.000000000000000000, 0.000000000000000000, 1.000000000000000000 ) ) ;
#209986=DIRECTION ( 'NONE',  ( 0.000000000000000000, 0.000000000000000000, -1.000000000000000000 ) ) ;
#210002=AXIS2_PLACEMENT_3D ( 'NONE', #150926, #12726, #51799 ) ;
#210034=DIRECTION ( 'NONE',  ( 1.000000000000000000, 0.000000000000000000, 0.000000000000000000 ) ) ;
#210085=( BOUNDED_CURVE ( )  B_SPLINE_CURVE ( 3, ( #231758, #53098, #33594, #13992 ),
 .UNSPECIFIED., .F., .F. ) 
 B_SPLINE_CURVE_WITH_KNOTS ( ( 4, 4 ),
 ( 4.712388980384689674, 6.231880751915386263 ),
 .UNSPECIFIED. ) 
 CURVE ( )  GEOMETRIC_REPRESENTATION_ITEM ( )  RATIONAL_B_SPLINE_CURVE ( ( 1.000000000000000000, 0.8166740347213228279, 0.8166740347213228279, 1.000000000000000000 ) ) 
 REPRESENTATION_ITEM ( '' )  );
#210096=DIRECTION ( 'NONE',  ( -1.000000000000000000, 0.000000000000000000, 0.000000000000000000 ) ) ;
#210104=VERTEX_POINT ( 'NONE', #42879 ) ;
#210113=CIRCLE ( 'NONE', #110128, 0.1000000000000028644 ) ;
#210116=CARTESIAN_POINT ( 'NONE',  ( 18.39999999999999858, -9.682403433465241349, -73.65684337741279819 ) ) ;
#210125=ORIENTED_EDGE ( 'NONE', *, *, #224833, .T. ) ;
#210131=DIRECTION ( 'NONE',  ( -2.952720810173289112E-16, 1.000000000000000000, -0.000000000000000000 ) ) ;
#210145=DIRECTION ( 'NONE',  ( -1.000000000000000000, -0.000000000000000000, 0.000000000000000000 ) ) ;
#210146=VECTOR ( 'NONE', #48385, 1000.000000000000114 ) ;
#210151=CARTESIAN_POINT ( 'NONE',  ( -20.64999999999999858, 4.350000000011156054, -54.75000000000000000 ) ) ;
#210173=CIRCLE ( 'NONE', #97710, 0.1000000000000028644 ) ;
#210184=ORIENTED_EDGE ( 'NONE', *, *, #230553, .F. ) ;
#210211=ORIENTED_EDGE ( 'NONE', *, *, #171698, .F. ) ;
#210224=ORIENTED_EDGE ( 'NONE', *, *, #249421, .F. ) ;
#210269=DIRECTION ( 'NONE',  ( 1.000000000000000000, 0.000000000000000000, 0.000000000000000000 ) ) ;
#210273=CARTESIAN_POINT ( 'NONE',  ( -22.39999999999999858, 0.1000000000111554016, -25.70922040162659883 ) ) ;
#210281=FACE_OUTER_BOUND ( 'NONE', #157020, .T. ) ;
#210291=DIRECTION ( 'NONE',  ( 0.000000000000000000, -1.000000000000000000, -2.891205793294679805E-16 ) ) ;
#210338=ORIENTED_EDGE ( 'NONE', *, *, #137173, .T. ) ;
#210413=DIRECTION ( 'NONE',  ( -1.000000000000000000, -2.952720810173289112E-16, 0.000000000000000000 ) ) ;
#210442=B_SPLINE_CURVE_WITH_KNOTS ( 'NONE', 3,
 ( #163496, #243020, #203895, #184327, #125645, #112517, #29165, #128225 ),
 .UNSPECIFIED., .F., .F.,
 ( 4, 2, 2, 4 ),
 ( 0.000000000000000000, 6.534141206311912362E-05, 0.0001306828241262382472, 0.0002613656482524788255 ),
 .UNSPECIFIED. ) ;
#210463=DIRECTION ( 'NONE',  ( 1.000000000000000000, -7.304098846218134667E-16, 4.607487905232622991E-31 ) ) ;
#210464=VECTOR ( 'NONE', #37024, 1000.000000000000000 ) ;
#210467=EDGE_CURVE ( 'NONE', #128224, #88400, #239389, .T. ) ;
#210481=SPHERICAL_SURFACE ( 'NONE', #29944, 0.1000000000000000056 ) ;
#210496=ORIENTED_EDGE ( 'NONE', *, *, #229452, .F. ) ;
#210514=AXIS2_PLACEMENT_3D ( 'NONE', #205365, #67158, #167569 ) ;
#210521=DIRECTION ( 'NONE',  ( -1.000000000000000000, 0.000000000000000000, 0.000000000000000000 ) ) ;
#210537=LINE ( 'NONE', #52728, #225862 ) ;
#210555=AXIS2_PLACEMENT_3D ( 'NONE', #150438, #229952, #74775 ) ;
#210565=SPHERICAL_SURFACE ( 'NONE', #74658, 0.1000000000000000056 ) ;
#210568=AXIS2_PLACEMENT_3D ( 'NONE', #70714, #165961, #111093 ) ;
#210599=EDGE_CURVE ( 'NONE', #78967, #197038, #118776, .T. ) ;
#210604=VERTEX_POINT ( 'NONE', #106366 ) ;
#210608=CARTESIAN_POINT ( 'NONE',  ( 21.05000000000000071, 10.42338541492406101, -40.99205192387010044 ) ) ;
#210619=FACE_OUTER_BOUND ( 'NONE', #8603, .T. ) ;
#210672=ADVANCED_FACE ( 'NONE', ( #16301 ), #194932, .T. ) ;
#210686=ADVANCED_FACE ( 'NONE', ( #209331 ), #235274, .T. ) ;
#210690=EDGE_LOOP ( 'NONE', ( #197915, #125608, #81999, #246724 ) ) ;
#210757=CIRCLE ( 'NONE', #177486, 11.74999999999999645 ) ;
#210763=DIRECTION ( 'NONE',  ( -0.000000000000000000, 1.000000000000000000, -1.224646799147352961E-16 ) ) ;
#210776=DIRECTION ( 'NONE',  ( 1.000000000000000000, 3.265361837132813093E-16, -0.000000000000000000 ) ) ;
#210808=CARTESIAN_POINT ( 'NONE',  ( 21.13498764882293557, 6.495618143485025975, -33.49834360526865851 ) ) ;
#210849=CARTESIAN_POINT ( 'NONE',  ( -18.50000000000000000, 11.75000000001115197, -54.85000000000000142 ) ) ;
#210852=DIRECTION ( 'NONE',  ( 1.000000000000000000, -0.000000000000000000, -0.000000000000000000 ) ) ;
#210860=ORIENTED_EDGE ( 'NONE', *, *, #69423, .T. ) ;
#210866=SPHERICAL_SURFACE ( 'NONE', #18996, 0.1000000000000000056 ) ;
#210871=ORIENTED_EDGE ( 'NONE', *, *, #138232, .F. ) ;
#210881=EDGE_LOOP ( 'NONE', ( #155912, #33049, #30225, #147621 ) ) ;
#210916=ORIENTED_EDGE ( 'NONE', *, *, #181461, .F. ) ;
#210919=ORIENTED_EDGE ( 'NONE', *, *, #50924, .F. ) ;
#210928=CARTESIAN_POINT ( 'NONE',  ( -20.00857864376270001, 9.150000000011157653, -54.65000000000000568 ) ) ;
#210975=AXIS2_PLACEMENT_3D ( 'NONE', #39876, #158541, #138906 ) ;
#210980=EDGE_CURVE ( 'NONE', #161314, #177537, #73409, .T. ) ;
#210995=CARTESIAN_POINT ( 'NONE',  ( -23.15000000000000213, -9.499999999988846255, -57.10603087734755690 ) ) ;
#211008=EDGE_LOOP ( 'NONE', ( #241301, #101416, #329, #139113 ) ) ;
#211032=DIRECTION ( 'NONE',  ( 0.000000000000000000, 0.000000000000000000, -1.000000000000000000 ) ) ;
#211040=AXIS2_PLACEMENT_3D ( 'NONE', #235319, #213184, #72425 ) ;
#211059=CARTESIAN_POINT ( 'NONE',  ( -18.45068461519105796, -9.486506529077932015, -40.56877716890470964 ) ) ;
#211060=ORIENTED_EDGE ( 'NONE', *, *, #119316, .F. ) ;
#211062=CARTESIAN_POINT ( 'NONE',  ( -20.64999999999999858, -8.663551401858001100, -57.47589888193270014 ) ) ;
#211090=AXIS2_PLACEMENT_3D ( 'NONE', #248801, #53153, #212248 ) ;
#211117=CARTESIAN_POINT ( 'NONE',  ( 21.00000000000000000, 9.750000000011153745, -54.65000000000000568 ) ) ;
#211123=DIRECTION ( 'NONE',  ( 0.000000000000000000, -0.9915357197604792727, 0.1298341882520473722 ) ) ;
#211144=CARTESIAN_POINT ( 'NONE',  ( -21.44999999999999929, 7.350000000011155166, -45.85000000000000142 ) ) ;
#211166=CARTESIAN_POINT ( 'NONE',  ( 23.14999999999999858, 4.813084112160680661, -45.44151775652382952 ) ) ;
#211169=CARTESIAN_POINT ( 'NONE',  ( -21.37071067811865532, 8.070710678129811910, -45.75000000000000000 ) ) ;
#211174=CARTESIAN_POINT ( 'NONE',  ( -20.00857864376270001, 9.150000000011157653, -45.85000000000000142 ) ) ;
#211177=ORIENTED_EDGE ( 'NONE', *, *, #83450, .T. ) ;
#211181=EDGE_LOOP ( 'NONE', ( #99136, #21709, #138712, #225256 ) ) ;
#211236=CYLINDRICAL_SURFACE ( 'NONE', #103653, 7.900000000000003908 ) ;
#211253=DIRECTION ( 'NONE',  ( 0.000000000000000000, 0.000000000000000000, -1.000000000000000000 ) ) ;
#211268=CARTESIAN_POINT ( 'NONE',  ( 21.56666275994539816, 1.115600667400684642E-11, -26.54263159310668030 ) ) ;
#211272=DIRECTION ( 'NONE',  ( 0.000000000000000000, 0.000000000000000000, -1.000000000000000000 ) ) ;
#211284=CARTESIAN_POINT ( 'NONE',  ( -21.07928932188134041, 6.328516656404449492, -33.40110485434561127 ) ) ;
#211297=CARTESIAN_POINT ( 'NONE',  ( 20.94999999999999574, 1.250000000011155299, -41.40000000000000568 ) ) ;
#211352=CIRCLE ( 'NONE', #82312, 0.1000000000000028644 ) ;
#211380=DIRECTION ( 'NONE',  ( 0.000000000000000000, 0.000000000000000000, -1.000000000000000000 ) ) ;
#211398=EDGE_CURVE ( 'NONE', #96922, #174796, #89891, .T. ) ;
#211405=FACE_OUTER_BOUND ( 'NONE', #219773, .T. ) ;
#211421=CARTESIAN_POINT ( 'NONE',  ( 20.94999999999999929, 6.550000000011156231, -45.74999999999999289 ) ) ;
#211449=CARTESIAN_POINT ( 'NONE',  ( -18.40000000000000213, -9.499999999988851584, -73.60018939122203108 ) ) ;
#211470=CARTESIAN_POINT ( 'NONE',  ( 21.06600267594171783, 8.775166069211060460, -45.70426278237474094 ) ) ;
#211502=CARTESIAN_POINT ( 'NONE',  ( -18.59999999999999787, -1.164121893230052995, -74.91484808557160591 ) ) ;
#211529=CIRCLE ( 'NONE', #219889, 0.1000000000000028644 ) ;
#211545=FACE_OUTER_BOUND ( 'NONE', #170142, .T. ) ;
#211551=CARTESIAN_POINT ( 'NONE',  ( 18.41789779300685481, -9.499999999988844479, -40.53206966636064124 ) ) ;
#211561=CARTESIAN_POINT ( 'NONE',  ( -21.05000000000000071, -1.835341550213255957, -45.05515129256298223 ) ) ;
#211577=TOROIDAL_SURFACE ( 'NONE', #244873, 12.97499999999999609, 0.1000000000000000056 ) ;
#211612=DIRECTION ( 'NONE',  ( 0.000000000000000000, 0.1350103645451876666, -0.9908441862701600211 ) ) ;
#211637=CARTESIAN_POINT ( 'NONE',  ( 21.05000000000000071, 1.115600667400684642E-11, -45.65000000000000568 ) ) ;
#211642=DIRECTION ( 'NONE',  ( 0.000000000000000000, 0.000000000000000000, -1.000000000000000000 ) ) ;
#211659=DIRECTION ( 'NONE',  ( 0.000000000000000000, 1.000000000000000000, 2.891205793294679805E-16 ) ) ;
#211666=EDGE_LOOP ( 'NONE', ( #162930, #80608, #147941, #22467 ) ) ;
#211678=AXIS2_PLACEMENT_3D ( 'NONE', #212778, #130654, #31596 ) ;
#211682=ADVANCED_FACE ( 'NONE', ( #211965 ), #251060, .T. ) ;
#211688=CARTESIAN_POINT ( 'NONE',  ( -18.50000000000000000, 1.115600667400684642E-11, -33.50000000000000000 ) ) ;
#211700=DIRECTION ( 'NONE',  ( 2.940209281316622495E-16, -1.000000000000000000, -2.352167425053297996E-15 ) ) ;
#211702=CARTESIAN_POINT ( 'NONE',  ( 21.93340585898988948, 1.115541036281197940E-11, -26.17585297787523047 ) ) ;
#211716=AXIS2_PLACEMENT_3D ( 'NONE', #236332, #100637, #255848 ) ;
#211721=ORIENTED_EDGE ( 'NONE', *, *, #120212, .F. ) ;
#211728=VECTOR ( 'NONE', #232150, 1000.000000000000000 ) ;
#211753=DIRECTION ( 'NONE',  ( 0.000000000000000000, 0.000000000000000000, -1.000000000000000000 ) ) ;
#211768=DIRECTION ( 'NONE',  ( 1.000000000000000000, 0.000000000000000000, 0.000000000000000000 ) ) ;
#211775=ORIENTED_EDGE ( 'NONE', *, *, #239726, .F. ) ;
#211795=CARTESIAN_POINT ( 'NONE',  ( -18.59999999999999787, -9.480686695267820596, -73.94111516875784673 ) ) ;
#211805=AXIS2_PLACEMENT_3D ( 'NONE', #243395, #64759, #144271 ) ;
#211816=DIRECTION ( 'NONE',  ( 0.000000000000000000, 0.000000000000000000, 1.000000000000000000 ) ) ;
#211821=VECTOR ( 'NONE', #54279, 1000.000000000000227 ) ;
#211846=CIRCLE ( 'NONE', #249448, 11.70000000000000284 ) ;
#211850=ADVANCED_FACE ( 'NONE', ( #38446 ), #63129, .T. ) ;
#211855=ADVANCED_FACE ( 'NONE', ( #57986 ), #117984, .T. ) ;
#211909=ORIENTED_EDGE ( 'NONE', *, *, #165949, .F. ) ;
#211913=CARTESIAN_POINT ( 'NONE',  ( 20.94999999999999574, 10.47338541492405994, -41.07865446424855094 ) ) ;
#211925=AXIS2_PLACEMENT_3D ( 'NONE', #222572, #63508, #47786 ) ;
#211941=DIRECTION ( 'NONE',  ( 1.000000000000000000, 0.000000000000000000, 0.000000000000000000 ) ) ;
#211965=FACE_OUTER_BOUND ( 'NONE', #78763, .T. ) ;
#211966=CARTESIAN_POINT ( 'NONE',  ( 20.04142135623731136, 11.75000000001116085, -58.26715728752539292 ) ) ;
#211981=CYLINDRICAL_SURFACE ( 'NONE', #18357, 0.1000000000000028644 ) ;
#212009=AXIS2_PLACEMENT_3D ( 'NONE', #148110, #211941, #189803 ) ;
#212017=ORIENTED_EDGE ( 'NONE', *, *, #112263, .T. ) ;
#212027=AXIS2_PLACEMENT_3D ( 'NONE', #186236, #23335, #166699 ) ;
#212037=CYLINDRICAL_SURFACE ( 'NONE', #219807, 0.1000000000000028644 ) ;
#212075=LINE ( 'NONE', #34733, #48414 ) ;
#212079=EDGE_CURVE ( 'NONE', #65499, #17436, #43148, .T. ) ;
#212101=DIRECTION ( 'NONE',  ( -4.336808689942053235E-15, -0.8660254037844482555, -0.4999999999999836797 ) ) ;
#212112=ADVANCED_FACE ( 'NONE', ( #130367 ), #65333, .T. ) ;
#212152=CARTESIAN_POINT ( 'NONE',  ( -22.59999999999999787, 11.74987124438766273, -33.43457040898632471 ) ) ;
#212159=EDGE_CURVE ( 'NONE', #244896, #71915, #190242, .T. ) ;
#212208=CARTESIAN_POINT ( 'NONE',  ( -20.85000000000000142, 6.846123162363745074, -70.73772626684986164 ) ) ;
#212248=DIRECTION ( 'NONE',  ( 0.000000000000000000, 0.000000000000000000, -1.000000000000000000 ) ) ;
#212251=DIRECTION ( 'NONE',  ( -0.000000000000000000, -0.8660254037844411501, -0.4999999999999956701 ) ) ;
#212252=FACE_OUTER_BOUND ( 'NONE', #235796, .T. ) ;
#212255=ORIENTED_EDGE ( 'NONE', *, *, #189177, .F. ) ;
#212264=VERTEX_POINT ( 'NONE', #235755 ) ;
#212292=VERTEX_POINT ( 'NONE', #195384 ) ;
#212298=AXIS2_PLACEMENT_3D ( 'NONE', #170386, #33430, #247286 ) ;
#212318=DIRECTION ( 'NONE',  ( 0.000000000000000000, 2.664535259100316927E-15, 1.000000000000000000 ) ) ;
#212332=CARTESIAN_POINT ( 'NONE',  ( -20.64999999999999858, -8.999999999988844479, -57.60603087734755690 ) ) ;
#212344=CIRCLE ( 'NONE', #16520, 0.1000000000000028644 ) ;
#212348=( BOUNDED_SURFACE ( )  B_SPLINE_SURFACE ( 3, 2, ( 
 ( #16, #78265, #176123 ),
 ( #157865, #216502, #196934 ),
 ( #18305, #177413, #138230 ),
 ( #39181, #118712, #198221 ) ),
 .UNSPECIFIED., .F., .F., .F. ) 
 B_SPLINE_SURFACE_WITH_KNOTS ( ( 4, 4 ),
 ( 3, 3 ),
 ( 0.000000000000000000, 0.001979672783031562362 ),
 ( 0.000000000000000000, 1.000000000000000000 ),
 .UNSPECIFIED. ) 
 GEOMETRIC_REPRESENTATION_ITEM ( )  RATIONAL_B_SPLINE_SURFACE ( (
 ( 1.000000000000000000, 0.7103081912008196719, 1.000000000000000000),
 ( 1.000000000000000000, 0.7104998333558631973, 1.000000000000000000),
 ( 1.000000000000000000, 0.7107238315755253222, 1.000000000000000000),
 ( 1.000000000000000000, 0.7110073749539376209, 1.000000000000000000) ) ) 
 REPRESENTATION_ITEM ( '' )  SURFACE ( )  );
#212353=DIRECTION ( 'NONE',  ( -1.000000000000000000, 0.000000000000000000, 0.000000000000000000 ) ) ;
#212361=DIRECTION ( 'NONE',  ( 2.952720810173289112E-16, -1.000000000000000000, 0.000000000000000000 ) ) ;
#212366=EDGE_LOOP ( 'NONE', ( #3004, #145363, #186257, #120523 ) ) ;
#212376=ORIENTED_EDGE ( 'NONE', *, *, #212642, .F. ) ;
#212384=MECHANICAL_DESIGN_GEOMETRIC_PRESENTATION_REPRESENTATION('',(#108331),#99905);
#212390=ORIENTED_EDGE ( 'NONE', *, *, #146302, .F. ) ;
#212398=DIRECTION ( 'NONE',  ( 4.239556034732056743E-17, -0.1298341882520022694, -0.9915357197604852679 ) ) ;
#212400=DIRECTION ( 'NONE',  ( -1.000000000000000000, 0.000000000000000000, 0.000000000000000000 ) ) ;
#212461=EDGE_LOOP ( 'NONE', ( #162203, #116449, #5929, #26127 ) ) ;
#212463=ORIENTED_EDGE ( 'NONE', *, *, #74632, .T. ) ;
#212524=EDGE_CURVE ( 'NONE', #205142, #31458, #36310, .T. ) ;
#212542=ORIENTED_EDGE ( 'NONE', *, *, #54382, .T. ) ;
#212553=EDGE_LOOP ( 'NONE', ( #206538, #226185, #127865, #205774 ) ) ;
#212561=CARTESIAN_POINT ( 'NONE',  ( -21.00023020733438273, 6.390869245278866018, -33.50000000000000711 ) ) ;
#212564=CARTESIAN_POINT ( 'NONE',  ( 21.05000000000000071, -1.249999999988843369, -41.40000000000000568 ) ) ;
#212591=DIRECTION ( 'NONE',  ( 0.000000000000000000, -1.776356839400189131E-15, 1.000000000000000000 ) ) ;
#212592=DIRECTION ( 'NONE',  ( -1.000000000000000000, 0.000000000000000000, 0.000000000000000000 ) ) ;
#212609=EDGE_CURVE ( 'NONE', #971, #67224, #188621, .T. ) ;
#212640=AXIS2_PLACEMENT_3D ( 'NONE', #161838, #150, #202226 ) ;
#212642=EDGE_CURVE ( 'NONE', #24511, #110094, #8712, .T. ) ;
#212655=DIRECTION ( 'NONE',  ( 0.000000000000000000, 0.000000000000000000, -1.000000000000000000 ) ) ;
#212657=DIRECTION ( 'NONE',  ( -0.000000000000000000, -0.000000000000000000, 1.000000000000000000 ) ) ;
#212676=ORIENTED_EDGE ( 'NONE', *, *, #168214, .T. ) ;
#212688=ORIENTED_EDGE ( 'NONE', *, *, #56243, .T. ) ;
#212690=CARTESIAN_POINT ( 'NONE',  ( -20.94999999999999929, 1.115600667400684642E-11, -67.00000000000000000 ) ) ;
#212698=CARTESIAN_POINT ( 'NONE',  ( 18.39999999999999858, -9.682403433465237796, -73.65684337741279819 ) ) ;
#212707=B_SPLINE_CURVE_WITH_KNOTS ( 'NONE', 3,
 ( #128778, #85749, #187476, #165331, #8825, #148331, #88323, #44099, #242285, #244852, #243579, #46641, #87046, #144452, #167926, #123643 ),
 .UNSPECIFIED., .F., .F.,
 ( 4, 3, 3, 3, 3, 4 ),
 ( 0.000000000000000000, 3.357088238233693503E-05, 6.714213034886854165E-05, 0.0001007408646120936052, 0.0001343627955914235370, 0.0001573956632896016355 ),
 .UNSPECIFIED. ) ;
#212709=DIRECTION ( 'NONE',  ( -2.602085213965226419E-14, -0.000000000000000000, 1.000000000000000000 ) ) ;
#212724=EDGE_LOOP ( 'NONE', ( #241613, #183236, #141260, #25288 ) ) ;
#212734=ADVANCED_FACE ( 'NONE', ( #253719 ), #153399, .T. ) ;
#212737=VERTEX_POINT ( 'NONE', #33449 ) ;
#212739=AXIS2_PLACEMENT_3D ( 'NONE', #136280, #158473, #59302 ) ;
#212744=CARTESIAN_POINT ( 'NONE',  ( -18.40000000000000213, -9.682403433465244902, -73.65684337741278398 ) ) ;
#212748=VERTEX_POINT ( 'NONE', #234163 ) ;
#212750=ORIENTED_EDGE ( 'NONE', *, *, #180165, .F. ) ;
#212755=ORIENTED_EDGE ( 'NONE', *, *, #135821, .F. ) ;
#212756=DIRECTION ( 'NONE',  ( 0.000000000000000000, 0.000000000000000000, -1.000000000000000000 ) ) ;
#212766=CARTESIAN_POINT ( 'NONE',  ( 21.13920837816993270, 8.783247050131068434, -45.75000000000000711 ) ) ;
#212769=DIRECTION ( 'NONE',  ( -1.000000000000000000, 0.000000000000000000, 0.000000000000000000 ) ) ;
#212770=FACE_OUTER_BOUND ( 'NONE', #179798, .T. ) ;
#212778=CARTESIAN_POINT ( 'NONE',  ( -20.94999999999999929, -11.74999999998884448, -36.39999999999999858 ) ) ;
#212795=CARTESIAN_POINT ( 'NONE',  ( 18.49999999999999289, 11.75000000001115907, -41.60000000000000142 ) ) ;
#212840=FACE_OUTER_BOUND ( 'NONE', #157415, .T. ) ;
#212851=DIRECTION ( 'NONE',  ( 1.000000000000000000, 2.952720810173289112E-16, -0.000000000000000000 ) ) ;
#212860=AXIS2_PLACEMENT_3D ( 'NONE', #184725, #145600, #30827 ) ;
#212872=ORIENTED_EDGE ( 'NONE', *, *, #251868, .F. ) ;
#212873=DIRECTION ( 'NONE',  ( 0.000000000000000000, 0.000000000000000000, -1.000000000000000000 ) ) ;
#212878=ORIENTED_EDGE ( 'NONE', *, *, #222530, .F. ) ;
#212880=ORIENTED_EDGE ( 'NONE', *, *, #179867, .T. ) ;
#212909=DIRECTION ( 'NONE',  ( 0.000000000000000000, 0.000000000000000000, 1.000000000000000000 ) ) ;
#212949=CYLINDRICAL_SURFACE ( 'NONE', #245754, 2.000000000000001776 ) ;
#212975=ORIENTED_EDGE ( 'NONE', *, *, #69470, .T. ) ;
#212998=ORIENTED_EDGE ( 'NONE', *, *, #207075, .T. ) ;
#213008=DIRECTION ( 'NONE',  ( 0.000000000000000000, 0.000000000000000000, -1.000000000000000000 ) ) ;
#213025=VERTEX_POINT ( 'NONE', #16131 ) ;
#213051=DIRECTION ( 'NONE',  ( 1.000000000000000000, 0.000000000000000000, 0.000000000000000000 ) ) ;
#213076=ORIENTED_EDGE ( 'NONE', *, *, #69402, .T. ) ;
#213079=EDGE_CURVE ( 'NONE', #69658, #200509, #153215, .T. ) ;
#213092=EDGE_CURVE ( 'NONE', #214929, #201200, #95105, .T. ) ;
#213121=EDGE_CURVE ( 'NONE', #230427, #85875, #179065, .T. ) ;
#213148=DIRECTION ( 'NONE',  ( -1.000000000000000000, -0.000000000000000000, 0.000000000000000000 ) ) ;
#213150=( BOUNDED_CURVE ( )  B_SPLINE_CURVE ( 3, ( #211913, #232759, #129785, #253574 ),
 .UNSPECIFIED., .F., .F. ) 
 B_SPLINE_CURVE_WITH_KNOTS ( ( 4, 4 ),
 ( 0.06456096931748307732, 3.077031684272310219 ),
 .UNSPECIFIED. ) 
 CURVE ( )  GEOMETRIC_REPRESENTATION_ITEM ( )  RATIONAL_B_SPLINE_CURVE ( ( 1.000000000000000000, 0.3763440860215093164, 0.3763440860215093164, 1.000000000000000000 ) ) 
 REPRESENTATION_ITEM ( '' )  );
#213169=CARTESIAN_POINT ( 'NONE',  ( 21.05000000000000071, 10.48459288120565702, -40.95671357058389361 ) ) ;
#213173=CARTESIAN_POINT ( 'NONE',  ( 18.53691006697098942, 10.30215155716143016, -58.20219871729846517 ) ) ;
#213184=DIRECTION ( 'NONE',  ( 9.044546369203339308E-15, -0.7397360091702694929, -0.6728971962616898672 ) ) ;
#213214=EDGE_CURVE ( 'NONE', #43175, #6368, #86315, .T. ) ;
#213219=LINE ( 'NONE', #34621, #137653 ) ;
#213225=ORIENTED_EDGE ( 'NONE', *, *, #235489, .F. ) ;
#213277=CARTESIAN_POINT ( 'NONE',  ( 21.05000000000000071, 8.876614585098257848, -41.88508047884467800 ) ) ;
#213283=ORIENTED_EDGE ( 'NONE', *, *, #92735, .F. ) ;
#213289=DIRECTION ( 'NONE',  ( 0.000000000000000000, -1.000000000000000000, 0.000000000000000000 ) ) ;
#213301=LINE ( 'NONE', #251134, #228725 ) ;
#213354=AXIS2_PLACEMENT_3D ( 'NONE', #142836, #9771, #123314 ) ;
#213419=CIRCLE ( 'NONE', #55186, 0.09999999999999943656 ) ;
#213452=CIRCLE ( 'NONE', #130054, 0.1000000000000028644 ) ;
#213508=CARTESIAN_POINT ( 'NONE',  ( -20.94999999999999929, 11.65000000001115232, -60.21613433702190576 ) ) ;
#213535=ORIENTED_EDGE ( 'NONE', *, *, #143947, .F. ) ;
#213570=DIRECTION ( 'NONE',  ( 0.000000000000000000, 0.01562500000001045344, 0.9998779222360096863 ) ) ;
#213587=DIRECTION ( 'NONE',  ( 1.000000000000000000, 0.000000000000000000, 0.000000000000000000 ) ) ;
#213601=LINE ( 'NONE', #252722, #7831 ) ;
#213612=CIRCLE ( 'NONE', #251196, 0.1000000000000002554 ) ;
#213633=CIRCLE ( 'NONE', #51107, 0.1000000000000008799 ) ;
#213640=ORIENTED_EDGE ( 'NONE', *, *, #239462, .F. ) ;
#213642=EDGE_CURVE ( 'NONE', #228375, #55828, #203441, .T. ) ;
#213646=ORIENTED_EDGE ( 'NONE', *, *, #196152, .F. ) ;
#213680=CARTESIAN_POINT ( 'NONE',  ( -23.15000000000000213, -11.64999999998884483, -63.89999999999999858 ) ) ;
#213688=DIRECTION ( 'NONE',  ( 1.000000000000000000, 1.875376730785737719E-16, 0.000000000000000000 ) ) ;
#213701=CARTESIAN_POINT ( 'NONE',  ( 18.39999999999999858, -9.399999999988843058, -21.75000000000000355 ) ) ;
#213702=CONICAL_SURFACE ( 'NONE', #47091, 4.299999999999956302, 0.7853981633974466137 ) ;
#213705=ADVANCED_FACE ( 'NONE', ( #214638 ), #252476, .F. ) ;
#213719=VECTOR ( 'NONE', #206905, 999.9999999999998863 ) ;
#213737=EDGE_CURVE ( 'NONE', #253488, #179315, #192526, .T. ) ;
#213770=VERTEX_POINT ( 'NONE', #13888 ) ;
#213772=DIRECTION ( 'NONE',  ( 0.000000000000000000, -0.000000000000000000, 1.000000000000000000 ) ) ;
#213775=VERTEX_POINT ( 'NONE', #33491 ) ;
#213788=ADVANCED_FACE ( 'NONE', ( #95968 ), #132718, .F. ) ;
#213791=DIRECTION ( 'NONE',  ( -1.000000000000000000, -0.000000000000000000, -0.000000000000000000 ) ) ;
#213793=EDGE_LOOP ( 'NONE', ( #32246, #184484, #244303, #91744 ) ) ;
#213805=CIRCLE ( 'NONE', #105623, 12.87500000000000000 ) ;
#213812=CIRCLE ( 'NONE', #176416, 0.1000000000000002831 ) ;
#213813=AXIS2_PLACEMENT_3D ( 'NONE', #199308, #140596, #101427 ) ;
#213824=DIRECTION ( 'NONE',  ( 1.000000000000000000, 0.000000000000000000, 0.000000000000000000 ) ) ;
#213834=DIRECTION ( 'NONE',  ( 0.000000000000000000, 0.000000000000000000, 1.000000000000000000 ) ) ;
#213838=CIRCLE ( 'NONE', #18006, 0.09999999999999939493 ) ;
#213841=DIRECTION ( 'NONE',  ( 1.000000000000000000, -0.000000000000000000, 0.000000000000000000 ) ) ;
#213844=LINE ( 'NONE', #194312, #161666 ) ;
#213848=CARTESIAN_POINT ( 'NONE',  ( 21.13461538461538325, 8.885417037985616773, -45.85000000000000142 ) ) ;
#213849=CARTESIAN_POINT ( 'NONE',  ( 22.46250603428203618, 0.02114417614996233138, -21.85013690265992281 ) ) ;
#213871=DIRECTION ( 'NONE',  ( 0.000000000000000000, 0.000000000000000000, -1.000000000000000000 ) ) ;
#213873=AXIS2_PLACEMENT_3D ( 'NONE', #171021, #13190, #250494 ) ;
#213904=EDGE_CURVE ( 'NONE', #9718, #181648, #201491, .T. ) ;
#213919=DIRECTION ( 'NONE',  ( 0.000000000000000000, -0.4999999999999949485, 0.8660254037844415942 ) ) ;
#213926=CARTESIAN_POINT ( 'NONE',  ( 20.94999999999999929, 1.115600667400684642E-11, -67.00000000000000000 ) ) ;
#213941=DIRECTION ( 'NONE',  ( 6.938893903907222067E-15, -1.000000000000000000, -0.000000000000000000 ) ) ;
#213952=FACE_OUTER_BOUND ( 'NONE', #88792, .T. ) ;
#213976=CARTESIAN_POINT ( 'NONE',  ( 18.60000000000000142, -9.480686695267818820, -73.94111516875786094 ) ) ;
#213988=CIRCLE ( 'NONE', #130580, 0.09999999999999491240 ) ;
#214015=CARTESIAN_POINT ( 'NONE',  ( -18.59999999999999787, -1.261786168553869603, -41.58649896354548048 ) ) ;
#214044=DIRECTION ( 'NONE',  ( 0.000000000000000000, -0.000000000000000000, 1.000000000000000000 ) ) ;
#214075=CIRCLE ( 'NONE', #118412, 0.09999999999999999167 ) ;
#214080=DIRECTION ( 'NONE',  ( 0.000000000000000000, 0.000000000000000000, -1.000000000000000000 ) ) ;
#214084=DIRECTION ( 'NONE',  ( 1.000000000000000000, -0.000000000000000000, -0.000000000000000000 ) ) ;
#214096=ADVANCED_FACE ( 'NONE', ( #56524 ), #112683, .T. ) ;
#214112=EDGE_LOOP ( 'NONE', ( #168102, #131882, #64688, #57289, #5780, #817, #67419, #62414, #145395, #177718 ) ) ;
#214134=ORIENTED_EDGE ( 'NONE', *, *, #246180, .F. ) ;
#214141=CARTESIAN_POINT ( 'NONE',  ( 21.12230431290519306, 0.005209851700162270761, -27.04243334670699284 ) ) ;
#214178=AXIS2_PLACEMENT_3D ( 'NONE', #33386, #153340, #232853 ) ;
#214185=DIRECTION ( 'NONE',  ( 0.000000000000000000, 0.000000000000000000, 1.000000000000000000 ) ) ;
#214221=CARTESIAN_POINT ( 'NONE',  ( -21.05000000000000071, -11.64999999998884306, -64.10000000000000853 ) ) ;
#214251=ORIENTED_EDGE ( 'NONE', *, *, #49665, .T. ) ;
#214285=ORIENTED_EDGE ( 'NONE', *, *, #60303, .F. ) ;
#214303=DIRECTION ( 'NONE',  ( 1.000000000000000000, 7.304098846218134667E-16, -4.607487905232622991E-31 ) ) ;
#214309=AXIS2_PLACEMENT_3D ( 'NONE', #56820, #196360, #17709 ) ;
#214316=LINE ( 'NONE', #252140, #222782 ) ;
#214344=ORIENTED_EDGE ( 'NONE', *, *, #242295, .F. ) ;
#214388=DIRECTION ( 'NONE',  ( 0.000000000000000000, 0.1350103645451876666, -0.9908441862701600211 ) ) ;
#214411=ORIENTED_EDGE ( 'NONE', *, *, #56660, .F. ) ;
#214462=EDGE_CURVE ( 'NONE', #195525, #167819, #190799, .T. ) ;
#214467=AXIS2_PLACEMENT_3D ( 'NONE', #42092, #121630, #62913 ) ;
#214468=CYLINDRICAL_SURFACE ( 'NONE', #257724, 0.09999999999999939493 ) ;
#214495=FACE_OUTER_BOUND ( 'NONE', #28144, .T. ) ;
#214523=LINE ( 'NONE', #230242, #129830 ) ;
#214536=DIRECTION ( 'NONE',  ( -4.408576920032448588E-17, 0.1350103645451876666, 0.9908441862701600211 ) ) ;
#214538=CARTESIAN_POINT ( 'NONE',  ( 18.59999999999997655, 1.115600667400684642E-11, -67.00000000000000000 ) ) ;
#214558=ADVANCED_FACE ( 'NONE', ( #212770 ), #32879, .T. ) ;
#214564=VERTEX_POINT ( 'NONE', #34158 ) ;
#214581=CYLINDRICAL_SURFACE ( 'NONE', #190574, 0.09999999999999939493 ) ;
#214590=ORIENTED_EDGE ( 'NONE', *, *, #55721, .T. ) ;
#214606=VECTOR ( 'NONE', #126076, 1000.000000000000000 ) ;
#214623=DIRECTION ( 'NONE',  ( 0.000000000000000000, 1.000000000000000000, 0.000000000000000000 ) ) ;
#214637=( BOUNDED_SURFACE ( )  B_SPLINE_SURFACE ( 3, 2, ( 
 ( #186202, #183638, #4956 ),
 ( #165353, #166665, #200630 ),
 ( #22001, #143204, #144475 ),
 ( #224024, #63671, #45399 ),
 ( #222736, #42836, #44122 ),
 ( #124946, #101474, #27158 ) ),
 .UNSPECIFIED., .F., .F., .F. ) 
 B_SPLINE_SURFACE_WITH_KNOTS ( ( 4, 2, 4 ),
 ( 3, 3 ),
 ( 0.0001342700090130081948, 0.0002909192928057395587, 0.0004475685765984709769 ),
 ( 0.000000000000000000, 1.000000000000000000 ),
 .UNSPECIFIED. ) 
 GEOMETRIC_REPRESENTATION_ITEM ( )  RATIONAL_B_SPLINE_SURFACE ( (
 ( 1.000000000000000000, 0.7250110520819876836, 1.000000000000000000),
 ( 1.000000000000000000, 0.7257599279138178261, 1.000000000000000000),
 ( 1.000000000000000000, 0.7137594617278574249, 1.000000000000000000),
 ( 1.000000000000000000, 0.6959270178815749608, 1.000000000000000000),
 ( 1.000000000000000000, 0.6919879549334437829, 1.000000000000000000),
 ( 1.000000000000000000, 0.7071067811865494601, 1.000000000000000000) ) ) 
 REPRESENTATION_ITEM ( '' )  SURFACE ( )  );
#214638=FACE_OUTER_BOUND ( 'NONE', #49684, .T. ) ;
#214639=CARTESIAN_POINT ( 'NONE',  ( -20.94999999999999929, 1.162701749949165642, -41.60000000000000142 ) ) ;
#214685=CARTESIAN_POINT ( 'NONE',  ( 20.95346350065193519, 8.887177249185649330, -42.01173194703538627 ) ) ;
#214720=AXIS2_PLACEMENT_3D ( 'NONE', #153803, #76770, #191628 ) ;
#214738=AXIS2_PLACEMENT_3D ( 'NONE', #70462, #129115, #209949 ) ;
#214770=DIRECTION ( 'NONE',  ( 1.000000000000000000, -0.000000000000000000, -0.000000000000000000 ) ) ;
#214784=AXIS2_PLACEMENT_3D ( 'NONE', #96780, #138479, #115098 ) ;
#214789=DIRECTION ( 'NONE',  ( 0.000000000000000000, -0.8700118002898321601, 0.4930308989875230030 ) ) ;
#214822=ORIENTED_EDGE ( 'NONE', *, *, #61522, .F. ) ;
#214841=EDGE_CURVE ( 'NONE', #240562, #181952, #84758, .T. ) ;
#214885=AXIS2_PLACEMENT_3D ( 'NONE', #45333, #122307, #123591 ) ;
#214894=FACE_OUTER_BOUND ( 'NONE', #184038, .T. ) ;
#214929=VERTEX_POINT ( 'NONE', #54646 ) ;
#214956=VERTEX_POINT ( 'NONE', #11700 ) ;
#214967=CIRCLE ( 'NONE', #102505, 0.09999999999999939493 ) ;
#214980=DIRECTION ( 'NONE',  ( 0.000000000000000000, 0.000000000000000000, -1.000000000000000000 ) ) ;
#214989=ORIENTED_EDGE ( 'NONE', *, *, #153555, .T. ) ;
#214999=CARTESIAN_POINT ( 'NONE',  ( -21.05000000000000071, 6.257814610487270279, -33.40220970869120265 ) ) ;
#215006=ORIENTED_EDGE ( 'NONE', *, *, #188023, .F. ) ;
#215012=CIRCLE ( 'NONE', #106663, 0.09999999999999939493 ) ;
#215013=CARTESIAN_POINT ( 'NONE',  ( -23.25000000000000000, 4.350000000011156054, -45.75000000000000711 ) ) ;
#215017=DIRECTION ( 'NONE',  ( -1.000000000000000000, 0.000000000000000000, 0.000000000000000000 ) ) ;
#215029=VERTEX_POINT ( 'NONE', #95064 ) ;
#215038=DIRECTION ( 'NONE',  ( 0.000000000000000000, 1.000000000000000000, 0.000000000000000000 ) ) ;
#215051=AXIS2_PLACEMENT_3D ( 'NONE', #43764, #125852, #82848 ) ;
#215065=DIRECTION ( 'NONE',  ( -1.000000000000000000, 0.000000000000000000, 0.000000000000000000 ) ) ;
#215102=ORIENTED_EDGE ( 'NONE', *, *, #180196, .F. ) ;
#215118=AXIS2_PLACEMENT_3D ( 'NONE', #231476, #193621, #77488 ) ;
#215123=VECTOR ( 'NONE', #156106, 1000.000000000000000 ) ;
#215148=DIRECTION ( 'NONE',  ( 0.000000000000000000, 0.000000000000000000, -1.000000000000000000 ) ) ;
#215169=PLANE ( 'NONE',  #249447 ) ;
#215182=CARTESIAN_POINT ( 'NONE',  ( -20.94999999999999929, -1.362429037182149694, -74.88888124792120493 ) ) ;
#215192=VERTEX_POINT ( 'NONE', #1073 ) ;
#215193=CARTESIAN_POINT ( 'NONE',  ( -18.39999999999999858, -9.682403433465239573, -73.65684337741279819 ) ) ;
#215196=EDGE_CURVE ( 'NONE', #23656, #241512, #66227, .T. ) ;
#215211=ADVANCED_FACE ( 'NONE', ( #117204 ), #196729, .T. ) ;
#215215=ADVANCED_FACE ( 'NONE', ( #247403 ), #27121, .F. ) ;
#215225=LINE ( 'NONE', #174867, #100880 ) ;
#215244=ORIENTED_EDGE ( 'NONE', *, *, #202355, .T. ) ;
#215253=EDGE_CURVE ( 'NONE', #173389, #214956, #47917, .T. ) ;
#215255=CARTESIAN_POINT ( 'NONE',  ( 18.50000000000000355, -9.399999999988846611, -73.88204184817267617 ) ) ;
#215287=EDGE_LOOP ( 'NONE', ( #137745, #3463, #231629, #182806 ) ) ;
#215295=ORIENTED_EDGE ( 'NONE', *, *, #51195, .T. ) ;
#215298=EDGE_LOOP ( 'NONE', ( #25165, #128890, #205921, #123185 ) ) ;
#215312=ORIENTED_EDGE ( 'NONE', *, *, #11166, .T. ) ;
#215328=ORIENTED_EDGE ( 'NONE', *, *, #137085, .F. ) ;
#215355=AXIS2_PLACEMENT_3D ( 'NONE', #34914, #114416, #15337 ) ;
#215366=DIRECTION ( 'NONE',  ( 0.000000000000000000, 0.000000000000000000, 1.000000000000000000 ) ) ;
#215388=DIRECTION ( 'NONE',  ( -1.000000000000000000, 0.000000000000000000, 0.000000000000000000 ) ) ;
#215394=EDGE_CURVE ( 'NONE', #140899, #38982, #13953, .T. ) ;
#215412=DIRECTION ( 'NONE',  ( 1.000000000000000000, -0.000000000000000000, -0.000000000000000000 ) ) ;
#215422=VECTOR ( 'NONE', #183587, 1000.000000000000000 ) ;
#215429=AXIS2_PLACEMENT_3D ( 'NONE', #213701, #129356, #146337 ) ;
#215436=AXIS2_PLACEMENT_3D ( 'NONE', #36420, #96341, #21977 ) ;
#215472=DIRECTION ( 'NONE',  ( -1.000000000000000000, 0.000000000000000000, 0.000000000000000000 ) ) ;
#215475=CARTESIAN_POINT ( 'NONE',  ( 23.24999999999999289, 6.450000000011156587, -45.85000000000000142 ) ) ;
#215481=CARTESIAN_POINT ( 'NONE',  ( -18.59999999999999787, 1.162701749949165642, -41.60000000000000142 ) ) ;
#215490=CARTESIAN_POINT ( 'NONE',  ( 18.59999999999999787, -10.35479209691423996, -60.75654098307376216 ) ) ;
#215512=CARTESIAN_POINT ( 'NONE',  ( 18.59999999999999787, -11.74999999998883737, -54.85000000000000142 ) ) ;
#215526=DIRECTION ( 'NONE',  ( -0.000000000000000000, 0.8660254037844411501, 0.4999999999999956146 ) ) ;
#215576=DIRECTION ( 'NONE',  ( 1.000000000000000000, 0.000000000000000000, 0.000000000000000000 ) ) ;
#215582=CARTESIAN_POINT ( 'NONE',  ( 23.14999999999999858, 1.115600667400684642E-11, -67.00000000000000000 ) ) ;
#215620=CARTESIAN_POINT ( 'NONE',  ( 19.99999999999998934, 11.65000000001115943, -54.75000000000000000 ) ) ;
#215639=EDGE_LOOP ( 'NONE', ( #11317, #67324, #144033, #112390 ) ) ;
#215647=ORIENTED_EDGE ( 'NONE', *, *, #176048, .T. ) ;
#215648=DIRECTION ( 'NONE',  ( 0.000000000000000000, 0.000000000000000000, -1.000000000000000000 ) ) ;
#215662=VERTEX_POINT ( 'NONE', #91566 ) ;
#215670=DIRECTION ( 'NONE',  ( 1.875376730785737719E-16, -1.000000000000000000, 0.000000000000000000 ) ) ;
#215697=DIRECTION ( 'NONE',  ( -1.000000000000000000, -1.836970198721029934E-16, -3.186635328391151676E-31 ) ) ;
#215722=AXIS2_PLACEMENT_3D ( 'NONE', #165977, #108542, #167264 ) ;
#215759=AXIS2_PLACEMENT_3D ( 'NONE', #114590, #132879, #211123 ) ;
#215760=FACE_OUTER_BOUND ( 'NONE', #15559, .T. ) ;
#215765=FACE_OUTER_BOUND ( 'NONE', #96715, .T. ) ;
#215787=AXIS2_PLACEMENT_3D ( 'NONE', #165630, #225556, #195471 ) ;
#215800=CARTESIAN_POINT ( 'NONE',  ( -23.25000000000000000, 4.250000000011156409, -54.64999999999999858 ) ) ;
#215805=CARTESIAN_POINT ( 'NONE',  ( -21.05000000000000071, -0.09999996528894644632, -27.02244781750650304 ) ) ;
#215823=ORIENTED_EDGE ( 'NONE', *, *, #160376, .F. ) ;
#215827=DIRECTION ( 'NONE',  ( -1.000000000000000000, -0.000000000000000000, -0.000000000000000000 ) ) ;
#215832=CARTESIAN_POINT ( 'NONE',  ( -21.14999999999999858, -11.64999999998884483, -33.50000000000000000 ) ) ;
#215877=DIRECTION ( 'NONE',  ( 0.000000000000000000, -1.000000000000000000, 0.000000000000000000 ) ) ;
#215893=EDGE_CURVE ( 'NONE', #194433, #82553, #130236, .T. ) ;
#215911=DIRECTION ( 'NONE',  ( 1.000000000000000000, 0.000000000000000000, 0.000000000000000000 ) ) ;
#215976=AXIS2_PLACEMENT_3D ( 'NONE', #113225, #50663, #212353 ) ;
#215988=CARTESIAN_POINT ( 'NONE',  ( 18.49999999999999645, -1.362429037182155023, -74.88888124792120493 ) ) ;
#215997=ORIENTED_EDGE ( 'NONE', *, *, #110446, .F. ) ;
#216023=EDGE_CURVE ( 'NONE', #187977, #238808, #162951, .T. ) ;
#216032=( LENGTH_UNIT ( ) NAMED_UNIT ( * ) SI_UNIT ( .MILLI., .METRE. ) );
#216108=DIRECTION ( 'NONE',  ( 1.000000000000000000, -0.000000000000000000, -0.000000000000000000 ) ) ;
#216121=VERTEX_POINT ( 'NONE', #231674 ) ;
#216129=CIRCLE ( 'NONE', #103682, 0.1000000000000028644 ) ;
#216132=EDGE_CURVE ( 'NONE', #179043, #208600, #189625, .T. ) ;
#216143=AXIS2_PLACEMENT_3D ( 'NONE', #133604, #110187, #34538 ) ;
#216149=DIRECTION ( 'NONE',  ( 0.000000000000000000, -1.776356839400308840E-15, 1.000000000000000000 ) ) ;
#216167=DIRECTION ( 'NONE',  ( -1.000000000000000000, 0.000000000000000000, 0.000000000000000000 ) ) ;
#216181=CARTESIAN_POINT ( 'NONE',  ( -21.05000000000000071, -1.249999999988843369, -41.50000000000000000 ) ) ;
#216196=VERTEX_POINT ( 'NONE', #13900 ) ;
#216204=VERTEX_POINT ( 'NONE', #154714 ) ;
#216205=DIRECTION ( 'NONE',  ( 0.000000000000000000, -0.8700118002898322711, 0.4930308989875231140 ) ) ;
#216222=VERTEX_POINT ( 'NONE', #73898 ) ;
#216310=EDGE_LOOP ( 'NONE', ( #134195, #247068, #36626, #120261, #186034, #65917 ) ) ;
#216334=VERTEX_POINT ( 'NONE', #223621 ) ;
#216360=DIRECTION ( 'NONE',  ( 0.000000000000000000, 0.000000000000000000, -1.000000000000000000 ) ) ;
#216378=CARTESIAN_POINT ( 'NONE',  ( -21.05000000000000071, 11.63687328911526642, -40.32175921332488855 ) ) ;
#216399=DIRECTION ( 'NONE',  ( 0.000000000000000000, 0.000000000000000000, 1.000000000000000000 ) ) ;
#216407=AXIS2_PLACEMENT_3D ( 'NONE', #258047, #7627, #66321 ) ;
#216434=CARTESIAN_POINT ( 'NONE',  ( -23.15000000000000213, 11.65000000001115588, -54.75000000000000000 ) ) ;
#216435=ORIENTED_EDGE ( 'NONE', *, *, #200758, .T. ) ;
#216450=AXIS2_PLACEMENT_3D ( 'NONE', #190516, #34024, #168411 ) ;
#216451=ORIENTED_EDGE ( 'NONE', *, *, #71944, .T. ) ;
#216454=AXIS2_PLACEMENT_3D ( 'NONE', #148836, #212657, #210096 ) ;
#216463=ORIENTED_EDGE ( 'NONE', *, *, #257938, .F. ) ;
#216468=DIRECTION ( 'NONE',  ( 0.000000000000000000, 0.000000000000000000, 1.000000000000000000 ) ) ;
#216494=VERTEX_POINT ( 'NONE', #129679 ) ;
#216500=ORIENTED_EDGE ( 'NONE', *, *, #159496, .F. ) ;
#216502=CARTESIAN_POINT ( 'NONE',  ( -22.00356870068577919, 8.752767083654352118E-12, -26.24575763824059749 ) ) ;
#216512=DIRECTION ( 'NONE',  ( 0.000000000000000000, -0.000000000000000000, 1.000000000000000000 ) ) ;
#216519=AXIS2_PLACEMENT_3D ( 'NONE', #136855, #15664, #57300 ) ;
#216550=LINE ( 'NONE', #195737, #198630 ) ;
#216588=EDGE_CURVE ( 'NONE', #5569, #19748, #255275, .T. ) ;
#216593=ORIENTED_EDGE ( 'NONE', *, *, #142843, .T. ) ;
#216634=CIRCLE ( 'NONE', #191740, 0.1000000000000028644 ) ;
#216638=DIRECTION ( 'NONE',  ( 1.000000000000000000, 0.000000000000000000, 0.000000000000000000 ) ) ;
#216691=DIRECTION ( 'NONE',  ( 1.000000000000000000, 0.000000000000000000, 0.000000000000000000 ) ) ;
#216692=EDGE_LOOP ( 'NONE', ( #154218, #196052, #8762, #174060 ) ) ;
#216725=DIRECTION ( 'NONE',  ( 0.000000000000000000, 0.000000000000000000, -1.000000000000000000 ) ) ;
#216740=DIRECTION ( 'NONE',  ( 0.000000000000000000, 0.000000000000000000, -1.000000000000000000 ) ) ;
#216742=ORIENTED_EDGE ( 'NONE', *, *, #20638, .F. ) ;
#216743=ORIENTED_EDGE ( 'NONE', *, *, #85816, .F. ) ;
#216750=ADVANCED_FACE ( 'NONE', ( #243858 ), #97068, .T. ) ;
#216794=PLANE ( 'NONE',  #41337 ) ;
#216807=CARTESIAN_POINT ( 'NONE',  ( -20.94999999999999929, 5.850000000011108092, -43.63249722427796939 ) ) ;
#216828=AXIS2_PLACEMENT_3D ( 'NONE', #98040, #18548, #19845 ) ;
#216848=FACE_OUTER_BOUND ( 'NONE', #180272, .T. ) ;
#216922=DIRECTION ( 'NONE',  ( -1.000000000000000000, 0.000000000000000000, 0.000000000000000000 ) ) ;
#216926=EDGE_CURVE ( 'NONE', #165708, #61363, #234864, .T. ) ;
#216937=CARTESIAN_POINT ( 'NONE',  ( 21.05000000000000071, 1.115600667400684642E-11, -33.50000000000000000 ) ) ;
#216960=EDGE_CURVE ( 'NONE', #16805, #6281, #57190, .T. ) ;
#216980=CARTESIAN_POINT ( 'NONE',  ( -23.25000000000000000, 1.115600667400684642E-11, -33.50000000000000000 ) ) ;
#216991=DIRECTION ( 'NONE',  ( 1.000000000000000000, 0.000000000000000000, -0.000000000000000000 ) ) ;
#216996=CARTESIAN_POINT ( 'NONE',  ( 20.94999999999999929, -12.41227409413852811, -64.00000000000000000 ) ) ;
#216998=ORIENTED_EDGE ( 'NONE', *, *, #194413, .F. ) ;
#217025=VERTEX_POINT ( 'NONE', #214999 ) ;
#217103=ADVANCED_FACE ( 'NONE', ( #62359 ), #47394, .F. ) ;
#217112=DIRECTION ( 'NONE',  ( 1.000000000000000000, 0.000000000000000000, 0.000000000000000000 ) ) ;
#217122=CARTESIAN_POINT ( 'NONE',  ( -20.85000000000000142, 11.75000000001115197, -60.21613433702190576 ) ) ;
#217123=ORIENTED_EDGE ( 'NONE', *, *, #33521, .F. ) ;
#217144=FACE_OUTER_BOUND ( 'NONE', #39243, .T. ) ;
#217163=DIRECTION ( 'NONE',  ( 0.000000000000000000, 0.000000000000000000, 1.000000000000000000 ) ) ;
#217175=VERTEX_POINT ( 'NONE', #191322 ) ;
#217190=CIRCLE ( 'NONE', #238046, 0.1000000000000000472 ) ;
#217194=EDGE_CURVE ( 'NONE', #65618, #178845, #126528, .T. ) ;
#217198=FACE_OUTER_BOUND ( 'NONE', #76335, .T. ) ;
#217234=DIRECTION ( 'NONE',  ( -1.000000000000000000, -2.952720810173289112E-16, 0.000000000000000000 ) ) ;
#217253=DIRECTION ( 'NONE',  ( 1.000000000000000000, 2.952720810173289112E-16, -0.000000000000000000 ) ) ;
#217267=ORIENTED_EDGE ( 'NONE', *, *, #111450, .T. ) ;
#217276=CARTESIAN_POINT ( 'NONE',  ( -20.85000000000000142, 1.115600667400684642E-11, -67.00000000000000000 ) ) ;
#217283=CARTESIAN_POINT ( 'NONE',  ( 21.04386569057627909, 11.75000000001121059, -60.14283735177934886 ) ) ;
#217299=EDGE_LOOP ( 'NONE', ( #202227, #249002, #17902, #43375 ) ) ;
#217310=EDGE_LOOP ( 'NONE', ( #97682, #79916, #173271 ) ) ;
#217320=CARTESIAN_POINT ( 'NONE',  ( -23.25000000000000000, 10.33248238083634440, -72.59484654391314962 ) ) ;
#217367=CARTESIAN_POINT ( 'NONE',  ( -20.94999999999999929, -1.835341550213255957, -45.05515129256298223 ) ) ;
#217383=CYLINDRICAL_SURFACE ( 'NONE', #126815, 2.000000000000001776 ) ;
#217386=EDGE_CURVE ( 'NONE', #171525, #204139, #245003, .T. ) ;
#217419=CARTESIAN_POINT ( 'NONE',  ( 19.99999999999998934, 11.75000000001115907, -58.35000000000000142 ) ) ;
#217446=CARTESIAN_POINT ( 'NONE',  ( -20.94999999999999929, 1.835341550235567887, -45.15515129256298366 ) ) ;
#217448=DIRECTION ( 'NONE',  ( 0.000000000000000000, 0.000000000000000000, -1.000000000000000000 ) ) ;
#217499=AXIS2_PLACEMENT_3D ( 'NONE', #13033, #96370, #35180 ) ;
#217504=AXIS2_PLACEMENT_3D ( 'NONE', #181357, #255687, #39284 ) ;
#217509=VERTEX_POINT ( 'NONE', #125854 ) ;
#217517=CARTESIAN_POINT ( 'NONE',  ( -20.54999999999999716, 1.115600667400684642E-11, -67.00000000000000000 ) ) ;
#217541=EDGE_LOOP ( 'NONE', ( #75923, #95933, #72434, #227214, #107636, #28061, #179084, #119833, #124971, #63390, #257222 ) ) ;
#217548=DIRECTION ( 'NONE',  ( -1.000000000000000000, 0.000000000000000000, 0.000000000000000000 ) ) ;
#217553=VECTOR ( 'NONE', #231919, 1000.000000000000000 ) ;
#217578=CARTESIAN_POINT ( 'NONE',  ( 18.59999999999999076, 6.650000000011155876, -54.65000000000000568 ) ) ;
#217584=DIRECTION ( 'NONE',  ( 0.000000000000000000, 0.000000000000000000, -1.000000000000000000 ) ) ;
#217596=DIRECTION ( 'NONE',  ( -0.000000000000000000, 3.469446951953635015E-14, 1.000000000000000000 ) ) ;
#217615=ORIENTED_EDGE ( 'NONE', *, *, #137615, .F. ) ;
#217617=AXIS2_PLACEMENT_3D ( 'NONE', #114699, #80685, #216360 ) ;
#217621=DIRECTION ( 'NONE',  ( 2.715809747126116508E-16, -1.000000000000000000, 0.000000000000000000 ) ) ;
#217676=CARTESIAN_POINT ( 'NONE',  ( 21.05000000000000071, -8.999999999988842703, -57.60603087734755690 ) ) ;
#217678=CARTESIAN_POINT ( 'NONE',  ( 18.59999999999999076, 1.835341550235567887, -45.05515129256298223 ) ) ;
#217705=ORIENTED_EDGE ( 'NONE', *, *, #204674, .F. ) ;
#217723=ORIENTED_EDGE ( 'NONE', *, *, #148433, .T. ) ;
#217762=ORIENTED_EDGE ( 'NONE', *, *, #37578, .T. ) ;
#217764=DIRECTION ( 'NONE',  ( -1.000000000000000000, 0.000000000000000000, 0.000000000000000000 ) ) ;
#217796=ORIENTED_EDGE ( 'NONE', *, *, #138318, .F. ) ;
#217814=CARTESIAN_POINT ( 'NONE',  ( -21.05000000000000071, -9.519327731081284938, -40.47297637655933755 ) ) ;
#217828=AXIS2_PLACEMENT_3D ( 'NONE', #133922, #114370, #195219 ) ;
#217861=DIRECTION ( 'NONE',  ( 0.000000000000000000, 0.1298341882520022972, 0.9915357197604853789 ) ) ;
#217892=VECTOR ( 'NONE', #166528, 1000.000000000000000 ) ;
#217939=DIRECTION ( 'NONE',  ( 0.000000000000000000, 1.000000000000000000, 0.000000000000000000 ) ) ;
#217943=CARTESIAN_POINT ( 'NONE',  ( 18.41416235934318735, -9.499999999988846255, -73.60018939122205950 ) ) ;
#217963=LINE ( 'NONE', #99299, #130517 ) ;
#217967=CIRCLE ( 'NONE', #172247, 0.1000000000000028644 ) ;
#217977=EDGE_LOOP ( 'NONE', ( #134203, #60419, #74408, #64350 ) ) ;
#217995=EDGE_CURVE ( 'NONE', #51091, #58399, #246785, .T. ) ;
#218027=LINE ( 'NONE', #255847, #230968 ) ;
#218030=DIRECTION ( 'NONE',  ( 1.000000000000000000, 0.000000000000000000, 0.000000000000000000 ) ) ;
#218035=DIRECTION ( 'NONE',  ( 2.840903330521633255E-16, -0.8700118002898322711, 0.4930308989875231696 ) ) ;
#218040=ORIENTED_EDGE ( 'NONE', *, *, #90985, .T. ) ;
#218049=TOROIDAL_SURFACE ( 'NONE', #59824, 0.2000000000000000111, 0.1000000000000000056 ) ;
#218063=CARTESIAN_POINT ( 'NONE',  ( -23.25000000000000000, -11.74999999998884448, -21.75000000000000355 ) ) ;
#218140=AXIS2_PLACEMENT_3D ( 'NONE', #96595, #99166, #139577 ) ;
#218146=DIRECTION ( 'NONE',  ( 1.000000000000000000, 0.000000000000000000, 0.000000000000000000 ) ) ;
#218171=ORIENTED_EDGE ( 'NONE', *, *, #32155, .T. ) ;
#218265=LINE ( 'NONE', #77464, #235033 ) ;
#218272=EDGE_LOOP ( 'NONE', ( #160113, #89917 ) ) ;
#218281=ORIENTED_EDGE ( 'NONE', *, *, #155063, .T. ) ;
#218293=CARTESIAN_POINT ( 'NONE',  ( 20.85000000000000142, -11.64999999998883595, -64.10000000000000853 ) ) ;
#218311=EDGE_CURVE ( 'NONE', #172722, #36165, #207049, .T. ) ;
#218336=ORIENTED_EDGE ( 'NONE', *, *, #24666, .F. ) ;
#218338=ADVANCED_FACE ( 'NONE', ( #1454 ), #161855, .T. ) ;
#218376=CARTESIAN_POINT ( 'NONE',  ( 18.49999999999999645, 1.728086936805617757, -20.38443500516777007 ) ) ;
#218380=AXIS2_PLACEMENT_3D ( 'NONE', #213680, #18042, #234521 ) ;
#218403=CIRCLE ( 'NONE', #160194, 0.09999999999999939493 ) ;
#218412=CARTESIAN_POINT ( 'NONE',  ( -21.05000000000000071, 11.75000000001115552, -59.98519422934605672 ) ) ;
#218449=DIRECTION ( 'NONE',  ( 0.000000000000000000, 0.000000000000000000, -1.000000000000000000 ) ) ;
#218457=EDGE_CURVE ( 'NONE', #242609, #164375, #250021, .T. ) ;
#218489=CARTESIAN_POINT ( 'NONE',  ( -20.94999999999999929, 10.29270135741298731, -72.45736188715193293 ) ) ;
#218516=DIRECTION ( 'NONE',  ( -0.7071067811865475727, -0.7071067811865475727, 0.000000000000000000 ) ) ;
#218556=DIRECTION ( 'NONE',  ( 1.000000000000000000, 0.000000000000000000, 0.000000000000000000 ) ) ;
#218562=DIRECTION ( 'NONE',  ( 0.000000000000000000, -1.000000000000000000, -0.000000000000000000 ) ) ;
#218575=CARTESIAN_POINT ( 'NONE',  ( -20.64999999999999858, 1.115600667400684642E-11, -33.50000000000000000 ) ) ;
#218591=ORIENTED_EDGE ( 'NONE', *, *, #36816, .F. ) ;
#218600=EDGE_CURVE ( 'NONE', #168958, #17700, #55630, .T. ) ;
#218613=ORIENTED_EDGE ( 'NONE', *, *, #135847, .T. ) ;
#218633=CIRCLE ( 'NONE', #168808, 0.1999999999999987899 ) ;
#218655=DIRECTION ( 'NONE',  ( 0.000000000000000000, 0.000000000000000000, -1.000000000000000000 ) ) ;
#218669=AXIS2_PLACEMENT_3D ( 'NONE', #65082, #190181, #207178 ) ;
#218674=FACE_OUTER_BOUND ( 'NONE', #233740, .T. ) ;
#218677=LINE ( 'NONE', #62198, #137105 ) ;
#218705=EDGE_CURVE ( 'NONE', #53755, #170769, #126873, .T. ) ;
#218706=CARTESIAN_POINT ( 'NONE',  ( 20.58091095332318332, 9.018470153363930208, -41.91865018215837324 ) ) ;
#218724=AXIS2_PLACEMENT_3D ( 'NONE', #244704, #23131, #145604 ) ;
#218731=CARTESIAN_POINT ( 'NONE',  ( -18.59999996769639097, -9.363273769819228320, -40.68149391546575089 ) ) ;
#218761=ORIENTED_EDGE ( 'NONE', *, *, #11241, .F. ) ;
#218769=EDGE_LOOP ( 'NONE', ( #193171, #185933, #152126 ) ) ;
#218771=DIRECTION ( 'NONE',  ( 0.000000000000000000, 1.000000000000000000, 0.000000000000000000 ) ) ;
#218799=VECTOR ( 'NONE', #68869, 1000.000000000000000 ) ;
#218882=EDGE_CURVE ( 'NONE', #146650, #60369, #218265, .T. ) ;
#218909=ORIENTED_EDGE ( 'NONE', *, *, #14973, .T. ) ;
#218928=CIRCLE ( 'NONE', #102193, 11.70000000000000284 ) ;
#218950=VECTOR ( 'NONE', #227006, 1000.000000000000000 ) ;
#218985=EDGE_LOOP ( 'NONE', ( #108726, #4284, #108226, #18439 ) ) ;
#219031=CIRCLE ( 'NONE', #2550, 6.258578643762703564 ) ;
#219034=CARTESIAN_POINT ( 'NONE',  ( -18.54270223418607344, -9.624105502871746154, -73.74093505040742969 ) ) ;
#219090=CYLINDRICAL_SURFACE ( 'NONE', #27297, 0.1000000000000028644 ) ;
#219093=DIRECTION ( 'NONE',  ( 1.000000000000000000, 0.000000000000000000, 0.000000000000000000 ) ) ;
#219097=DIRECTION ( 'NONE',  ( 0.000000000000000000, 0.000000000000000000, -1.000000000000000000 ) ) ;
#219110=AXIS2_PLACEMENT_3D ( 'NONE', #190364, #169543, #52096 ) ;
#219124=ORIENTED_EDGE ( 'NONE', *, *, #154416, .T. ) ;
#219135=VERTEX_POINT ( 'NONE', #6941 ) ;
#219144=EDGE_LOOP ( 'NONE', ( #212750, #56647, #182475, #246709 ) ) ;
#219161=DIRECTION ( 'NONE',  ( 0.000000000000000000, 0.000000000000000000, 1.000000000000000000 ) ) ;
#219204=DIRECTION ( 'NONE',  ( -3.469446951953635015E-14, 1.000000000000000000, 0.000000000000000000 ) ) ;
#219220=CIRCLE ( 'NONE', #211040, 0.1000000000000020595 ) ;
#219237=CARTESIAN_POINT ( 'NONE',  ( 21.05000000000000071, -11.64999999998883595, -36.39999999999999858 ) ) ;
#219240=CARTESIAN_POINT ( 'NONE',  ( 18.39999999999999858, -9.499999999988842703, -73.60018939122203108 ) ) ;
#219263=DIRECTION ( 'NONE',  ( 0.000000000000000000, 0.000000000000000000, -1.000000000000000000 ) ) ;
#219270=EDGE_CURVE ( 'NONE', #181952, #207975, #56116, .T. ) ;
#219316=CARTESIAN_POINT ( 'NONE',  ( 21.00000000000000000, 9.750000000011153745, -45.85000000000000142 ) ) ;
#219335=DIRECTION ( 'NONE',  ( 0.000000000000000000, -1.000000000000000000, -0.000000000000000000 ) ) ;
#219380=FACE_OUTER_BOUND ( 'NONE', #192217, .T. ) ;
#219382=AXIS2_PLACEMENT_3D ( 'NONE', #239149, #21410, #183038 ) ;
#219412=ORIENTED_EDGE ( 'NONE', *, *, #192042, .T. ) ;
#219440=DIRECTION ( 'NONE',  ( -6.938893903907222067E-15, 1.000000000000000000, 0.000000000000000000 ) ) ;
#219449=DIRECTION ( 'NONE',  ( 0.000000000000000000, 2.168404344971021884E-15, 1.000000000000000000 ) ) ;
#219483=VECTOR ( 'NONE', #175013, 1000.000000000000000 ) ;
#219489=LINE ( 'NONE', #89927, #37634 ) ;
#219501=EDGE_CURVE ( 'NONE', #19663, #131047, #160594, .T. ) ;
#219572=VECTOR ( 'NONE', #35374, 1000.000000000000000 ) ;
#219595=SURFACE_STYLE_FILL_AREA ( #1826 ) ;
#219628=DIRECTION ( 'NONE',  ( 1.000000000000000000, 0.000000000000000000, 0.000000000000000000 ) ) ;
#219643=CIRCLE ( 'NONE', #98812, 0.1000000000000028644 ) ;
#219644=CARTESIAN_POINT ( 'NONE',  ( 21.05000000000000071, -1.835341550213257733, -45.05515129256298223 ) ) ;
#219650=CIRCLE ( 'NONE', #124380, 0.1999999999999987899 ) ;
#219657=DIRECTION ( 'NONE',  ( 0.000000000000000000, 0.000000000000000000, 1.000000000000000000 ) ) ;
#219671=CARTESIAN_POINT ( 'NONE',  ( -21.05000000000000071, 1.115527483754042032E-11, -26.95934304829876282 ) ) ;
#219687=ORIENTED_EDGE ( 'NONE', *, *, #81930, .T. ) ;
#219707=CARTESIAN_POINT ( 'NONE',  ( 21.04999999999999716, 8.871279686006799281, -45.64999999999999858 ) ) ;
#219725=ORIENTED_EDGE ( 'NONE', *, *, #140112, .F. ) ;
#219727=DIRECTION ( 'NONE',  ( 0.000000000000000000, 0.1350103645451876666, 0.9908441862701600211 ) ) ;
#219769=DIRECTION ( 'NONE',  ( -1.000000000000000000, 0.000000000000000000, 0.000000000000000000 ) ) ;
#219773=EDGE_LOOP ( 'NONE', ( #69484, #224556, #79813, #130616, #191814 ) ) ;
#219788=CARTESIAN_POINT ( 'NONE',  ( -20.94983749550516450, 10.29766095125292402, -72.47436639332755703 ) ) ;
#219807=AXIS2_PLACEMENT_3D ( 'NONE', #195044, #73821, #152069 ) ;
#219818=CARTESIAN_POINT ( 'NONE',  ( 21.05000000000000071, 8.776282895303632259, -45.65000000000000568 ) ) ;
#219825=VECTOR ( 'NONE', #23768, 1000.000000000000114 ) ;
#219868=DIRECTION ( 'NONE',  ( 1.000000000000000000, 0.000000000000000000, -6.938893903907270030E-14 ) ) ;
#219889=AXIS2_PLACEMENT_3D ( 'NONE', #219927, #101215, #2148 ) ;
#219927=CARTESIAN_POINT ( 'NONE',  ( -18.59999999999999787, 7.021664781911246322, -70.83356540189728889 ) ) ;
#219951=DIRECTION ( 'NONE',  ( -0.000000000000000000, 0.1350103645451876666, 0.9908441862701600211 ) ) ;
#219994=FACE_OUTER_BOUND ( 'NONE', #111130, .T. ) ;
#220005=CARTESIAN_POINT ( 'NONE',  ( 20.19326291201655366, 10.15606098791449519, -41.26186180760268485 ) ) ;
#220012=DIRECTION ( 'NONE',  ( 0.000000000000000000, -0.9908441862701596881, 0.1350103645451904977 ) ) ;
#220038=CARTESIAN_POINT ( 'NONE',  ( -18.41799967126732795, -9.499999999988851584, -40.53206981325593006 ) ) ;
#220044=ORIENTED_EDGE ( 'NONE', *, *, #3216, .T. ) ;
#220061=ORIENTED_EDGE ( 'NONE', *, *, #24088, .T. ) ;
#220064=ORIENTED_EDGE ( 'NONE', *, *, #141732, .T. ) ;
#220065=CARTESIAN_POINT ( 'NONE',  ( 21.11825140030075332, 0.007203620643842375236, -27.05459243457999818 ) ) ;
#220077=EDGE_CURVE ( 'NONE', #36405, #109174, #88636, .T. ) ;
#220085=ORIENTED_EDGE ( 'NONE', *, *, #172724, .T. ) ;
#220112=ORIENTED_EDGE ( 'NONE', *, *, #33328, .F. ) ;
#220116=LINE ( 'NONE', #143118, #30864 ) ;
#220133=EDGE_LOOP ( 'NONE', ( #124443, #35729, #31946, #142209 ) ) ;
#220143=ORIENTED_EDGE ( 'NONE', *, *, #62629, .F. ) ;
#220149=DIRECTION ( 'NONE',  ( 0.000000000000000000, -1.000000000000000000, -1.387778780781442047E-14 ) ) ;
#220160=ORIENTED_EDGE ( 'NONE', *, *, #158241, .T. ) ;
#220181=CARTESIAN_POINT ( 'NONE',  ( 23.14999999999999858, 1.115600667400684642E-11, -33.50000000000000000 ) ) ;
#220191=EDGE_CURVE ( 'NONE', #14799, #38057, #102428, .T. ) ;
#220200=VECTOR ( 'NONE', #242424, 999.9999999999998863 ) ;
#220220=CARTESIAN_POINT ( 'NONE',  ( 18.39999999999999858, -9.519327731081283162, -40.47297637655933755 ) ) ;
#220257=ORIENTED_EDGE ( 'NONE', *, *, #182724, .T. ) ;
#220274=LINE ( 'NONE', #128871, #44796 ) ;
#220278=CARTESIAN_POINT ( 'NONE',  ( 20.95575313997065336, 10.61455330328599089, -41.12129070194482239 ) ) ;
#220290=CARTESIAN_POINT ( 'NONE',  ( 23.14999999999999858, 11.60000000001116227, -60.07179676972450011 ) ) ;
#220300=DIRECTION ( 'NONE',  ( 0.000000000000000000, -1.000000000000000000, -0.000000000000000000 ) ) ;
#220348=AXIS2_PLACEMENT_3D ( 'NONE', #198410, #60172, #82283 ) ;
#220377=EDGE_CURVE ( 'NONE', #195498, #81754, #73474, .T. ) ;
#220408=ORIENTED_EDGE ( 'NONE', *, *, #137085, .T. ) ;
#220431=ORIENTED_EDGE ( 'NONE', *, *, #171032, .F. ) ;
#220458=EDGE_CURVE ( 'NONE', #201739, #158454, #189962, .T. ) ;
#220500=DIRECTION ( 'NONE',  ( -0.000000000000000000, -1.265107689135680095E-16, 1.000000000000000000 ) ) ;
#220512=ORIENTED_EDGE ( 'NONE', *, *, #111450, .F. ) ;
#220525=DIRECTION ( 'NONE',  ( 0.000000000000000000, 0.8700118002898322711, -0.4930308989875231140 ) ) ;
#220528=DIRECTION ( 'NONE',  ( -0.000000000000000000, -0.000000000000000000, 1.000000000000000000 ) ) ;
#220529=EDGE_CURVE ( 'NONE', #100799, #254615, #131707, .T. ) ;
#220539=ORIENTED_EDGE ( 'NONE', *, *, #132995, .F. ) ;
#220554=DIRECTION ( 'NONE',  ( 1.000000000000000000, 0.000000000000000000, 0.000000000000000000 ) ) ;
#220558=DIRECTION ( 'NONE',  ( -1.000000000000000000, 0.000000000000000000, 0.000000000000000000 ) ) ;
#220559=CARTESIAN_POINT ( 'NONE',  ( 20.95512820512820440, 10.62384868372303615, -45.65000000000000568 ) ) ;
#220560=ADVANCED_FACE ( 'NONE', ( #75675 ), #194350, .T. ) ;
#220570=AXIS2_PLACEMENT_3D ( 'NONE', #174114, #194933, #253587 ) ;
#220572=AXIS2_PLACEMENT_3D ( 'NONE', #237250, #191734, #114736 ) ;
#220579=ORIENTED_EDGE ( 'NONE', *, *, #87750, .F. ) ;
#220602=FACE_OUTER_BOUND ( 'NONE', #211008, .T. ) ;
#220628=DIRECTION ( 'NONE',  ( 3.616040088954497272E-32, -1.224646799147352961E-16, 1.000000000000000000 ) ) ;
#220650=CIRCLE ( 'NONE', #158150, 0.1000000000000028644 ) ;
#220670=ORIENTED_EDGE ( 'NONE', *, *, #235489, .T. ) ;
#220720=CARTESIAN_POINT ( 'NONE',  ( -18.59999999999999787, -1.164121893230052995, -74.91484808557160591 ) ) ;
#220734=EDGE_CURVE ( 'NONE', #239491, #109070, #190163, .T. ) ;
#220756=DIRECTION ( 'NONE',  ( 1.000000000000000000, -0.000000000000000000, -0.000000000000000000 ) ) ;
#220757=ORIENTED_EDGE ( 'NONE', *, *, #140100, .F. ) ;
#220842=CIRCLE ( 'NONE', #241700, 12.77500000000000036 ) ;
#220844=CARTESIAN_POINT ( 'NONE',  ( 20.94999999999999929, 5.000000000011153745, -54.99473398108690958 ) ) ;
#220878=CARTESIAN_POINT ( 'NONE',  ( -18.50000000000000000, -1.164121893230052995, -74.91484808557160591 ) ) ;
#220881=SURFACE_SIDE_STYLE ('',( #219595 ) ) ;
#220915=EDGE_CURVE ( 'NONE', #168958, #165708, #152352, .T. ) ;
#220933=DIRECTION ( 'NONE',  ( 1.000000000000000000, -7.304098846218133681E-16, 4.607487905232622991E-31 ) ) ;
#220966=DIRECTION ( 'NONE',  ( 0.000000000000000000, 0.000000000000000000, -1.000000000000000000 ) ) ;
#220994=FACE_OUTER_BOUND ( 'NONE', #246846, .T. ) ;
#221005=ORIENTED_EDGE ( 'NONE', *, *, #121148, .T. ) ;
#221038=DIRECTION ( 'NONE',  ( -1.000000000000000000, -2.952720810173289112E-16, 0.000000000000000000 ) ) ;
#221040=DIRECTION ( 'NONE',  ( 0.000000000000000000, -0.8068669527896844551, -0.5907332058517525963 ) ) ;
#221086=AXIS2_PLACEMENT_3D ( 'NONE', #244424, #223561, #241853 ) ;
#221096=ORIENTED_EDGE ( 'NONE', *, *, #240229, .F. ) ;
#221101=LINE ( 'NONE', #239402, #244977 ) ;
#221194=EDGE_LOOP ( 'NONE', ( #72521, #117414, #148333, #191243 ) ) ;
#221216=DIRECTION ( 'NONE',  ( 0.000000000000000000, -0.000000000000000000, -1.000000000000000000 ) ) ;
#221269=AXIS2_PLACEMENT_3D ( 'NONE', #76277, #16339, #95830 ) ;
#221274=AXIS2_PLACEMENT_3D ( 'NONE', #130896, #12263, #34398 ) ;
#221295=DIRECTION ( 'NONE',  ( 1.000000000000000000, 0.000000000000000000, 0.000000000000000000 ) ) ;
#221306=CARTESIAN_POINT ( 'NONE',  ( 18.59999999999999076, 6.400000000011158541, -43.43042463006157305 ) ) ;
#221308=CARTESIAN_POINT ( 'NONE',  ( 22.39999999999999503, 0.1000000000111554016, -25.70922040162662014 ) ) ;
#221313=CIRCLE ( 'NONE', #129750, 0.1000000000000000472 ) ;
#221346=CARTESIAN_POINT ( 'NONE',  ( -21.05000000000000071, 1.750000000011155743, -45.16951155790164307 ) ) ;
#221357=EDGE_CURVE ( 'NONE', #203889, #162457, #97124, .T. ) ;
#221358=CIRCLE ( 'NONE', #204804, 12.87500000000000000 ) ;
#221367=DIRECTION ( 'NONE',  ( -1.000000000000000000, -0.000000000000000000, -0.000000000000000000 ) ) ;
#221371=ORIENTED_EDGE ( 'NONE', *, *, #56023, .F. ) ;
#221384=ORIENTED_EDGE ( 'NONE', *, *, #154477, .F. ) ;
#221422=DIRECTION ( 'NONE',  ( 0.000000000000000000, -0.8660254037844459241, -0.4999999999999873990 ) ) ;
#221471=ORIENTED_EDGE ( 'NONE', *, *, #155063, .F. ) ;
#221479=( BOUNDED_CURVE ( )  B_SPLINE_CURVE ( 3, ( #70048, #50431, #110427, #189975 ),
 .UNSPECIFIED., .F., .F. ) 
 B_SPLINE_CURVE_WITH_KNOTS ( ( 4, 4 ),
 ( 3.141592653589793116, 4.712388980384689674 ),
 .UNSPECIFIED. ) 
 CURVE ( )  GEOMETRIC_REPRESENTATION_ITEM ( )  RATIONAL_B_SPLINE_CURVE ( ( 1.000000000000000000, 0.8047378541243649375, 0.8047378541243649375, 1.000000000000000000 ) ) 
 REPRESENTATION_ITEM ( '' )  );
#221517=DIRECTION ( 'NONE',  ( 0.000000000000000000, 0.000000000000000000, 1.000000000000000000 ) ) ;
#221539=VERTEX_POINT ( 'NONE', #200130 ) ;
#221562=DIRECTION ( 'NONE',  ( 1.000000000000000000, 0.000000000000000000, -0.000000000000000000 ) ) ;
#221566=CARTESIAN_POINT ( 'NONE',  ( -20.54999999999999716, 7.150000000011155876, -54.65000000000000568 ) ) ;
#221638=DIRECTION ( 'NONE',  ( -1.000000000000000000, 0.000000000000000000, 0.000000000000000000 ) ) ;
#221826=VECTOR ( 'NONE', #193427, 1000.000000000000000 ) ;
#221831=EDGE_CURVE ( 'NONE', #254615, #45873, #244842, .T. ) ;
#221843=ORIENTED_EDGE ( 'NONE', *, *, #237002, .T. ) ;
#221846=EDGE_LOOP ( 'NONE', ( #2722, #207201, #229109, #239527 ) ) ;
#221864=FACE_OUTER_BOUND ( 'NONE', #10732, .T. ) ;
#221907=AXIS2_PLACEMENT_3D ( 'NONE', #81836, #161438, #126119 ) ;
#221925=CARTESIAN_POINT ( 'NONE',  ( 21.05000000000000071, 11.65000000001116298, -33.50000000000000000 ) ) ;
#221927=ORIENTED_EDGE ( 'NONE', *, *, #163374, .F. ) ;
#221947=CARTESIAN_POINT ( 'NONE',  ( 20.94788355080264353, 10.30207779525983014, -72.48955207167824710 ) ) ;
#221963=AXIS2_PLACEMENT_3D ( 'NONE', #97735, #135596, #92617 ) ;
#221989=TOROIDAL_SURFACE ( 'NONE', #80518, 12.77500000000000036, 0.1000000000000000056 ) ;
#221992=TOROIDAL_SURFACE ( 'NONE', #146989, 11.89999999999999858, 0.1000000000000000056 ) ;
#222001=EDGE_CURVE ( 'NONE', #61108, #27454, #190913, .T. ) ;
#222003=ORIENTED_EDGE ( 'NONE', *, *, #104922, .T. ) ;
#222006=ORIENTED_EDGE ( 'NONE', *, *, #218705, .F. ) ;
#222025=DIRECTION ( 'NONE',  ( 1.000000000000000000, 0.000000000000000000, 0.000000000000000000 ) ) ;
#222038=DIRECTION ( 'NONE',  ( 0.000000000000000000, 0.8700118002898321601, -0.4930308989875230030 ) ) ;
#222049=ORIENTED_EDGE ( 'NONE', *, *, #213121, .F. ) ;
#222053=CARTESIAN_POINT ( 'NONE',  ( -20.64999999999999858, -9.399999999988850163, -43.39396912265245021 ) ) ;
#222056=DIRECTION ( 'NONE',  ( 1.000000000000000000, 2.952720810173289112E-16, -0.000000000000000000 ) ) ;
#222072=EDGE_CURVE ( 'NONE', #227982, #227593, #203539, .T. ) ;
#222086=DIRECTION ( 'NONE',  ( 0.000000000000000000, -1.000000000000000000, 0.000000000000000000 ) ) ;
#222104=AXIS2_PLACEMENT_3D ( 'NONE', #102219, #243051, #141380 ) ;
#222156=VECTOR ( 'NONE', #194781, 999.9999999999998863 ) ;
#222157=ADVANCED_FACE ( 'NONE', ( #252723 ), #130208, .T. ) ;
#222196=AXIS2_PLACEMENT_3D ( 'NONE', #254075, #33802, #135407 ) ;
#222223=EDGE_LOOP ( 'NONE', ( #122779, #42993, #88977, #27881 ) ) ;
#222267=CARTESIAN_POINT ( 'NONE',  ( 20.94999999999999929, -8.730841121484166578, -57.40192528101566438 ) ) ;
#222281=AXIS2_PLACEMENT_3D ( 'NONE', #3818, #42949, #65071 ) ;
#222289=CARTESIAN_POINT ( 'NONE',  ( 20.94999999999999929, 5.500000000011153745, -54.59473398108690390 ) ) ;
#222293=ORIENTED_EDGE ( 'NONE', *, *, #182313, .T. ) ;
#222368=DIRECTION ( 'NONE',  ( 0.000000000000000000, 0.000000000000000000, 1.000000000000000000 ) ) ;
#222374=DIRECTION ( 'NONE',  ( 1.000000000000000000, 0.000000000000000000, 0.000000000000000000 ) ) ;
#222378=EDGE_CURVE ( 'NONE', #64314, #26511, #195182, .T. ) ;
#222401=CYLINDRICAL_SURFACE ( 'NONE', #118028, 0.1000000000000028644 ) ;
#222420=CARTESIAN_POINT ( 'NONE',  ( 23.14999999999999858, 1.115600667400684642E-11, -67.00000000000000000 ) ) ;
#222449=CARTESIAN_POINT ( 'NONE',  ( 18.59999999999999076, -1.851617760457748618, -78.60318971960367662 ) ) ;
#222460=EDGE_CURVE ( 'NONE', #118577, #24660, #166157, .T. ) ;
#222462=CARTESIAN_POINT ( 'NONE',  ( -20.54999999999999716, 2.500000000011154633, -53.77537807723790309 ) ) ;
#222469=EDGE_CURVE ( 'NONE', #132417, #28509, #74008, .T. ) ;
#222475=ORIENTED_EDGE ( 'NONE', *, *, #134535, .F. ) ;
#222494=DIRECTION ( 'NONE',  ( 1.000000000000000000, -0.000000000000000000, -0.000000000000000000 ) ) ;
#222504=DIRECTION ( 'NONE',  ( -0.000000000000000000, -0.000000000000000000, -1.000000000000000000 ) ) ;
#222530=EDGE_CURVE ( 'NONE', #256921, #5569, #211352, .T. ) ;
#222564=VERTEX_POINT ( 'NONE', #150765 ) ;
#222572=CARTESIAN_POINT ( 'NONE',  ( 20.85000000000000142, -1.835859311432481045, -78.50443916879852679 ) ) ;
#222600=CARTESIAN_POINT ( 'NONE',  ( 21.04999999999999716, 0.05148288189283987265, -27.19982018208539998 ) ) ;
#222605=FACE_OUTER_BOUND ( 'NONE', #233761, .T. ) ;
#222624=DIRECTION ( 'NONE',  ( -1.000000000000000000, -1.836970198721029934E-16, -3.186635328391151676E-31 ) ) ;
#222644=EDGE_CURVE ( 'NONE', #130981, #121226, #199462, .T. ) ;
#222736=CARTESIAN_POINT ( 'NONE',  ( 21.08804281139605408, 10.62183430185232069, -45.84999996737845862 ) ) ;
#222737=AXIS2_PLACEMENT_3D ( 'NONE', #238792, #139656, #197075 ) ;
#222739=CIRCLE ( 'NONE', #26970, 0.1000000000000029476 ) ;
#222770=FACE_OUTER_BOUND ( 'NONE', #43450, .T. ) ;
#222782=VECTOR ( 'NONE', #73548, 1000.000000000000000 ) ;
#222784=ORIENTED_EDGE ( 'NONE', *, *, #75517, .T. ) ;
#222793=LINE ( 'NONE', #208407, #240360 ) ;
#222864=DIRECTION ( 'NONE',  ( 0.000000000000000000, 0.000000000000000000, 1.000000000000000000 ) ) ;
#222872=LINE ( 'NONE', #23432, #160913 ) ;
#222879=CARTESIAN_POINT ( 'NONE',  ( -18.59999999999999787, -1.866714910046153308, -45.25267524628200988 ) ) ;
#222921=DIRECTION ( 'NONE',  ( 0.7070776581708965169, 0.000000000000000000, 0.7071359030027827286 ) ) ;
#222930=DIRECTION ( 'NONE',  ( 0.000000000000000000, 0.01562500000001045344, 0.9998779222360096863 ) ) ;
#222941=DIRECTION ( 'NONE',  ( -0.000000000000000000, 0.000000000000000000, 1.000000000000000000 ) ) ;
#222942=CARTESIAN_POINT ( 'NONE',  ( -21.14250536705909411, 1.115600667400684642E-11, -26.98182782311924655 ) ) ;
#222947=CARTESIAN_POINT ( 'NONE',  ( -21.05000000000000071, 1.835341550235567887, -45.15515129256298366 ) ) ;
#222956=DIRECTION ( 'NONE',  ( -0.000000000000000000, 0.000000000000000000, 1.000000000000000000 ) ) ;
#222980=CARTESIAN_POINT ( 'NONE',  ( 22.00411653962166625, 7.253442868381227093, -33.40096189421769424 ) ) ;
#222989=ORIENTED_EDGE ( 'NONE', *, *, #15416, .T. ) ;
#223056=ORIENTED_EDGE ( 'NONE', *, *, #153555, .F. ) ;
#223057=ORIENTED_EDGE ( 'NONE', *, *, #172724, .F. ) ;
#223067=CYLINDRICAL_SURFACE ( 'NONE', #98648, 0.5000000000000004441 ) ;
#223122=AXIS2_PLACEMENT_3D ( 'NONE', #48757, #86578, #147881 ) ;
#223137=EDGE_LOOP ( 'NONE', ( #34050, #115703, #62693, #198140 ) ) ;
#223139=LINE ( 'NONE', #182757, #100798 ) ;
#223187=VERTEX_POINT ( 'NONE', #233433 ) ;
#223238=EDGE_CURVE ( 'NONE', #104039, #180952, #213844, .T. ) ;
#223242=CIRCLE ( 'NONE', #110827, 0.1000000000000028644 ) ;
#223249=DIRECTION ( 'NONE',  ( 0.000000000000000000, 0.000000000000000000, -1.000000000000000000 ) ) ;
#223250=CARTESIAN_POINT ( 'NONE',  ( 20.94999999999999929, 10.29288807859936838, -72.45800201601217339 ) ) ;
#223271=AXIS2_PLACEMENT_3D ( 'NONE', #193359, #152971, #212909 ) ;
#223279=ORIENTED_EDGE ( 'NONE', *, *, #208004, .F. ) ;
#223303=EDGE_LOOP ( 'NONE', ( #91211, #64523, #215823, #188726 ) ) ;
#223336=DIRECTION ( 'NONE',  ( -1.000000000000000000, -0.000000000000000000, 0.000000000000000000 ) ) ;
#223343=ADVANCED_FACE ( 'NONE', ( #136870 ), #128501, .T. ) ;
#223348=ORIENTED_EDGE ( 'NONE', *, *, #253647, .F. ) ;
#223379=ORIENTED_EDGE ( 'NONE', *, *, #220191, .F. ) ;
#223380=DIRECTION ( 'NONE',  ( 0.7071067811865475727, 0.7071067811865475727, 2.044391222244500083E-16 ) ) ;
#223468=AXIS2_PLACEMENT_3D ( 'NONE', #216996, #78765, #138716 ) ;
#223472=DIRECTION ( 'NONE',  ( 1.000000000000000000, 0.000000000000000000, -0.000000000000000000 ) ) ;
#223476=CARTESIAN_POINT ( 'NONE',  ( -21.15000000000000213, 6.540656951712399803, -33.50000000000000000 ) ) ;
#223488=DIRECTION ( 'NONE',  ( 0.000000000000000000, 0.000000000000000000, -1.000000000000000000 ) ) ;
#223535=CARTESIAN_POINT ( 'NONE',  ( -20.00857864376270001, 9.250000000011157297, -45.85000000000000142 ) ) ;
#223561=DIRECTION ( 'NONE',  ( 1.000000000000000000, -0.000000000000000000, -0.000000000000000000 ) ) ;
#223567=ORIENTED_EDGE ( 'NONE', *, *, #55832, .F. ) ;
#223581=CIRCLE ( 'NONE', #77850, 11.75000000000000000 ) ;
#223595=CARTESIAN_POINT ( 'NONE',  ( -20.85000000000000142, -1.164121893230052995, -74.91484808557160591 ) ) ;
#223617=B_SPLINE_CURVE_WITH_KNOTS ( 'NONE', 3,
 ( #26358, #68041, #203706, #5470 ),
 .UNSPECIFIED., .F., .F.,
 ( 4, 4 ),
 ( 0.000000000000000000, 0.001767853679387130974 ),
 .UNSPECIFIED. ) ;
#223621=CARTESIAN_POINT ( 'NONE',  ( -23.15000000000000213, 1.925233644870967487, -54.26975646687386501 ) ) ;
#223682=AXIS2_PLACEMENT_3D ( 'NONE', #254766, #59144, #40938 ) ;
#223725=CARTESIAN_POINT ( 'NONE',  ( 20.94999999999999574, 1.835341550235567887, -45.05515129256298223 ) ) ;
#223742=CARTESIAN_POINT ( 'NONE',  ( -20.54999999999999716, 9.350000000011156942, -54.65000000000000568 ) ) ;
#223825=DIRECTION ( 'NONE',  ( -3.469446951953660258E-14, 0.5000000000000209832, 0.8660254037844264952 ) ) ;
#223836=( BOUNDED_CURVE ( )  B_SPLINE_CURVE ( 3, ( #189599, #33127, #232594, #73522 ),
 .UNSPECIFIED., .F., .F. ) 
 B_SPLINE_CURVE_WITH_KNOTS ( ( 4, 4 ),
 ( 3.141592653589793116, 4.712388980384689674 ),
 .UNSPECIFIED. ) 
 CURVE ( )  GEOMETRIC_REPRESENTATION_ITEM ( )  RATIONAL_B_SPLINE_CURVE ( ( 1.000000000000000000, 0.8047378541243649375, 0.8047378541243649375, 1.000000000000000000 ) ) 
 REPRESENTATION_ITEM ( '' )  );
#223865=DIRECTION ( 'NONE',  ( -0.000000000000000000, -1.000000000000000000, 0.000000000000000000 ) ) ;
#223872=ORIENTED_EDGE ( 'NONE', *, *, #193578, .T. ) ;
#223897=DIRECTION ( 'NONE',  ( 1.000000000000000000, 0.000000000000000000, 0.000000000000000000 ) ) ;
#223912=CARTESIAN_POINT ( 'NONE',  ( -23.25000000000000000, 1.115600667400684642E-11, -74.90000000000000568 ) ) ;
#223916=ORIENTED_EDGE ( 'NONE', *, *, #120066, .T. ) ;
#223923=EDGE_CURVE ( 'NONE', #134939, #182341, #141167, .T. ) ;
#223980=EDGE_CURVE ( 'NONE', #75871, #126699, #105922, .T. ) ;
#223996=VECTOR ( 'NONE', #15074, 1000.000000000000000 ) ;
#224013=DIRECTION ( 'NONE',  ( 0.000000000000000000, 0.000000000000000000, -1.000000000000000000 ) ) ;
#224014=ORIENTED_EDGE ( 'NONE', *, *, #165745, .F. ) ;
#224024=CARTESIAN_POINT ( 'NONE',  ( 21.04116576186320131, 10.62466307876251115, -45.82858176862794863 ) ) ;
#224030=CYLINDRICAL_SURFACE ( 'NONE', #9551, 0.5000000000000004441 ) ;
#224038=FACE_OUTER_BOUND ( 'NONE', #149331, .T. ) ;
#224052=DIRECTION ( 'NONE',  ( 1.000000000000000000, -0.000000000000000000, -0.000000000000000000 ) ) ;
#224062=ORIENTED_EDGE ( 'NONE', *, *, #137577, .F. ) ;
#224090=ADVANCED_FACE ( 'NONE', ( #14582 ), #176215, .T. ) ;
#224099=ORIENTED_EDGE ( 'NONE', *, *, #24165, .T. ) ;
#224149=FACE_OUTER_BOUND ( 'NONE', #224175, .T. ) ;
#224173=CARTESIAN_POINT ( 'NONE',  ( -18.59999999999999787, -9.523954320741633950, -73.88201705682730847 ) ) ;
#224175=EDGE_LOOP ( 'NONE', ( #135719, #126782, #168236, #154705 ) ) ;
#224190=ORIENTED_EDGE ( 'NONE', *, *, #72040, .T. ) ;
#224193=ORIENTED_EDGE ( 'NONE', *, *, #69453, .F. ) ;
#224198=CARTESIAN_POINT ( 'NONE',  ( 21.00000000000000000, 9.750000000011153745, -45.85000000000000142 ) ) ;
#224234=LINE ( 'NONE', #222947, #206328 ) ;
#224244=ORIENTED_EDGE ( 'NONE', *, *, #170019, .F. ) ;
#224272=AXIS2_PLACEMENT_3D ( 'NONE', #196363, #215911, #78957 ) ;
#224294=DIRECTION ( 'NONE',  ( 0.000000000000000000, 0.000000000000000000, -1.000000000000000000 ) ) ;
#224296=ADVANCED_FACE ( 'NONE', ( #178805 ), #159222, .T. ) ;
#224311=ORIENTED_EDGE ( 'NONE', *, *, #250258, .T. ) ;
#224321=ORIENTED_EDGE ( 'NONE', *, *, #206211, .F. ) ;
#224339=LINE ( 'NONE', #204765, #186922 ) ;
#224348=ORIENTED_EDGE ( 'NONE', *, *, #82167, .T. ) ;
#224351=ORIENTED_EDGE ( 'NONE', *, *, #203394, .F. ) ;
#224401=VECTOR ( 'NONE', #124395, 1000.000000000000000 ) ;
#224457=DIRECTION ( 'NONE',  ( -0.000000000000000000, 0.000000000000000000, 1.000000000000000000 ) ) ;
#224459=CARTESIAN_POINT ( 'NONE',  ( -20.54999999999999716, -8.999999999988844479, -57.10603087734755690 ) ) ;
#224490=VERTEX_POINT ( 'NONE', #211166 ) ;
#224512=CARTESIAN_POINT ( 'NONE',  ( 18.49999999999999289, 10.29270135741298731, -72.45736188715193293 ) ) ;
#224523=AXIS2_PLACEMENT_3D ( 'NONE', #238269, #157503, #76635 ) ;
#224536=LINE ( 'NONE', #125453, #249298 ) ;
#224548=ORIENTED_EDGE ( 'NONE', *, *, #100641, .F. ) ;
#224556=ORIENTED_EDGE ( 'NONE', *, *, #163805, .T. ) ;
#224583=VERTEX_POINT ( 'NONE', #250291 ) ;
#224599=VERTEX_POINT ( 'NONE', #21964 ) ;
#224636=ORIENTED_EDGE ( 'NONE', *, *, #103472, .F. ) ;
#224691=EDGE_CURVE ( 'NONE', #199100, #82771, #117203, .T. ) ;
#224718=ADVANCED_FACE ( 'NONE', ( #138024 ), #83229, .T. ) ;
#224731=FILL_AREA_STYLE_COLOUR ( '', #224831 ) ;
#224734=AXIS2_PLACEMENT_3D ( 'NONE', #81163, #202414, #75112 ) ;
#224739=EDGE_CURVE ( 'NONE', #81995, #67087, #37488, .T. ) ;
#224745=CARTESIAN_POINT ( 'NONE',  ( 23.14999999999999503, 14.10000000001115694, -61.39970238886063925 ) ) ;
#224754=DIRECTION ( 'NONE',  ( 0.000000000000000000, 0.000000000000000000, -1.000000000000000000 ) ) ;
#224760=CARTESIAN_POINT ( 'NONE',  ( 23.15000000000000213, -8.999999999988844479, -43.39396912265245021 ) ) ;
#224806=CARTESIAN_POINT ( 'NONE',  ( -20.54999999999999716, 7.150000000011155876, -45.85000000000000142 ) ) ;
#224813=CARTESIAN_POINT ( 'NONE',  ( 20.97438252431638972, 8.925423506087151182, -41.97237068901081614 ) ) ;
#224820=DIRECTION ( 'NONE',  ( 0.000000000000000000, 0.000000000000000000, -1.000000000000000000 ) ) ;
#224831=COLOUR_RGB ( '', 0.31764706, 0.68627451, 0.89019608) ;
#224833=EDGE_CURVE ( 'NONE', #244974, #153506, #45848, .T. ) ;
#224895=EDGE_CURVE ( 'NONE', #86684, #127278, #192004, .T. ) ;
#224931=VECTOR ( 'NONE', #235567, 1000.000000000000000 ) ;
#224951=LINE ( 'NONE', #247086, #130160 ) ;
#224959=DIRECTION ( 'NONE',  ( 1.000000000000000000, -0.000000000000000000, -0.000000000000000000 ) ) ;
#224997=CARTESIAN_POINT ( 'NONE',  ( 18.43565242384934066, -9.519327731081281385, -40.47297637655933755 ) ) ;
#225007=EDGE_LOOP ( 'NONE', ( #94025, #50398, #167277 ) ) ;
#225052=CARTESIAN_POINT ( 'NONE',  ( 21.05000000000000071, 8.815452279208702890, -41.92039255261426689 ) ) ;
#225055=DIRECTION ( 'NONE',  ( 0.000000000000000000, 0.000000000000000000, -1.000000000000000000 ) ) ;
#225058=ORIENTED_EDGE ( 'NONE', *, *, #59055, .T. ) ;
#225065=ORIENTED_EDGE ( 'NONE', *, *, #158787, .F. ) ;
#225103=AXIS2_PLACEMENT_3D ( 'NONE', #76991, #174869, #78267 ) ;
#225118=ADVANCED_FACE ( 'NONE', ( #185530 ), #245512, .T. ) ;
#225120=CARTESIAN_POINT ( 'NONE',  ( -23.25000000000000000, 7.021664781911246322, -70.83356540189728889 ) ) ;
#225137=FACE_OUTER_BOUND ( 'NONE', #189055, .T. ) ;
#225146=ORIENTED_EDGE ( 'NONE', *, *, #62932, .T. ) ;
#225157=CIRCLE ( 'NONE', #246039, 0.1000000000000008937 ) ;
#225174=DIRECTION ( 'NONE',  ( 0.000000000000000000, 0.000000000000000000, -1.000000000000000000 ) ) ;
#225188=ORIENTED_EDGE ( 'NONE', *, *, #171140, .T. ) ;
#225191=LINE ( 'NONE', #109105, #115997 ) ;
#225220=EDGE_CURVE ( 'NONE', #180952, #116556, #54398, .T. ) ;
#225249=DIRECTION ( 'NONE',  ( 1.000000000000000000, 0.000000000000000000, 0.000000000000000000 ) ) ;
#225256=ORIENTED_EDGE ( 'NONE', *, *, #175466, .F. ) ;
#225294=CARTESIAN_POINT ( 'NONE',  ( 21.07928932188134397, 0.09889514566555242248, -27.17148334360669537 ) ) ;
#225298=AXIS2_PLACEMENT_3D ( 'NONE', #17572, #119272, #219628 ) ;
#225300=ORIENTED_EDGE ( 'NONE', *, *, #144550, .F. ) ;
#225302=CARTESIAN_POINT ( 'NONE',  ( 23.25000000000000000, -11.48912529306489994, -63.89999999999999858 ) ) ;
#225330=DIRECTION ( 'NONE',  ( 1.000000000000000000, 0.000000000000000000, 0.000000000000000000 ) ) ;
#225346=DIRECTION ( 'NONE',  ( 1.000000000000000000, -0.000000000000000000, -0.000000000000000000 ) ) ;
#225394=VERTEX_POINT ( 'NONE', #80969 ) ;
#225414=DIRECTION ( 'NONE',  ( 0.000000000000000000, 1.734723475976757554E-14, -1.000000000000000000 ) ) ;
#225425=ORIENTED_EDGE ( 'NONE', *, *, #226399, .T. ) ;
#225442=EDGE_CURVE ( 'NONE', #40042, #181952, #17009, .T. ) ;
#225443=AXIS2_PLACEMENT_3D ( 'NONE', #168917, #187172, #248409 ) ;
#225474=CYLINDRICAL_SURFACE ( 'NONE', #140074, 0.1000000000000028644 ) ;
#225480=DIRECTION ( 'NONE',  ( 1.000000000000000000, 0.000000000000000000, 0.000000000000000000 ) ) ;
#225522=EDGE_LOOP ( 'NONE', ( #93201, #74425, #223348, #76035 ) ) ;
#225532=EDGE_CURVE ( 'NONE', #207975, #241304, #137769, .T. ) ;
#225556=DIRECTION ( 'NONE',  ( 1.000000000000000000, 0.000000000000000000, 0.000000000000000000 ) ) ;
#225577=DIRECTION ( 'NONE',  ( 0.000000000000000000, 1.224646799142015331E-16, 1.000000000000000000 ) ) ;
#225585=DIRECTION ( 'NONE',  ( 0.000000000000000000, 1.000000000000000000, 1.626303258728238113E-15 ) ) ;
#225614=CARTESIAN_POINT ( 'NONE',  ( 23.15000000000000213, -11.64999999998883595, -63.89999999999999858 ) ) ;
#225626=ORIENTED_EDGE ( 'NONE', *, *, #27449, .F. ) ;
#225629=DIRECTION ( 'NONE',  ( -3.265361837132813586E-16, 1.000000000000000000, 0.000000000000000000 ) ) ;
#225633=ORIENTED_EDGE ( 'NONE', *, *, #161599, .F. ) ;
#225650=DIRECTION ( 'NONE',  ( 0.000000000000000000, 1.000000000000000000, 0.000000000000000000 ) ) ;
#225671=EDGE_CURVE ( 'NONE', #28056, #172722, #213452, .T. ) ;
#225700=VECTOR ( 'NONE', #90240, 999.9999999999998863 ) ;
#225712=AXIS2_PLACEMENT_3D ( 'NONE', #24614, #207078, #23331 ) ;
#225772=ORIENTED_EDGE ( 'NONE', *, *, #213079, .T. ) ;
#225798=DIRECTION ( 'NONE',  ( 0.000000000000000000, -0.3738317757009718689, 0.9274965247785342815 ) ) ;
#225801=DIRECTION ( 'NONE',  ( 1.000000000000000000, -0.000000000000000000, -0.000000000000000000 ) ) ;
#225803=CARTESIAN_POINT ( 'NONE',  ( 20.93302460841142931, 10.31565961587945424, -72.53641941191781939 ) ) ;
#225825=VERTEX_POINT ( 'NONE', #143209 ) ;
#225830=AXIS2_PLACEMENT_3D ( 'NONE', #139539, #178721, #40496 ) ;
#225832=DIRECTION ( 'NONE',  ( -0.000000000000000000, 0.8660254037844383745, -0.5000000000000003331 ) ) ;
#225834=VERTEX_POINT ( 'NONE', #23307 ) ;
#225838=CARTESIAN_POINT ( 'NONE',  ( -18.44204374631831200, -9.491036389587213407, -73.62620127022113081 ) ) ;
#225862=VECTOR ( 'NONE', #250922, 1000.000000000000000 ) ;
#225878=ORIENTED_EDGE ( 'NONE', *, *, #88227, .F. ) ;
#225884=ORIENTED_EDGE ( 'NONE', *, *, #227484, .T. ) ;
#225889=CIRCLE ( 'NONE', #171795, 7.800000000000001599 ) ;
#225961=VERTEX_POINT ( 'NONE', #126218 ) ;
#225983=CARTESIAN_POINT ( 'NONE',  ( 21.00000000000000000, 9.750000000011153745, -45.85000000000000142 ) ) ;
#226003=DIRECTION ( 'NONE',  ( 0.000000000000000000, 0.000000000000000000, -1.000000000000000000 ) ) ;
#226007=EDGE_LOOP ( 'NONE', ( #243087, #80340, #100233, #185494 ) ) ;
#226022=VERTEX_POINT ( 'NONE', #225302 ) ;
#226028=CARTESIAN_POINT ( 'NONE',  ( -23.15000000000000213, -11.48912529306489994, -63.89999999999999858 ) ) ;
#226033=CARTESIAN_POINT ( 'NONE',  ( -18.59999999999999787, -9.321008403350132809, -40.73593824907788274 ) ) ;
#226044=ADVANCED_FACE ( 'NONE', ( #127517 ), #224030, .F. ) ;
#226072=DIRECTION ( 'NONE',  ( 0.000000000000000000, -0.6728971962616697722, -0.7397360091702875895 ) ) ;
#226080=CARTESIAN_POINT ( 'NONE',  ( 20.30531438145591139, 10.09690106110208596, -41.29601780727334415 ) ) ;
#226097=CIRCLE ( 'NONE', #138598, 0.1000000000000028644 ) ;
#226100=EDGE_CURVE ( 'NONE', #86723, #146761, #134441, .T. ) ;
#226137=CARTESIAN_POINT ( 'NONE',  ( 22.50497660315937054, -0.07871793021434789206, -21.75020449510456189 ) ) ;
#226143=CARTESIAN_POINT ( 'NONE',  ( -21.05000000000000071, 5.850000000011156942, -56.86750277572208034 ) ) ;
#226185=ORIENTED_EDGE ( 'NONE', *, *, #131507, .F. ) ;
#226190=CIRCLE ( 'NONE', #13850, 0.1000000000000000472 ) ;
#226214=DIRECTION ( 'NONE',  ( 1.000000000000000000, 1.836970198721029934E-16, 3.186635328391151676E-31 ) ) ;
#226239=PLANE ( 'NONE',  #192228 ) ;
#226240=EDGE_LOOP ( 'NONE', ( #166330, #244187, #16832, #171179 ) ) ;
#226284=ADVANCED_FACE ( 'NONE', ( #68523 ), #103757, .T. ) ;
#226292=AXIS2_PLACEMENT_3D ( 'NONE', #169177, #248685, #249968 ) ;
#226315=DIRECTION ( 'NONE',  ( 0.000000000000000000, 1.776356839400277286E-15, -1.000000000000000000 ) ) ;
#226327=ADVANCED_FACE ( 'NONE', ( #45100 ), #185889, .F. ) ;
#226399=EDGE_CURVE ( 'NONE', #80932, #215192, #142887, .T. ) ;
#226447=VERTEX_POINT ( 'NONE', #205442 ) ;
#226471=ORIENTED_EDGE ( 'NONE', *, *, #193431, .T. ) ;
#226494=CARTESIAN_POINT ( 'NONE',  ( -21.05000000000000071, 1.115650877919449575E-11, -71.09999999999999432 ) ) ;
#226527=DIRECTION ( 'NONE',  ( 0.000000000000000000, 0.000000000000000000, 1.000000000000000000 ) ) ;
#226562=ORIENTED_EDGE ( 'NONE', *, *, #178086, .T. ) ;
#226567=CARTESIAN_POINT ( 'NONE',  ( -22.50000000000000000, 1.115600667400684642E-11, -33.50000000000000000 ) ) ;
#226570=EDGE_CURVE ( 'NONE', #36408, #2508, #172298, .T. ) ;
#226572=DIRECTION ( 'NONE',  ( 0.000000000000000000, 0.000000000000000000, -1.000000000000000000 ) ) ;
#226595=SPHERICAL_SURFACE ( 'NONE', #140028, 0.1000000000000000056 ) ;
#226599=DIRECTION ( 'NONE',  ( -1.000000000000000000, 0.000000000000000000, 0.000000000000000000 ) ) ;
#226617=LINE ( 'NONE', #187532, #67518 ) ;
#226685=DIRECTION ( 'NONE',  ( 1.000000000000000000, -7.304098846218134667E-16, -4.217023435051626718E-16 ) ) ;
#226686=DIRECTION ( 'NONE',  ( 0.000000000000000000, 0.5000000000000078826, 0.8660254037844340447 ) ) ;
#226706=DIRECTION ( 'NONE',  ( -1.000000000000000000, 0.000000000000000000, 0.000000000000000000 ) ) ;
#226715=DIRECTION ( 'NONE',  ( -1.000000000000000000, 0.000000000000000000, 0.000000000000000000 ) ) ;
#226730=DIRECTION ( 'NONE',  ( 1.000000000000000000, 0.000000000000000000, 0.000000000000000000 ) ) ;
#226750=FACE_OUTER_BOUND ( 'NONE', #17283, .T. ) ;
#226768=VERTEX_POINT ( 'NONE', #43520 ) ;
#226769=DIRECTION ( 'NONE',  ( -1.000000000000000000, -7.304098846218134667E-16, 4.217023435051678980E-16 ) ) ;
#226770=CARTESIAN_POINT ( 'NONE',  ( 21.05000000000000071, 1.115600667400684642E-11, -71.09999999999999432 ) ) ;
#226790=DIRECTION ( 'NONE',  ( 0.000000000000000000, 0.000000000000000000, -1.000000000000000000 ) ) ;
#226803=AXIS2_PLACEMENT_3D ( 'NONE', #101009, #18945, #198874 ) ;
#226808=CARTESIAN_POINT ( 'NONE',  ( 21.14999999999999503, -0.09999999998884338825, -21.85042919245520210 ) ) ;
#226811=ORIENTED_EDGE ( 'NONE', *, *, #105244, .F. ) ;
#226871=CIRCLE ( 'NONE', #35389, 0.09999999999999939493 ) ;
#226881=ORIENTED_EDGE ( 'NONE', *, *, #163174, .F. ) ;
#226906=EDGE_CURVE ( 'NONE', #55121, #164375, #109865, .T. ) ;
#226915=VERTEX_POINT ( 'NONE', #182599 ) ;
#226947=EDGE_CURVE ( 'NONE', #176243, #25637, #150822, .T. ) ;
#226951=CARTESIAN_POINT ( 'NONE',  ( 18.59999999999999076, 1.115600667400684642E-11, -67.00000000000000000 ) ) ;
#226964=AXIS2_PLACEMENT_3D ( 'NONE', #182159, #124751, #7358 ) ;
#227006=DIRECTION ( 'NONE',  ( 0.000000000000000000, 1.000000000000000000, -6.308085367188393199E-16 ) ) ;
#227029=DIRECTION ( 'NONE',  ( -1.000000000000000000, -0.000000000000000000, -0.000000000000000000 ) ) ;
#227031=DIRECTION ( 'NONE',  ( 0.000000000000000000, 0.000000000000000000, -1.000000000000000000 ) ) ;
#227041=CARTESIAN_POINT ( 'NONE',  ( -20.54999999999999716, 9.350000000011156942, -54.75000000000000000 ) ) ;
#227056=ORIENTED_EDGE ( 'NONE', *, *, #66477, .T. ) ;
#227068=DIRECTION ( 'NONE',  ( 1.000000000000000000, 0.000000000000000000, 0.000000000000000000 ) ) ;
#227080=ORIENTED_EDGE ( 'NONE', *, *, #201513, .F. ) ;
#227150=CARTESIAN_POINT ( 'NONE',  ( -18.46919391072058403, -9.670724388266654259, -73.67380353179945018 ) ) ;
#227182=CIRCLE ( 'NONE', #156312, 0.1000000000000028644 ) ;
#227183=EDGE_CURVE ( 'NONE', #148274, #42457, #22793, .T. ) ;
#227214=ORIENTED_EDGE ( 'NONE', *, *, #171698, .T. ) ;
#227215=EDGE_CURVE ( 'NONE', #189211, #226915, #37633, .T. ) ;
#227239=FACE_OUTER_BOUND ( 'NONE', #175615, .T. ) ;
#227276=TOROIDAL_SURFACE ( 'NONE', #114857, 11.70000000000000462, 0.1000000000000000056 ) ;
#227284=ORIENTED_EDGE ( 'NONE', *, *, #165647, .T. ) ;
#227312=CARTESIAN_POINT ( 'NONE',  ( -18.59999999999999787, 9.150000000011157653, -45.85000000000000142 ) ) ;
#227338=DIRECTION ( 'NONE',  ( 1.000000000000000000, 0.000000000000000000, -0.000000000000000000 ) ) ;
#227360=ORIENTED_EDGE ( 'NONE', *, *, #130813, .F. ) ;
#227378=DIRECTION ( 'NONE',  ( 1.000000000000000000, -0.000000000000000000, -0.000000000000000000 ) ) ;
#227410=CIRCLE ( 'NONE', #135825, 2.000000000000001776 ) ;
#227413=EDGE_CURVE ( 'NONE', #24511, #100761, #114343, .T. ) ;
#227420=CARTESIAN_POINT ( 'NONE',  ( 20.85000000000000142, 1.115600667400684642E-11, -67.00000000000000000 ) ) ;
#227444=DIRECTION ( 'NONE',  ( 1.441126678808781001E-14, 0.9876197685951252359, 0.1568667991644863424 ) ) ;
#227475=CIRCLE ( 'NONE', #248166, 0.1000000000000028644 ) ;
#227484=EDGE_CURVE ( 'NONE', #127120, #255180, #72874, .T. ) ;
#227499=DIRECTION ( 'NONE',  ( 3.469446951953646374E-14, -0.7899159663865635839, -0.6132151058540398214 ) ) ;
#227502=CARTESIAN_POINT ( 'NONE',  ( -22.46246831459151494, 0.02191216695058596786, -21.85013543879003350 ) ) ;
#227507=EDGE_CURVE ( 'NONE', #119088, #200872, #64467, .T. ) ;
#227555=ORIENTED_EDGE ( 'NONE', *, *, #85742, .T. ) ;
#227565=CARTESIAN_POINT ( 'NONE',  ( -18.54148534481894472, 10.32532329027886497, -72.56993430183595706 ) ) ;
#227571=FACE_OUTER_BOUND ( 'NONE', #101336, .T. ) ;
#227582=EDGE_LOOP ( 'NONE', ( #53351, #252040, #252269, #185019, #1771 ) ) ;
#227593=VERTEX_POINT ( 'NONE', #60693 ) ;
#227604=LINE ( 'NONE', #248465, #206528 ) ;
#227656=VECTOR ( 'NONE', #177787, 1000.000000000000000 ) ;
#227673=ADVANCED_FACE ( 'NONE', ( #217198 ), #257566, .T. ) ;
#227676=ORIENTED_EDGE ( 'NONE', *, *, #175827, .T. ) ;
#227697=EDGE_LOOP ( 'NONE', ( #230570, #168215, #62682, #36929 ) ) ;
#227701=CARTESIAN_POINT ( 'NONE',  ( 23.14999999999999858, 4.775700934590591196, -55.15123189595403375 ) ) ;
#227708=AXIS2_PLACEMENT_3D ( 'NONE', #48249, #187780, #62690 ) ;
#227746=LINE ( 'NONE', #149525, #217892 ) ;
#227773=ORIENTED_EDGE ( 'NONE', *, *, #109130, .F. ) ;
#227799=CARTESIAN_POINT ( 'NONE',  ( -22.50000000000000000, 0.1000000000111554016, -21.85042919245520210 ) ) ;
#227812=CARTESIAN_POINT ( 'NONE',  ( -18.59999999999999787, 11.65000000001115232, -54.85000000000000142 ) ) ;
#227845=AXIS2_PLACEMENT_3D ( 'NONE', #176313, #173777, #137158 ) ;
#227978=CARTESIAN_POINT ( 'NONE',  ( 20.99142135623731065, 11.60000000001116049, -60.07179676972450721 ) ) ;
#227982=VERTEX_POINT ( 'NONE', #96930 ) ;
#227991=CARTESIAN_POINT ( 'NONE',  ( 22.59066674512243722, 11.75000000001115552, -33.46949587636930090 ) ) ;
#228047=CARTESIAN_POINT ( 'NONE',  ( 18.59999999999999432, 5.699452464332755319, -20.95772604343016710 ) ) ;
#228048=EDGE_CURVE ( 'NONE', #147289, #189211, #6372, .T. ) ;
#228066=ORIENTED_EDGE ( 'NONE', *, *, #172551, .T. ) ;
#228086=VECTOR ( 'NONE', #120565, 1000.000000000000000 ) ;
#228131=AXIS2_PLACEMENT_3D ( 'NONE', #131830, #211380, #95274 ) ;
#228173=EDGE_LOOP ( 'NONE', ( #12632, #206356, #142397, #9624 ) ) ;
#228184=EDGE_CURVE ( 'NONE', #256777, #90926, #114899, .T. ) ;
#228196=DIRECTION ( 'NONE',  ( 0.000000000000000000, 0.000000000000000000, -1.000000000000000000 ) ) ;
#228200=CARTESIAN_POINT ( 'NONE',  ( -20.94999999999999929, -1.736257131586239844, -45.06865232901750318 ) ) ;
#228239=AXIS2_PLACEMENT_3D ( 'NONE', #226808, #148568, #49463 ) ;
#228253=EDGE_LOOP ( 'NONE', ( #105383, #51703, #7794, #49436 ) ) ;
#228260=CYLINDRICAL_SURFACE ( 'NONE', #179042, 0.1000000000000001443 ) ;
#228320=DIRECTION ( 'NONE',  ( 0.000000000000000000, 1.000000000000000000, 0.000000000000000000 ) ) ;
#228329=CARTESIAN_POINT ( 'NONE',  ( 20.94999999999999929, 6.846123162363745074, -70.73772626684986164 ) ) ;
#228337=DIRECTION ( 'NONE',  ( 0.000000000000000000, 0.000000000000000000, -1.000000000000000000 ) ) ;
#228345=ORIENTED_EDGE ( 'NONE', *, *, #4183, .T. ) ;
#228351=CARTESIAN_POINT ( 'NONE',  ( 18.39999999999999858, -9.499999999988842703, -73.60018939122203108 ) ) ;
#228374=CARTESIAN_POINT ( 'NONE',  ( 19.75857864376268935, 11.65000000001115943, -58.35000000000000142 ) ) ;
#228375=VERTEX_POINT ( 'NONE', #106583 ) ;
#228405=EDGE_CURVE ( 'NONE', #225834, #19166, #64816, .T. ) ;
#228439=PRODUCT ( 'Injection Molded Chain Links 2', 'Injection Molded Chain Links 2', '', ( #177348 ) ) ;
#228441=VECTOR ( 'NONE', #225832, 1000.000000000000114 ) ;
#228442=AXIS2_PLACEMENT_3D ( 'NONE', #144896, #23720, #161933 ) ;
#228457=DIRECTION ( 'NONE',  ( -1.000000000000000000, -0.000000000000000000, -0.000000000000000000 ) ) ;
#228462=CARTESIAN_POINT ( 'NONE',  ( -18.50000000000000000, -9.421290279511815413, -73.82388217902615679 ) ) ;
#228463=VERTEX_POINT ( 'NONE', #253802 ) ;
#228518=DIRECTION ( 'NONE',  ( 1.000000000000000000, 0.000000000000000000, -0.000000000000000000 ) ) ;
#228539=EDGE_LOOP ( 'NONE', ( #55113, #16557, #204500, #12636 ) ) ;
#228548=ORIENTED_EDGE ( 'NONE', *, *, #234307, .F. ) ;
#228618=ORIENTED_EDGE ( 'NONE', *, *, #215196, .T. ) ;
#228621=ADVANCED_BREP_SHAPE_REPRESENTATION ( '', ( #193366, #2425 ), #35604 ) ;
#228633=EDGE_CURVE ( 'NONE', #182341, #232170, #176874, .T. ) ;
#228682=ADVANCED_FACE ( 'NONE', ( #140265 ), #180713, .F. ) ;
#228687=CYLINDRICAL_SURFACE ( 'NONE', #202367, 0.1000000000000028644 ) ;
#228695=CARTESIAN_POINT ( 'NONE',  ( 21.53699400384778428, 1.434816042522701864E-11, -26.71228820676085647 ) ) ;
#228700=DIRECTION ( 'NONE',  ( 1.000000000000000000, -0.000000000000000000, -0.000000000000000000 ) ) ;
#228708=VECTOR ( 'NONE', #126002, 1000.000000000000000 ) ;
#228725=VECTOR ( 'NONE', #231606, 1000.000000000000000 ) ;
#228733=CARTESIAN_POINT ( 'NONE',  ( 20.94999999999999574, 1.162701749949165642, -41.60000000000000142 ) ) ;
#228749=AXIS2_PLACEMENT_3D ( 'NONE', #126874, #245545, #146408 ) ;
#228786=FACE_OUTER_BOUND ( 'NONE', #215639, .T. ) ;
#228806=ORIENTED_EDGE ( 'NONE', *, *, #185052, .F. ) ;
#228822=DIRECTION ( 'NONE',  ( 1.000000000000000000, 0.000000000000000000, 0.000000000000000000 ) ) ;
#228833=CYLINDRICAL_SURFACE ( 'NONE', #140578, 11.80000000000000426 ) ;
#228843=CARTESIAN_POINT ( 'NONE',  ( 21.05000000000000071, -11.29603075032412995, -36.54789915966387071 ) ) ;
#228877=AXIS2_PLACEMENT_3D ( 'NONE', #93905, #142017, #162900 ) ;
#228881=SPHERICAL_SURFACE ( 'NONE', #169370, 0.1000000000000000056 ) ;
#228897=CARTESIAN_POINT ( 'NONE',  ( 20.85000000000000142, 1.115600667400684642E-11, -67.00000000000000000 ) ) ;
#228935=AXIS2_PLACEMENT_3D ( 'NONE', #50972, #69300, #190540 ) ;
#228940=EDGE_CURVE ( 'NONE', #100799, #84436, #206657, .T. ) ;
#228947=AXIS2_PLACEMENT_3D ( 'NONE', #159024, #201976, #143272 ) ;
#228953=CARTESIAN_POINT ( 'NONE',  ( 20.04142135623730070, 11.75000000001115907, -58.15000000000000568 ) ) ;
#228986=ADVANCED_FACE ( 'NONE', ( #40919 ), #190293, .T. ) ;
#229002=ORIENTED_EDGE ( 'NONE', *, *, #53792, .F. ) ;
#229026=PLANE ( 'NONE',  #78163 ) ;
#229068=APPLICATION_CONTEXT ( 'automotive_design' ) ;
#229096=CARTESIAN_POINT ( 'NONE',  ( 23.15000000000000213, -11.74999999998883737, -45.75000000000000711 ) ) ;
#229109=ORIENTED_EDGE ( 'NONE', *, *, #195982, .F. ) ;
#229112=VERTEX_POINT ( 'NONE', #25197 ) ;
#229138=VECTOR ( 'NONE', #238530, 1000.000000000000000 ) ;
#229159=ORIENTED_EDGE ( 'NONE', *, *, #211398, .T. ) ;
#229160=ORIENTED_EDGE ( 'NONE', *, *, #74829, .T. ) ;
#229178=EDGE_CURVE ( 'NONE', #54754, #239491, #248527, .T. ) ;
#229235=ORIENTED_EDGE ( 'NONE', *, *, #64260, .F. ) ;
#229316=DIRECTION ( 'NONE',  ( 0.000000000000000000, -1.000000000000000000, 0.000000000000000000 ) ) ;
#229322=SPHERICAL_SURFACE ( 'NONE', #256292, 0.1000000000000000056 ) ;
#229369=EDGE_CURVE ( 'NONE', #18621, #80050, #15919, .T. ) ;
#229378=CIRCLE ( 'NONE', #116937, 0.1000000000000004496 ) ;
#229411=FACE_OUTER_BOUND ( 'NONE', #242253, .T. ) ;
#229444=DIRECTION ( 'NONE',  ( 1.000000000000000000, 2.952720810173289112E-16, -0.000000000000000000 ) ) ;
#229452=EDGE_CURVE ( 'NONE', #104231, #18666, #177830, .T. ) ;
#229487=DIRECTION ( 'NONE',  ( -0.000000000000000000, 0.7397360091702694929, 0.6728971962616898672 ) ) ;
#229495=ORIENTED_EDGE ( 'NONE', *, *, #144550, .T. ) ;
#229502=ORIENTED_EDGE ( 'NONE', *, *, #158862, .F. ) ;
#229543=DIRECTION ( 'NONE',  ( 0.7071067811865475727, 0.7071067811865475727, 0.000000000000000000 ) ) ;
#229548=DIRECTION ( 'NONE',  ( 0.000000000000000000, 0.000000000000000000, -1.000000000000000000 ) ) ;
#229553=CARTESIAN_POINT ( 'NONE',  ( -22.47007471830799119, 7.720710651937631397, -33.50000000000001421 ) ) ;
#229556=CARTESIAN_POINT ( 'NONE',  ( 20.94999999999999929, 1.115600667400684642E-11, -33.50000000000000000 ) ) ;
#229557=DIRECTION ( 'NONE',  ( 2.952720810173289112E-16, -1.000000000000000000, 0.000000000000000000 ) ) ;
#229561=ADVANCED_FACE ( 'NONE', ( #40631 ), #223067, .F. ) ;
#229562=EDGE_CURVE ( 'NONE', #17420, #189223, #142249, .T. ) ;
#229568=EDGE_CURVE ( 'NONE', #214956, #70987, #43163, .T. ) ;
#229630=ORIENTED_EDGE ( 'NONE', *, *, #101539, .F. ) ;
#229635=CARTESIAN_POINT ( 'NONE',  ( -20.85000000000000142, 1.115600667400684642E-11, -67.00000000000000000 ) ) ;
#229654=ORIENTED_EDGE ( 'NONE', *, *, #11440, .T. ) ;
#229661=EDGE_LOOP ( 'NONE', ( #49589, #49542, #141977, #69542, #27295 ) ) ;
#229666=AXIS2_PLACEMENT_3D ( 'NONE', #102138, #222086, #8224 ) ;
#229679=DIRECTION ( 'NONE',  ( -0.000000000000000000, 1.000000000000000000, 0.000000000000000000 ) ) ;
#229725=ORIENTED_EDGE ( 'NONE', *, *, #208667, .T. ) ;
#229729=CARTESIAN_POINT ( 'NONE',  ( -23.25000000000000000, 1.115600667400684642E-11, -33.50000000000000000 ) ) ;
#229730=ORIENTED_EDGE ( 'NONE', *, *, #92735, .T. ) ;
#229748=EDGE_CURVE ( 'NONE', #179511, #150811, #166996, .T. ) ;
#229811=CARTESIAN_POINT ( 'NONE',  ( 23.14999999999999503, 11.65000000001116298, -54.85000000000000142 ) ) ;
#229858=EDGE_CURVE ( 'NONE', #119088, #137736, #169839, .T. ) ;
#229878=CARTESIAN_POINT ( 'NONE',  ( 23.14999999999998437, 1.115600667400684642E-11, -33.50000000000000000 ) ) ;
#229890=ORIENTED_EDGE ( 'NONE', *, *, #48018, .F. ) ;
#229910=ORIENTED_EDGE ( 'NONE', *, *, #178427, .F. ) ;
#229911=DIRECTION ( 'NONE',  ( 0.000000000000000000, 0.000000000000000000, -1.000000000000000000 ) ) ;
#229922=FACE_OUTER_BOUND ( 'NONE', #66777, .T. ) ;
#229952=DIRECTION ( 'NONE',  ( 1.000000000000000000, 1.836970198721029934E-16, 0.000000000000000000 ) ) ;
#229955=DIRECTION ( 'NONE',  ( 0.000000000000000000, 0.000000000000000000, -1.000000000000000000 ) ) ;
#229976=DIRECTION ( 'NONE',  ( -1.000000000000000000, 0.000000000000000000, 0.000000000000000000 ) ) ;
#229979=EDGE_LOOP ( 'NONE', ( #225065, #71760, #97670, #154761 ) ) ;
#230017=VECTOR ( 'NONE', #24977, 1000.000000000000000 ) ;
#230031=EDGE_LOOP ( 'NONE', ( #5437, #160371, #144325, #251935 ) ) ;
#230053=EDGE_CURVE ( 'NONE', #17741, #141916, #19442, .T. ) ;
#230120=SPHERICAL_SURFACE ( 'NONE', #232847, 0.1000000000000000056 ) ;
#230135=CIRCLE ( 'NONE', #138540, 0.09999999999999939493 ) ;
#230159=EDGE_CURVE ( 'NONE', #200640, #2443, #252257, .T. ) ;
#230160=ORIENTED_EDGE ( 'NONE', *, *, #176296, .F. ) ;
#230167=CARTESIAN_POINT ( 'NONE',  ( 21.04999999999999361, 10.50253167713717595, -41.05882981707473078 ) ) ;
#230170=DIRECTION ( 'NONE',  ( -0.000000000000000000, 1.000000000000000000, 1.734723475976807292E-15 ) ) ;
#230174=CARTESIAN_POINT ( 'NONE',  ( 18.58143601961912950, 10.43572941510548624, -58.25000000000000000 ) ) ;
#230183=LINE ( 'NONE', #13700, #163130 ) ;
#230195=AXIS2_PLACEMENT_3D ( 'NONE', #152427, #16752, #250215 ) ;
#230242=CARTESIAN_POINT ( 'NONE',  ( -20.94999999999999929, -11.48912529306489994, -64.00000000000000000 ) ) ;
#230250=DIRECTION ( 'NONE',  ( -1.000000000000000000, -0.000000000000000000, -0.000000000000000000 ) ) ;
#230254=DIRECTION ( 'NONE',  ( 0.000000000000000000, 0.000000000000000000, 1.000000000000000000 ) ) ;
#230268=ORIENTED_EDGE ( 'NONE', *, *, #30463, .T. ) ;
#230270=DIRECTION ( 'NONE',  ( 1.000000000000000000, 0.000000000000000000, 0.000000000000000000 ) ) ;
#230302=DIRECTION ( 'NONE',  ( -1.000000000000000000, -0.000000000000000000, -0.000000000000000000 ) ) ;
#230313=CARTESIAN_POINT ( 'NONE',  ( 18.59999999999999076, 11.65000000001115943, -58.35000000000000142 ) ) ;
#230373=ORIENTED_EDGE ( 'NONE', *, *, #150055, .T. ) ;
#230412=AXIS2_PLACEMENT_3D ( 'NONE', #54595, #134120, #75480 ) ;
#230413=DIRECTION ( 'NONE',  ( 0.000000000000000000, 0.000000000000000000, -1.000000000000000000 ) ) ;
#230427=VERTEX_POINT ( 'NONE', #44784 ) ;
#230521=ORIENTED_EDGE ( 'NONE', *, *, #135250, .T. ) ;
#230523=CARTESIAN_POINT ( 'NONE',  ( -21.05000000000000071, 11.75000000001115552, -60.15839931010295771 ) ) ;
#230528=AXIS2_PLACEMENT_3D ( 'NONE', #10669, #11971, #90175 ) ;
#230553=EDGE_CURVE ( 'NONE', #194433, #207476, #48779, .T. ) ;
#230570=ORIENTED_EDGE ( 'NONE', *, *, #189861, .T. ) ;
#230574=PRODUCT_DEFINITION_SHAPE ( 'NONE', 'NONE',  #40537 ) ;
#230602=DIRECTION ( 'NONE',  ( 0.000000000000000000, 0.000000000000000000, 1.000000000000000000 ) ) ;
#230615=AXIS2_PLACEMENT_3D ( 'NONE', #124587, #63304, #161142 ) ;
#230623=DIRECTION ( 'NONE',  ( 1.000000000000000000, -0.000000000000000000, -0.000000000000000000 ) ) ;
#230629=CARTESIAN_POINT ( 'NONE',  ( 20.94999999999999574, 1.736257131608553550, -45.06865232901750318 ) ) ;
#230631=CARTESIAN_POINT ( 'NONE',  ( 18.59999999999999076, 6.550000000011156231, -54.65000000000000568 ) ) ;
#230662=CARTESIAN_POINT ( 'NONE',  ( 21.14999999999999858, 6.550000000011156231, -45.65000000000000568 ) ) ;
#230667=EDGE_CURVE ( 'NONE', #190151, #120355, #169458, .T. ) ;
#230708=ORIENTED_EDGE ( 'NONE', *, *, #242385, .F. ) ;
#230716=VERTEX_POINT ( 'NONE', #257054 ) ;
#230739=DIRECTION ( 'NONE',  ( 0.000000000000000000, -0.01283462868041992250, -0.9999176327611367654 ) ) ;
#230748=LINE ( 'NONE', #211169, #250644 ) ;
#230754=CIRCLE ( 'NONE', #55727, 0.09999999999999939493 ) ;
#230814=TOROIDAL_SURFACE ( 'NONE', #68475, 6.258578643762700899, 0.1000000000000000056 ) ;
#230824=FACE_OUTER_BOUND ( 'NONE', #199386, .T. ) ;
#230856=DIRECTION ( 'NONE',  ( -1.000000000000000000, -0.000000000000000000, 0.000000000000000000 ) ) ;
#230859=ORIENTED_EDGE ( 'NONE', *, *, #79590, .F. ) ;
#230903=DIRECTION ( 'NONE',  ( 0.000000000000000000, -0.9908441862701596881, 0.1350103645451904977 ) ) ;
#230926=ORIENTED_EDGE ( 'NONE', *, *, #110628, .F. ) ;
#230958=CARTESIAN_POINT ( 'NONE',  ( -20.94999999999999929, -11.48912529306490349, -36.50000000000000711 ) ) ;
#230968=VECTOR ( 'NONE', #135930, 1000.000000000000000 ) ;
#230983=CARTESIAN_POINT ( 'NONE',  ( 20.94999999999999929, 5.850000000011160495, -56.86750277572208034 ) ) ;
#230987=CARTESIAN_POINT ( 'NONE',  ( 18.31572054635736890, -9.548475435767633357, -73.85057016474850400 ) ) ;
#230994=FACE_OUTER_BOUND ( 'NONE', #159244, .T. ) ;
#230998=CARTESIAN_POINT ( 'NONE',  ( -21.44999999999999929, 7.350000000011155166, -54.75000000000000000 ) ) ;
#231021=ORIENTED_EDGE ( 'NONE', *, *, #21237, .F. ) ;
#231035=EDGE_LOOP ( 'NONE', ( #74882, #85065 ) ) ;
#231120=VERTEX_POINT ( 'NONE', #166970 ) ;
#231176=CARTESIAN_POINT ( 'NONE',  ( -23.15000000000000213, -8.596261682231830292, -57.54987248284972878 ) ) ;
#231187=DIRECTION ( 'NONE',  ( 0.000000000000000000, 0.000000000000000000, -1.000000000000000000 ) ) ;
#231220=EDGE_LOOP ( 'NONE', ( #15493, #73570, #125983, #119421 ) ) ;
#231229=CYLINDRICAL_SURFACE ( 'NONE', #17561, 0.1000000000000028644 ) ;
#231277=CARTESIAN_POINT ( 'NONE',  ( -23.15000000000000213, 1.115648428625851357E-11, -63.10000000000000142 ) ) ;
#231278=CARTESIAN_POINT ( 'NONE',  ( 18.49999999999999289, 6.650000000011155876, -54.65000000000000568 ) ) ;
#231329=ADVANCED_FACE ( 'NONE', ( #18122 ), #115789, .T. ) ;
#231332=CIRCLE ( 'NONE', #6453, 0.1999999999999996503 ) ;
#231342=CARTESIAN_POINT ( 'NONE',  ( -22.39999999999999858, 11.65000000001115588, -33.60000000000000142 ) ) ;
#231359=ORIENTED_EDGE ( 'NONE', *, *, #141008, .T. ) ;
#231409=AXIS2_PLACEMENT_3D ( 'NONE', #45601, #66447, #26049 ) ;
#231424=DIRECTION ( 'NONE',  ( 0.000000000000000000, 1.000000000000000000, 0.000000000000000000 ) ) ;
#231432=( BOUNDED_SURFACE ( )  B_SPLINE_SURFACE ( 3, 2, ( 
 ( #105576, #165605, #66488 ),
 ( #222980, #46901, #202150 ),
 ( #181319, #203437, #122633 ),
 ( #160482, #23551, #140896 ) ),
 .UNSPECIFIED., .F., .F., .F. ) 
 B_SPLINE_SURFACE_WITH_KNOTS ( ( 4, 4 ),
 ( 3, 3 ),
 ( 0.04058434257139475337, 0.04256401539001600232 ),
 ( 0.000000000000000000, 1.000000000000000000 ),
 .UNSPECIFIED. ) 
 GEOMETRIC_REPRESENTATION_ITEM ( )  RATIONAL_B_SPLINE_SURFACE ( (
 ( 1.000000000000000000, 0.7103081912008053500, 1.000000000000000000),
 ( 1.000000000000000000, 0.7104998333555551104, 1.000000000000000000),
 ( 1.000000000000000000, 0.7107238315755428637, 1.000000000000000000),
 ( 1.000000000000000000, 0.7110073749539292942, 1.000000000000000000) ) ) 
 REPRESENTATION_ITEM ( '' )  SURFACE ( )  );
#231448=DIRECTION ( 'NONE',  ( 0.000000000000000000, 0.000000000000000000, 1.000000000000000000 ) ) ;
#231460=CARTESIAN_POINT ( 'NONE',  ( -23.15000000000000213, 11.65000000001115588, -45.65000000000000568 ) ) ;
#231476=CARTESIAN_POINT ( 'NONE',  ( -23.15000000000000213, 1.115600667400684642E-11, -33.50000000000000000 ) ) ;
#231499=CIRCLE ( 'NONE', #19086, 0.1000000000000028644 ) ;
#231525=CARTESIAN_POINT ( 'NONE',  ( -23.15000000000000213, 5.900000000011162093, -56.78090023534362984 ) ) ;
#231528=EDGE_CURVE ( 'NONE', #28509, #61108, #44107, .T. ) ;
#231536=AXIS2_PLACEMENT_3D ( 'NONE', #140136, #141436, #220966 ) ;
#231557=DIRECTION ( 'NONE',  ( -1.000000000000000000, 0.000000000000000000, 0.000000000000000000 ) ) ;
#231580=DIRECTION ( 'NONE',  ( 0.000000000000000000, -1.000000000000000000, 0.000000000000000000 ) ) ;
#231606=DIRECTION ( 'NONE',  ( -3.265361837132813093E-16, 1.000000000000000000, -0.000000000000000000 ) ) ;
#231612=DIRECTION ( 'NONE',  ( 1.000000000000000000, -7.304098846218134667E-16, -4.217023435051625732E-16 ) ) ;
#231629=ORIENTED_EDGE ( 'NONE', *, *, #135250, .F. ) ;
#231630=ADVANCED_FACE ( 'NONE', ( #209599 ), #251273, .F. ) ;
#231644=EDGE_CURVE ( 'NONE', #133244, #72626, #148339, .T. ) ;
#231667=DIRECTION ( 'NONE',  ( 1.000000000000000000, 0.000000000000000000, 0.000000000000000000 ) ) ;
#231674=CARTESIAN_POINT ( 'NONE',  ( 21.05000000000000071, 6.650000000011155876, -45.65000000000000568 ) ) ;
#231708=DIRECTION ( 'NONE',  ( 1.000000000000000000, -0.000000000000000000, -0.000000000000000000 ) ) ;
#231712=CARTESIAN_POINT ( 'NONE',  ( -21.05000000000000071, -1.835341550213255957, -45.05515129256298223 ) ) ;
#231743=DIRECTION ( 'NONE',  ( 1.000000000000000000, 0.000000000000000000, 0.000000000000000000 ) ) ;
#231758=CARTESIAN_POINT ( 'NONE',  ( 20.12500000000000000, 9.750000000011153745, -41.61177128211428311 ) ) ;
#231789=CARTESIAN_POINT ( 'NONE',  ( 23.14999999999999503, 6.550000000011156231, -54.75000000000000000 ) ) ;
#231817=VERTEX_POINT ( 'NONE', #10774 ) ;
#231863=CARTESIAN_POINT ( 'NONE',  ( -23.25000000000000000, -8.999999999988844479, -57.70603087734755832 ) ) ;
#231876=EDGE_CURVE ( 'NONE', #126429, #74863, #36911, .T. ) ;
#231912=CYLINDRICAL_SURFACE ( 'NONE', #141415, 0.1000000000000000056 ) ;
#231919=DIRECTION ( 'NONE',  ( 1.000000000000000000, -0.000000000000000000, -0.000000000000000000 ) ) ;
#231946=CIRCLE ( 'NONE', #165283, 0.09999999999999939493 ) ;
#231976=EDGE_CURVE ( 'NONE', #16861, #11590, #57507, .T. ) ;
#231988=ORIENTED_EDGE ( 'NONE', *, *, #61522, .T. ) ;
#231989=FACE_OUTER_BOUND ( 'NONE', #207091, .T. ) ;
#231990=DIRECTION ( 'NONE',  ( 1.000000000000000000, 0.000000000000000000, 0.000000000000000000 ) ) ;
#231992=AXIS2_PLACEMENT_3D ( 'NONE', #14626, #234943, #159 ) ;
#231994=ORIENTED_EDGE ( 'NONE', *, *, #80572, .F. ) ;
#232040=DIRECTION ( 'NONE',  ( -0.000000000000000000, -2.891205793294679805E-16, 1.000000000000000000 ) ) ;
#232043=ORIENTED_EDGE ( 'NONE', *, *, #31639, .F. ) ;
#232070=VECTOR ( 'NONE', #212251, 999.9999999999998863 ) ;
#232081=FACE_OUTER_BOUND ( 'NONE', #72679, .T. ) ;
#232103=CARTESIAN_POINT ( 'NONE',  ( -22.50000000000000000, 11.64987090377452894, -33.41748010912702682 ) ) ;
#232115=ORIENTED_EDGE ( 'NONE', *, *, #92317, .T. ) ;
#232122=AXIS2_PLACEMENT_3D ( 'NONE', #242074, #222494, #218655 ) ;
#232135=DIRECTION ( 'NONE',  ( 0.000000000000000000, 1.000000000000000000, 0.000000000000000000 ) ) ;
#232148=CARTESIAN_POINT ( 'NONE',  ( -23.15000000000000213, -11.74999999998884448, -63.89999999999999858 ) ) ;
#232150=DIRECTION ( 'NONE',  ( -0.000000000000000000, 0.1350103645451876666, 0.9908441862701600211 ) ) ;
#232168=CARTESIAN_POINT ( 'NONE',  ( -18.59999999999999787, 11.75000000001115552, -67.00000000000000000 ) ) ;
#232170=VERTEX_POINT ( 'NONE', #126567 ) ;
#232184=DIRECTION ( 'NONE',  ( -0.000000000000000000, 0.000000000000000000, 1.000000000000000000 ) ) ;
#232185=AXIS2_PLACEMENT_3D ( 'NONE', #19457, #18163, #181108 ) ;
#232198=DIRECTION ( 'NONE',  ( 1.000000000000000000, 0.000000000000000000, 0.000000000000000000 ) ) ;
#232221=LINE ( 'NONE', #53562, #56147 ) ;
#232225=DIRECTION ( 'NONE',  ( 0.000000000000000000, 0.9887567792719341719, -0.1495327102803664099 ) ) ;
#232235=EDGE_LOOP ( 'NONE', ( #22176, #163094, #2334, #81426 ) ) ;
#232244=CARTESIAN_POINT ( 'NONE',  ( 18.55807992284871588, 10.32898536001801659, -72.58266832227644727 ) ) ;
#232269=DIRECTION ( 'NONE',  ( -1.000000000000000000, 0.000000000000000000, 0.000000000000000000 ) ) ;
#232272=CARTESIAN_POINT ( 'NONE',  ( -21.76363531954647357, 0.09900187431060442078, -26.48706345212826108 ) ) ;
#232274=CARTESIAN_POINT ( 'NONE',  ( 18.40000000000000213, -9.499999999988844479, -73.92214984933046651 ) ) ;
#232279=ADVANCED_FACE ( 'NONE', ( #114702 ), #211236, .T. ) ;
#232294=CARTESIAN_POINT ( 'NONE',  ( -21.05000000000000071, -11.48912529306489994, -64.10000000000000853 ) ) ;
#232302=DIRECTION ( 'NONE',  ( 1.000000000000000000, 0.000000000000000000, 0.000000000000000000 ) ) ;
#232317=CARTESIAN_POINT ( 'NONE',  ( -20.94999999999999929, 1.115600667400684642E-11, -67.00000000000000000 ) ) ;
#232323=ORIENTED_EDGE ( 'NONE', *, *, #217194, .F. ) ;
#232326=ORIENTED_EDGE ( 'NONE', *, *, #183919, .T. ) ;
#232335=AXIS2_PLACEMENT_3D ( 'NONE', #211688, #64760, #45200 ) ;
#232347=DIRECTION ( 'NONE',  ( -1.000000000000000000, -2.952720810173289112E-16, 0.000000000000000000 ) ) ;
#232364=ORIENTED_EDGE ( 'NONE', *, *, #149491, .T. ) ;
#232436=DIRECTION ( 'NONE',  ( 0.000000000000000000, 1.000000000000000000, 1.265107689135680095E-16 ) ) ;
#232444=CARTESIAN_POINT ( 'NONE',  ( 21.14999999999999858, 6.540656951712400691, -33.50000000000000000 ) ) ;
#232465=CARTESIAN_POINT ( 'NONE',  ( -21.05000000000000071, 11.60000000001115517, -60.07179676972450011 ) ) ;
#232495=CARTESIAN_POINT ( 'NONE',  ( 23.25000000000000000, -8.999999999988842703, -57.10603087734755690 ) ) ;
#232568=AXIS2_PLACEMENT_3D ( 'NONE', #45636, #66478, #174620 ) ;
#232570=ADVANCED_FACE ( 'NONE', ( #46701 ), #128821, .F. ) ;
#232571=VECTOR ( 'NONE', #45834, 1000.000000000000000 ) ;
#232574=ORIENTED_EDGE ( 'NONE', *, *, #179867, .F. ) ;
#232594=CARTESIAN_POINT ( 'NONE',  ( -20.94999999999999574, 11.62071067812980907, -60.13158334765903845 ) ) ;
#232604=CYLINDRICAL_SURFACE ( 'NONE', #151519, 0.1000000000000028644 ) ;
#232614=EDGE_LOOP ( 'NONE', ( #168824, #48953, #145766, #34739 ) ) ;
#232627=ORIENTED_EDGE ( 'NONE', *, *, #21165, .F. ) ;
#232628=ADVANCED_FACE ( 'NONE', ( #188789 ), #132681, .T. ) ;
#232629=DIRECTION ( 'NONE',  ( -1.000000000000000000, 0.000000000000000000, 0.000000000000000000 ) ) ;
#232644=AXIS2_PLACEMENT_3D ( 'NONE', #138999, #218556, #119489 ) ;
#232658=VERTEX_POINT ( 'NONE', #74021 ) ;
#232690=CARTESIAN_POINT ( 'NONE',  ( -20.94999999999999929, -11.64999999998884483, -64.00000000000000000 ) ) ;
#232699=CIRCLE ( 'NONE', #195303, 0.1000000000000028644 ) ;
#232728=AXIS2_PLACEMENT_3D ( 'NONE', #26351, #245400, #225798 ) ;
#232756=CARTESIAN_POINT ( 'NONE',  ( 20.95262331984753956, 10.50415726280101758, -41.06088832959332535 ) ) ;
#232759=CARTESIAN_POINT ( 'NONE',  ( 19.58285714285715073, 10.38499851036257837, -41.12968466738995232 ) ) ;
#232763=CARTESIAN_POINT ( 'NONE',  ( 18.50000000000094502, 10.44006789215635322, -58.26711774888727291 ) ) ;
#232765=EDGE_LOOP ( 'NONE', ( #18695, #28506, #111757, #75107 ) ) ;
#232783=EDGE_CURVE ( 'NONE', #221539, #195077, #91582, .T. ) ;
#232811=ADVANCED_FACE ( 'NONE', ( #7267 ), #203995, .T. ) ;
#232813=ORIENTED_EDGE ( 'NONE', *, *, #138525, .F. ) ;
#232823=CIRCLE ( 'NONE', #137128, 0.1000000000000028644 ) ;
#232843=ORIENTED_EDGE ( 'NONE', *, *, #134860, .T. ) ;
#232847=AXIS2_PLACEMENT_3D ( 'NONE', #91890, #51455, #131019 ) ;
#232853=DIRECTION ( 'NONE',  ( 0.000000000000000000, 0.000000000000000000, -1.000000000000000000 ) ) ;
#232870=ADVANCED_FACE ( 'NONE', ( #245900 ), #122101, .F. ) ;
#232969=DIRECTION ( 'NONE',  ( 0.000000000000000000, 1.000000000000000000, 0.000000000000000000 ) ) ;
#232976=ORIENTED_EDGE ( 'NONE', *, *, #248982, .T. ) ;
#232978=DIRECTION ( 'NONE',  ( 1.000000000000000000, 0.000000000000000000, 0.000000000000000000 ) ) ;
#232993=EDGE_CURVE ( 'NONE', #168869, #129370, #4089, .T. ) ;
#233008=CIRCLE ( 'NONE', #220348, 0.1000000000000028644 ) ;
#233009=ORIENTED_EDGE ( 'NONE', *, *, #188921, .F. ) ;
#233045=ADVANCED_FACE ( 'NONE', ( #128514 ), #29451, .F. ) ;
#233046=ORIENTED_EDGE ( 'NONE', *, *, #11166, .F. ) ;
#233064=AXIS2_PLACEMENT_3D ( 'NONE', #238263, #157492, #235698 ) ;
#233071=CIRCLE ( 'NONE', #129014, 0.09999999999999439892 ) ;
#233076=CARTESIAN_POINT ( 'NONE',  ( -21.05000000000000071, 6.300000000011169554, -33.60000000000000142 ) ) ;
#233092=VERTEX_POINT ( 'NONE', #157076 ) ;
#233120=ADVANCED_FACE ( 'NONE', ( #239165 ), #57937, .F. ) ;
#233142=VECTOR ( 'NONE', #8511, 1000.000000000000000 ) ;
#233168=DIRECTION ( 'NONE',  ( 0.000000000000000000, 0.000000000000000000, -1.000000000000000000 ) ) ;
#233193=FACE_OUTER_BOUND ( 'NONE', #44380, .T. ) ;
#233200=FACE_OUTER_BOUND ( 'NONE', #167804, .T. ) ;
#233222=CARTESIAN_POINT ( 'NONE',  ( 20.94999999999999929, 1.835341550235569663, -45.05515129256298223 ) ) ;
#233236=ORIENTED_EDGE ( 'NONE', *, *, #171444, .T. ) ;
#233263=CARTESIAN_POINT ( 'NONE',  ( -20.94999999999999929, 1.115600667400684642E-11, -33.50000000000000000 ) ) ;
#233289=AXIS2_PLACEMENT_3D ( 'NONE', #237725, #77348, #18678 ) ;
#233298=CARTESIAN_POINT ( 'NONE',  ( 21.05000000000000071, -8.663551401857999323, -57.47589888193269303 ) ) ;
#233310=CYLINDRICAL_SURFACE ( 'NONE', #60595, 0.09999999999999939493 ) ;
#233416=LINE ( 'NONE', #255467, #17430 ) ;
#233425=ORIENTED_EDGE ( 'NONE', *, *, #89405, .F. ) ;
#233433=CARTESIAN_POINT ( 'NONE',  ( -18.59999999999999787, -1.164121893230052995, -74.81484808557161159 ) ) ;
#233434=EDGE_CURVE ( 'NONE', #134912, #81995, #20878, .T. ) ;
#233481=VECTOR ( 'NONE', #86664, 1000.000000000000000 ) ;
#233495=DIRECTION ( 'NONE',  ( 1.000000000000000000, -0.000000000000000000, 0.000000000000000000 ) ) ;
#233506=CARTESIAN_POINT ( 'NONE',  ( 20.85000000000000142, -1.362429037182151470, -74.88888124792120493 ) ) ;
#233510=CYLINDRICAL_SURFACE ( 'NONE', #122211, 4.000000000000003553 ) ;
#233542=EDGE_CURVE ( 'NONE', #78788, #48124, #121200, .T. ) ;
#233550=CARTESIAN_POINT ( 'NONE',  ( 18.54271179734059061, -9.624084290087575155, -73.74096485270030144 ) ) ;
#233565=ORIENTED_EDGE ( 'NONE', *, *, #255629, .F. ) ;
#233613=CARTESIAN_POINT ( 'NONE',  ( 21.11747605621531321, 8.778708005504054057, -45.74456316978977810 ) ) ;
#233626=ORIENTED_EDGE ( 'NONE', *, *, #227413, .T. ) ;
#233691=CARTESIAN_POINT ( 'NONE',  ( 18.59999999999999076, 6.650000000011155876, -54.85000000000000142 ) ) ;
#233728=VERTEX_POINT ( 'NONE', #135262 ) ;
#233729=ORIENTED_EDGE ( 'NONE', *, *, #56886, .F. ) ;
#233736=ADVANCED_FACE ( 'NONE', ( #131425 ), #71484, .F. ) ;
#233740=EDGE_LOOP ( 'NONE', ( #193884, #76597, #66448, #81902 ) ) ;
#233741=DIRECTION ( 'NONE',  ( -0.000000000000000000, 1.000000000000000000, -0.000000000000000000 ) ) ;
#233761=EDGE_LOOP ( 'NONE', ( #125195, #238294, #169996, #130957 ) ) ;
#233809=CYLINDRICAL_SURFACE ( 'NONE', #196104, 0.1000000000000028644 ) ;
#233843=AXIS2_PLACEMENT_3D ( 'NONE', #104445, #103170, #129184 ) ;
#233859=CYLINDRICAL_SURFACE ( 'NONE', #14540, 0.1000000000000028644 ) ;
#233864=LINE ( 'NONE', #36978, #173841 ) ;
#233866=EDGE_CURVE ( 'NONE', #22210, #201200, #20487, .T. ) ;
#233885=CYLINDRICAL_SURFACE ( 'NONE', #250245, 11.80000000000000426 ) ;
#233892=ORIENTED_EDGE ( 'NONE', *, *, #78744, .F. ) ;
#233902=ORIENTED_EDGE ( 'NONE', *, *, #58034, .T. ) ;
#233914=ORIENTED_EDGE ( 'NONE', *, *, #212609, .F. ) ;
#233932=ORIENTED_EDGE ( 'NONE', *, *, #8493, .F. ) ;
#233953=CARTESIAN_POINT ( 'NONE',  ( -21.05000000000000071, 1.115600667400684642E-11, -33.50000000000000000 ) ) ;
#233968=ADVANCED_FACE ( 'NONE', ( #187264 ), #123422, .T. ) ;
#233984=CARTESIAN_POINT ( 'NONE',  ( -23.15000000000000213, 2.000000000011154189, -54.37537807723790451 ) ) ;
#233989=DIRECTION ( 'NONE',  ( 0.000000000000000000, -1.000000000000000000, 0.000000000000000000 ) ) ;
#233999=EDGE_CURVE ( 'NONE', #46326, #24103, #247207, .T. ) ;
#234002=PLANE ( 'NONE',  #223468 ) ;
#234030=DIRECTION ( 'NONE',  ( 1.000000000000000000, -0.000000000000000000, -0.000000000000000000 ) ) ;
#234037=DIRECTION ( 'NONE',  ( 1.734723475976817507E-14, -1.000000000000000000, 0.000000000000000000 ) ) ;
#234075=VECTOR ( 'NONE', #131966, 1000.000000000000000 ) ;
#234092=CARTESIAN_POINT ( 'NONE',  ( 23.14999999999998437, 1.115650265596050101E-11, -29.45000000000000284 ) ) ;
#234120=ORIENTED_EDGE ( 'NONE', *, *, #3216, .F. ) ;
#234126=ORIENTED_EDGE ( 'NONE', *, *, #56923, .T. ) ;
#234158=CARTESIAN_POINT ( 'NONE',  ( -18.50000000000000711, 11.65000000001115232, -40.51480577065400013 ) ) ;
#234163=CARTESIAN_POINT ( 'NONE',  ( -20.00857864376270001, 9.350000000011156942, -54.75000000000000000 ) ) ;
#234242=DIRECTION ( 'NONE',  ( 0.000000000000000000, 0.5000000000000004441, 0.8660254037844384856 ) ) ;
#234249=CARTESIAN_POINT ( 'NONE',  ( 18.47654891039378455, -9.465274948371154906, -40.62597590519465740 ) ) ;
#234260=ORIENTED_EDGE ( 'NONE', *, *, #102243, .T. ) ;
#234262=AXIS2_PLACEMENT_3D ( 'NONE', #133666, #54120, #150670 ) ;
#234301=ORIENTED_EDGE ( 'NONE', *, *, #182672, .T. ) ;
#234307=EDGE_CURVE ( 'NONE', #96705, #165365, #196174, .T. ) ;
#234323=CARTESIAN_POINT ( 'NONE',  ( -18.59999999999999787, 7.120270961708750512, -70.65956304183931991 ) ) ;
#234369=DIRECTION ( 'NONE',  ( 0.000000000000000000, -0.9915357197604853789, 0.1298341882520022694 ) ) ;
#234405=CARTESIAN_POINT ( 'NONE',  ( 20.94999999999999929, 1.835341550235569663, -45.05515129256298223 ) ) ;
#234428=ADVANCED_FACE ( 'NONE', ( #185657 ), #43581, .F. ) ;
#234429=EDGE_LOOP ( 'NONE', ( #190983, #57122, #219687, #190625 ) ) ;
#234447=CIRCLE ( 'NONE', #113656, 0.1000000000000028644 ) ;
#234455=CIRCLE ( 'NONE', #151291, 0.09999999999999939493 ) ;
#234480=ORIENTED_EDGE ( 'NONE', *, *, #49665, .F. ) ;
#234489=DIRECTION ( 'NONE',  ( 1.000000000000000000, -7.304098846218133681E-16, 4.217023435051677994E-16 ) ) ;
#234515=DIRECTION ( 'NONE',  ( -0.7071067811865475727, -0.7071067811865475727, -0.000000000000000000 ) ) ;
#234521=DIRECTION ( 'NONE',  ( 1.000000000000000000, 0.000000000000000000, 0.000000000000000000 ) ) ;
#234522=VERTEX_POINT ( 'NONE', #58666 ) ;
#234525=ORIENTED_EDGE ( 'NONE', *, *, #58742, .T. ) ;
#234526=CARTESIAN_POINT ( 'NONE',  ( 18.39999999999999858, -9.599999999988842347, -40.53206939669966857 ) ) ;
#234573=AXIS2_PLACEMENT_3D ( 'NONE', #18058, #20652, #100136 ) ;
#234620=ORIENTED_EDGE ( 'NONE', *, *, #52569, .F. ) ;
#234640=ORIENTED_EDGE ( 'NONE', *, *, #53724, .T. ) ;
#234645=CARTESIAN_POINT ( 'NONE',  ( 21.05000000000000071, 1.115653327213047955E-11, -37.80000000000003268 ) ) ;
#234646=VECTOR ( 'NONE', #152559, 1000.000000000000000 ) ;
#234651=DIRECTION ( 'NONE',  ( -1.000000000000000000, -2.952720810173289112E-16, 0.000000000000000000 ) ) ;
#234660=VECTOR ( 'NONE', #155070, 1000.000000000000000 ) ;
#234670=CARTESIAN_POINT ( 'NONE',  ( -18.43569575749026157, -9.519327731081286714, -40.47297637655933045 ) ) ;
#234680=FACE_OUTER_BOUND ( 'NONE', #242413, .T. ) ;
#234685=DIRECTION ( 'NONE',  ( 0.000000000000000000, -1.000000000000000000, 0.000000000000000000 ) ) ;
#234695=EDGE_CURVE ( 'NONE', #2508, #133095, #113161, .T. ) ;
#234697=ORIENTED_EDGE ( 'NONE', *, *, #4183, .F. ) ;
#234713=DIRECTION ( 'NONE',  ( 0.000000000000000000, -1.000000000000000000, 0.000000000000000000 ) ) ;
#234731=DIRECTION ( 'NONE',  ( 1.000000000000000000, 7.304098846218134667E-16, 0.000000000000000000 ) ) ;
#234740=ORIENTED_EDGE ( 'NONE', *, *, #17010, .F. ) ;
#234757=CARTESIAN_POINT ( 'NONE',  ( -23.25000000000000000, 4.250000000011156409, -45.65000000000000568 ) ) ;
#234797=CIRCLE ( 'NONE', #1541, 0.2000000000000057288 ) ;
#234817=SPHERICAL_SURFACE ( 'NONE', #58762, 0.1000000000000000056 ) ;
#234818=CARTESIAN_POINT ( 'NONE',  ( 18.58725287972291440, -9.566626910680582796, -73.82250480576544760 ) ) ;
#234845=ORIENTED_EDGE ( 'NONE', *, *, #204511, .T. ) ;
#234846=AXIS2_PLACEMENT_3D ( 'NONE', #30996, #28437, #29710 ) ;
#234864=CIRCLE ( 'NONE', #134863, 4.049999999999998934 ) ;
#234879=VERTEX_POINT ( 'NONE', #627 ) ;
#234896=DIRECTION ( 'NONE',  ( -5.603264701231743991E-32, 1.897661533703519897E-16, -1.000000000000000000 ) ) ;
#234913=EDGE_LOOP ( 'NONE', ( #56788, #242264, #46624, #707 ) ) ;
#234920=ORIENTED_EDGE ( 'NONE', *, *, #56844, .F. ) ;
#234943=DIRECTION ( 'NONE',  ( 1.224646799147353207E-16, 1.000000000000000000, 0.000000000000000000 ) ) ;
#234946=FACE_OUTER_BOUND ( 'NONE', #150153, .T. ) ;
#234964=EDGE_LOOP ( 'NONE', ( #71173, #195583, #186899, #27752 ) ) ;
#234972=AXIS2_PLACEMENT_3D ( 'NONE', #241564, #81185, #199892 ) ;
#234979=FACE_OUTER_BOUND ( 'NONE', #93480, .T. ) ;
#234980=CARTESIAN_POINT ( 'NONE',  ( 20.94999999999999929, 5.400000000011154988, -54.59473398108690390 ) ) ;
#234993=LINE ( 'NONE', #195878, #133139 ) ;
#235022=ADVANCED_FACE ( 'NONE', ( #128326 ), #171632, .T. ) ;
#235031=LINE ( 'NONE', #257099, #83526 ) ;
#235033=VECTOR ( 'NONE', #56605, 1000.000000000000000 ) ;
#235050=CARTESIAN_POINT ( 'NONE',  ( 18.49999999999998934, 6.550000000011156231, -43.51702717044002355 ) ) ;
#235052=CARTESIAN_POINT ( 'NONE',  ( -20.54999999999999716, 1.115600667400684642E-11, -33.50000000000000000 ) ) ;
#235064=DIRECTION ( 'NONE',  ( 1.000000000000000000, -0.000000000000000000, -0.000000000000000000 ) ) ;
#235070=DIRECTION ( 'NONE',  ( 0.000000000000000000, 0.000000000000000000, -1.000000000000000000 ) ) ;
#235086=AXIS2_PLACEMENT_3D ( 'NONE', #235052, #215472, #58938 ) ;
#235088=ORIENTED_EDGE ( 'NONE', *, *, #84347, .T. ) ;
#235154=B_SPLINE_CURVE_WITH_KNOTS ( 'NONE', 3,
 ( #160272, #239786, #158992, #61138, #201941, #140673, #45428, #84502, #164099, #104092 ),
 .UNSPECIFIED., .F., .F.,
 ( 4, 3, 3, 4 ),
 ( 0.000000000000000000, 0.0002000000000002884074, 0.001000000000045112589, 0.001967863649472103085 ),
 .UNSPECIFIED. ) ;
#235183=CIRCLE ( 'NONE', #56091, 0.1000000000000028644 ) ;
#235194=ORIENTED_EDGE ( 'NONE', *, *, #116483, .T. ) ;
#235234=DIRECTION ( 'NONE',  ( 3.265361837132813093E-16, -1.000000000000000000, -0.000000000000000000 ) ) ;
#235253=AXIS2_PLACEMENT_3D ( 'NONE', #47882, #208271, #46590 ) ;
#235258=VERTEX_POINT ( 'NONE', #23805 ) ;
#235274=TOROIDAL_SURFACE ( 'NONE', #60312, 0.2000000000000000111, 0.1000000000000000056 ) ;
#235276=AXIS2_PLACEMENT_3D ( 'NONE', #35221, #114724, #155167 ) ;
#235310=VECTOR ( 'NONE', #4181, 1000.000000000000000 ) ;
#235319=CARTESIAN_POINT ( 'NONE',  ( -20.64999999999999858, -8.730841121484170131, -57.40192528101567149 ) ) ;
#235361=AXIS2_PLACEMENT_3D ( 'NONE', #49798, #228457, #71946 ) ;
#235379=VERTEX_POINT ( 'NONE', #26347 ) ;
#235403=CARTESIAN_POINT ( 'NONE',  ( -21.05000000000000071, -11.64999999998884306, -63.89999999999999858 ) ) ;
#235406=CARTESIAN_POINT ( 'NONE',  ( 21.05000000000000071, 8.776282648982402179, -41.98759237851939474 ) ) ;
#235438=EDGE_CURVE ( 'NONE', #138330, #233092, #96193, .T. ) ;
#235448=AXIS2_PLACEMENT_3D ( 'NONE', #206915, #107810, #8716 ) ;
#235489=EDGE_CURVE ( 'NONE', #5569, #209893, #190568, .T. ) ;
#235523=ORIENTED_EDGE ( 'NONE', *, *, #43092, .T. ) ;
#235556=DIRECTION ( 'NONE',  ( -1.000000000000000000, 0.000000000000000000, 0.000000000000000000 ) ) ;
#235567=DIRECTION ( 'NONE',  ( -1.000000000000000000, -1.836970198721029934E-16, -0.000000000000000000 ) ) ;
#235568=DIRECTION ( 'NONE',  ( 0.000000000000000000, -1.000000000000000000, 0.000000000000000000 ) ) ;
#235569=VERTEX_POINT ( 'NONE', #51000 ) ;
#235571=CYLINDRICAL_SURFACE ( 'NONE', #74867, 0.5000000000000004441 ) ;
#235595=CARTESIAN_POINT ( 'NONE',  ( 20.85000000000000142, 6.933893972137497030, -70.78564583437358237 ) ) ;
#235610=DIRECTION ( 'NONE',  ( -0.000000000000000000, -0.000000000000000000, -1.000000000000000000 ) ) ;
#235630=ORIENTED_EDGE ( 'NONE', *, *, #102243, .F. ) ;
#235633=EDGE_LOOP ( 'NONE', ( #90044, #102246, #73576, #10237 ) ) ;
#235673=EDGE_CURVE ( 'NONE', #212292, #133095, #13651, .T. ) ;
#235680=ORIENTED_EDGE ( 'NONE', *, *, #164164, .F. ) ;
#235698=DIRECTION ( 'NONE',  ( 0.000000000000000000, 0.000000000000000000, -1.000000000000000000 ) ) ;
#235708=EDGE_LOOP ( 'NONE', ( #92839, #40471, #48203 ) ) ;
#235724=VECTOR ( 'NONE', #30940, 1000.000000000000000 ) ;
#235752=CIRCLE ( 'NONE', #243953, 0.1000000000000028644 ) ;
#235755=CARTESIAN_POINT ( 'NONE',  ( -20.94999999999999929, 5.850000000011160495, -56.86750277572207324 ) ) ;
#235790=ORIENTED_EDGE ( 'NONE', *, *, #168038, .F. ) ;
#235791=EDGE_CURVE ( 'NONE', #204355, #173321, #127707, .T. ) ;
#235796=EDGE_LOOP ( 'NONE', ( #180857, #9322, #98970, #84792 ) ) ;
#235803=EDGE_CURVE ( 'NONE', #126699, #195545, #188428, .T. ) ;
#235889=DIRECTION ( 'NONE',  ( 0.000000000000000000, -1.000000000000000000, 3.469446951953614189E-14 ) ) ;
#235951=EDGE_CURVE ( 'NONE', #239047, #126429, #100728, .T. ) ;
#235972=CARTESIAN_POINT ( 'NONE',  ( -23.15000000000000213, 1.925233644870972816, -46.23024353312612789 ) ) ;
#235980=DIRECTION ( 'NONE',  ( -0.000000000000000000, -0.000000000000000000, 1.000000000000000000 ) ) ;
#236003=AXIS2_PLACEMENT_3D ( 'NONE', #135888, #36849, #100598 ) ;
#236035=CARTESIAN_POINT ( 'NONE',  ( 20.94999999999999574, -11.74999999998883560, -36.60000000000000853 ) ) ;
#236108=DIRECTION ( 'NONE',  ( 0.000000000000000000, 0.000000000000000000, 1.000000000000000000 ) ) ;
#236170=DIRECTION ( 'NONE',  ( 0.000000000000000000, 1.000000000000000000, 0.000000000000000000 ) ) ;
#236178=CARTESIAN_POINT ( 'NONE',  ( 23.24999999999999289, 11.65000000001116298, -33.50000000000000000 ) ) ;
#236206=EDGE_LOOP ( 'NONE', ( #64034, #131535, #139574, #169598 ) ) ;
#236216=DIRECTION ( 'NONE',  ( 0.000000000000000000, 0.01562499999998609446, -0.9998779222360101304 ) ) ;
#236251=EDGE_CURVE ( 'NONE', #43027, #80050, #105732, .T. ) ;
#236261=CARTESIAN_POINT ( 'NONE',  ( -23.25000000000000000, -11.48912529306489994, -63.89999999999999858 ) ) ;
#236307=CARTESIAN_POINT ( 'NONE',  ( -23.15000000000000213, 11.65000000001115588, -21.75000000000000355 ) ) ;
#236317=DIRECTION ( 'NONE',  ( 0.000000000000000000, 9.769962616701369667E-15, 1.000000000000000000 ) ) ;
#236325=DIRECTION ( 'NONE',  ( 0.000000000000000000, 0.000000000000000000, 1.000000000000000000 ) ) ;
#236332=CARTESIAN_POINT ( 'NONE',  ( -18.50000000000000000, -1.164121893230052995, -74.91484808557160591 ) ) ;
#236374=DIRECTION ( 'NONE',  ( 0.000000000000000000, 0.000000000000000000, -1.000000000000000000 ) ) ;
#236399=ADVANCED_FACE ( 'NONE', ( #254961 ), #5964, .F. ) ;
#236418=FACE_OUTER_BOUND ( 'NONE', #50140, .T. ) ;
#236419=FACE_OUTER_BOUND ( 'NONE', #1604, .T. ) ;
#236430=ORIENTED_EDGE ( 'NONE', *, *, #167461, .T. ) ;
#236483=EDGE_LOOP ( 'NONE', ( #26675, #84446, #116132, #107309 ) ) ;
#236508=DIRECTION ( 'NONE',  ( -1.836970198721029934E-16, 1.000000000000000000, 0.000000000000000000 ) ) ;
#236520=DIRECTION ( 'NONE',  ( 0.000000000000000000, -0.9908441862701596881, -0.1350103645451904977 ) ) ;
#236522=ADVANCED_FACE ( 'NONE', ( #26388 ), #61973, .F. ) ;
#236539=CARTESIAN_POINT ( 'NONE',  ( 18.49999999999999289, 10.29270135741298731, -72.45736188715193293 ) ) ;
#236593=DIRECTION ( 'NONE',  ( 0.000000000000000000, -1.000000000000000000, 0.000000000000000000 ) ) ;
#236622=CARTESIAN_POINT ( 'NONE',  ( 20.94999999999999929, 5.400000000011154988, -45.90526601891310321 ) ) ;
#236645=ORIENTED_EDGE ( 'NONE', *, *, #47275, .F. ) ;
#236661=SPHERICAL_SURFACE ( 'NONE', #119368, 0.1000000000000000056 ) ;
#236668=DIRECTION ( 'NONE',  ( 1.000000000000000000, 0.000000000000000000, 0.000000000000000000 ) ) ;
#236670=CARTESIAN_POINT ( 'NONE',  ( 20.94999999999999929, 1.115600667400684642E-11, -67.00000000000000000 ) ) ;
#236682=CARTESIAN_POINT ( 'NONE',  ( 20.85000000000000142, 1.115600667400684642E-11, -67.00000000000000000 ) ) ;
#236696=CARTESIAN_POINT ( 'NONE',  ( 21.13461538461538680, 8.885417037985614996, -45.85000000000000142 ) ) ;
#236802=ADVANCED_FACE ( 'NONE', ( #160477 ), #122627, .T. ) ;
#236871=EDGE_LOOP ( 'NONE', ( #196616, #166588, #35644, #74630 ) ) ;
#236873=ORIENTED_EDGE ( 'NONE', *, *, #212609, .T. ) ;
#236904=CARTESIAN_POINT ( 'NONE',  ( -23.25000000000000000, 1.910280373842936141, -46.13136785519893834 ) ) ;
#236940=ORIENTED_EDGE ( 'NONE', *, *, #118525, .T. ) ;
#236944=ORIENTED_EDGE ( 'NONE', *, *, #34970, .F. ) ;
#236952=DIRECTION ( 'NONE',  ( 1.000000000000000000, 0.000000000000000000, 0.000000000000000000 ) ) ;
#236958=CARTESIAN_POINT ( 'NONE',  ( -21.44999999999999929, 7.150000000011155876, -45.75000000000000000 ) ) ;
#236976=DIRECTION ( 'NONE',  ( 0.000000000000000000, 0.7397360091702755991, -0.6728971962616832059 ) ) ;
#236979=CYLINDRICAL_SURFACE ( 'NONE', #175729, 0.5000000000000004441 ) ;
#237002=EDGE_CURVE ( 'NONE', #197707, #204139, #52030, .T. ) ;
#237003=CARTESIAN_POINT ( 'NONE',  ( -20.64999999999999858, -8.999999999988844479, -57.10603087734755690 ) ) ;
#237116=EDGE_CURVE ( 'NONE', #224583, #182882, #118797, .T. ) ;
#237119=ORIENTED_EDGE ( 'NONE', *, *, #114467, .T. ) ;
#237124=AXIS2_PLACEMENT_3D ( 'NONE', #94253, #173855, #253327 ) ;
#237238=CARTESIAN_POINT ( 'NONE',  ( -21.14999999893415250, 11.75000000001115197, -40.34449534352650346 ) ) ;
#237250=CARTESIAN_POINT ( 'NONE',  ( -20.64999999999999858, 1.115600667400684642E-11, -67.00000000000000000 ) ) ;
#237258=AXIS2_PLACEMENT_3D ( 'NONE', #73050, #52145, #152583 ) ;
#237259=FACE_OUTER_BOUND ( 'NONE', #188813, .T. ) ;
#237274=CARTESIAN_POINT ( 'NONE',  ( 22.40736611211992368, 1.115600667400684642E-11, -21.85042919245520210 ) ) ;
#237309=FACE_OUTER_BOUND ( 'NONE', #112450, .T. ) ;
#237326=DIRECTION ( 'NONE',  ( 0.000000000000000000, -1.000000000000000000, -0.000000000000000000 ) ) ;
#237327=VERTEX_POINT ( 'NONE', #227799 ) ;
#237329=AXIS2_PLACEMENT_3D ( 'NONE', #143674, #157175, #236668 ) ;
#237331=DIRECTION ( 'NONE',  ( 0.000000000000000000, -1.000000000000000000, -2.891205793294679805E-16 ) ) ;
#237335=AXIS2_PLACEMENT_3D ( 'NONE', #48753, #207865, #47454 ) ;
#237345=CARTESIAN_POINT ( 'NONE',  ( 21.05000000000000071, -0.09999999998884510910, -27.02295361821015263 ) ) ;
#237399=VERTEX_POINT ( 'NONE', #45321 ) ;
#237400=DIRECTION ( 'NONE',  ( 0.000000000000000000, 0.000000000000000000, 1.000000000000000000 ) ) ;
#237404=ORIENTED_EDGE ( 'NONE', *, *, #246433, .T. ) ;
#237432=ORIENTED_EDGE ( 'NONE', *, *, #182304, .F. ) ;
#237481=FACE_OUTER_BOUND ( 'NONE', #11682, .T. ) ;
#237510=FACE_OUTER_BOUND ( 'NONE', #38284, .T. ) ;
#237539=CARTESIAN_POINT ( 'NONE',  ( 18.47688499308724985, -9.464855950272971441, -73.70134775313735531 ) ) ;
#237574=DIRECTION ( 'NONE',  ( 1.000000000000000000, 0.000000000000000000, 0.000000000000000000 ) ) ;
#237623=FACE_OUTER_BOUND ( 'NONE', #246274, .T. ) ;
#237633=CYLINDRICAL_SURFACE ( 'NONE', #20480, 0.09999999999999804878 ) ;
#237635=DIRECTION ( 'NONE',  ( -1.836970198721029934E-16, 1.000000000000000000, 0.000000000000000000 ) ) ;
#237653=TOROIDAL_SURFACE ( 'NONE', #125224, 0.2000000000000000111, 0.1000000000000000056 ) ;
#237660=CYLINDRICAL_SURFACE ( 'NONE', #190770, 0.09999999999999939493 ) ;
#237669=CYLINDRICAL_SURFACE ( 'NONE', #66746, 0.09999999999999781286 ) ;
#237699=ORIENTED_EDGE ( 'NONE', *, *, #15627, .T. ) ;
#237706=CARTESIAN_POINT ( 'NONE',  ( -22.60000000000080789, 0.04781698047652394035, -21.74997756884724964 ) ) ;
#237720=EDGE_LOOP ( 'NONE', ( #95396, #119468, #148861, #90705, #227080, #232115, #34573 ) ) ;
#237725=CARTESIAN_POINT ( 'NONE',  ( -21.05000000000000071, 1.115600667400684642E-11, -33.50000000000000000 ) ) ;
#237753=EDGE_CURVE ( 'NONE', #17420, #95339, #148178, .T. ) ;
#237757=CARTESIAN_POINT ( 'NONE',  ( -22.50000000000000000, 11.65000000001113278, -33.50000000000000000 ) ) ;
#237804=FACE_OUTER_BOUND ( 'NONE', #105412, .T. ) ;
#237834=DIRECTION ( 'NONE',  ( 0.000000000000000000, 0.000000000000000000, -1.000000000000000000 ) ) ;
#237849=AXIS2_PLACEMENT_3D ( 'NONE', #12238, #7069, #229976 ) ;
#237854=TOROIDAL_SURFACE ( 'NONE', #54692, 0.6000000000000006439, 0.1000000000000000056 ) ;
#237855=ORIENTED_EDGE ( 'NONE', *, *, #78976, .F. ) ;
#237856=DIRECTION ( 'NONE',  ( 0.000000000000000000, 0.000000000000000000, -1.000000000000000000 ) ) ;
#237903=ADVANCED_FACE ( 'NONE', ( #83657 ), #131615, .F. ) ;
#237911=ORIENTED_EDGE ( 'NONE', *, *, #235791, .F. ) ;
#237912=DIRECTION ( 'NONE',  ( 0.000000000000000000, 0.000000000000000000, -1.000000000000000000 ) ) ;
#237915=CARTESIAN_POINT ( 'NONE',  ( -21.05000000000000071, -11.48912529306490349, -36.50000000000000711 ) ) ;
#237930=AXIS2_PLACEMENT_3D ( 'NONE', #91345, #7956, #207443 ) ;
#237951=CARTESIAN_POINT ( 'NONE',  ( -21.05000000000000071, -0.01771943329748255566, -27.05891531152877860 ) ) ;
#237969=DIRECTION ( 'NONE',  ( -1.000000000000000000, 0.000000000000000000, 0.000000000000000000 ) ) ;
#237985=CIRCLE ( 'NONE', #125572, 3.999999999999999112 ) ;
#238021=ADVANCED_FACE ( 'NONE', ( #175399 ), #94192, .F. ) ;
#238029=EDGE_LOOP ( 'NONE', ( #33073, #249414, #67789, #19648 ) ) ;
#238046=AXIS2_PLACEMENT_3D ( 'NONE', #30812, #167754, #128604 ) ;
#238059=FACE_OUTER_BOUND ( 'NONE', #51828, .T. ) ;
#238067=ADVANCED_FACE ( 'NONE', ( #179244 ), #127529, .T. ) ;
#238104=CIRCLE ( 'NONE', #163303, 2.100000000000002309 ) ;
#238107=ORIENTED_EDGE ( 'NONE', *, *, #83553, .T. ) ;
#238112=ADVANCED_FACE ( 'NONE', ( #215760 ), #37161, .T. ) ;
#238124=CARTESIAN_POINT ( 'NONE',  ( -18.59999999999999787, -1.835859311432481045, -78.50443916879852679 ) ) ;
#238129=ORIENTED_EDGE ( 'NONE', *, *, #91189, .T. ) ;
#238136=DIRECTION ( 'NONE',  ( 1.000000000000000000, -0.000000000000000000, -0.000000000000000000 ) ) ;
#238139=CARTESIAN_POINT ( 'NONE',  ( 21.05000000000000071, 11.75000000001115907, -59.98519422934606382 ) ) ;
#238149=ORIENTED_EDGE ( 'NONE', *, *, #228048, .T. ) ;
#238174=DIRECTION ( 'NONE',  ( 1.000000000000000000, 0.000000000000000000, 0.000000000000000000 ) ) ;
#238177=CARTESIAN_POINT ( 'NONE',  ( 21.05000000000000071, 1.115600667400684642E-11, -33.50000000000000000 ) ) ;
#238201=CARTESIAN_POINT ( 'NONE',  ( 20.94999999999999929, -8.730841121484171907, -43.09807471898433562 ) ) ;
#238226=DIRECTION ( 'NONE',  ( 0.000000000000000000, 0.000000000000000000, -1.000000000000000000 ) ) ;
#238241=CARTESIAN_POINT ( 'NONE',  ( -18.59999999999999787, 1.115600667400684642E-11, -67.00000000000000000 ) ) ;
#238263=CARTESIAN_POINT ( 'NONE',  ( -23.25000000000000000, 1.115600667400684642E-11, -33.50000000000000000 ) ) ;
#238269=CARTESIAN_POINT ( 'NONE',  ( 21.14999999999999858, 10.71339244341104013, -45.85000000000000142 ) ) ;
#238277=CARTESIAN_POINT ( 'NONE',  ( 20.22894356738450838, 9.278498222849625776, -41.76852290624416497 ) ) ;
#238284=DIRECTION ( 'NONE',  ( 0.000000000000000000, 0.000000000000000000, -1.000000000000000000 ) ) ;
#238287=AXIS2_PLACEMENT_3D ( 'NONE', #96141, #175723, #137835 ) ;
#238294=ORIENTED_EDGE ( 'NONE', *, *, #76404, .F. ) ;
#238308=CARTESIAN_POINT ( 'NONE',  ( -18.40000000000000213, -9.499999999988851584, -40.53206939669966147 ) ) ;
#238315=ORIENTED_EDGE ( 'NONE', *, *, #38426, .T. ) ;
#238335=EDGE_LOOP ( 'NONE', ( #193605, #171700, #220512, #238759, #102342 ) ) ;
#238361=ORIENTED_EDGE ( 'NONE', *, *, #225220, .T. ) ;
#238421=AXIS2_PLACEMENT_3D ( 'NONE', #1879, #18894, #219657 ) ;
#238431=DIRECTION ( 'NONE',  ( 0.000000000000000000, -0.01283462868041992250, -0.9999176327611367654 ) ) ;
#238434=CARTESIAN_POINT ( 'NONE',  ( -23.15000000000000213, 1.115600667400684642E-11, -37.65000000000000568 ) ) ;
#238437=EDGE_LOOP ( 'NONE', ( #222989, #53133, #159196, #76130 ) ) ;
#238481=DIRECTION ( 'NONE',  ( 0.000000000000000000, 0.000000000000000000, 1.000000000000000000 ) ) ;
#238499=CARTESIAN_POINT ( 'NONE',  ( 23.14999999999999858, 1.115600667400684642E-11, -67.00000000000000000 ) ) ;
#238530=DIRECTION ( 'NONE',  ( -0.000000000000000000, -0.000000000000000000, 1.000000000000000000 ) ) ;
#238535=CARTESIAN_POINT ( 'NONE',  ( 20.95556889135987788, 10.62194358774625336, -41.14239422185752204 ) ) ;
#238542=CARTESIAN_POINT ( 'NONE',  ( -18.59999999999999787, 1.866714910068465239, -45.25267524628200988 ) ) ;
#238564=AXIS2_PLACEMENT_3D ( 'NONE', #7138, #247032, #146640 ) ;
#238569=CARTESIAN_POINT ( 'NONE',  ( -23.25000000000000000, -0.1008583690875562017, -21.75043287651061164 ) ) ;
#238592=TOROIDAL_SURFACE ( 'NONE', #184417, 0.2000000000000000111, 0.1000000000000000056 ) ;
#238603=DIRECTION ( 'NONE',  ( 0.000000000000000000, 0.9876197685951252359, -0.1568667991644863424 ) ) ;
#238610=ADVANCED_FACE ( 'NONE', ( #61538 ), #2823, .T. ) ;
#238622=CARTESIAN_POINT ( 'NONE',  ( 21.04999999999999716, -0.03753606327451294855, -27.16772772606433861 ) ) ;
#238660=EDGE_CURVE ( 'NONE', #71326, #206237, #124090, .T. ) ;
#238722=ORIENTED_EDGE ( 'NONE', *, *, #222644, .F. ) ;
#238746=AXIS2_PLACEMENT_3D ( 'NONE', #179585, #199130, #157472 ) ;
#238755=DIRECTION ( 'NONE',  ( 0.000000000000000000, 0.000000000000000000, -1.000000000000000000 ) ) ;
#238759=ORIENTED_EDGE ( 'NONE', *, *, #185934, .F. ) ;
#238767=CIRCLE ( 'NONE', #1418, 0.09999999999999939493 ) ;
#238783=CARTESIAN_POINT ( 'NONE',  ( -20.94999999999999929, 1.115600667400684642E-11, -67.00000000000000000 ) ) ;
#238786=DIRECTION ( 'NONE',  ( 1.000000000000000000, 3.469446951953704435E-14, -2.003086131649669752E-14 ) ) ;
#238792=CARTESIAN_POINT ( 'NONE',  ( -20.64999999999999858, -8.999999999988844479, -57.10603087734755690 ) ) ;
#238797=CYLINDRICAL_SURFACE ( 'NONE', #107977, 0.1000000000000028644 ) ;
#238808=VERTEX_POINT ( 'NONE', #195630 ) ;
#238833=DIRECTION ( 'NONE',  ( 2.952720810173289112E-16, -1.000000000000000000, -0.000000000000000000 ) ) ;
#238863=ADVANCED_FACE ( 'NONE', ( #118659 ), #198165, .F. ) ;
#238929=EDGE_CURVE ( 'NONE', #186437, #67087, #140346, .T. ) ;
#238999=DIRECTION ( 'NONE',  ( 0.000000000000000000, 0.000000000000000000, -1.000000000000000000 ) ) ;
#239023=EDGE_CURVE ( 'NONE', #205142, #19663, #83322, .T. ) ;
#239047=VERTEX_POINT ( 'NONE', #144595 ) ;
#239055=CIRCLE ( 'NONE', #172463, 0.09999999999999939493 ) ;
#239057=CARTESIAN_POINT ( 'NONE',  ( -18.59999999999999787, 11.65000000001115232, -40.51480577065400013 ) ) ;
#239084=ADVANCED_FACE ( 'NONE', ( #49370 ), #126330, .F. ) ;
#239086=( BOUNDED_SURFACE ( )  B_SPLINE_SURFACE ( 3, 2, ( 
 ( #223476, #205194, #102216 ),
 ( #81373, #85227, #83926 ),
 ( #201357, #25313, #82659 ),
 ( #26598, #185653, #47406 ),
 ( #44857, #104789, #181799 ),
 ( #3135, #103522, #124403 ) ),
 .UNSPECIFIED., .F., .F., .F. ) 
 B_SPLINE_SURFACE_WITH_KNOTS ( ( 4, 2, 4 ),
 ( 3, 3 ),
 ( 0.0001300404313046710908, 0.0003183318589266773265, 0.0005066232865486835352 ),
 ( 0.000000000000000000, 1.000000000000000000 ),
 .UNSPECIFIED. ) 
 GEOMETRIC_REPRESENTATION_ITEM ( )  RATIONAL_B_SPLINE_SURFACE ( (
 ( 1.000000000000000000, 0.7071067811865352493, 1.000000000000000000),
 ( 1.000000000000000000, 0.7625113560539796831, 1.000000000000000000),
 ( 1.000000000000000000, 0.8126073484689130266, 1.000000000000000000),
 ( 1.000000000000000000, 0.8923049332731979311, 1.000000000000000000),
 ( 1.000000000000000000, 0.9231914937769916119, 1.000000000000000000),
 ( 1.000000000000000000, 0.9238795325112915124, 1.000000000000000000) ) ) 
 REPRESENTATION_ITEM ( '' )  SURFACE ( )  );
#239094=ADVANCED_FACE ( 'NONE', ( #188880 ), #91060, .F. ) ;
#239102=AXIS2_PLACEMENT_3D ( 'NONE', #75420, #55785, #154955 ) ;
#239103=DIRECTION ( 'NONE',  ( 1.000000000000000000, 0.000000000000000000, -0.000000000000000000 ) ) ;
#239142=AXIS2_PLACEMENT_3D ( 'NONE', #252207, #115276, #31917 ) ;
#239149=CARTESIAN_POINT ( 'NONE',  ( 23.24999999999999645, 1.115600667400684642E-11, -33.50000000000000000 ) ) ;
#239165=FACE_OUTER_BOUND ( 'NONE', #190240, .T. ) ;
#239171=DIRECTION ( 'NONE',  ( 1.000000000000000000, 0.000000000000000000, 0.000000000000000000 ) ) ;
#239179=CARTESIAN_POINT ( 'NONE',  ( 18.49999999999999289, 10.49142135624846439, -58.35000000000000142 ) ) ;
#239190=EDGE_CURVE ( 'NONE', #35121, #25637, #219643, .T. ) ;
#239240=CARTESIAN_POINT ( 'NONE',  ( 21.05000000000000071, 1.115600667400684642E-11, -67.00000000000000000 ) ) ;
#239251=CARTESIAN_POINT ( 'NONE',  ( 23.14999999999999858, 5.600000000011153389, -54.59473398108690390 ) ) ;
#239253=CARTESIAN_POINT ( 'NONE',  ( -21.05000000000000071, -0.01465611850188162056, -27.00331341423204279 ) ) ;
#239257=TOROIDAL_SURFACE ( 'NONE', #126827, 0.2000000000000000111, 0.1000000000000000056 ) ;
#239258=DIRECTION ( 'NONE',  ( 0.000000000000000000, -1.000000000000000000, 0.000000000000000000 ) ) ;
#239269=ORIENTED_EDGE ( 'NONE', *, *, #212642, .T. ) ;
#239279=AXIS2_PLACEMENT_3D ( 'NONE', #246337, #132819, #212361 ) ;
#239298=TOROIDAL_SURFACE ( 'NONE', #214178, 12.97499999999999787, 0.1000000000000000056 ) ;
#239309=B_SPLINE_CURVE_WITH_KNOTS ( 'NONE', 3,
 ( #257060, #160614, #101865, #78461, #61486, #220559 ),
 .UNSPECIFIED., .F., .F.,
 ( 4, 2, 4 ),
 ( 0.000000000000000000, 0.0001497467027049212147, 0.0002994934054098424294 ),
 .UNSPECIFIED. ) ;
#239313=VECTOR ( 'NONE', #227338, 1000.000000000000000 ) ;
#239329=EDGE_LOOP ( 'NONE', ( #195980, #250326, #162300, #90202 ) ) ;
#239388=ORIENTED_EDGE ( 'NONE', *, *, #41505, .F. ) ;
#239389=CIRCLE ( 'NONE', #143705, 0.1000000000000028644 ) ;
#239402=CARTESIAN_POINT ( 'NONE',  ( 21.05000000000000071, 1.115600667400684642E-11, -45.65000000000000568 ) ) ;
#239433=CIRCLE ( 'NONE', #226964, 0.1000000000000028644 ) ;
#239462=EDGE_CURVE ( 'NONE', #138871, #226022, #198983, .T. ) ;
#239491=VERTEX_POINT ( 'NONE', #171312 ) ;
#239527=ORIENTED_EDGE ( 'NONE', *, *, #140878, .F. ) ;
#239528=EDGE_CURVE ( 'NONE', #139486, #41986, #136613, .T. ) ;
#239570=AXIS2_PLACEMENT_3D ( 'NONE', #79645, #236170, #120117 ) ;
#239609=DIRECTION ( 'NONE',  ( -0.7071067811865389130, 0.000000000000000000, 0.7071067811865561215 ) ) ;
#239610=CARTESIAN_POINT ( 'NONE',  ( -18.59999999999999787, 11.65000000001115232, -45.75000000000000000 ) ) ;
#239623=CARTESIAN_POINT ( 'NONE',  ( -18.50000000000000000, 1.115600667400684642E-11, -67.00000000000000000 ) ) ;
#239642=DIRECTION ( 'NONE',  ( 0.000000000000000000, 0.000000000000000000, -1.000000000000000000 ) ) ;
#239660=CARTESIAN_POINT ( 'NONE',  ( 20.94999999999999574, -1.851028230129704522, -45.15391326942249606 ) ) ;
#239681=AXIS2_PLACEMENT_3D ( 'NONE', #173361, #114619, #57187 ) ;
#239726=EDGE_CURVE ( 'NONE', #63552, #182014, #185376, .T. ) ;
#239731=B_SPLINE_CURVE_WITH_KNOTS ( 'NONE', 3,
 ( #184858, #148314, #88302, #89604, #126161, #67482, #167907 ),
 .UNSPECIFIED., .F., .F.,
 ( 4, 3, 4 ),
 ( 0.000000000000000000, 1.860045280646151707E-05, 5.251155757304620461E-05 ),
 .UNSPECIFIED. ) ;
#239786=CARTESIAN_POINT ( 'NONE',  ( 22.42357213249528769, 7.672932386371071445, -33.40091303599844252 ) ) ;
#239789=DIRECTION ( 'NONE',  ( 0.000000000000000000, 0.000000000000000000, 1.000000000000000000 ) ) ;
#239796=ORIENTED_EDGE ( 'NONE', *, *, #204702, .F. ) ;
#239800=EDGE_CURVE ( 'NONE', #139968, #234879, #125413, .T. ) ;
#239813=AXIS2_PLACEMENT_3D ( 'NONE', #96783, #116394, #229911 ) ;
#239871=CARTESIAN_POINT ( 'NONE',  ( 20.94999999999999929, 1.115600667400684642E-11, -71.09999999999999432 ) ) ;
#239929=DIRECTION ( 'NONE',  ( -0.000000000000000000, 1.000000000000000000, 0.000000000000000000 ) ) ;
#239947=EDGE_LOOP ( 'NONE', ( #86002, #161370, #239388, #101436 ) ) ;
#240016=AXIS2_PLACEMENT_3D ( 'NONE', #99791, #56810, #221040 ) ;
#240047=ORIENTED_EDGE ( 'NONE', *, *, #160629, .T. ) ;
#240061=CARTESIAN_POINT ( 'NONE',  ( -20.54999999999999716, -9.399999999988846611, -57.10603087734755690 ) ) ;
#240067=CIRCLE ( 'NONE', #69385, 11.80000000000000426 ) ;
#240097=EDGE_CURVE ( 'NONE', #111434, #52403, #148796, .T. ) ;
#240219=ORIENTED_EDGE ( 'NONE', *, *, #241675, .F. ) ;
#240224=TOROIDAL_SURFACE ( 'NONE', #227708, 0.4000000000000012990, 0.1000000000000000056 ) ;
#240229=EDGE_CURVE ( 'NONE', #119487, #64202, #149813, .T. ) ;
#240245=CARTESIAN_POINT ( 'NONE',  ( -18.59999999999999787, 11.75000000001115552, -54.75000000000000000 ) ) ;
#240257=DIRECTION ( 'NONE',  ( -1.836970198721029934E-16, 1.000000000000000000, 0.000000000000000000 ) ) ;
#240294=DIRECTION ( 'NONE',  ( 1.000000000000000000, 0.000000000000000000, -0.000000000000000000 ) ) ;
#240301=CYLINDRICAL_SURFACE ( 'NONE', #170958, 0.1000000000000028644 ) ;
#240323=ADVANCED_FACE ( 'NONE', ( #226750 ), #28615, .F. ) ;
#240360=VECTOR ( 'NONE', #186265, 1000.000000000000000 ) ;
#240395=EDGE_CURVE ( 'NONE', #14640, #222564, #213601, .T. ) ;
#240410=LINE ( 'NONE', #85141, #120415 ) ;
#240455=DIRECTION ( 'NONE',  ( 1.000000000000000000, -0.000000000000000000, -0.000000000000000000 ) ) ;
#240462=DIRECTION ( 'NONE',  ( -1.000000000000000000, -0.000000000000000000, 0.000000000000000000 ) ) ;
#240463=EDGE_CURVE ( 'NONE', #126285, #199100, #191187, .T. ) ;
#240472=EDGE_CURVE ( 'NONE', #80054, #168194, #36517, .T. ) ;
#240479=LINE ( 'NONE', #87798, #157640 ) ;
#240481=VECTOR ( 'NONE', #152393, 999.9999999999998863 ) ;
#240489=CARTESIAN_POINT ( 'NONE',  ( -23.25000000000000000, 11.75000000001115552, -21.75000000000000355 ) ) ;
#240500=DIRECTION ( 'NONE',  ( -1.000000000000000000, -0.000000000000000000, -0.000000000000000000 ) ) ;
#240516=SPHERICAL_SURFACE ( 'NONE', #47372, 0.1000000000000000056 ) ;
#240562=VERTEX_POINT ( 'NONE', #64796 ) ;
#240574=FACE_BOUND ( 'NONE', #112181, .T. ) ;
#240587=CARTESIAN_POINT ( 'NONE',  ( 21.05000000000000071, -11.64999999998883595, -33.50000000000000000 ) ) ;
#240612=ADVANCED_FACE ( 'NONE', ( #225137 ), #229026, .F. ) ;
#240688=DIRECTION ( 'NONE',  ( -0.000000000000000000, -0.000000000000000000, -1.000000000000000000 ) ) ;
#240709=DIRECTION ( 'NONE',  ( 1.000000000000000000, 0.000000000000000000, 0.000000000000000000 ) ) ;
#240724=ADVANCED_FACE ( 'NONE', ( #35964 ), #212037, .T. ) ;
#240738=ORIENTED_EDGE ( 'NONE', *, *, #46602, .T. ) ;
#240800=EDGE_CURVE ( 'NONE', #135854, #86031, #11556, .T. ) ;
#240839=DIRECTION ( 'NONE',  ( -1.000000000000000000, 0.000000000000000000, 0.000000000000000000 ) ) ;
#240843=CIRCLE ( 'NONE', #36868, 11.64999999999999325 ) ;
#240852=CARTESIAN_POINT ( 'NONE',  ( -20.94999999999999929, -11.48912529306489994, -64.10000000000000853 ) ) ;
#240875=ORIENTED_EDGE ( 'NONE', *, *, #213214, .F. ) ;
#240903=DIRECTION ( 'NONE',  ( -0.000000000000000000, -0.000000000000000000, 1.000000000000000000 ) ) ;
#240928=AXIS2_PLACEMENT_3D ( 'NONE', #1833, #78799, #158399 ) ;
#240993=CIRCLE ( 'NONE', #57807, 0.1000000000000028644 ) ;
#241064=CARTESIAN_POINT ( 'NONE',  ( -18.59999999999999787, -1.164121893230052995, -74.71484808557160306 ) ) ;
#241070=DIRECTION ( 'NONE',  ( -3.265361837132813093E-16, 1.000000000000000000, 0.000000000000000000 ) ) ;
#241089=EDGE_CURVE ( 'NONE', #195545, #104039, #8396, .T. ) ;
#241122=ADVANCED_FACE ( 'NONE', ( #90476 ), #124490, .F. ) ;
#241205=CARTESIAN_POINT ( 'NONE',  ( -21.05000000000000071, 6.400000000011158541, -43.43042463006157305 ) ) ;
#241212=CARTESIAN_POINT ( 'NONE',  ( -20.94999999999999929, -1.261786168553869603, -41.58649896354548048 ) ) ;
#241246=DIRECTION ( 'NONE',  ( -0.000000000000000000, -0.1298341882520022694, -0.9915357197604853789 ) ) ;
#241265=CARTESIAN_POINT ( 'NONE',  ( 20.94999999999999929, 5.000000000011153745, -55.09473398108690390 ) ) ;
#241292=CARTESIAN_POINT ( 'NONE',  ( -21.44999999999999929, 7.350000000011155166, -45.75000000000000000 ) ) ;
#241296=AXIS2_PLACEMENT_3D ( 'NONE', #79565, #20929, #22202 ) ;
#241299=AXIS2_PLACEMENT_3D ( 'NONE', #81022, #158064, #139714 ) ;
#241301=ORIENTED_EDGE ( 'NONE', *, *, #60544, .T. ) ;
#241304=VERTEX_POINT ( 'NONE', #205953 ) ;
#241309=ORIENTED_EDGE ( 'NONE', *, *, #183556, .F. ) ;
#241326=EDGE_LOOP ( 'NONE', ( #37760, #76421, #107065, #217615 ) ) ;
#241333=DIRECTION ( 'NONE',  ( -0.000000000000000000, 0.000000000000000000, 1.000000000000000000 ) ) ;
#241335=ORIENTED_EDGE ( 'NONE', *, *, #220529, .F. ) ;
#241352=AXIS2_PLACEMENT_3D ( 'NONE', #181849, #241812, #146544 ) ;
#241367=ORIENTED_EDGE ( 'NONE', *, *, #235803, .T. ) ;
#241378=DIRECTION ( 'NONE',  ( 1.000000000000000000, 0.000000000000000000, 0.000000000000000000 ) ) ;
#241387=ADVANCED_FACE ( 'NONE', ( #29914 ), #95290, .T. ) ;
#241422=EDGE_CURVE ( 'NONE', #253318, #207476, #91141, .T. ) ;
#241434=CIRCLE ( 'NONE', #83160, 0.09999999999999867328 ) ;
#241454=DIRECTION ( 'NONE',  ( 0.000000000000000000, 0.000000000000000000, 1.000000000000000000 ) ) ;
#241512=VERTEX_POINT ( 'NONE', #89847 ) ;
#241516=FACE_OUTER_BOUND ( 'NONE', #88730, .T. ) ;
#241563=VECTOR ( 'NONE', #93345, 1000.000000000000000 ) ;
#241564=CARTESIAN_POINT ( 'NONE',  ( 21.05000000000000071, -11.64999999998883595, -64.10000000000000853 ) ) ;
#241611=LINE ( 'NONE', #237757, #80482 ) ;
#241613=ORIENTED_EDGE ( 'NONE', *, *, #231876, .T. ) ;
#241664=( BOUNDED_SURFACE ( )  B_SPLINE_SURFACE ( 3, 2, ( 
 ( #224813, #166175, #7056 ),
 ( #158783, #79197, #125720 ),
 ( #218706, #65752, #245678 ),
 ( #40123, #238277, #205245 ),
 ( #59617, #26650, #44913 ),
 ( #196587, #38818, #178343 ),
 ( #226080, #220005, #185708 ),
 ( #19239, #177060, #119642 ),
 ( #199165, #118358, #20548 ),
 ( #25368, #86569, #67041 ),
 ( #257797, #164863, #179619 ),
 ( #146549, #17948, #124455 ) ),
 .UNSPECIFIED., .F., .F., .T. ) 
 B_SPLINE_SURFACE_WITH_KNOTS ( ( 4, 2, 2, 2, 2, 4 ),
 ( 3, 3 ),
 ( 3.174653483277205090, 3.943930578431714018, 4.713207673586222946, 5.482484768740731873, 5.867123316317986337, 6.251761863895240801 ),
 ( 0.000000000000000000, 1.000000000000000000 ),
 .UNSPECIFIED. ) 
 GEOMETRIC_REPRESENTATION_ITEM ( )  RATIONAL_B_SPLINE_SURFACE ( (
 ( 1.000000000000000000, 0.8659465255642401216, 1.000000000000000000),
 ( 1.000000000000000000, 0.8648614068488893469, 1.000000000000000000),
 ( 1.000000000000000000, 0.8489031841323232408, 1.000000000000000000),
 ( 1.000000000000000000, 0.7927507630162343721, 1.000000000000000000),
 ( 1.000000000000000000, 0.7523013859014273663, 1.000000000000000000),
 ( 1.000000000000000000, 0.6616226951191639394, 1.000000000000000000),
 ( 1.000000000000000000, 0.6112214368725455982, 1.000000000000000000),
 ( 1.000000000000000000, 0.5507684314497544031, 1.000000000000000000),
 ( 1.000000000000000000, 0.5333267243152143289, 1.000000000000000000),
 ( 1.000000000000000000, 0.5084565446480221462, 1.000000000000000000),
 ( 1.000000000000000000, 0.5010722703450330995, 1.000000000000000000),
 ( 1.000000000000000000, 0.5001234037138393429, 1.000000000000000000) ) ) 
 REPRESENTATION_ITEM ( '' )  SURFACE ( )  );
#241675=EDGE_CURVE ( 'NONE', #145730, #3674, #253670, .T. ) ;
#241685=LINE ( 'NONE', #202558, #117907 ) ;
#241686=ADVANCED_FACE ( 'NONE', ( #51532 ), #11164, .F. ) ;
#241698=AXIS2_PLACEMENT_3D ( 'NONE', #48443, #107132, #208812 ) ;
#241700=AXIS2_PLACEMENT_3D ( 'NONE', #175053, #212851, #74661 ) ;
#241724=VERTEX_POINT ( 'NONE', #13727 ) ;
#241739=( NAMED_UNIT ( * ) PLANE_ANGLE_UNIT ( ) SI_UNIT ( $, .RADIAN. ) );
#241748=DIRECTION ( 'NONE',  ( 1.000000000000000000, 0.000000000000000000, 0.000000000000000000 ) ) ;
#241782=ORIENTED_EDGE ( 'NONE', *, *, #209530, .T. ) ;
#241811=DIRECTION ( 'NONE',  ( 0.000000000000000000, 0.000000000000000000, -1.000000000000000000 ) ) ;
#241812=DIRECTION ( 'NONE',  ( -1.000000000000000000, -3.265361837132813093E-16, 0.000000000000000000 ) ) ;
#241826=DIRECTION ( 'NONE',  ( -1.000000000000000000, -0.000000000000000000, -0.000000000000000000 ) ) ;
#241829=CIRCLE ( 'NONE', #150266, 0.09999999999999761857 ) ;
#241830=CARTESIAN_POINT ( 'NONE',  ( 18.49999999999999645, -1.162701749926855266, -41.60000000000000142 ) ) ;
#241844=CARTESIAN_POINT ( 'NONE',  ( 22.39999999999999503, 11.65000000001116298, -33.50000000000000000 ) ) ;
#241853=DIRECTION ( 'NONE',  ( 0.000000000000000000, 0.000000000000000000, 1.000000000000000000 ) ) ;
#241857=DIRECTION ( 'NONE',  ( -1.000000000000000000, -2.952720810173289112E-16, 0.000000000000000000 ) ) ;
#241879=FACE_OUTER_BOUND ( 'NONE', #62988, .T. ) ;
#241896=EDGE_LOOP ( 'NONE', ( #81819, #207695, #31874 ) ) ;
#241907=ORIENTED_EDGE ( 'NONE', *, *, #186406, .F. ) ;
#241920=CARTESIAN_POINT ( 'NONE',  ( -20.85000000000000142, 10.33248238083634440, -72.59484654391314962 ) ) ;
#241925=VERTEX_POINT ( 'NONE', #150405 ) ;
#241928=CARTESIAN_POINT ( 'NONE',  ( -22.45372860728439690, 0.01492061955964464615, -21.85020286529612576 ) ) ;
#241941=ADVANCED_FACE ( 'NONE', ( #35610 ), #14759, .F. ) ;
#241984=DIRECTION ( 'NONE',  ( 0.000000000000000000, 0.000000000000000000, -1.000000000000000000 ) ) ;
#241986=ADVANCED_FACE ( 'NONE', ( #100646 ), #237633, .T. ) ;
#242023=ORIENTED_EDGE ( 'NONE', *, *, #160082, .T. ) ;
#242039=CARTESIAN_POINT ( 'NONE',  ( 23.15000000000000213, -8.999999999988842703, -57.60603087734755690 ) ) ;
#242058=VECTOR ( 'NONE', #192683, 1000.000000000000000 ) ;
#242064=FACE_OUTER_BOUND ( 'NONE', #251574, .T. ) ;
#242074=CARTESIAN_POINT ( 'NONE',  ( -23.25000000000000000, 1.115600667400684642E-11, -67.00000000000000000 ) ) ;
#242082=DIRECTION ( 'NONE',  ( 0.000000000000000000, 0.000000000000000000, -1.000000000000000000 ) ) ;
#242113=DIRECTION ( 'NONE',  ( -2.978066053179067751E-16, 1.000000000000000000, 0.000000000000000000 ) ) ;
#242144=VERTEX_POINT ( 'NONE', #164522 ) ;
#242150=ADVANCED_FACE ( 'NONE', ( #65401 ), #53949, .T. ) ;
#242160=CARTESIAN_POINT ( 'NONE',  ( -18.50000000000001066, -9.421308209728413985, -40.74236321405096106 ) ) ;
#242180=ORIENTED_EDGE ( 'NONE', *, *, #3809, .F. ) ;
#242202=DIRECTION ( 'NONE',  ( -0.000000000000000000, -1.000000000000000000, -0.000000000000000000 ) ) ;
#242210=CIRCLE ( 'NONE', #188060, 1.899999999999999023 ) ;
#242212=ORIENTED_EDGE ( 'NONE', *, *, #254212, .T. ) ;
#242227=DIRECTION ( 'NONE',  ( -0.000000000000000000, -1.000000000000000000, 0.000000000000000000 ) ) ;
#242234=AXIS2_PLACEMENT_3D ( 'NONE', #7333, #243370, #242082 ) ;
#242253=EDGE_LOOP ( 'NONE', ( #83717, #132020, #28238, #202804 ) ) ;
#242264=ORIENTED_EDGE ( 'NONE', *, *, #228405, .F. ) ;
#242266=DIRECTION ( 'NONE',  ( -1.000000000000000000, -0.000000000000000000, -0.000000000000000000 ) ) ;
#242277=DIRECTION ( 'NONE',  ( 1.000000000000000000, -0.000000000000000000, 0.000000000000000000 ) ) ;
#242285=CARTESIAN_POINT ( 'NONE',  ( 21.08750232978087524, 10.72486338602132250, -45.72885817299957267 ) ) ;
#242288=DIRECTION ( 'NONE',  ( 0.000000000000000000, 0.000000000000000000, -1.000000000000000000 ) ) ;
#242295=EDGE_CURVE ( 'NONE', #29148, #9105, #99718, .T. ) ;
#242318=ORIENTED_EDGE ( 'NONE', *, *, #6697, .T. ) ;
#242321=EDGE_CURVE ( 'NONE', #207108, #142401, #124879, .T. ) ;
#242345=CARTESIAN_POINT ( 'NONE',  ( 20.85000000000000142, 1.115600667400684642E-11, -67.00000000000000000 ) ) ;
#242346=CARTESIAN_POINT ( 'NONE',  ( 20.94999999999999574, 10.47338541492405994, -41.07865446424855094 ) ) ;
#242377=FACE_OUTER_BOUND ( 'NONE', #6618, .T. ) ;
#242385=EDGE_CURVE ( 'NONE', #176891, #125880, #79506, .T. ) ;
#242397=DIRECTION ( 'NONE',  ( 0.000000000000000000, 0.8660254037844384856, -0.5000000000000003331 ) ) ;
#242404=CARTESIAN_POINT ( 'NONE',  ( -21.45000000000000284, 7.708578643773852157, -54.75000000000000000 ) ) ;
#242413=EDGE_LOOP ( 'NONE', ( #84386, #255398, #137551, #111198 ) ) ;
#242419=AXIS2_PLACEMENT_3D ( 'NONE', #29905, #246362, #32483 ) ;
#242424=DIRECTION ( 'NONE',  ( 2.827886303505249259E-16, -0.8660254037844411501, -0.4999999999999956701 ) ) ;
#242453=ORIENTED_EDGE ( 'NONE', *, *, #99344, .F. ) ;
#242502=ORIENTED_EDGE ( 'NONE', *, *, #80957, .T. ) ;
#242516=CARTESIAN_POINT ( 'NONE',  ( -18.59999999999999787, 6.846123162363745074, -70.73772626684986164 ) ) ;
#242520=CIRCLE ( 'NONE', #130080, 12.97499999999999964 ) ;
#242557=ORIENTED_EDGE ( 'NONE', *, *, #131343, .T. ) ;
#242574=ORIENTED_EDGE ( 'NONE', *, *, #187468, .T. ) ;
#242578=ORIENTED_EDGE ( 'NONE', *, *, #222460, .T. ) ;
#242591=ORIENTED_EDGE ( 'NONE', *, *, #136590, .F. ) ;
#242596=VECTOR ( 'NONE', #27359, 1000.000000000000000 ) ;
#242609=VERTEX_POINT ( 'NONE', #143346 ) ;
#242620=ORIENTED_EDGE ( 'NONE', *, *, #193395, .F. ) ;
#242622=DIRECTION ( 'NONE',  ( 5.421010862427554711E-16, -1.000000000000000000, -3.252606517456533024E-15 ) ) ;
#242701=DIRECTION ( 'NONE',  ( 0.000000000000000000, 0.000000000000000000, -1.000000000000000000 ) ) ;
#242706=EDGE_CURVE ( 'NONE', #166959, #11590, #216634, .T. ) ;
#242735=DIRECTION ( 'NONE',  ( 1.000000000000000000, -0.000000000000000000, -0.000000000000000000 ) ) ;
#242766=ADVANCED_FACE ( 'NONE', ( #111947 ), #99894, .F. ) ;
#242768=CARTESIAN_POINT ( 'NONE',  ( 18.49999999999999645, -1.299733671219632791, -23.52812952286940273 ) ) ;
#242793=EDGE_CURVE ( 'NONE', #31458, #82011, #50646, .T. ) ;
#242798=CARTESIAN_POINT ( 'NONE',  ( -2.995603634470884209E-16, 6.650000000011155876, -54.65000000000000568 ) ) ;
#242801=DIRECTION ( 'NONE',  ( -1.000000000000000000, 0.000000000000000000, 0.000000000000000000 ) ) ;
#242827=LINE ( 'NONE', #244108, #120720 ) ;
#242853=AXIS2_PLACEMENT_3D ( 'NONE', #109904, #12132, #132053 ) ;
#242865=DIRECTION ( 'NONE',  ( 0.000000000000000000, 0.000000000000000000, -1.000000000000000000 ) ) ;
#243018=TOROIDAL_SURFACE ( 'NONE', #30660, 0.9750000000000019762, 0.1000000000000000056 ) ;
#243020=CARTESIAN_POINT ( 'NONE',  ( -21.07946286933445279, 6.329037319018855356, -33.42331615674359568 ) ) ;
#243043=CIRCLE ( 'NONE', #180704, 0.5000000000000004441 ) ;
#243051=DIRECTION ( 'NONE',  ( -1.000000000000000000, -3.265361837132813093E-16, 0.000000000000000000 ) ) ;
#243086=FACE_OUTER_BOUND ( 'NONE', #73733, .T. ) ;
#243087=ORIENTED_EDGE ( 'NONE', *, *, #144061, .T. ) ;
#243089=ORIENTED_EDGE ( 'NONE', *, *, #158525, .T. ) ;
#243118=CARTESIAN_POINT ( 'NONE',  ( 20.94999999999999574, 10.62357026049396680, -40.99194520323055713 ) ) ;
#243203=CARTESIAN_POINT ( 'NONE',  ( -20.85882249326303040, 10.33248238083634796, -72.59484654391314962 ) ) ;
#243204=ORIENTED_EDGE ( 'NONE', *, *, #253283, .F. ) ;
#243221=TOROIDAL_SURFACE ( 'NONE', #147380, 0.6000000000000009770, 0.1000000000000000056 ) ;
#243235=EDGE_CURVE ( 'NONE', #166959, #16861, #175338, .T. ) ;
#243298=ORIENTED_EDGE ( 'NONE', *, *, #92982, .T. ) ;
#243307=DIRECTION ( 'NONE',  ( 0.000000000000000000, 0.000000000000000000, -1.000000000000000000 ) ) ;
#243309=EDGE_CURVE ( 'NONE', #192117, #189211, #158774, .T. ) ;
#243335=LINE ( 'NONE', #42571, #144869 ) ;
#243367=AXIS2_PLACEMENT_3D ( 'NONE', #163014, #177454, #237400 ) ;
#243370=DIRECTION ( 'NONE',  ( 1.000000000000000000, 0.000000000000000000, 0.000000000000000000 ) ) ;
#243395=CARTESIAN_POINT ( 'NONE',  ( 22.50000000000000000, 1.115600667400684642E-11, -33.50000000000000000 ) ) ;
#243425=ORIENTED_EDGE ( 'NONE', *, *, #56105, .F. ) ;
#243434=CARTESIAN_POINT ( 'NONE',  ( 22.45380639572303494, 1.426796658862355976E-07, -21.74956710889332356 ) ) ;
#243435=EDGE_CURVE ( 'NONE', #25677, #115688, #166979, .T. ) ;
#243440=CARTESIAN_POINT ( 'NONE',  ( 20.94999999999999574, 1.835341550235567887, -45.15515129256298366 ) ) ;
#243454=DIRECTION ( 'NONE',  ( 1.000000000000000000, 0.000000000000000000, -0.000000000000000000 ) ) ;
#243459=EDGE_CURVE ( 'NONE', #57195, #104231, #125441, .T. ) ;
#243484=CARTESIAN_POINT ( 'NONE',  ( 21.05000000000000071, 1.115600667400684642E-11, -33.50000000000000000 ) ) ;
#243579=CARTESIAN_POINT ( 'NONE',  ( 21.10642757222115407, 10.72315628916975250, -45.74069752378520093 ) ) ;
#243587=CARTESIAN_POINT ( 'NONE',  ( -20.94999999999999929, 1.115649653272650466E-11, -71.00000000000001421 ) ) ;
#243600=CIRCLE ( 'NONE', #172915, 0.1000000000000028644 ) ;
#243624=DIRECTION ( 'NONE',  ( -1.000000000000000000, 0.000000000000000000, 0.000000000000000000 ) ) ;
#243688=CARTESIAN_POINT ( 'NONE',  ( 21.05000000000000071, 11.60000000001116227, -60.07179676972450011 ) ) ;
#243689=AXIS2_PLACEMENT_3D ( 'NONE', #165326, #242277, #44092 ) ;
#243691=CARTESIAN_POINT ( 'NONE',  ( -18.59999999999999787, 1.736257131608553550, -45.06865232901750318 ) ) ;
#243718=EDGE_CURVE ( 'NONE', #212748, #177537, #204699, .T. ) ;
#243736=PLANE ( 'NONE',  #89361 ) ;
#243758=EDGE_CURVE ( 'NONE', #57243, #22952, #96364, .T. ) ;
#243780=ADVANCED_FACE ( 'NONE', ( #28634 ), #9015, .T. ) ;
#243831=DIRECTION ( 'NONE',  ( 0.000000000000000000, -1.000000000000000000, 0.000000000000000000 ) ) ;
#243844=CARTESIAN_POINT ( 'NONE',  ( 22.39999999999999503, 1.115600667400684642E-11, -25.70922040162662370 ) ) ;
#243858=FACE_OUTER_BOUND ( 'NONE', #22203, .T. ) ;
#243861=EDGE_CURVE ( 'NONE', #226915, #137139, #134081, .T. ) ;
#243890=AXIS2_PLACEMENT_3D ( 'NONE', #59940, #157830, #161205 ) ;
#243902=ORIENTED_EDGE ( 'NONE', *, *, #160376, .T. ) ;
#243953=AXIS2_PLACEMENT_3D ( 'NONE', #105285, #244822, #4909 ) ;
#243958=ORIENTED_EDGE ( 'NONE', *, *, #166601, .F. ) ;
#244000=DIRECTION ( 'NONE',  ( -1.000000000000000000, 0.000000000000000000, 0.000000000000000000 ) ) ;
#244021=AXIS2_PLACEMENT_3D ( 'NONE', #187447, #231708, #28398 ) ;
#244034=DIRECTION ( 'NONE',  ( 0.000000000000000000, 0.000000000000000000, -1.000000000000000000 ) ) ;
#244039=EDGE_LOOP ( 'NONE', ( #194802, #102484, #193795, #247995 ) ) ;
#244072=VECTOR ( 'NONE', #6701, 1000.000000000000227 ) ;
#244081=ADVANCED_FACE ( 'NONE', ( #163933 ), #244728, .T. ) ;
#244108=CARTESIAN_POINT ( 'NONE',  ( -21.05000000000000071, -1.835341550213255957, -45.15515129256298366 ) ) ;
#244115=DIRECTION ( 'NONE',  ( 1.000000000000000000, 0.000000000000000000, 0.000000000000000000 ) ) ;
#244138=CARTESIAN_POINT ( 'NONE',  ( -18.33981767444254984, -9.569575789793166365, -73.81916184372514067 ) ) ;
#244147=EDGE_CURVE ( 'NONE', #95143, #96628, #63230, .T. ) ;
#244156=CIRCLE ( 'NONE', #131744, 0.3999999999999975797 ) ;
#244175=VECTOR ( 'NONE', #187795, 1000.000000000000000 ) ;
#244179=EDGE_CURVE ( 'NONE', #72990, #115688, #86928, .T. ) ;
#244180=ORIENTED_EDGE ( 'NONE', *, *, #231876, .F. ) ;
#244187=ORIENTED_EDGE ( 'NONE', *, *, #228184, .T. ) ;
#244194=DIRECTION ( 'NONE',  ( 0.000000000000000000, 0.000000000000000000, -1.000000000000000000 ) ) ;
#244202=DIRECTION ( 'NONE',  ( 2.978066053179067751E-16, -1.000000000000000000, 0.000000000000000000 ) ) ;
#244220=CIRCLE ( 'NONE', #119348, 0.1999999999999996503 ) ;
#244239=DIRECTION ( 'NONE',  ( 0.000000000000000000, -1.000000000000000000, 0.000000000000000000 ) ) ;
#244245=FACE_OUTER_BOUND ( 'NONE', #221846, .T. ) ;
#244258=EDGE_CURVE ( 'NONE', #186437, #162457, #254738, .T. ) ;
#244298=EDGE_LOOP ( 'NONE', ( #72242, #220160, #233729, #103562 ) ) ;
#244303=ORIENTED_EDGE ( 'NONE', *, *, #203332, .F. ) ;
#244307=AXIS2_PLACEMENT_3D ( 'NONE', #180715, #218516, #21638 ) ;
#244316=CIRCLE ( 'NONE', #106951, 11.65000000000000036 ) ;
#244317=CIRCLE ( 'NONE', #44619, 0.1000000000000000472 ) ;
#244349=CIRCLE ( 'NONE', #19323, 0.1000000000000028644 ) ;
#244424=CARTESIAN_POINT ( 'NONE',  ( -20.64999999999999858, 4.350000000011156054, -45.85000000000000142 ) ) ;
#244445=CIRCLE ( 'NONE', #11431, 0.09999999999999939493 ) ;
#244451=EDGE_CURVE ( 'NONE', #99123, #241925, #80190, .T. ) ;
#244463=CARTESIAN_POINT ( 'NONE',  ( -20.94999999999999929, -1.249999999988843369, -41.50000000000000000 ) ) ;
#244519=CIRCLE ( 'NONE', #132118, 0.1000000000000002831 ) ;
#244530=DIRECTION ( 'NONE',  ( 1.000000000000000000, -0.000000000000000000, 0.000000000000000000 ) ) ;
#244552=CIRCLE ( 'NONE', #248662, 0.09999999999999939493 ) ;
#244598=CARTESIAN_POINT ( 'NONE',  ( -21.65000000000000213, 7.708578643773852157, -45.85000000000000142 ) ) ;
#244605=CARTESIAN_POINT ( 'NONE',  ( 23.15000000000000213, -9.599999999988842347, -57.10603087734755690 ) ) ;
#244638=DIRECTION ( 'NONE',  ( -4.408576920032448588E-17, 0.1350103645451876944, 0.9908441862701601321 ) ) ;
#244665=VECTOR ( 'NONE', #38197, 1000.000000000000000 ) ;
#244666=ORIENTED_EDGE ( 'NONE', *, *, #64412, .T. ) ;
#244671=FACE_OUTER_BOUND ( 'NONE', #21749, .T. ) ;
#244677=CARTESIAN_POINT ( 'NONE',  ( 23.14999999999999503, 6.450000000011156587, -45.85000000000000142 ) ) ;
#244695=VERTEX_POINT ( 'NONE', #127063 ) ;
#244701=ORIENTED_EDGE ( 'NONE', *, *, #118936, .T. ) ;
#244704=CARTESIAN_POINT ( 'NONE',  ( 20.94999999999999929, 1.360870587203197646, -41.57299792709095954 ) ) ;
#244708=CARTESIAN_POINT ( 'NONE',  ( 22.40000000000010161, 1.020945264940608290E-11, -21.74956710754107547 ) ) ;
#244711=DIRECTION ( 'NONE',  ( 1.000000000000000000, -0.000000000000000000, -0.000000000000000000 ) ) ;
#244725=CARTESIAN_POINT ( 'NONE',  ( -21.05000000000000071, 14.05000000001115623, -39.01369507076099552 ) ) ;
#244728=CYLINDRICAL_SURFACE ( 'NONE', #159143, 0.09999999999999939493 ) ;
#244764=EDGE_LOOP ( 'NONE', ( #185512, #182299, #54232 ) ) ;
#244767=ORIENTED_EDGE ( 'NONE', *, *, #64260, .T. ) ;
#244773=DIRECTION ( 'NONE',  ( 0.000000000000000000, 0.000000000000000000, -1.000000000000000000 ) ) ;
#244802=AXIS2_PLACEMENT_3D ( 'NONE', #248775, #243624, #106659 ) ;
#244820=DIRECTION ( 'NONE',  ( 1.000000000000000000, 0.000000000000000000, 0.000000000000000000 ) ) ;
#244822=DIRECTION ( 'NONE',  ( 0.000000000000000000, 1.000000000000000000, -0.000000000000000000 ) ) ;
#244842=CIRCLE ( 'NONE', #95011, 0.09999999999999971412 ) ;
#244852=CARTESIAN_POINT ( 'NONE',  ( 21.09696443733127325, 10.72400988392963228, -45.73477752704822308 ) ) ;
#244873=AXIS2_PLACEMENT_3D ( 'NONE', #156833, #117670, #56396 ) ;
#244896=VERTEX_POINT ( 'NONE', #116494 ) ;
#244899=ADVANCED_FACE ( 'NONE', ( #96881 ), #164048, .T. ) ;
#244914=LINE ( 'NONE', #8879, #185500 ) ;
#244952=ADVANCED_FACE ( 'NONE', ( #40832 ), #251524, .T. ) ;
#244974=VERTEX_POINT ( 'NONE', #25113 ) ;
#244977=VECTOR ( 'NONE', #42469, 1000.000000000000000 ) ;
#244983=CARTESIAN_POINT ( 'NONE',  ( 20.94999999999999929, -8.999999999988842703, -57.50603087734755547 ) ) ;
#245003=B_SPLINE_CURVE_WITH_KNOTS ( 'NONE', 3,
 ( #19063, #198984, #20375, #234249, #175589, #55585, #178166, #94744, #750, #96019 ),
 .UNSPECIFIED., .F., .F.,
 ( 4, 2, 2, 2, 4 ),
 ( 0.000000000000000000, 0.0001584437871624913314, 0.0002376656807437476358, 0.0002772766275343836349, 0.0003168875743250196882 ),
 .UNSPECIFIED. ) ;
#245033=ADVANCED_FACE ( 'NONE', ( #179061 ), #89384, .T. ) ;
#245057=DIRECTION ( 'NONE',  ( 1.000000000000000000, 0.000000000000000000, 0.000000000000000000 ) ) ;
#245078=LINE ( 'NONE', #50696, #34662 ) ;
#245087=CARTESIAN_POINT ( 'NONE',  ( -20.94999999999999929, -1.164121893230052995, -74.91484808557160591 ) ) ;
#245110=DIRECTION ( 'NONE',  ( -1.000000000000000000, -1.875376730785737719E-16, -0.000000000000000000 ) ) ;
#245127=DIRECTION ( 'NONE',  ( 0.000000000000000000, 2.891205793294679805E-16, -1.000000000000000000 ) ) ;
#245133=CARTESIAN_POINT ( 'NONE',  ( -23.24999999999999645, -9.599999999988845900, -73.60018939122203108 ) ) ;
#245137=VERTEX_POINT ( 'NONE', #168499 ) ;
#245171=DIRECTION ( 'NONE',  ( 0.000000000000000000, 0.000000000000000000, 1.000000000000000000 ) ) ;
#245194=CYLINDRICAL_SURFACE ( 'NONE', #102820, 7.900000000000003908 ) ;
#245214=ORIENTED_EDGE ( 'NONE', *, *, #130486, .F. ) ;
#245260=ORIENTED_EDGE ( 'NONE', *, *, #64439, .T. ) ;
#245267=ADVANCED_FACE ( 'NONE', ( #91042 ), #110597, .F. ) ;
#245273=CIRCLE ( 'NONE', #195392, 0.09999999999999971412 ) ;
#245320=AXIS2_PLACEMENT_3D ( 'NONE', #12449, #191093, #251016 ) ;
#245374=ORIENTED_EDGE ( 'NONE', *, *, #228633, .T. ) ;
#245386=AXIS2_PLACEMENT_3D ( 'NONE', #162998, #205950, #186408 ) ;
#245400=DIRECTION ( 'NONE',  ( -0.000000000000000000, 0.9274965247785350586, 0.3738317757009704811 ) ) ;
#245416=DIRECTION ( 'NONE',  ( 1.000000000000000000, -0.000000000000000000, -0.000000000000000000 ) ) ;
#245422=ADVANCED_FACE ( 'NONE', ( #98694 ), #217383, .F. ) ;
#245490=ORIENTED_EDGE ( 'NONE', *, *, #107725, .T. ) ;
#245511=EDGE_LOOP ( 'NONE', ( #242502, #123394, #252816, #204535, #84738 ) ) ;
#245512=SPHERICAL_SURFACE ( 'NONE', #195891, 0.1000000000000000056 ) ;
#245515=FACE_OUTER_BOUND ( 'NONE', #10982, .T. ) ;
#245517=CIRCLE ( 'NONE', #220572, 2.000000000000001776 ) ;
#245543=DIRECTION ( 'NONE',  ( -0.7071067811865388020, 0.7071067811865561215, 0.000000000000000000 ) ) ;
#245545=DIRECTION ( 'NONE',  ( 0.000000000000000000, 0.000000000000000000, -1.000000000000000000 ) ) ;
#245601=CARTESIAN_POINT ( 'NONE',  ( -22.59999999999999787, 0.1000000000111554016, -21.85042919245520210 ) ) ;
#245611=DIRECTION ( 'NONE',  ( 0.000000000000000000, 0.000000000000000000, -1.000000000000000000 ) ) ;
#245641=EDGE_CURVE ( 'NONE', #204996, #40541, #217963, .T. ) ;
#245646=CARTESIAN_POINT ( 'NONE',  ( 21.05000000000000071, -11.48912529306489994, -64.10000000000000853 ) ) ;
#245652=DIRECTION ( 'NONE',  ( 0.000000000000000000, 0.000000000000000000, -1.000000000000000000 ) ) ;
#245653=EDGE_CURVE ( 'NONE', #77835, #96815, #106123, .T. ) ;
#245655=CARTESIAN_POINT ( 'NONE',  ( -20.54999999999999716, 4.350000000011156054, -45.85000000000000142 ) ) ;
#245678=CARTESIAN_POINT ( 'NONE',  ( 20.52683494730037239, 8.980530818312608687, -42.00525272253644715 ) ) ;
#245693=DIRECTION ( 'NONE',  ( -1.000000000000000000, -2.952720810173289112E-16, 0.000000000000000000 ) ) ;
#245731=DIRECTION ( 'NONE',  ( 0.000000000000000000, 0.6728971962616697722, 0.7397360091702875895 ) ) ;
#245744=CONICAL_SURFACE ( 'NONE', #216519, 7.750000000000027534, 0.7853981633974531640 ) ;
#245754=AXIS2_PLACEMENT_3D ( 'NONE', #155575, #250779, #12202 ) ;
#245796=CARTESIAN_POINT ( 'NONE',  ( -22.50000000000000000, 0.09263750062063526303, -21.85030279295925126 ) ) ;
#245804=CYLINDRICAL_SURFACE ( 'NONE', #178227, 0.1000000000000028644 ) ;
#245839=DIRECTION ( 'NONE',  ( -0.000000000000000000, 0.000000000000000000, -1.000000000000000000 ) ) ;
#245876=CARTESIAN_POINT ( 'NONE',  ( 18.54116936837188234, -9.463564198361282820, -40.54854249088825213 ) ) ;
#245900=FACE_OUTER_BOUND ( 'NONE', #19484, .T. ) ;
#245933=EDGE_CURVE ( 'NONE', #4740, #82553, #203758, .T. ) ;
#245950=AXIS2_PLACEMENT_3D ( 'NONE', #178843, #238786, #219204 ) ;
#245983=ORIENTED_EDGE ( 'NONE', *, *, #207607, .F. ) ;
#246006=DIRECTION ( 'NONE',  ( 0.000000000000000000, 0.000000000000000000, -1.000000000000000000 ) ) ;
#246023=DIRECTION ( 'NONE',  ( 0.000000000000000000, 0.000000000000000000, -1.000000000000000000 ) ) ;
#246032=CIRCLE ( 'NONE', #117035, 0.1000000000000000472 ) ;
#246039=AXIS2_PLACEMENT_3D ( 'NONE', #231176, #72091, #75932 ) ;
#246052=EDGE_CURVE ( 'NONE', #118577, #134638, #232823, .T. ) ;
#246080=CIRCLE ( 'NONE', #108705, 0.09999999999999939493 ) ;
#246085=DIRECTION ( 'NONE',  ( 0.000000000000000000, 0.000000000000000000, -1.000000000000000000 ) ) ;
#246113=ORIENTED_EDGE ( 'NONE', *, *, #173553, .T. ) ;
#246150=ORIENTED_EDGE ( 'NONE', *, *, #83781, .F. ) ;
#246159=DIRECTION ( 'NONE',  ( -1.000000000000000000, -0.000000000000000000, 0.000000000000000000 ) ) ;
#246180=EDGE_CURVE ( 'NONE', #161272, #183810, #199691, .T. ) ;
#246182=CARTESIAN_POINT ( 'NONE',  ( -18.59999999999999787, -1.835859311432481045, -78.50443916879852679 ) ) ;
#246185=ORIENTED_EDGE ( 'NONE', *, *, #134829, .F. ) ;
#246197=ORIENTED_EDGE ( 'NONE', *, *, #232993, .T. ) ;
#246222=VECTOR ( 'NONE', #17261, 1000.000000000000000 ) ;
#246248=AXIS2_PLACEMENT_3D ( 'NONE', #102305, #80176, #41114 ) ;
#246255=DIRECTION ( 'NONE',  ( 0.7071067811865475727, -0.7071067811865475727, 0.000000000000000000 ) ) ;
#246261=CIRCLE ( 'NONE', #58783, 0.1000000000000028644 ) ;
#246274=EDGE_LOOP ( 'NONE', ( #115564, #23640, #185247, #73026 ) ) ;
#246297=CYLINDRICAL_SURFACE ( 'NONE', #218669, 0.09999999999999939493 ) ;
#246304=LINE ( 'NONE', #29850, #145281 ) ;
#246336=LINE ( 'NONE', #66415, #53733 ) ;
#246337=CARTESIAN_POINT ( 'NONE',  ( 23.14999999999999147, 1.115600667400684642E-11, -33.50000000000000000 ) ) ;
#246362=DIRECTION ( 'NONE',  ( 0.000000000000000000, 0.1350103645451876666, -0.9908441862701600211 ) ) ;
#246376=CARTESIAN_POINT ( 'NONE',  ( -20.64999999999999858, -8.999999999988846255, -43.39396912265245021 ) ) ;
#246389=LINE ( 'NONE', #147281, #141718 ) ;
#246395=DIRECTION ( 'NONE',  ( 0.000000000000000000, 5.329070518200686707E-15, 1.000000000000000000 ) ) ;
#246413=SPHERICAL_SURFACE ( 'NONE', #162724, 0.1000000000000000056 ) ;
#246433=EDGE_CURVE ( 'NONE', #33939, #54754, #12423, .T. ) ;
#246456=ORIENTED_EDGE ( 'NONE', *, *, #66069, .F. ) ;
#246462=ORIENTED_EDGE ( 'NONE', *, *, #204426, .T. ) ;
#246472=DIRECTION ( 'NONE',  ( 1.000000000000000000, 0.000000000000000000, 0.000000000000000000 ) ) ;
#246518=CARTESIAN_POINT ( 'NONE',  ( -23.15000000000000213, -11.64999999998884483, -63.89999999999999858 ) ) ;
#246520=FACE_OUTER_BOUND ( 'NONE', #249194, .T. ) ;
#246523=FACE_OUTER_BOUND ( 'NONE', #114507, .T. ) ;
#246654=ORIENTED_EDGE ( 'NONE', *, *, #69339, .F. ) ;
#246656=ORIENTED_EDGE ( 'NONE', *, *, #27353, .F. ) ;
#246657=EDGE_CURVE ( 'NONE', #42457, #234879, #62486, .T. ) ;
#246663=AXIS2_PLACEMENT_3D ( 'NONE', #165441, #246255, #66335 ) ;
#246689=VECTOR ( 'NONE', #222368, 1000.000000000000000 ) ;
#246699=ADVANCED_FACE ( 'NONE', ( #251034 ), #149990, .F. ) ;
#246709=ORIENTED_EDGE ( 'NONE', *, *, #193178, .F. ) ;
#246711=CARTESIAN_POINT ( 'NONE',  ( -18.52309608778520911, -9.642476320044279348, -73.71459634116931170 ) ) ;
#246724=ORIENTED_EDGE ( 'NONE', *, *, #241422, .T. ) ;
#246735=FACE_OUTER_BOUND ( 'NONE', #100218, .T. ) ;
#246741=CARTESIAN_POINT ( 'NONE',  ( -23.15000000000000213, -8.999999999988844479, -57.10603087734755690 ) ) ;
#246758=CIRCLE ( 'NONE', #71821, 0.09999999999999939493 ) ;
#246769=DIRECTION ( 'NONE',  ( -0.000000000000000000, -0.4791956752371546724, -0.8777080977375153470 ) ) ;
#246770=ORIENTED_EDGE ( 'NONE', *, *, #216132, .F. ) ;
#246785=LINE ( 'NONE', #207692, #143053 ) ;
#246839=CARTESIAN_POINT ( 'NONE',  ( -18.59999999999999787, 1.637172712981537659, -45.08215336547201701 ) ) ;
#246846=EDGE_LOOP ( 'NONE', ( #166670, #22605, #10782, #113587 ) ) ;
#246857=ORIENTED_EDGE ( 'NONE', *, *, #171940, .F. ) ;
#246874=ADVANCED_FACE ( 'NONE', ( #220602 ), #253, .F. ) ;
#246890=CARTESIAN_POINT ( 'NONE',  ( 21.14999999999999858, 6.650000000011155876, -45.85000000000000142 ) ) ;
#246903=FACE_OUTER_BOUND ( 'NONE', #66506, .T. ) ;
#246995=EDGE_CURVE ( 'NONE', #193788, #173035, #83467, .T. ) ;
#247032=DIRECTION ( 'NONE',  ( 0.000000000000000000, 1.000000000000000000, 0.000000000000000000 ) ) ;
#247058=CARTESIAN_POINT ( 'NONE',  ( -22.47886152344871036, 0.03750093887284931815, -21.85001135695206997 ) ) ;
#247063=AXIS2_PLACEMENT_3D ( 'NONE', #189817, #248500, #32048 ) ;
#247067=DIRECTION ( 'NONE',  ( -0.000000000000000000, 0.000000000000000000, 1.000000000000000000 ) ) ;
#247068=ORIENTED_EDGE ( 'NONE', *, *, #61711, .T. ) ;
#247086=CARTESIAN_POINT ( 'NONE',  ( -23.25000000000000000, -1.835859311432481045, -78.60443916879853532 ) ) ;
#247141=FACE_OUTER_BOUND ( 'NONE', #6853, .T. ) ;
#247161=CARTESIAN_POINT ( 'NONE',  ( 18.49999999999999289, 10.49142135624846439, -58.35000000000000853 ) ) ;
#247175=EDGE_CURVE ( 'NONE', #71326, #67212, #67111, .T. ) ;
#247207=LINE ( 'NONE', #206811, #250353 ) ;
#247218=LINE ( 'NONE', #43896, #117358 ) ;
#247225=DIRECTION ( 'NONE',  ( 0.000000000000000000, 0.000000000000000000, -1.000000000000000000 ) ) ;
#247247=EDGE_CURVE ( 'NONE', #174796, #42536, #33846, .T. ) ;
#247258=EDGE_CURVE ( 'NONE', #25677, #197537, #8669, .T. ) ;
#247271=CIRCLE ( 'NONE', #201485, 0.09999999999999484301 ) ;
#247286=DIRECTION ( 'NONE',  ( 0.000000000000000000, 0.000000000000000000, -1.000000000000000000 ) ) ;
#247337=LINE ( 'NONE', #223912, #82618 ) ;
#247374=CIRCLE ( 'NONE', #39314, 0.09999999999999939493 ) ;
#247390=CARTESIAN_POINT ( 'NONE',  ( 18.59999999999999076, 6.450000000011156587, -43.51702717044002355 ) ) ;
#247403=FACE_OUTER_BOUND ( 'NONE', #210690, .T. ) ;
#247415=CARTESIAN_POINT ( 'NONE',  ( -20.94999999999999929, 1.835341550235569663, -45.05515129256298223 ) ) ;
#247425=CARTESIAN_POINT ( 'NONE',  ( 18.59999999999999432, -9.480686695267811714, -73.94111516875786094 ) ) ;
#247456=DIRECTION ( 'NONE',  ( 1.000000000000000000, 0.000000000000000000, 0.000000000000000000 ) ) ;
#247483=CARTESIAN_POINT ( 'NONE',  ( -20.94999999999999929, 11.65000000001115232, -67.00000000000000000 ) ) ;
#247517=DIRECTION ( 'NONE',  ( 0.000000000000000000, -1.000000000000000000, 0.000000000000000000 ) ) ;
#247536=EDGE_CURVE ( 'NONE', #205763, #234522, #100584, .T. ) ;
#247553=VERTEX_POINT ( 'NONE', #244983 ) ;
#247560=ORIENTED_EDGE ( 'NONE', *, *, #25261, .F. ) ;
#247588=DIRECTION ( 'NONE',  ( -3.265361837132813093E-16, 1.000000000000000000, -0.000000000000000000 ) ) ;
#247619=EDGE_LOOP ( 'NONE', ( #255420, #166572 ) ) ;
#247638=DIRECTION ( 'NONE',  ( 1.000000000000000000, -0.000000000000000000, -0.000000000000000000 ) ) ;
#247663=DIRECTION ( 'NONE',  ( -1.000000000000000000, -0.000000000000000000, 0.000000000000000000 ) ) ;
#247675=CARTESIAN_POINT ( 'NONE',  ( -23.25000000000000000, 1.115600667400684642E-11, -33.50000000000000000 ) ) ;
#247689=CIRCLE ( 'NONE', #64344, 0.1000000000000028644 ) ;
#247745=ORIENTED_EDGE ( 'NONE', *, *, #222644, .T. ) ;
#247773=DIRECTION ( 'NONE',  ( 1.000000000000000000, -0.000000000000000000, -0.000000000000000000 ) ) ;
#247783=ORIENTED_EDGE ( 'NONE', *, *, #132208, .T. ) ;
#247824=CARTESIAN_POINT ( 'NONE',  ( 21.14999999999999858, 1.115600667400684642E-11, -26.95934304829875927 ) ) ;
#247878=CARTESIAN_POINT ( 'NONE',  ( -21.14999999999999858, -0.1008583690875562017, -21.75043287651061164 ) ) ;
#247880=CIRCLE ( 'NONE', #10569, 0.09999999999999939493 ) ;
#247890=CARTESIAN_POINT ( 'NONE',  ( 23.14999999999998437, -11.74999999998884448, -33.50000000000000000 ) ) ;
#247910=DIRECTION ( 'NONE',  ( 0.000000000000000000, 0.000000000000000000, 1.000000000000000000 ) ) ;
#247913=ORIENTED_EDGE ( 'NONE', *, *, #240463, .T. ) ;
#247926=ORIENTED_EDGE ( 'NONE', *, *, #24106, .T. ) ;
#247969=CIRCLE ( 'NONE', #60690, 0.1000000000000000472 ) ;
#247995=ORIENTED_EDGE ( 'NONE', *, *, #174471, .T. ) ;
#248004=DIRECTION ( 'NONE',  ( 1.000000000000000000, 0.000000000000000000, 0.000000000000000000 ) ) ;
#248013=CYLINDRICAL_SURFACE ( 'NONE', #215429, 0.09999999999999939493 ) ;
#248026=EDGE_LOOP ( 'NONE', ( #123038, #199719, #236645 ) ) ;
#248050=CIRCLE ( 'NONE', #239681, 0.6000000000000033085 ) ;
#248076=CARTESIAN_POINT ( 'NONE',  ( -21.05000000000000071, 6.258316057343176197, -33.43429838967790602 ) ) ;
#248080=ORIENTED_EDGE ( 'NONE', *, *, #146038, .T. ) ;
#248093=CARTESIAN_POINT ( 'NONE',  ( 18.49351773456760029, -9.443025695134176445, -40.68532552602730590 ) ) ;
#248096=ORIENTED_EDGE ( 'NONE', *, *, #9076, .F. ) ;
#248099=AXIS2_PLACEMENT_3D ( 'NONE', #70867, #90385, #211642 ) ;
#248107=LINE ( 'NONE', #12099, #44077 ) ;
#248109=EDGE_CURVE ( 'NONE', #32344, #138653, #214523, .T. ) ;
#248166=AXIS2_PLACEMENT_3D ( 'NONE', #88647, #91252, #228196 ) ;
#248189=DIRECTION ( 'NONE',  ( -1.000000000000000000, -2.952720810173289112E-16, 0.000000000000000000 ) ) ;
#248198=CARTESIAN_POINT ( 'NONE',  ( -18.50000000000000000, 9.250000000011157297, -54.85000000000000142 ) ) ;
#248230=LINE ( 'NONE', #109989, #253787 ) ;
#248270=ADVANCED_FACE ( 'NONE', ( #163551 ), #85260, .F. ) ;
#248271=VERTEX_POINT ( 'NONE', #107425 ) ;
#248273=EDGE_CURVE ( 'NONE', #219135, #2368, #162284, .T. ) ;
#248279=ORIENTED_EDGE ( 'NONE', *, *, #209040, .F. ) ;
#248297=B_SPLINE_CURVE_WITH_KNOTS ( 'NONE', 3,
 ( #37929, #57450, #117448, #97843, #39216, #198252, #19636 ),
 .UNSPECIFIED., .F., .F.,
 ( 4, 3, 4 ),
 ( 0.000000000000000000, 0.0009834301579439998740, 0.001767853679402675614 ),
 .UNSPECIFIED. ) ;
#248301=CARTESIAN_POINT ( 'NONE',  ( -20.94999999999999929, 1.835341550235567887, -45.05515129256298223 ) ) ;
#248321=DIRECTION ( 'NONE',  ( 0.000000000000000000, 0.1568667991644863147, 0.9876197685951252359 ) ) ;
#248368=VECTOR ( 'NONE', #55583, 1000.000000000000000 ) ;
#248375=ADVANCED_FACE ( 'NONE', ( #14781 ), #233809, .T. ) ;
#248379=CIRCLE ( 'NONE', #44388, 0.2000000000000057288 ) ;
#248409=DIRECTION ( 'NONE',  ( 0.000000000000000000, 0.000000000000000000, 1.000000000000000000 ) ) ;
#248427=CARTESIAN_POINT ( 'NONE',  ( 18.59999999999999787, -11.74999999998883737, -58.35000000000000142 ) ) ;
#248465=CARTESIAN_POINT ( 'NONE',  ( -23.25000000000000000, -11.74999999998884448, -33.50000000000000000 ) ) ;
#248481=ORIENTED_EDGE ( 'NONE', *, *, #239800, .T. ) ;
#248500=DIRECTION ( 'NONE',  ( 1.000000000000000000, 0.000000000000000000, 0.000000000000000000 ) ) ;
#248527=CIRCLE ( 'NONE', #185989, 0.5000000000000004441 ) ;
#248561=DIRECTION ( 'NONE',  ( -1.000000000000000000, 0.000000000000000000, 0.000000000000000000 ) ) ;
#248576=UNCERTAINTY_MEASURE_WITH_UNIT (LENGTH_MEASURE( 1.000000000000000082E-05 ), #120538, 'distance_accuracy_value', 'NONE');
#248605=ORIENTED_EDGE ( 'NONE', *, *, #120550, .F. ) ;
#248613=ORIENTED_EDGE ( 'NONE', *, *, #23072, .F. ) ;
#248629=DIRECTION ( 'NONE',  ( 1.000000000000000000, -0.000000000000000000, -0.000000000000000000 ) ) ;
#248662=AXIS2_PLACEMENT_3D ( 'NONE', #141690, #119592, #236952 ) ;
#248677=PRODUCT_DEFINITION_FORMATION_WITH_SPECIFIED_SOURCE ( 'ANY', '', #228439, .NOT_KNOWN. ) ;
#248685=DIRECTION ( 'NONE',  ( -0.000000000000000000, 1.000000000000000000, -0.000000000000000000 ) ) ;
#248749=EDGE_LOOP ( 'NONE', ( #118581, #218040, #145319, #104940, #179710, #20484, #257886, #67092, #116734, #184225, #210338, #102718, #178176, #123647, #98704, #255594 ) ) ;
#248763=TOROIDAL_SURFACE ( 'NONE', #136289, 11.90000000000000391, 0.1000000000000000056 ) ;
#248775=CARTESIAN_POINT ( 'NONE',  ( -18.59999999999999787, 1.115600667400684642E-11, -33.50000000000000000 ) ) ;
#248787=ORIENTED_EDGE ( 'NONE', *, *, #185934, .T. ) ;
#248801=CARTESIAN_POINT ( 'NONE',  ( -20.54999999999999716, -8.999999999988844479, -57.10603087734755690 ) ) ;
#248839=EDGE_LOOP ( 'NONE', ( #257365, #6332, #33877, #204710, #125092, #10825 ) ) ;
#248843=VERTEX_POINT ( 'NONE', #100038 ) ;
#248903=DIRECTION ( 'NONE',  ( 0.000000000000000000, -0.1298341882520022694, -0.9915357197604853789 ) ) ;
#248905=CARTESIAN_POINT ( 'NONE',  ( 18.49999999999998934, 10.25000000001115552, -58.25000000000000000 ) ) ;
#248925=ADVANCED_FACE ( 'NONE', ( #118364 ), #42172, .T. ) ;
#248926=DIRECTION ( 'NONE',  ( 0.000000000000000000, -0.9887567792719341719, -0.1495327102803664099 ) ) ;
#248973=DIRECTION ( 'NONE',  ( 1.000000000000000000, -0.000000000000000000, -0.000000000000000000 ) ) ;
#248982=EDGE_CURVE ( 'NONE', #96815, #28931, #179553, .T. ) ;
#248990=EDGE_CURVE ( 'NONE', #117247, #188642, #67097, .T. ) ;
#249002=ORIENTED_EDGE ( 'NONE', *, *, #143947, .T. ) ;
#249012=CARTESIAN_POINT ( 'NONE',  ( 20.04142135623730070, 11.65000000001115943, -54.85000000000000142 ) ) ;
#249021=FACE_OUTER_BOUND ( 'NONE', #187527, .T. ) ;
#249040=B_SPLINE_CURVE_WITH_KNOTS ( 'NONE', 3,
 ( #77185, #96724, #214141, #55038, #255787, #137165, #159321, #197129 ),
 .UNSPECIFIED., .F., .F.,
 ( 4, 2, 2, 4 ),
 ( 0.000000000000000000, 0.0001306511400391282358, 0.0001959767100586970294, 0.0002613022800782658500 ),
 .UNSPECIFIED. ) ;
#249045=ORIENTED_EDGE ( 'NONE', *, *, #160720, .F. ) ;
#249046=CARTESIAN_POINT ( 'NONE',  ( 21.05000000000000071, 6.477067021135910707, -33.60000000000000142 ) ) ;
#249079=DIRECTION ( 'NONE',  ( -1.000000000000000000, 0.000000000000000000, 0.000000000000000000 ) ) ;
#249094=VECTOR ( 'NONE', #132207, 1000.000000000000000 ) ;
#249125=AXIS2_PLACEMENT_3D ( 'NONE', #209314, #250994, #114062 ) ;
#249135=CIRCLE ( 'NONE', #90878, 0.1000000000000001027 ) ;
#249194=EDGE_LOOP ( 'NONE', ( #256741, #61994, #256480, #139642 ) ) ;
#249215=CIRCLE ( 'NONE', #136761, 4.150000000000001243 ) ;
#249250=CARTESIAN_POINT ( 'NONE',  ( -20.54999999999999716, 1.115600667400684642E-11, -67.00000000000000000 ) ) ;
#249252=EDGE_CURVE ( 'NONE', #201039, #190257, #247218, .T. ) ;
#249266=CARTESIAN_POINT ( 'NONE',  ( -23.15000000000000213, 2.000000000011154189, -54.27537807723790309 ) ) ;
#249287=CARTESIAN_POINT ( 'NONE',  ( -21.45000000000000284, 7.708578643773852157, -54.65000000000000568 ) ) ;
#249290=EDGE_CURVE ( 'NONE', #142140, #61821, #192367, .T. ) ;
#249291=DIRECTION ( 'NONE',  ( 0.000000000000000000, 1.000000000000000000, 0.000000000000000000 ) ) ;
#249298=VECTOR ( 'NONE', #43349, 1000.000000000000000 ) ;
#249302=CYLINDRICAL_SURFACE ( 'NONE', #47913, 4.000000000000003553 ) ;
#249307=CARTESIAN_POINT ( 'NONE',  ( -18.59999999999999787, -9.480686695267820596, -73.94111516875786094 ) ) ;
#249321=EDGE_LOOP ( 'NONE', ( #203366, #251440 ) ) ;
#249363=EDGE_LOOP ( 'NONE', ( #218761, #17910, #228806 ) ) ;
#249367=CARTESIAN_POINT ( 'NONE',  ( -20.54999999999999716, 7.250000000011155521, -45.75000000000000000 ) ) ;
#249397=CARTESIAN_POINT ( 'NONE',  ( 18.45036689428335208, -9.490184143317806686, -40.51269582748633269 ) ) ;
#249406=DIRECTION ( 'NONE',  ( 0.000000000000000000, 0.000000000000000000, 1.000000000000000000 ) ) ;
#249414=ORIENTED_EDGE ( 'NONE', *, *, #130813, .T. ) ;
#249421=EDGE_CURVE ( 'NONE', #46286, #188358, #183995, .T. ) ;
#249447=AXIS2_PLACEMENT_3D ( 'NONE', #195633, #19551, #254276 ) ;
#249448=AXIS2_PLACEMENT_3D ( 'NONE', #101493, #178543, #183658 ) ;
#249466=DIRECTION ( 'NONE',  ( 0.000000000000000000, 0.000000000000000000, 1.000000000000000000 ) ) ;
#249484=CARTESIAN_POINT ( 'NONE',  ( 20.94999999999999929, 5.000000000011153745, -45.90526601891310321 ) ) ;
#249490=CARTESIAN_POINT ( 'NONE',  ( 20.94999999999999929, 1.115600667400684642E-11, -64.10000000000000853 ) ) ;
#249537=CARTESIAN_POINT ( 'NONE',  ( 21.53752568622134689, 0.09897446127753155298, -26.71319212545141752 ) ) ;
#249551=CIRCLE ( 'NONE', #91129, 0.1000000000000028644 ) ;
#249610=CARTESIAN_POINT ( 'NONE',  ( -23.25000000000000000, -11.74999999998884448, -63.89999999999999858 ) ) ;
#249646=VERTEX_POINT ( 'NONE', #25332 ) ;
#249654=DIRECTION ( 'NONE',  ( 0.000000000000000000, 8.881784197002011602E-16, -1.000000000000000000 ) ) ;
#249669=EDGE_LOOP ( 'NONE', ( #252894, #154849, #52214, #206603 ) ) ;
#249705=CARTESIAN_POINT ( 'NONE',  ( 20.84999999999998721, 11.75000000001115552, -67.00000000000000000 ) ) ;
#249707=EDGE_CURVE ( 'NONE', #65618, #25637, #17560, .T. ) ;
#249716=AXIS2_PLACEMENT_3D ( 'NONE', #4998, #62442, #160282 ) ;
#249719=( BOUNDED_SURFACE ( )  B_SPLINE_SURFACE ( 3, 2, ( 
 ( #88691, #48308, #129137 ),
 ( #232103, #91297, #170883 ),
 ( #173454, #53449, #127860 ),
 ( #14351, #10475, #93849 ) ),
 .UNSPECIFIED., .F., .F., .F. ) 
 B_SPLINE_SURFACE_WITH_KNOTS ( ( 4, 4 ),
 ( 3, 3 ),
 ( 0.0006461284895273970708, 0.0007503702773986317210 ),
 ( 0.000000000000000000, 1.000000000000000000 ),
 .UNSPECIFIED. ) 
 GEOMETRIC_REPRESENTATION_ITEM ( )  RATIONAL_B_SPLINE_SURFACE ( (
 ( 1.000000000000000000, 0.7071067811865475727, 1.000000000000000000),
 ( 1.000000000000000000, 0.7076476444648772679, 1.000000000000000000),
 ( 1.000000000000000000, 0.7075727925191758194, 1.000000000000000000),
 ( 1.000000000000000000, 0.7071067811865475727, 1.000000000000000000) ) ) 
 REPRESENTATION_ITEM ( '' )  SURFACE ( )  );
#249739=CARTESIAN_POINT ( 'NONE',  ( 21.05000000000000071, 10.62872031401550288, -41.16491356908760224 ) ) ;
#249745=CARTESIAN_POINT ( 'NONE',  ( 18.56308993302899069, 10.38069115533549969, -58.23922263893885543 ) ) ;
#249789=CIRCLE ( 'NONE', #45604, 2.000000000000002665 ) ;
#249820=FACE_OUTER_BOUND ( 'NONE', #184375, .T. ) ;
#249821=ORIENTED_EDGE ( 'NONE', *, *, #109820, .F. ) ;
#249903=ADVANCED_FACE ( 'NONE', ( #36907 ), #138356, .T. ) ;
#249937=CARTESIAN_POINT ( 'NONE',  ( 21.09316766718127667, 6.370153312485568264, -33.46073659768530462 ) ) ;
#249950=DIRECTION ( 'NONE',  ( 1.000000000000000000, 3.265361837132813093E-16, -0.000000000000000000 ) ) ;
#249963=CARTESIAN_POINT ( 'NONE',  ( -18.49513951962167013, -9.437725026666541339, -73.77807257502912819 ) ) ;
#249968=DIRECTION ( 'NONE',  ( 0.000000000000000000, 0.000000000000000000, -1.000000000000000000 ) ) ;
#249988=CARTESIAN_POINT ( 'NONE',  ( 23.24999999999999289, 6.450000000011156587, -21.75000000000000355 ) ) ;
#250000=VERTEX_POINT ( 'NONE', #124120 ) ;
#250021=LINE ( 'NONE', #252573, #197406 ) ;
#250022=CIRCLE ( 'NONE', #121058, 0.6000000000000033085 ) ;
#250056=ORIENTED_EDGE ( 'NONE', *, *, #181160, .T. ) ;
#250080=CARTESIAN_POINT ( 'NONE',  ( -20.99780126800942170, 11.60538868788778544, -60.08735257170526012 ) ) ;
#250082=DIRECTION ( 'NONE',  ( 0.000000000000000000, -1.000000000000000000, 0.000000000000000000 ) ) ;
#250102=CARTESIAN_POINT ( 'NONE',  ( -18.59999999999999787, 11.65000000001115232, -40.51480577065400013 ) ) ;
#250139=CARTESIAN_POINT ( 'NONE',  ( -20.54999999999999716, 2.000000000011154189, -46.72462192276210402 ) ) ;
#250140=CARTESIAN_POINT ( 'NONE',  ( -23.25000000000000000, 1.115600667400684642E-11, -37.54999999999999716 ) ) ;
#250159=DIRECTION ( 'NONE',  ( -0.000000000000000000, -1.000000000000000000, -0.000000000000000000 ) ) ;
#250170=VECTOR ( 'NONE', #219951, 1000.000000000000000 ) ;
#250215=DIRECTION ( 'NONE',  ( 2.694716079187272946E-16, -1.000000000000000000, 0.000000000000000000 ) ) ;
#250218=ORIENTED_EDGE ( 'NONE', *, *, #27939, .T. ) ;
#250219=DIRECTION ( 'NONE',  ( -0.000000000000000000, -0.000000000000000000, -1.000000000000000000 ) ) ;
#250227=VERTEX_POINT ( 'NONE', #90092 ) ;
#250233=DIRECTION ( 'NONE',  ( 0.000000000000000000, 0.000000000000000000, -1.000000000000000000 ) ) ;
#250245=AXIS2_PLACEMENT_3D ( 'NONE', #68721, #67430, #246085 ) ;
#250258=EDGE_CURVE ( 'NONE', #165365, #81754, #74441, .T. ) ;
#250291=CARTESIAN_POINT ( 'NONE',  ( -20.94999999999999929, 5.900000000011102586, -43.71909976465641989 ) ) ;
#250307=CIRCLE ( 'NONE', #67145, 0.1000000000000028644 ) ;
#250326=ORIENTED_EDGE ( 'NONE', *, *, #209040, .T. ) ;
#250353=VECTOR ( 'NONE', #221216, 1000.000000000000000 ) ;
#250359=VERTEX_POINT ( 'NONE', #236035 ) ;
#250385=AXIS2_PLACEMENT_3D ( 'NONE', #70050, #249950, #92152 ) ;
#250398=EDGE_CURVE ( 'NONE', #79720, #145358, #80441, .T. ) ;
#250404=CARTESIAN_POINT ( 'NONE',  ( -20.94999999999999929, 7.021664781911246322, -70.63356540189728605 ) ) ;
#250441=CARTESIAN_POINT ( 'NONE',  ( 20.95512820512820440, 10.62384868372303615, -54.75000000000000000 ) ) ;
#250466=CARTESIAN_POINT ( 'NONE',  ( -22.39999999999999858, 11.75000000001115552, -33.60000000000000142 ) ) ;
#250494=DIRECTION ( 'NONE',  ( 0.000000000000000000, 0.000000000000000000, -1.000000000000000000 ) ) ;
#250527=AXIS2_PLACEMENT_3D ( 'NONE', #237003, #94904, #17938 ) ;
#250591=DIRECTION ( 'NONE',  ( 1.000000000000000000, 0.000000000000000000, 0.000000000000000000 ) ) ;
#250612=DIRECTION ( 'NONE',  ( 0.000000000000000000, 0.000000000000000000, 1.000000000000000000 ) ) ;
#250613=ORIENTED_EDGE ( 'NONE', *, *, #70252, .F. ) ;
#250626=DIRECTION ( 'NONE',  ( -0.000000000000000000, 0.1350103645451626311, 0.9908441862701635738 ) ) ;
#250635=ADVANCED_FACE ( 'NONE', ( #233193 ), #152371, .F. ) ;
#250644=VECTOR ( 'NONE', #33863, 1000.000000000000114 ) ;
#250671=CARTESIAN_POINT ( 'NONE',  ( 18.59999999999999787, -1.835859311432481045, -78.50443916879852679 ) ) ;
#250696=VECTOR ( 'NONE', #46551, 1000.000000000000000 ) ;
#250749=ORIENTED_EDGE ( 'NONE', *, *, #201216, .F. ) ;
#250756=DIRECTION ( 'NONE',  ( 0.000000000000000000, -0.4791956752371546169, -0.8777080977375152360 ) ) ;
#250772=EDGE_CURVE ( 'NONE', #38057, #136029, #188823, .T. ) ;
#250779=DIRECTION ( 'NONE',  ( 1.000000000000000000, -0.000000000000000000, -0.000000000000000000 ) ) ;
#250799=CARTESIAN_POINT ( 'NONE',  ( 22.00411653889210228, 0.09903810579712941931, -26.24655713235960164 ) ) ;
#250814=ORIENTED_EDGE ( 'NONE', *, *, #80957, .F. ) ;
#250863=ORIENTED_EDGE ( 'NONE', *, *, #181382, .T. ) ;
#250910=DIRECTION ( 'NONE',  ( 0.000000000000000000, 0.000000000000000000, -1.000000000000000000 ) ) ;
#250915=ORIENTED_EDGE ( 'NONE', *, *, #134740, .F. ) ;
#250922=DIRECTION ( 'NONE',  ( -0.000000000000000000, 1.000000000000000000, 0.000000000000000000 ) ) ;
#250926=DIRECTION ( 'NONE',  ( 0.000000000000000000, -0.1568667991644863147, -0.9876197685951252359 ) ) ;
#250932=EDGE_CURVE ( 'NONE', #34405, #88666, #68200, .T. ) ;
#250975=DIRECTION ( 'NONE',  ( -0.000000000000000000, -1.000000000000000000, -0.000000000000000000 ) ) ;
#250994=DIRECTION ( 'NONE',  ( 0.000000000000000000, 1.000000000000000000, 0.000000000000000000 ) ) ;
#251013=VERTEX_POINT ( 'NONE', #187324 ) ;
#251016=DIRECTION ( 'NONE',  ( 0.000000000000000000, -0.9654727137038715545, 0.2605042016806676242 ) ) ;
#251034=FACE_OUTER_BOUND ( 'NONE', #226240, .T. ) ;
#251060=SPHERICAL_SURFACE ( 'NONE', #94179, 0.1000000000000000056 ) ;
#251076=ADVANCED_FACE ( 'NONE', ( #219380 ), #160741, .T. ) ;
#251090=CARTESIAN_POINT ( 'NONE',  ( -23.15000000000000213, 2.600000000011156054, -21.75000000000000355 ) ) ;
#251122=UNCERTAINTY_MEASURE_WITH_UNIT (LENGTH_MEASURE( 1.000000000000000082E-05 ), #169260, 'distance_accuracy_value', 'NONE');
#251123=DIRECTION ( 'NONE',  ( 0.000000000000000000, 0.000000000000000000, -1.000000000000000000 ) ) ;
#251134=CARTESIAN_POINT ( 'NONE',  ( 18.49999999999999289, 10.25000000001115552, -54.85000000000000142 ) ) ;
#251192=DIRECTION ( 'NONE',  ( 0.000000000000000000, 0.4999999999999949485, -0.8660254037844415942 ) ) ;
#251196=AXIS2_PLACEMENT_3D ( 'NONE', #217578, #81903, #38984 ) ;
#251209=EDGE_LOOP ( 'NONE', ( #215328, #68452, #56533, #191341, #117732 ) ) ;
#251219=EDGE_LOOP ( 'NONE', ( #74506, #191793, #149763, #44434 ) ) ;
#251229=ADVANCED_FACE ( 'NONE', ( #6764 ), #193293, .T. ) ;
#251255=EDGE_LOOP ( 'NONE', ( #214344, #244701, #249821, #99836 ) ) ;
#251273=CYLINDRICAL_SURFACE ( 'NONE', #11575, 0.09999999999999939493 ) ;
#251348=CARTESIAN_POINT ( 'NONE',  ( -21.05000000000000071, 11.75000000001115197, -59.98519422934605672 ) ) ;
#251395=DIRECTION ( 'NONE',  ( 0.000000000000000000, 0.000000000000000000, -1.000000000000000000 ) ) ;
#251399=ADVANCED_FACE ( 'NONE', ( #174881 ), #78274, .T. ) ;
#251413=DIRECTION ( 'NONE',  ( 2.694716079187272946E-16, -1.000000000000000000, 0.000000000000000000 ) ) ;
#251427=DIRECTION ( 'NONE',  ( 0.000000000000000000, 0.000000000000000000, -1.000000000000000000 ) ) ;
#251440=ORIENTED_EDGE ( 'NONE', *, *, #23388, .T. ) ;
#251473=EDGE_CURVE ( 'NONE', #195077, #186448, #64287, .T. ) ;
#251497=DIRECTION ( 'NONE',  ( -0.000000000000000000, 0.000000000000000000, -1.000000000000000000 ) ) ;
#251502=CARTESIAN_POINT ( 'NONE',  ( -18.59999999999999787, -1.162701749926853712, -41.60000000000000142 ) ) ;
#251517=AXIS2_PLACEMENT_3D ( 'NONE', #218575, #137756, #38681 ) ;
#251522=DIRECTION ( 'NONE',  ( 0.000000000000000000, 0.000000000000000000, 1.000000000000000000 ) ) ;
#251524=TOROIDAL_SURFACE ( 'NONE', #43429, 0.6000000000000004219, 0.1000000000000000056 ) ;
#251554=DIRECTION ( 'NONE',  ( 1.000000000000000000, 0.000000000000000000, 0.000000000000000000 ) ) ;
#251559=DIRECTION ( 'NONE',  ( 0.000000000000000000, -1.000000000000000000, 0.000000000000000000 ) ) ;
#251574=EDGE_LOOP ( 'NONE', ( #51150, #48594, #58111, #111374, #211721 ) ) ;
#251651=ORIENTED_EDGE ( 'NONE', *, *, #49349, .T. ) ;
#251658=DIRECTION ( 'NONE',  ( 1.000000000000000000, 0.000000000000000000, 0.000000000000000000 ) ) ;
#251661=DIRECTION ( 'NONE',  ( -0.000000000000000000, -1.000000000000000000, -5.421010862427649374E-16 ) ) ;
#251671=DIRECTION ( 'NONE',  ( -0.000000000000000000, 1.000000000000000000, 1.626303258728266709E-15 ) ) ;
#251675=DIRECTION ( 'NONE',  ( -1.000000000000000000, -2.952720810173289112E-16, 0.000000000000000000 ) ) ;
#251688=CARTESIAN_POINT ( 'NONE',  ( 20.95512820512820795, 8.876151316299273120, -45.70017285912874883 ) ) ;
#251719=ORIENTED_EDGE ( 'NONE', *, *, #188921, .T. ) ;
#251726=DIRECTION ( 'NONE',  ( 1.000000000000000000, 0.000000000000000000, 0.000000000000000000 ) ) ;
#251730=LINE ( 'NONE', #250441, #91035 ) ;
#251739=CARTESIAN_POINT ( 'NONE',  ( -22.39999999999999858, 11.75000000001115552, -33.40000000000000568 ) ) ;
#251752=TOROIDAL_SURFACE ( 'NONE', #60198, 11.65000000000000036, 0.1000000000000000056 ) ;
#251781=CARTESIAN_POINT ( 'NONE',  ( 18.59117750673696179, 10.33248238083634796, -72.59484654391314962 ) ) ;
#251811=CARTESIAN_POINT ( 'NONE',  ( 18.59999999999999432, -1.162701749926853712, -41.50000000000000000 ) ) ;
#251845=DIRECTION ( 'NONE',  ( -1.000000000000000000, -0.000000000000000000, -0.000000000000000000 ) ) ;
#251849=EDGE_LOOP ( 'NONE', ( #43898, #176174, #222475, #156443 ) ) ;
#251868=EDGE_CURVE ( 'NONE', #69658, #95143, #72881, .T. ) ;
#251877=ORIENTED_EDGE ( 'NONE', *, *, #235791, .T. ) ;
#251935=ORIENTED_EDGE ( 'NONE', *, *, #238660, .F. ) ;
#251939=AXIS2_PLACEMENT_3D ( 'NONE', #207422, #124026, #225650 ) ;
#251952=CARTESIAN_POINT ( 'NONE',  ( -21.05000000000000071, 14.05000000001115623, -39.01369507076099552 ) ) ;
#251972=CARTESIAN_POINT ( 'NONE',  ( 23.24999999999999289, 11.65000000001116298, -33.60000000000000142 ) ) ;
#251980=ORIENTED_EDGE ( 'NONE', *, *, #222001, .T. ) ;
#251984=CYLINDRICAL_SURFACE ( 'NONE', #256862, 12.87499999999999822 ) ;
#251985=ORIENTED_EDGE ( 'NONE', *, *, #102290, .T. ) ;
#252011=CARTESIAN_POINT ( 'NONE',  ( 18.52928932188133970, 10.27928932189250411, -54.85000000000000142 ) ) ;
#252017=DIRECTION ( 'NONE',  ( 1.000000000000000000, 0.000000000000000000, 0.000000000000000000 ) ) ;
#252027=DIRECTION ( 'NONE',  ( 1.000000000000000000, -0.000000000000000000, -0.000000000000000000 ) ) ;
#252036=ORIENTED_EDGE ( 'NONE', *, *, #142428, .F. ) ;
#252040=ORIENTED_EDGE ( 'NONE', *, *, #5033, .F. ) ;
#252093=ORIENTED_EDGE ( 'NONE', *, *, #130354, .T. ) ;
#252100=ORIENTED_EDGE ( 'NONE', *, *, #176262, .T. ) ;
#252126=CARTESIAN_POINT ( 'NONE',  ( 21.09096482362054559, 6.363544365415513937, -33.46055172122586896 ) ) ;
#252140=CARTESIAN_POINT ( 'NONE',  ( 21.05000000000000071, 1.115600667400684642E-11, -33.60000000000000142 ) ) ;
#252188=EDGE_CURVE ( 'NONE', #201418, #195545, #172962, .T. ) ;
#252193=CARTESIAN_POINT ( 'NONE',  ( -18.59999999999999787, -9.399999999988787991, -40.79725975966329088 ) ) ;
#252197=SPHERICAL_SURFACE ( 'NONE', #122913, 0.1000000000000000056 ) ;
#252207=CARTESIAN_POINT ( 'NONE',  ( 22.39999999999999503, 7.790779598384535376, -33.39999999999999858 ) ) ;
#252257=LINE ( 'NONE', #253540, #132376 ) ;
#252269=ORIENTED_EDGE ( 'NONE', *, *, #18531, .F. ) ;
#252283=AXIS2_PLACEMENT_3D ( 'NONE', #155049, #55883, #214980 ) ;
#252337=VERTEX_POINT ( 'NONE', #138883 ) ;
#252341=EDGE_LOOP ( 'NONE', ( #12118, #13636, #162768, #225626 ) ) ;
#252342=DIRECTION ( 'NONE',  ( 2.952720810173289112E-16, -1.000000000000000000, 0.000000000000000000 ) ) ;
#252407=CARTESIAN_POINT ( 'NONE',  ( 23.14999999999999858, 2.100000000011158274, -67.00000000000000000 ) ) ;
#252427=CARTESIAN_POINT ( 'NONE',  ( -23.25000000000000000, -1.149570369564537842, -74.81591248450196474 ) ) ;
#252450=ORIENTED_EDGE ( 'NONE', *, *, #235438, .T. ) ;
#252476=CYLINDRICAL_SURFACE ( 'NONE', #224272, 0.1000000000000028644 ) ;
#252510=CIRCLE ( 'NONE', #94306, 0.09999999999999939493 ) ;
#252514=DIRECTION ( 'NONE',  ( 0.000000000000000000, -0.9908441862701596881, -0.1350103645451904977 ) ) ;
#252516=ORIENTED_EDGE ( 'NONE', *, *, #176371, .T. ) ;
#252519=ADVANCED_FACE ( 'NONE', ( #141063 ), #64821, .F. ) ;
#252522=CARTESIAN_POINT ( 'NONE',  ( 20.95289811251229750, 8.893168004469750088, -42.00180949391852181 ) ) ;
#252538=CARTESIAN_POINT ( 'NONE',  ( 23.14999999999999858, 1.115600667400684642E-11, -67.00000000000000000 ) ) ;
#252546=ORIENTED_EDGE ( 'NONE', *, *, #48834, .T. ) ;
#252573=CARTESIAN_POINT ( 'NONE',  ( -23.25000000000000000, -11.64999999998884483, -64.00000000000000000 ) ) ;
#252587=DIRECTION ( 'NONE',  ( 0.000000000000000000, -0.8777080977375132376, 0.4791956752371582251 ) ) ;
#252629=LINE ( 'NONE', #153598, #117174 ) ;
#252714=AXIS2_PLACEMENT_3D ( 'NONE', #95522, #98054, #194660 ) ;
#252722=CARTESIAN_POINT ( 'NONE',  ( -20.54999999999999716, 9.350000000011156942, -45.75000000000000000 ) ) ;
#252723=FACE_OUTER_BOUND ( 'NONE', #5218, .T. ) ;
#252762=ADVANCED_FACE ( 'NONE', ( #6671 ), #208751, .T. ) ;
#252767=CARTESIAN_POINT ( 'NONE',  ( -20.85000000000000142, 1.115600667400684642E-11, -67.00000000000000000 ) ) ;
#252799=CARTESIAN_POINT ( 'NONE',  ( -20.94999999999999929, 5.900000000011162093, -56.78090023534362984 ) ) ;
#252807=EDGE_CURVE ( 'NONE', #26532, #213775, #7977, .T. ) ;
#252809=CARTESIAN_POINT ( 'NONE',  ( 23.14999999999999503, 11.65000000001116298, -45.65000000000000568 ) ) ;
#252811=EDGE_LOOP ( 'NONE', ( #76094, #133933, #21019, #243958 ) ) ;
#252816=ORIENTED_EDGE ( 'NONE', *, *, #73781, .T. ) ;
#252850=VERTEX_POINT ( 'NONE', #232168 ) ;
#252881=ORIENTED_EDGE ( 'NONE', *, *, #25871, .F. ) ;
#252894=ORIENTED_EDGE ( 'NONE', *, *, #4805, .T. ) ;
#252900=DIRECTION ( 'NONE',  ( 1.000000000000000000, 0.000000000000000000, 0.000000000000000000 ) ) ;
#252907=DIRECTION ( 'NONE',  ( -1.000000000000000000, -2.952720810173289112E-16, 0.000000000000000000 ) ) ;
#252934=CARTESIAN_POINT ( 'NONE',  ( -18.39999999999999858, -9.519327731081281385, -40.47297637655933045 ) ) ;
#252937=CIRCLE ( 'NONE', #194718, 0.1000000000000028644 ) ;
#252943=FACE_OUTER_BOUND ( 'NONE', #66304, .T. ) ;
#252966=DIRECTION ( 'NONE',  ( 0.000000000000000000, -0.5000000000000004441, -0.8660254037844384856 ) ) ;
#252993=AXIS2_PLACEMENT_3D ( 'NONE', #61551, #242735, #227031 ) ;
#253001=CARTESIAN_POINT ( 'NONE',  ( 21.05000000000000071, 1.115600667400684642E-11, -33.50000000000000000 ) ) ;
#253022=DIRECTION ( 'NONE',  ( 0.000000000000000000, 0.000000000000000000, -1.000000000000000000 ) ) ;
#253027=CARTESIAN_POINT ( 'NONE',  ( -18.39999999999999858, -9.599999999988849453, -73.60018939122203108 ) ) ;
#253040=CARTESIAN_POINT ( 'NONE',  ( 21.05000000000000426, 0.03486800302426364129, -27.22991413631085678 ) ) ;
#253063=ORIENTED_EDGE ( 'NONE', *, *, #220734, .T. ) ;
#253077=CARTESIAN_POINT ( 'NONE',  ( 23.25000000000000000, -11.74999999998883560, -63.89999999999999858 ) ) ;
#253110=VERTEX_POINT ( 'NONE', #170463 ) ;
#253144=ORIENTED_EDGE ( 'NONE', *, *, #182304, .T. ) ;
#253151=CARTESIAN_POINT ( 'NONE',  ( 21.12802099929860944, 8.780552590233368093, -45.74818998493161359 ) ) ;
#253159=CARTESIAN_POINT ( 'NONE',  ( 20.94999999999999929, 4.813084112160680661, -45.44151775652382952 ) ) ;
#253165=ORIENTED_EDGE ( 'NONE', *, *, #217386, .T. ) ;
#253178=DIRECTION ( 'NONE',  ( 1.000000000000000000, 0.000000000000000000, 0.000000000000000000 ) ) ;
#253229=ORIENTED_EDGE ( 'NONE', *, *, #111114, .F. ) ;
#253269=CARTESIAN_POINT ( 'NONE',  ( 21.05000000000000071, -9.499999999988844479, -57.10603087734755690 ) ) ;
#253277=ORIENTED_EDGE ( 'NONE', *, *, #207799, .T. ) ;
#253283=EDGE_CURVE ( 'NONE', #168869, #179511, #210757, .T. ) ;
#253295=ADVANCED_FACE ( 'NONE', ( #102391 ), #255013, .T. ) ;
#253297=CARTESIAN_POINT ( 'NONE',  ( -18.39999999999999858, -9.682403433465239573, -73.65684337741279819 ) ) ;
#253307=LINE ( 'NONE', #29183, #92651 ) ;
#253309=VECTOR ( 'NONE', #189312, 1000.000000000000000 ) ;
#253314=AXIS2_PLACEMENT_3D ( 'NONE', #188296, #205279, #106174 ) ;
#253318=VERTEX_POINT ( 'NONE', #87972 ) ;
#253327=DIRECTION ( 'NONE',  ( 1.000000000000000000, 0.000000000000000000, 0.000000000000000000 ) ) ;
#253362=EDGE_CURVE ( 'NONE', #237327, #173389, #158922, .T. ) ;
#253374=CARTESIAN_POINT ( 'NONE',  ( 20.94999999999999574, -1.349084418615859482, -41.48649896354548616 ) ) ;
#253383=AXIS2_PLACEMENT_3D ( 'NONE', #200754, #22137, #143338 ) ;
#253387=EDGE_LOOP ( 'NONE', ( #172578, #65279, #228548, #89955 ) ) ;
#253393=ADVANCED_FACE ( 'NONE', ( #172729 ), #252197, .T. ) ;
#253396=CARTESIAN_POINT ( 'NONE',  ( 21.05000000000000071, 4.813084112160684214, -55.05848224347618469 ) ) ;
#253398=AXIS2_PLACEMENT_3D ( 'NONE', #31402, #110901, #112211 ) ;
#253402=CARTESIAN_POINT ( 'NONE',  ( 21.05000000000000071, 11.75000000001116263, -59.98519422934605672 ) ) ;
#253412=CARTESIAN_POINT ( 'NONE',  ( 21.05000000000000071, 6.477552182504587641, -33.59999996530019928 ) ) ;
#253432=EDGE_CURVE ( 'NONE', #184556, #100083, #143738, .T. ) ;
#253458=DIRECTION ( 'NONE',  ( 1.000000000000000000, 0.000000000000000000, 0.000000000000000000 ) ) ;
#253459=ORIENTED_EDGE ( 'NONE', *, *, #146369, .T. ) ;
#253488=VERTEX_POINT ( 'NONE', #150553 ) ;
#253497=DIRECTION ( 'NONE',  ( 0.000000000000000000, -0.8700118002898321601, 0.4930308989875230030 ) ) ;
#253524=DIRECTION ( 'NONE',  ( 1.000000000000000000, 0.000000000000000000, -0.000000000000000000 ) ) ;
#253540=CARTESIAN_POINT ( 'NONE',  ( 18.49999999999998934, 11.65000000001115943, -58.25000000000000000 ) ) ;
#253542=DIRECTION ( 'NONE',  ( 0.000000000000000000, -1.000000000000000000, 0.000000000000000000 ) ) ;
#253548=FACE_OUTER_BOUND ( 'NONE', #56420, .T. ) ;
#253574=CARTESIAN_POINT ( 'NONE',  ( 20.94999999999999574, 8.926614585098251453, -41.97168301922312850 ) ) ;
#253587=DIRECTION ( 'NONE',  ( 1.000000000000000000, 0.000000000000000000, 0.000000000000000000 ) ) ;
#253597=DIRECTION ( 'NONE',  ( 0.000000000000000000, -0.4999999999999649170, 0.8660254037844589137 ) ) ;
#253616=DIRECTION ( 'NONE',  ( 0.000000000000000000, -6.308085367188393199E-16, -1.000000000000000000 ) ) ;
#253644=AXIS2_PLACEMENT_3D ( 'NONE', #172276, #194387, #213919 ) ;
#253647=EDGE_CURVE ( 'NONE', #102738, #163909, #206293, .T. ) ;
#253670=CIRCLE ( 'NONE', #212009, 0.4000000000000045186 ) ;
#253719=FACE_OUTER_BOUND ( 'NONE', #10422, .T. ) ;
#253778=EDGE_CURVE ( 'NONE', #36405, #181631, #72000, .T. ) ;
#253781=EDGE_LOOP ( 'NONE', ( #200452, #140977, #69572, #72343 ) ) ;
#253787=VECTOR ( 'NONE', #190857, 1000.000000000000000 ) ;
#253802=CARTESIAN_POINT ( 'NONE',  ( 23.24999999999999645, 3.900000000011155432, -67.00000000000000000 ) ) ;
#253838=AXIS2_PLACEMENT_3D ( 'NONE', #233691, #134553, #77164 ) ;
#253852=AXIS2_PLACEMENT_3D ( 'NONE', #127953, #45840, #144922 ) ;
#253860=DIRECTION ( 'NONE',  ( 0.000000000000000000, 0.000000000000000000, -1.000000000000000000 ) ) ;
#253861=FACE_OUTER_BOUND ( 'NONE', #148762, .T. ) ;
#253875=( NAMED_UNIT ( * ) SI_UNIT ( $, .STERADIAN. ) SOLID_ANGLE_UNIT ( ) );
#253876=AXIS2_PLACEMENT_3D ( 'NONE', #223742, #145497, #146757 ) ;
#253911=EDGE_CURVE ( 'NONE', #88007, #117767, #128115, .T. ) ;
#253979=CARTESIAN_POINT ( 'NONE',  ( -21.05000000000000071, -0.09999999998884338825, -21.85000000000000142 ) ) ;
#253985=CARTESIAN_POINT ( 'NONE',  ( -20.54999999999999716, 2.000000000011154189, -46.72462192276210402 ) ) ;
#254028=DIRECTION ( 'NONE',  ( 0.000000000000000000, 0.1350103645451876666, 0.9908441862701600211 ) ) ;
#254070=CIRCLE ( 'NONE', #237335, 0.1000000000000004496 ) ;
#254075=CARTESIAN_POINT ( 'NONE',  ( -21.05000000000000071, 1.115600667400684642E-11, -55.30000000000000426 ) ) ;
#254111=ORIENTED_EDGE ( 'NONE', *, *, #51924, .T. ) ;
#254120=LINE ( 'NONE', #195475, #234660 ) ;
#254148=SPHERICAL_SURFACE ( 'NONE', #164946, 0.1000000000000000056 ) ;
#254158=AXIS2_PLACEMENT_3D ( 'NONE', #68012, #169725, #171019 ) ;
#254192=ADVANCED_FACE ( 'NONE', ( #110799 ), #149955, .T. ) ;
#254212=EDGE_CURVE ( 'NONE', #248271, #36408, #202372, .T. ) ;
#254215=EDGE_CURVE ( 'NONE', #6281, #100799, #227475, .T. ) ;
#254224=FACE_OUTER_BOUND ( 'NONE', #164539, .T. ) ;
#254229=CARTESIAN_POINT ( 'NONE',  ( 20.94999999999999574, 10.47338541492405994, -41.07865446424855094 ) ) ;
#254234=DIRECTION ( 'NONE',  ( 0.000000000000000000, 0.000000000000000000, 1.000000000000000000 ) ) ;
#254239=CARTESIAN_POINT ( 'NONE',  ( 22.48508240969612615, 0.04627641452807086664, -21.84998926842643385 ) ) ;
#254247=CARTESIAN_POINT ( 'NONE',  ( -22.50000000000000000, 1.115600667400684642E-11, -27.25000000000000355 ) ) ;
#254276=DIRECTION ( 'NONE',  ( 0.000000000000000000, 0.000000000000000000, -1.000000000000000000 ) ) ;
#254288=DIRECTION ( 'NONE',  ( 1.000000000000000000, 0.000000000000000000, 0.000000000000000000 ) ) ;
#254294=ADVANCED_FACE ( 'NONE', ( #113375 ), #254148, .F. ) ;
#254396=AXIS2_PLACEMENT_3D ( 'NONE', #150061, #152641, #16965 ) ;
#254403=AXIS2_PLACEMENT_3D ( 'NONE', #159459, #78616, #238999 ) ;
#254438=ORIENTED_EDGE ( 'NONE', *, *, #156724, .F. ) ;
#254483=SPHERICAL_SURFACE ( 'NONE', #186839, 0.1000000000000000056 ) ;
#254489=PLANE ( 'NONE',  #100674 ) ;
#254493=CIRCLE ( 'NONE', #75487, 11.65000000000000036 ) ;
#254499=EDGE_CURVE ( 'NONE', #210104, #200509, #56761, .T. ) ;
#254522=VERTEX_POINT ( 'NONE', #149321 ) ;
#254525=EDGE_LOOP ( 'NONE', ( #27438, #94550, #136967, #96289 ) ) ;
#254539=ORIENTED_EDGE ( 'NONE', *, *, #72040, .F. ) ;
#254581=EDGE_LOOP ( 'NONE', ( #97374, #37666, #153734, #115520, #19414 ) ) ;
#254615=VERTEX_POINT ( 'NONE', #228843 ) ;
#254678=CARTESIAN_POINT ( 'NONE',  ( 21.05000000000000071, 5.850000000011105428, -43.63249722427796939 ) ) ;
#254692=ORIENTED_EDGE ( 'NONE', *, *, #103472, .T. ) ;
#254737=ORIENTED_EDGE ( 'NONE', *, *, #73687, .F. ) ;
#254738=CIRCLE ( 'NONE', #96546, 0.1000000000000008937 ) ;
#254743=ADVANCED_FACE ( 'NONE', ( #227239 ), #184262, .F. ) ;
#254766=CARTESIAN_POINT ( 'NONE',  ( 18.49999999999998934, 6.450000000011156587, -43.51702717044002355 ) ) ;
#254772=TOROIDAL_SURFACE ( 'NONE', #138108, 12.77499999999999858, 0.1000000000000000056 ) ;
#254774=ORIENTED_EDGE ( 'NONE', *, *, #144061, .F. ) ;
#254808=CIRCLE ( 'NONE', #21644, 0.1000000000000001860 ) ;
#254813=CARTESIAN_POINT ( 'NONE',  ( -18.59999999999999787, 11.65000000001115232, -40.51480577065400013 ) ) ;
#254880=VECTOR ( 'NONE', #205980, 1000.000000000000114 ) ;
#254889=ORIENTED_EDGE ( 'NONE', *, *, #199095, .T. ) ;
#254919=ORIENTED_EDGE ( 'NONE', *, *, #200813, .T. ) ;
#254929=CARTESIAN_POINT ( 'NONE',  ( -20.93284271247462058, 11.75000000001115019, -59.98519422934605672 ) ) ;
#254948=AXIS2_PLACEMENT_3D ( 'NONE', #49284, #6297, #47996 ) ;
#254961=FACE_OUTER_BOUND ( 'NONE', #82097, .T. ) ;
#254967=DIRECTION ( 'NONE',  ( -1.000000000000000000, -0.000000000000000000, -0.000000000000000000 ) ) ;
#254989=CARTESIAN_POINT ( 'NONE',  ( -20.64999999999999858, -8.999999999988846255, -43.39396912265245021 ) ) ;
#254993=CIRCLE ( 'NONE', #167601, 0.09999999999999939493 ) ;
#255013=CYLINDRICAL_SURFACE ( 'NONE', #173401, 0.09999999999999892308 ) ;
#255029=ORIENTED_EDGE ( 'NONE', *, *, #181825, .F. ) ;
#255053=ADVANCED_FACE ( 'NONE', ( #15937 ), #254483, .T. ) ;
#255078=DIRECTION ( 'NONE',  ( 1.000000000000000000, -0.000000000000000000, -0.000000000000000000 ) ) ;
#255107=PLANE ( 'NONE',  #185838 ) ;
#255109=DIRECTION ( 'NONE',  ( -0.000000000000000000, -0.000000000000000000, 1.000000000000000000 ) ) ;
#255146=FACE_OUTER_BOUND ( 'NONE', #116914, .T. ) ;
#255177=DIRECTION ( 'NONE',  ( 0.000000000000000000, 0.000000000000000000, -1.000000000000000000 ) ) ;
#255179=ADVANCED_FACE ( 'NONE', ( #146117 ), #170306, .T. ) ;
#255180=VERTEX_POINT ( 'NONE', #161862 ) ;
#255230=DIRECTION ( 'NONE',  ( -1.000000000000000000, -0.000000000000000000, 0.000000000000000000 ) ) ;
#255250=DIRECTION ( 'NONE',  ( 2.952720810173289112E-16, -1.000000000000000000, 0.000000000000000000 ) ) ;
#255257=CARTESIAN_POINT ( 'NONE',  ( -18.46856557590792747, -9.474215907775342060, -40.60198624088229735 ) ) ;
#255260=DIRECTION ( 'NONE',  ( 0.000000000000000000, 0.000000000000000000, -1.000000000000000000 ) ) ;
#255275=CIRCLE ( 'NONE', #42960, 0.1999999999999987899 ) ;
#255290=CARTESIAN_POINT ( 'NONE',  ( -22.24259225415828567, 7.491937870576586889, -33.40093411654716959 ) ) ;
#255305=DIRECTION ( 'NONE',  ( -1.000000000000000000, -0.000000000000000000, -0.000000000000000000 ) ) ;
#255367=CARTESIAN_POINT ( 'NONE',  ( -21.45000000000000284, 7.708578643773852157, -45.75000000000000000 ) ) ;
#255373=EDGE_CURVE ( 'NONE', #1139, #172722, #199395, .T. ) ;
#255374=EDGE_CURVE ( 'NONE', #1409, #192117, #256725, .T. ) ;
#255387=ORIENTED_EDGE ( 'NONE', *, *, #70619, .F. ) ;
#255398=ORIENTED_EDGE ( 'NONE', *, *, #153479, .T. ) ;
#255411=CARTESIAN_POINT ( 'NONE',  ( 18.59999999999999076, -1.835859311432481045, -78.60443916879853532 ) ) ;
#255415=ADVANCED_FACE ( 'NONE', ( #177275 ), #184312, .T. ) ;
#255417=CARTESIAN_POINT ( 'NONE',  ( 23.14999999999999503, 6.650000000011155876, -54.75000000000000000 ) ) ;
#255418=ORIENTED_EDGE ( 'NONE', *, *, #39115, .T. ) ;
#255420=ORIENTED_EDGE ( 'NONE', *, *, #209295, .T. ) ;
#255452=DIRECTION ( 'NONE',  ( -1.000000000000000000, 9.012599976028471648E-15, 6.882867235861662930E-14 ) ) ;
#255462=DIRECTION ( 'NONE',  ( -3.265361837132813093E-16, 1.000000000000000000, 0.000000000000000000 ) ) ;
#255467=CARTESIAN_POINT ( 'NONE',  ( 20.94999999999999929, -9.399999999988844834, -57.10603087734755690 ) ) ;
#255491=CARTESIAN_POINT ( 'NONE',  ( 22.47809213839789066, 0.03753706763967752658, -21.85002666521219794 ) ) ;
#255518=CARTESIAN_POINT ( 'NONE',  ( 21.05095171578076574, 8.776179878782192745, -45.66587327663788187 ) ) ;
#255520=CARTESIAN_POINT ( 'NONE',  ( -22.47071067811865319, 1.115600667400684642E-11, -33.50000000000000000 ) ) ;
#255578=CYLINDRICAL_SURFACE ( 'NONE', #36804, 0.09999999999999939493 ) ;
#255594=ORIENTED_EDGE ( 'NONE', *, *, #39115, .F. ) ;
#255610=CARTESIAN_POINT ( 'NONE',  ( 18.41815437325349691, -9.498709853130264946, -73.60394583880211883 ) ) ;
#255629=EDGE_CURVE ( 'NONE', #110700, #12767, #41608, .T. ) ;
#255640=ORIENTED_EDGE ( 'NONE', *, *, #88190, .T. ) ;
#255653=AXIS2_PLACEMENT_3D ( 'NONE', #224760, #61856, #121837 ) ;
#255687=DIRECTION ( 'NONE',  ( -1.000000000000000000, 7.304098846218133681E-16, -4.217023435051677994E-16 ) ) ;
#255698=CARTESIAN_POINT ( 'NONE',  ( -21.52071067811865746, 7.779289321892505882, -54.75000000000000000 ) ) ;
#255699=ADVANCED_FACE ( 'NONE', ( #187534 ), #207081, .T. ) ;
#255741=AXIS2_PLACEMENT_3D ( 'NONE', #249250, #232269, #10637 ) ;
#255747=AXIS2_PLACEMENT_3D ( 'NONE', #186751, #249291, #8105 ) ;
#255787=CARTESIAN_POINT ( 'NONE',  ( 21.09610168723073187, 0.03358950690264995292, -27.12104428477520912 ) ) ;
#255790=EDGE_LOOP ( 'NONE', ( #157904, #185859, #49222, #38422 ) ) ;
#255802=DIRECTION ( 'NONE',  ( 0.000000000000000000, 0.000000000000000000, 1.000000000000000000 ) ) ;
#255809=ORIENTED_EDGE ( 'NONE', *, *, #166259, .F. ) ;
#255816=ORIENTED_EDGE ( 'NONE', *, *, #72632, .F. ) ;
#255843=CIRCLE ( 'NONE', #139343, 0.3999999999999975797 ) ;
#255847=CARTESIAN_POINT ( 'NONE',  ( 23.25000000000000000, 11.75000000001116263, -54.85000000000000142 ) ) ;
#255848=DIRECTION ( 'NONE',  ( 0.000000000000000000, 1.810617628050740656E-13, 1.000000000000000000 ) ) ;
#255854=LINE ( 'NONE', #92972, #167626 ) ;
#255892=CYLINDRICAL_SURFACE ( 'NONE', #64032, 0.1000000000000000472 ) ;
#255894=VERTEX_POINT ( 'NONE', #81641 ) ;
#255919=CIRCLE ( 'NONE', #143545, 0.1000000000000028644 ) ;
#256002=ADVANCED_FACE ( 'NONE', ( #187220 ), #163662, .T. ) ;
#256036=EDGE_CURVE ( 'NONE', #121164, #65499, #88621, .T. ) ;
#256044=EDGE_LOOP ( 'NONE', ( #21971, #36100, #85762, #218909 ) ) ;
#256067=VECTOR ( 'NONE', #41761, 1000.000000000000000 ) ;
#256075=DIRECTION ( 'NONE',  ( 1.000000000000000000, -0.000000000000000000, -0.000000000000000000 ) ) ;
#256078=ORIENTED_EDGE ( 'NONE', *, *, #123917, .F. ) ;
#256085=CARTESIAN_POINT ( 'NONE',  ( 21.05000000000000071, 10.47338541492405817, -41.07865446424855094 ) ) ;
#256086=DIRECTION ( 'NONE',  ( 0.000000000000000000, -0.9999631594459056361, -0.008583690987124413183 ) ) ;
#256116=AXIS2_PLACEMENT_3D ( 'NONE', #124759, #144282, #162607 ) ;
#256127=FACE_OUTER_BOUND ( 'NONE', #72501, .T. ) ;
#256140=CARTESIAN_POINT ( 'NONE',  ( -20.54999999999999716, 7.150000000011155876, -45.85000000000000142 ) ) ;
#256155=FACE_OUTER_BOUND ( 'NONE', #160317, .T. ) ;
#256169=CARTESIAN_POINT ( 'NONE',  ( -21.14999999999999858, 1.115527483754041871E-11, -26.95934304829875927 ) ) ;
#256286=CARTESIAN_POINT ( 'NONE',  ( 18.59999999999996945, 7.021664781911246322, -70.83356540189728889 ) ) ;
#256292=AXIS2_PLACEMENT_3D ( 'NONE', #164215, #226730, #50648 ) ;
#256315=AXIS2_PLACEMENT_3D ( 'NONE', #137345, #17418, #406 ) ;
#256318=DIRECTION ( 'NONE',  ( 0.000000000000000000, 0.000000000000000000, -1.000000000000000000 ) ) ;
#256342=ORIENTED_EDGE ( 'NONE', *, *, #139836, .T. ) ;
#256363=CARTESIAN_POINT ( 'NONE',  ( 20.94999999999999929, 5.000000000011153745, -54.59473398108690390 ) ) ;
#256391=ORIENTED_EDGE ( 'NONE', *, *, #202355, .F. ) ;
#256425=CARTESIAN_POINT ( 'NONE',  ( -18.59999999999999787, 3.912899247244609580, -44.98182297301097066 ) ) ;
#256448=DIRECTION ( 'NONE',  ( -1.000000000000000000, 0.000000000000000000, 0.000000000000000000 ) ) ;
#256480=ORIENTED_EDGE ( 'NONE', *, *, #59317, .F. ) ;
#256524=ADVANCED_FACE ( 'NONE', ( #40225 ), #196691, .F. ) ;
#256555=B_SPLINE_CURVE_WITH_KNOTS ( 'NONE', 3,
 ( #137702, #197684, #135136, #116878, #252522, #214685, #36072, #19058, #98550, #158599 ),
 .UNSPECIFIED., .F., .F.,
 ( 4, 3, 3, 4 ),
 ( 0.000000000000000000, 3.394313611810755905E-05, 6.779740500699793829E-05, 0.0001049857339142623287 ),
 .UNSPECIFIED. ) ;
#256557=DIRECTION ( 'NONE',  ( 1.000000000000000000, 0.000000000000000000, 0.000000000000000000 ) ) ;
#256566=CIRCLE ( 'NONE', #2534, 0.09999999999999967248 ) ;
#256573=CARTESIAN_POINT ( 'NONE',  ( -21.40925344232282512, 6.658518859401606704, -33.40104981138036067 ) ) ;
#256574=ORIENTED_EDGE ( 'NONE', *, *, #128452, .F. ) ;
#256575=ADVANCED_FACE ( 'NONE', ( #31260 ), #28698, .T. ) ;
#256579=CARTESIAN_POINT ( 'NONE',  ( 21.30000000000002558, 1.115600667400684642E-11, -33.50000000000000000 ) ) ;
#256592=PLANE ( 'NONE',  #14632 ) ;
#256595=ORIENTED_EDGE ( 'NONE', *, *, #213904, .F. ) ;
#256613=FACE_OUTER_BOUND ( 'NONE', #45595, .T. ) ;
#256634=ORIENTED_EDGE ( 'NONE', *, *, #25261, .T. ) ;
#256643=DIRECTION ( 'NONE',  ( 0.000000000000000000, 0.000000000000000000, -1.000000000000000000 ) ) ;
#256669=ORIENTED_EDGE ( 'NONE', *, *, #240472, .T. ) ;
#256682=ADVANCED_FACE ( 'NONE', ( #137996 ), #194162, .T. ) ;
#256707=DIRECTION ( 'NONE',  ( 0.000000000000000000, -1.000000000000000000, 0.000000000000000000 ) ) ;
#256725=LINE ( 'NONE', #40340, #166008 ) ;
#256732=ORIENTED_EDGE ( 'NONE', *, *, #152364, .F. ) ;
#256741=ORIENTED_EDGE ( 'NONE', *, *, #103038, .F. ) ;
#256777=VERTEX_POINT ( 'NONE', #97574 ) ;
#256779=CARTESIAN_POINT ( 'NONE',  ( -21.05000000000000071, 14.00000000001115374, -61.57290746961752603 ) ) ;
#256809=CARTESIAN_POINT ( 'NONE',  ( 18.50000000000000000, -10.35479209691423996, -60.75654098307376216 ) ) ;
#256862=AXIS2_PLACEMENT_3D ( 'NONE', #111196, #73385, #89049 ) ;
#256888=DIRECTION ( 'NONE',  ( 3.616040088954497272E-32, -1.224646799147352961E-16, 1.000000000000000000 ) ) ;
#256896=CARTESIAN_POINT ( 'NONE',  ( -21.08376601933334271, 0.06377601094103470258, -27.15805272872427523 ) ) ;
#256910=LINE ( 'NONE', #156619, #187551 ) ;
#256921=VERTEX_POINT ( 'NONE', #122306 ) ;
#256958=DIRECTION ( 'NONE',  ( 0.000000000000000000, 0.000000000000000000, -1.000000000000000000 ) ) ;
#256977=EDGE_CURVE ( 'NONE', #47498, #24511, #105919, .T. ) ;
#257012=ORIENTED_EDGE ( 'NONE', *, *, #168683, .F. ) ;
#257027=ORIENTED_EDGE ( 'NONE', *, *, #243459, .T. ) ;
#257054=CARTESIAN_POINT ( 'NONE',  ( -23.25000000000000000, 1.115600667400684642E-11, -46.27499999999999858 ) ) ;
#257060=CARTESIAN_POINT ( 'NONE',  ( 21.13461538461538325, 10.61458296203669249, -45.85000000000000142 ) ) ;
#257064=CARTESIAN_POINT ( 'NONE',  ( -23.15000000000000213, -8.663551401858001100, -57.47589888193270014 ) ) ;
#257095=CARTESIAN_POINT ( 'NONE',  ( -20.94999999999999929, 11.75000000001115552, -40.51480577065400013 ) ) ;
#257099=CARTESIAN_POINT ( 'NONE',  ( -20.54999999999999716, 1.925233644870967487, -54.26975646687386501 ) ) ;
#257102=ORIENTED_EDGE ( 'NONE', *, *, #175511, .F. ) ;
#257107=EDGE_CURVE ( 'NONE', #9105, #232658, #180785, .T. ) ;
#257118=CIRCLE ( 'NONE', #82349, 0.1000000000000002831 ) ;
#257206=TOROIDAL_SURFACE ( 'NONE', #144820, 11.65000000000000036, 0.1000000000000000056 ) ;
#257220=CARTESIAN_POINT ( 'NONE',  ( 20.95512820512820440, 8.876151316299271343, -45.65000000000000568 ) ) ;
#257222=ORIENTED_EDGE ( 'NONE', *, *, #36768, .T. ) ;
#257227=ORIENTED_EDGE ( 'NONE', *, *, #125960, .T. ) ;
#257252=AXIS2_PLACEMENT_3D ( 'NONE', #38734, #96110, #214789 ) ;
#257323=FACE_OUTER_BOUND ( 'NONE', #25795, .T. ) ;
#257365=ORIENTED_EDGE ( 'NONE', *, *, #229369, .F. ) ;
#257374=CARTESIAN_POINT ( 'NONE',  ( 23.15000000000000213, -11.48912529306489994, -64.00000000000000000 ) ) ;
#257396=VECTOR ( 'NONE', #198764, 1000.000000000000114 ) ;
#257450=EDGE_CURVE ( 'NONE', #113714, #225825, #188387, .T. ) ;
#257458=VERTEX_POINT ( 'NONE', #56241 ) ;
#257462=CARTESIAN_POINT ( 'NONE',  ( -21.05000000000000071, -0.08579911626297659355, -27.08602111851157090 ) ) ;
#257467=CARTESIAN_POINT ( 'NONE',  ( -23.15000000000000213, 11.75000000001115552, -54.84999999999999432 ) ) ;
#257468=EDGE_CURVE ( 'NONE', #131237, #83073, #1871, .T. ) ;
#257497=CARTESIAN_POINT ( 'NONE',  ( 20.95512828230152280, 8.876151312336450161, -45.70243026550310361 ) ) ;
#257531=ORIENTED_EDGE ( 'NONE', *, *, #58034, .F. ) ;
#257566=CYLINDRICAL_SURFACE ( 'NONE', #27074, 0.09999999999999939493 ) ;
#257603=DIRECTION ( 'NONE',  ( 1.000000000000000000, 0.000000000000000000, 0.000000000000000000 ) ) ;
#257604=CARTESIAN_POINT ( 'NONE',  ( -20.54999999999999716, 7.150000000011155876, -45.75000000000000000 ) ) ;
#257715=CIRCLE ( 'NONE', #141254, 2.100000000000004530 ) ;
#257724=AXIS2_PLACEMENT_3D ( 'NONE', #20142, #59209, #99632 ) ;
#257748=AXIS2_PLACEMENT_3D ( 'NONE', #173134, #54413, #34889 ) ;
#257794=ORIENTED_EDGE ( 'NONE', *, *, #176048, .F. ) ;
#257797=CARTESIAN_POINT ( 'NONE',  ( 20.87631937322882081, 10.47149503677605509, -41.07974587458117099 ) ) ;
#257804=CARTESIAN_POINT ( 'NONE',  ( -23.15000000000000213, 1.115600667400684642E-11, -67.00000000000000000 ) ) ;
#257815=DIRECTION ( 'NONE',  ( 0.000000000000000000, 0.000000000000000000, -1.000000000000000000 ) ) ;
#257823=CARTESIAN_POINT ( 'NONE',  ( -18.42609945526390902, -9.499999710479542614, -40.49936249024798229 ) ) ;
#257825=ORIENTED_EDGE ( 'NONE', *, *, #157983, .T. ) ;
#257827=CARTESIAN_POINT ( 'NONE',  ( -20.64999999999999858, -8.999999999988844479, -57.50603087734755547 ) ) ;
#257860=DIRECTION ( 'NONE',  ( 0.000000000000000000, 1.776356839400303713E-15, 1.000000000000000000 ) ) ;
#257886=ORIENTED_EDGE ( 'NONE', *, *, #35056, .T. ) ;
#257891=DIRECTION ( 'NONE',  ( -1.000000000000000000, -0.000000000000000000, -0.000000000000000000 ) ) ;
#257892=VECTOR ( 'NONE', #142075, 1000.000000000000000 ) ;
#257912=CARTESIAN_POINT ( 'NONE',  ( 21.05000000000000071, 11.65000000001116298, -45.65000000000000568 ) ) ;
#257938=EDGE_CURVE ( 'NONE', #104231, #57195, #85421, .T. ) ;
#257941=EDGE_CURVE ( 'NONE', #32344, #194844, #31346, .T. ) ;
#257943=DIRECTION ( 'NONE',  ( -1.000000000000000000, 0.000000000000000000, 0.000000000000000000 ) ) ;
#257961=ORIENTED_EDGE ( 'NONE', *, *, #248109, .F. ) ;
#257972=ORIENTED_EDGE ( 'NONE', *, *, #166456, .F. ) ;
#257993=CARTESIAN_POINT ( 'NONE',  ( 18.49999999999999289, 11.75000000001115907, -21.75000000000000355 ) ) ;
#258002=DIRECTION ( 'NONE',  ( 0.000000000000000000, 0.000000000000000000, -1.000000000000000000 ) ) ;
#258024=AXIS2_PLACEMENT_3D ( 'NONE', #64204, #2925, #25101 ) ;
#258038=DIRECTION ( 'NONE',  ( 0.000000000000000000, 0.000000000000000000, 1.000000000000000000 ) ) ;
#258047=CARTESIAN_POINT ( 'NONE',  ( 23.15000000000000213, -9.599999999988842347, -57.10603087734755690 ) ) ;
#258071=CARTESIAN_POINT ( 'NONE',  ( 23.25000000000000000, -11.74999999998883560, -45.65000000000000568 ) ) ;
#258094=ADVANCED_FACE ( 'NONE', ( #29692 ), #210866, .T. ) ;
ENDSEC;
END-ISO-10303-21;
